ISO-10303-21;
HEADER;
/* Generated by software containing ST-Developer
 * from STEP Tools, Inc. (www.steptools.com) 
 */

FILE_DESCRIPTION(
/* description */ (''),
/* implementation_level */ '2;1');

FILE_NAME(
/* name */ 'Screw.step',
/* time_stamp */ '2026-10-19T01:17:59+06:00',
/* author */ (''),
/* organization */ (''),
/* preprocessor_version */ 'ST-DEVELOPER v20.2',
/* originating_system */ 'Autodesk Translation Framework v15.15.0.0',
/* authorisation */ '');

FILE_SCHEMA (('AUTOMOTIVE_DESIGN { 1 0 10303 214 3 1 1 }'));
ENDSEC;

DATA;
#10=MECHANICAL_DESIGN_GEOMETRIC_PRESENTATION_REPRESENTATION('',(#748),#48369);
#67=B_SPLINE_SURFACE_WITH_KNOTS('',3,3,((#40580,#40581,#40582,#40583,#40584,
#40585,#40586,#40587,#40588,#40589,#40590,#40591,#40592,#40593,#40594,#40595,
#40596,#40597,#40598,#40599,#40600,#40601,#40602,#40603,#40604,#40605,#40606,
#40607,#40608,#40609,#40610,#40611,#40612,#40613,#40614,#40615,#40616,#40617,
#40618,#40619,#40620,#40621,#40622,#40623,#40624,#40625,#40626,#40627,#40628,
#40629,#40630,#40631,#40632,#40633,#40634,#40635,#40636,#40637,#40638,#40639,
#40640,#40641,#40642,#40643,#40644,#40645,#40646,#40647,#40648,#40649,#40650,
#40651,#40652,#40653,#40654,#40655,#40656,#40657,#40658,#40659,#40660,#40661,
#40662,#40663,#40664,#40665,#40666,#40667,#40668,#40669,#40670,#40671,#40672,
#40673,#40674,#40675,#40676,#40677,#40678,#40679,#40680,#40681,#40682,#40683,
#40684,#40685,#40686,#40687,#40688,#40689,#40690,#40691,#40692,#40693,#40694,
#40695,#40696,#40697,#40698,#40699,#40700,#40701,#40702,#40703,#40704,#40705,
#40706,#40707,#40708,#40709,#40710,#40711,#40712,#40713,#40714,#40715,#40716,
#40717,#40718,#40719,#40720,#40721,#40722,#40723,#40724,#40725,#40726,#40727,
#40728,#40729,#40730,#40731,#40732,#40733,#40734,#40735,#40736,#40737,#40738,
#40739,#40740,#40741,#40742,#40743,#40744,#40745,#40746,#40747,#40748,#40749,
#40750,#40751,#40752,#40753,#40754,#40755,#40756,#40757,#40758,#40759,#40760,
#40761,#40762,#40763,#40764,#40765,#40766,#40767,#40768,#40769,#40770,#40771,
#40772,#40773,#40774,#40775,#40776,#40777,#40778,#40779,#40780,#40781,#40782,
#40783,#40784,#40785,#40786,#40787,#40788,#40789,#40790,#40791,#40792,#40793,
#40794,#40795,#40796,#40797,#40798,#40799,#40800,#40801,#40802,#40803,#40804,
#40805,#40806,#40807,#40808,#40809,#40810,#40811,#40812,#40813,#40814,#40815,
#40816,#40817,#40818,#40819,#40820,#40821,#40822,#40823,#40824,#40825,#40826,
#40827,#40828,#40829,#40830,#40831,#40832,#40833,#40834,#40835,#40836,#40837,
#40838,#40839,#40840,#40841,#40842,#40843,#40844,#40845,#40846,#40847,#40848,
#40849,#40850,#40851,#40852,#40853,#40854,#40855,#40856,#40857,#40858,#40859,
#40860,#40861,#40862,#40863,#40864,#40865,#40866,#40867,#40868,#40869,#40870,
#40871,#40872,#40873,#40874,#40875,#40876,#40877,#40878,#40879,#40880,#40881,
#40882,#40883,#40884,#40885,#40886,#40887,#40888,#40889,#40890,#40891,#40892,
#40893,#40894,#40895,#40896,#40897,#40898,#40899,#40900,#40901,#40902,#40903,
#40904,#40905,#40906,#40907,#40908,#40909,#40910,#40911,#40912,#40913,#40914,
#40915,#40916,#40917,#40918,#40919,#40920,#40921,#40922,#40923,#40924,#40925,
#40926,#40927,#40928,#40929,#40930,#40931,#40932,#40933,#40934,#40935,#40936,
#40937,#40938,#40939,#40940,#40941,#40942,#40943,#40944,#40945,#40946,#40947,
#40948,#40949,#40950,#40951,#40952,#40953,#40954,#40955,#40956,#40957,#40958,
#40959,#40960,#40961,#40962,#40963,#40964,#40965,#40966,#40967,#40968,#40969,
#40970,#40971,#40972,#40973,#40974,#40975,#40976,#40977,#40978,#40979,#40980,
#40981,#40982,#40983,#40984,#40985,#40986,#40987,#40988,#40989,#40990,#40991,
#40992,#40993,#40994,#40995,#40996,#40997,#40998,#40999,#41000,#41001,#41002,
#41003,#41004,#41005,#41006,#41007,#41008,#41009,#41010,#41011,#41012,#41013,
#41014,#41015,#41016,#41017,#41018,#41019,#41020,#41021,#41022,#41023,#41024,
#41025,#41026,#41027,#41028,#41029,#41030,#41031,#41032,#41033,#41034,#41035,
#41036,#41037,#41038,#41039,#41040,#41041,#41042,#41043,#41044,#41045,#41046,
#41047,#41048,#41049,#41050,#41051,#41052,#41053,#41054,#41055,#41056,#41057,
#41058,#41059,#41060,#41061,#41062,#41063,#41064,#41065,#41066,#41067,#41068,
#41069,#41070,#41071,#41072,#41073,#41074,#41075,#41076,#41077,#41078,#41079,
#41080,#41081,#41082,#41083,#41084,#41085,#41086,#41087,#41088,#41089,#41090,
#41091,#41092,#41093,#41094,#41095,#41096,#41097,#41098,#41099,#41100,#41101,
#41102,#41103,#41104,#41105,#41106,#41107,#41108,#41109,#41110,#41111,#41112,
#41113,#41114,#41115,#41116,#41117,#41118,#41119,#41120,#41121,#41122,#41123,
#41124,#41125,#41126,#41127,#41128,#41129,#41130,#41131,#41132,#41133,#41134,
#41135,#41136,#41137,#41138,#41139,#41140,#41141,#41142,#41143,#41144,#41145,
#41146,#41147,#41148,#41149,#41150,#41151,#41152,#41153,#41154,#41155,#41156,
#41157,#41158,#41159,#41160,#41161,#41162,#41163,#41164,#41165,#41166,#41167,
#41168,#41169,#41170,#41171,#41172,#41173,#41174,#41175,#41176,#41177,#41178,
#41179,#41180,#41181,#41182,#41183,#41184,#41185,#41186,#41187,#41188,#41189,
#41190,#41191,#41192,#41193,#41194,#41195,#41196,#41197,#41198,#41199,#41200,
#41201,#41202,#41203,#41204,#41205,#41206,#41207,#41208,#41209,#41210,#41211,
#41212,#41213,#41214,#41215,#41216,#41217,#41218,#41219,#41220,#41221,#41222,
#41223,#41224,#41225,#41226,#41227,#41228,#41229,#41230,#41231,#41232,#41233,
#41234,#41235,#41236,#41237,#41238,#41239,#41240,#41241,#41242,#41243,#41244,
#41245,#41246,#41247,#41248,#41249,#41250,#41251,#41252,#41253,#41254,#41255,
#41256,#41257,#41258,#41259,#41260,#41261,#41262,#41263,#41264,#41265,#41266,
#41267,#41268,#41269,#41270,#41271,#41272,#41273,#41274,#41275,#41276,#41277,
#41278,#41279,#41280,#41281,#41282,#41283,#41284,#41285,#41286,#41287,#41288,
#41289,#41290,#41291,#41292,#41293,#41294,#41295,#41296,#41297,#41298,#41299,
#41300,#41301,#41302,#41303,#41304),(#41305,#41306,#41307,#41308,#41309,
#41310,#41311,#41312,#41313,#41314,#41315,#41316,#41317,#41318,#41319,#41320,
#41321,#41322,#41323,#41324,#41325,#41326,#41327,#41328,#41329,#41330,#41331,
#41332,#41333,#41334,#41335,#41336,#41337,#41338,#41339,#41340,#41341,#41342,
#41343,#41344,#41345,#41346,#41347,#41348,#41349,#41350,#41351,#41352,#41353,
#41354,#41355,#41356,#41357,#41358,#41359,#41360,#41361,#41362,#41363,#41364,
#41365,#41366,#41367,#41368,#41369,#41370,#41371,#41372,#41373,#41374,#41375,
#41376,#41377,#41378,#41379,#41380,#41381,#41382,#41383,#41384,#41385,#41386,
#41387,#41388,#41389,#41390,#41391,#41392,#41393,#41394,#41395,#41396,#41397,
#41398,#41399,#41400,#41401,#41402,#41403,#41404,#41405,#41406,#41407,#41408,
#41409,#41410,#41411,#41412,#41413,#41414,#41415,#41416,#41417,#41418,#41419,
#41420,#41421,#41422,#41423,#41424,#41425,#41426,#41427,#41428,#41429,#41430,
#41431,#41432,#41433,#41434,#41435,#41436,#41437,#41438,#41439,#41440,#41441,
#41442,#41443,#41444,#41445,#41446,#41447,#41448,#41449,#41450,#41451,#41452,
#41453,#41454,#41455,#41456,#41457,#41458,#41459,#41460,#41461,#41462,#41463,
#41464,#41465,#41466,#41467,#41468,#41469,#41470,#41471,#41472,#41473,#41474,
#41475,#41476,#41477,#41478,#41479,#41480,#41481,#41482,#41483,#41484,#41485,
#41486,#41487,#41488,#41489,#41490,#41491,#41492,#41493,#41494,#41495,#41496,
#41497,#41498,#41499,#41500,#41501,#41502,#41503,#41504,#41505,#41506,#41507,
#41508,#41509,#41510,#41511,#41512,#41513,#41514,#41515,#41516,#41517,#41518,
#41519,#41520,#41521,#41522,#41523,#41524,#41525,#41526,#41527,#41528,#41529,
#41530,#41531,#41532,#41533,#41534,#41535,#41536,#41537,#41538,#41539,#41540,
#41541,#41542,#41543,#41544,#41545,#41546,#41547,#41548,#41549,#41550,#41551,
#41552,#41553,#41554,#41555,#41556,#41557,#41558,#41559,#41560,#41561,#41562,
#41563,#41564,#41565,#41566,#41567,#41568,#41569,#41570,#41571,#41572,#41573,
#41574,#41575,#41576,#41577,#41578,#41579,#41580,#41581,#41582,#41583,#41584,
#41585,#41586,#41587,#41588,#41589,#41590,#41591,#41592,#41593,#41594,#41595,
#41596,#41597,#41598,#41599,#41600,#41601,#41602,#41603,#41604,#41605,#41606,
#41607,#41608,#41609,#41610,#41611,#41612,#41613,#41614,#41615,#41616,#41617,
#41618,#41619,#41620,#41621,#41622,#41623,#41624,#41625,#41626,#41627,#41628,
#41629,#41630,#41631,#41632,#41633,#41634,#41635,#41636,#41637,#41638,#41639,
#41640,#41641,#41642,#41643,#41644,#41645,#41646,#41647,#41648,#41649,#41650,
#41651,#41652,#41653,#41654,#41655,#41656,#41657,#41658,#41659,#41660,#41661,
#41662,#41663,#41664,#41665,#41666,#41667,#41668,#41669,#41670,#41671,#41672,
#41673,#41674,#41675,#41676,#41677,#41678,#41679,#41680,#41681,#41682,#41683,
#41684,#41685,#41686,#41687,#41688,#41689,#41690,#41691,#41692,#41693,#41694,
#41695,#41696,#41697,#41698,#41699,#41700,#41701,#41702,#41703,#41704,#41705,
#41706,#41707,#41708,#41709,#41710,#41711,#41712,#41713,#41714,#41715,#41716,
#41717,#41718,#41719,#41720,#41721,#41722,#41723,#41724,#41725,#41726,#41727,
#41728,#41729,#41730,#41731,#41732,#41733,#41734,#41735,#41736,#41737,#41738,
#41739,#41740,#41741,#41742,#41743,#41744,#41745,#41746,#41747,#41748,#41749,
#41750,#41751,#41752,#41753,#41754,#41755,#41756,#41757,#41758,#41759,#41760,
#41761,#41762,#41763,#41764,#41765,#41766,#41767,#41768,#41769,#41770,#41771,
#41772,#41773,#41774,#41775,#41776,#41777,#41778,#41779,#41780,#41781,#41782,
#41783,#41784,#41785,#41786,#41787,#41788,#41789,#41790,#41791,#41792,#41793,
#41794,#41795,#41796,#41797,#41798,#41799,#41800,#41801,#41802,#41803,#41804,
#41805,#41806,#41807,#41808,#41809,#41810,#41811,#41812,#41813,#41814,#41815,
#41816,#41817,#41818,#41819,#41820,#41821,#41822,#41823,#41824,#41825,#41826,
#41827,#41828,#41829,#41830,#41831,#41832,#41833,#41834,#41835,#41836,#41837,
#41838,#41839,#41840,#41841,#41842,#41843,#41844,#41845,#41846,#41847,#41848,
#41849,#41850,#41851,#41852,#41853,#41854,#41855,#41856,#41857,#41858,#41859,
#41860,#41861,#41862,#41863,#41864,#41865,#41866,#41867,#41868,#41869,#41870,
#41871,#41872,#41873,#41874,#41875,#41876,#41877,#41878,#41879,#41880,#41881,
#41882,#41883,#41884,#41885,#41886,#41887,#41888,#41889,#41890,#41891,#41892,
#41893,#41894,#41895,#41896,#41897,#41898,#41899,#41900,#41901,#41902,#41903,
#41904,#41905,#41906,#41907,#41908,#41909,#41910,#41911,#41912,#41913,#41914,
#41915,#41916,#41917,#41918,#41919,#41920,#41921,#41922,#41923,#41924,#41925,
#41926,#41927,#41928,#41929,#41930,#41931,#41932,#41933,#41934,#41935,#41936,
#41937,#41938,#41939,#41940,#41941,#41942,#41943,#41944,#41945,#41946,#41947,
#41948,#41949,#41950,#41951,#41952,#41953,#41954,#41955,#41956,#41957,#41958,
#41959,#41960,#41961,#41962,#41963,#41964,#41965,#41966,#41967,#41968,#41969,
#41970,#41971,#41972,#41973,#41974,#41975,#41976,#41977,#41978,#41979,#41980,
#41981,#41982,#41983,#41984,#41985,#41986,#41987,#41988,#41989,#41990,#41991,
#41992,#41993,#41994,#41995,#41996,#41997,#41998,#41999,#42000,#42001,#42002,
#42003,#42004,#42005,#42006,#42007,#42008,#42009,#42010,#42011,#42012,#42013,
#42014,#42015,#42016,#42017,#42018,#42019,#42020,#42021,#42022,#42023,#42024,
#42025,#42026,#42027,#42028,#42029),(#42030,#42031,#42032,#42033,#42034,
#42035,#42036,#42037,#42038,#42039,#42040,#42041,#42042,#42043,#42044,#42045,
#42046,#42047,#42048,#42049,#42050,#42051,#42052,#42053,#42054,#42055,#42056,
#42057,#42058,#42059,#42060,#42061,#42062,#42063,#42064,#42065,#42066,#42067,
#42068,#42069,#42070,#42071,#42072,#42073,#42074,#42075,#42076,#42077,#42078,
#42079,#42080,#42081,#42082,#42083,#42084,#42085,#42086,#42087,#42088,#42089,
#42090,#42091,#42092,#42093,#42094,#42095,#42096,#42097,#42098,#42099,#42100,
#42101,#42102,#42103,#42104,#42105,#42106,#42107,#42108,#42109,#42110,#42111,
#42112,#42113,#42114,#42115,#42116,#42117,#42118,#42119,#42120,#42121,#42122,
#42123,#42124,#42125,#42126,#42127,#42128,#42129,#42130,#42131,#42132,#42133,
#42134,#42135,#42136,#42137,#42138,#42139,#42140,#42141,#42142,#42143,#42144,
#42145,#42146,#42147,#42148,#42149,#42150,#42151,#42152,#42153,#42154,#42155,
#42156,#42157,#42158,#42159,#42160,#42161,#42162,#42163,#42164,#42165,#42166,
#42167,#42168,#42169,#42170,#42171,#42172,#42173,#42174,#42175,#42176,#42177,
#42178,#42179,#42180,#42181,#42182,#42183,#42184,#42185,#42186,#42187,#42188,
#42189,#42190,#42191,#42192,#42193,#42194,#42195,#42196,#42197,#42198,#42199,
#42200,#42201,#42202,#42203,#42204,#42205,#42206,#42207,#42208,#42209,#42210,
#42211,#42212,#42213,#42214,#42215,#42216,#42217,#42218,#42219,#42220,#42221,
#42222,#42223,#42224,#42225,#42226,#42227,#42228,#42229,#42230,#42231,#42232,
#42233,#42234,#42235,#42236,#42237,#42238,#42239,#42240,#42241,#42242,#42243,
#42244,#42245,#42246,#42247,#42248,#42249,#42250,#42251,#42252,#42253,#42254,
#42255,#42256,#42257,#42258,#42259,#42260,#42261,#42262,#42263,#42264,#42265,
#42266,#42267,#42268,#42269,#42270,#42271,#42272,#42273,#42274,#42275,#42276,
#42277,#42278,#42279,#42280,#42281,#42282,#42283,#42284,#42285,#42286,#42287,
#42288,#42289,#42290,#42291,#42292,#42293,#42294,#42295,#42296,#42297,#42298,
#42299,#42300,#42301,#42302,#42303,#42304,#42305,#42306,#42307,#42308,#42309,
#42310,#42311,#42312,#42313,#42314,#42315,#42316,#42317,#42318,#42319,#42320,
#42321,#42322,#42323,#42324,#42325,#42326,#42327,#42328,#42329,#42330,#42331,
#42332,#42333,#42334,#42335,#42336,#42337,#42338,#42339,#42340,#42341,#42342,
#42343,#42344,#42345,#42346,#42347,#42348,#42349,#42350,#42351,#42352,#42353,
#42354,#42355,#42356,#42357,#42358,#42359,#42360,#42361,#42362,#42363,#42364,
#42365,#42366,#42367,#42368,#42369,#42370,#42371,#42372,#42373,#42374,#42375,
#42376,#42377,#42378,#42379,#42380,#42381,#42382,#42383,#42384,#42385,#42386,
#42387,#42388,#42389,#42390,#42391,#42392,#42393,#42394,#42395,#42396,#42397,
#42398,#42399,#42400,#42401,#42402,#42403,#42404,#42405,#42406,#42407,#42408,
#42409,#42410,#42411,#42412,#42413,#42414,#42415,#42416,#42417,#42418,#42419,
#42420,#42421,#42422,#42423,#42424,#42425,#42426,#42427,#42428,#42429,#42430,
#42431,#42432,#42433,#42434,#42435,#42436,#42437,#42438,#42439,#42440,#42441,
#42442,#42443,#42444,#42445,#42446,#42447,#42448,#42449,#42450,#42451,#42452,
#42453,#42454,#42455,#42456,#42457,#42458,#42459,#42460,#42461,#42462,#42463,
#42464,#42465,#42466,#42467,#42468,#42469,#42470,#42471,#42472,#42473,#42474,
#42475,#42476,#42477,#42478,#42479,#42480,#42481,#42482,#42483,#42484,#42485,
#42486,#42487,#42488,#42489,#42490,#42491,#42492,#42493,#42494,#42495,#42496,
#42497,#42498,#42499,#42500,#42501,#42502,#42503,#42504,#42505,#42506,#42507,
#42508,#42509,#42510,#42511,#42512,#42513,#42514,#42515,#42516,#42517,#42518,
#42519,#42520,#42521,#42522,#42523,#42524,#42525,#42526,#42527,#42528,#42529,
#42530,#42531,#42532,#42533,#42534,#42535,#42536,#42537,#42538,#42539,#42540,
#42541,#42542,#42543,#42544,#42545,#42546,#42547,#42548,#42549,#42550,#42551,
#42552,#42553,#42554,#42555,#42556,#42557,#42558,#42559,#42560,#42561,#42562,
#42563,#42564,#42565,#42566,#42567,#42568,#42569,#42570,#42571,#42572,#42573,
#42574,#42575,#42576,#42577,#42578,#42579,#42580,#42581,#42582,#42583,#42584,
#42585,#42586,#42587,#42588,#42589,#42590,#42591,#42592,#42593,#42594,#42595,
#42596,#42597,#42598,#42599,#42600,#42601,#42602,#42603,#42604,#42605,#42606,
#42607,#42608,#42609,#42610,#42611,#42612,#42613,#42614,#42615,#42616,#42617,
#42618,#42619,#42620,#42621,#42622,#42623,#42624,#42625,#42626,#42627,#42628,
#42629,#42630,#42631,#42632,#42633,#42634,#42635,#42636,#42637,#42638,#42639,
#42640,#42641,#42642,#42643,#42644,#42645,#42646,#42647,#42648,#42649,#42650,
#42651,#42652,#42653,#42654,#42655,#42656,#42657,#42658,#42659,#42660,#42661,
#42662,#42663,#42664,#42665,#42666,#42667,#42668,#42669,#42670,#42671,#42672,
#42673,#42674,#42675,#42676,#42677,#42678,#42679,#42680,#42681,#42682,#42683,
#42684,#42685,#42686,#42687,#42688,#42689,#42690,#42691,#42692,#42693,#42694,
#42695,#42696,#42697,#42698,#42699,#42700,#42701,#42702,#42703,#42704,#42705,
#42706,#42707,#42708,#42709,#42710,#42711,#42712,#42713,#42714,#42715,#42716,
#42717,#42718,#42719,#42720,#42721,#42722,#42723,#42724,#42725,#42726,#42727,
#42728,#42729,#42730,#42731,#42732,#42733,#42734,#42735,#42736,#42737,#42738,
#42739,#42740,#42741,#42742,#42743,#42744,#42745,#42746,#42747,#42748,#42749,
#42750,#42751,#42752,#42753,#42754),(#42755,#42756,#42757,#42758,#42759,
#42760,#42761,#42762,#42763,#42764,#42765,#42766,#42767,#42768,#42769,#42770,
#42771,#42772,#42773,#42774,#42775,#42776,#42777,#42778,#42779,#42780,#42781,
#42782,#42783,#42784,#42785,#42786,#42787,#42788,#42789,#42790,#42791,#42792,
#42793,#42794,#42795,#42796,#42797,#42798,#42799,#42800,#42801,#42802,#42803,
#42804,#42805,#42806,#42807,#42808,#42809,#42810,#42811,#42812,#42813,#42814,
#42815,#42816,#42817,#42818,#42819,#42820,#42821,#42822,#42823,#42824,#42825,
#42826,#42827,#42828,#42829,#42830,#42831,#42832,#42833,#42834,#42835,#42836,
#42837,#42838,#42839,#42840,#42841,#42842,#42843,#42844,#42845,#42846,#42847,
#42848,#42849,#42850,#42851,#42852,#42853,#42854,#42855,#42856,#42857,#42858,
#42859,#42860,#42861,#42862,#42863,#42864,#42865,#42866,#42867,#42868,#42869,
#42870,#42871,#42872,#42873,#42874,#42875,#42876,#42877,#42878,#42879,#42880,
#42881,#42882,#42883,#42884,#42885,#42886,#42887,#42888,#42889,#42890,#42891,
#42892,#42893,#42894,#42895,#42896,#42897,#42898,#42899,#42900,#42901,#42902,
#42903,#42904,#42905,#42906,#42907,#42908,#42909,#42910,#42911,#42912,#42913,
#42914,#42915,#42916,#42917,#42918,#42919,#42920,#42921,#42922,#42923,#42924,
#42925,#42926,#42927,#42928,#42929,#42930,#42931,#42932,#42933,#42934,#42935,
#42936,#42937,#42938,#42939,#42940,#42941,#42942,#42943,#42944,#42945,#42946,
#42947,#42948,#42949,#42950,#42951,#42952,#42953,#42954,#42955,#42956,#42957,
#42958,#42959,#42960,#42961,#42962,#42963,#42964,#42965,#42966,#42967,#42968,
#42969,#42970,#42971,#42972,#42973,#42974,#42975,#42976,#42977,#42978,#42979,
#42980,#42981,#42982,#42983,#42984,#42985,#42986,#42987,#42988,#42989,#42990,
#42991,#42992,#42993,#42994,#42995,#42996,#42997,#42998,#42999,#43000,#43001,
#43002,#43003,#43004,#43005,#43006,#43007,#43008,#43009,#43010,#43011,#43012,
#43013,#43014,#43015,#43016,#43017,#43018,#43019,#43020,#43021,#43022,#43023,
#43024,#43025,#43026,#43027,#43028,#43029,#43030,#43031,#43032,#43033,#43034,
#43035,#43036,#43037,#43038,#43039,#43040,#43041,#43042,#43043,#43044,#43045,
#43046,#43047,#43048,#43049,#43050,#43051,#43052,#43053,#43054,#43055,#43056,
#43057,#43058,#43059,#43060,#43061,#43062,#43063,#43064,#43065,#43066,#43067,
#43068,#43069,#43070,#43071,#43072,#43073,#43074,#43075,#43076,#43077,#43078,
#43079,#43080,#43081,#43082,#43083,#43084,#43085,#43086,#43087,#43088,#43089,
#43090,#43091,#43092,#43093,#43094,#43095,#43096,#43097,#43098,#43099,#43100,
#43101,#43102,#43103,#43104,#43105,#43106,#43107,#43108,#43109,#43110,#43111,
#43112,#43113,#43114,#43115,#43116,#43117,#43118,#43119,#43120,#43121,#43122,
#43123,#43124,#43125,#43126,#43127,#43128,#43129,#43130,#43131,#43132,#43133,
#43134,#43135,#43136,#43137,#43138,#43139,#43140,#43141,#43142,#43143,#43144,
#43145,#43146,#43147,#43148,#43149,#43150,#43151,#43152,#43153,#43154,#43155,
#43156,#43157,#43158,#43159,#43160,#43161,#43162,#43163,#43164,#43165,#43166,
#43167,#43168,#43169,#43170,#43171,#43172,#43173,#43174,#43175,#43176,#43177,
#43178,#43179,#43180,#43181,#43182,#43183,#43184,#43185,#43186,#43187,#43188,
#43189,#43190,#43191,#43192,#43193,#43194,#43195,#43196,#43197,#43198,#43199,
#43200,#43201,#43202,#43203,#43204,#43205,#43206,#43207,#43208,#43209,#43210,
#43211,#43212,#43213,#43214,#43215,#43216,#43217,#43218,#43219,#43220,#43221,
#43222,#43223,#43224,#43225,#43226,#43227,#43228,#43229,#43230,#43231,#43232,
#43233,#43234,#43235,#43236,#43237,#43238,#43239,#43240,#43241,#43242,#43243,
#43244,#43245,#43246,#43247,#43248,#43249,#43250,#43251,#43252,#43253,#43254,
#43255,#43256,#43257,#43258,#43259,#43260,#43261,#43262,#43263,#43264,#43265,
#43266,#43267,#43268,#43269,#43270,#43271,#43272,#43273,#43274,#43275,#43276,
#43277,#43278,#43279,#43280,#43281,#43282,#43283,#43284,#43285,#43286,#43287,
#43288,#43289,#43290,#43291,#43292,#43293,#43294,#43295,#43296,#43297,#43298,
#43299,#43300,#43301,#43302,#43303,#43304,#43305,#43306,#43307,#43308,#43309,
#43310,#43311,#43312,#43313,#43314,#43315,#43316,#43317,#43318,#43319,#43320,
#43321,#43322,#43323,#43324,#43325,#43326,#43327,#43328,#43329,#43330,#43331,
#43332,#43333,#43334,#43335,#43336,#43337,#43338,#43339,#43340,#43341,#43342,
#43343,#43344,#43345,#43346,#43347,#43348,#43349,#43350,#43351,#43352,#43353,
#43354,#43355,#43356,#43357,#43358,#43359,#43360,#43361,#43362,#43363,#43364,
#43365,#43366,#43367,#43368,#43369,#43370,#43371,#43372,#43373,#43374,#43375,
#43376,#43377,#43378,#43379,#43380,#43381,#43382,#43383,#43384,#43385,#43386,
#43387,#43388,#43389,#43390,#43391,#43392,#43393,#43394,#43395,#43396,#43397,
#43398,#43399,#43400,#43401,#43402,#43403,#43404,#43405,#43406,#43407,#43408,
#43409,#43410,#43411,#43412,#43413,#43414,#43415,#43416,#43417,#43418,#43419,
#43420,#43421,#43422,#43423,#43424,#43425,#43426,#43427,#43428,#43429,#43430,
#43431,#43432,#43433,#43434,#43435,#43436,#43437,#43438,#43439,#43440,#43441,
#43442,#43443,#43444,#43445,#43446,#43447,#43448,#43449,#43450,#43451,#43452,
#43453,#43454,#43455,#43456,#43457,#43458,#43459,#43460,#43461,#43462,#43463,
#43464,#43465,#43466,#43467,#43468,#43469,#43470,#43471,#43472,#43473,#43474,
#43475,#43476,#43477,#43478,#43479)),.UNSPECIFIED.,.F.,.F.,.F.,(4,4),(4,
1,1,1,1,1,1,1,1,1,1,1,1,1,1,1,1,1,1,1,1,1,1,1,1,1,1,1,1,1,1,1,1,1,1,1,1,
1,1,1,1,1,1,1,1,1,1,1,1,1,1,1,1,1,1,1,1,1,1,1,1,1,1,1,1,1,1,1,1,1,1,1,1,
1,1,1,1,1,1,1,1,1,1,1,1,1,1,1,1,1,1,1,1,1,1,1,1,1,1,1,1,1,1,1,1,1,1,1,1,
1,1,1,1,1,1,1,1,1,1,1,1,1,1,1,1,1,1,1,1,1,1,1,1,1,1,1,1,1,1,1,1,1,1,1,1,
1,1,1,1,1,1,1,1,1,1,1,1,1,1,1,1,1,1,1,1,1,1,1,1,1,1,1,1,1,1,1,1,1,1,1,1,
1,1,1,1,1,1,1,1,1,1,1,1,1,1,1,1,1,1,1,1,1,1,1,1,1,1,1,1,1,1,1,1,1,1,1,1,
1,1,1,1,1,1,1,1,1,1,1,1,1,1,1,1,1,1,1,1,1,1,1,1,1,1,1,1,1,1,1,1,1,1,1,1,
1,1,1,1,1,1,1,1,1,1,1,1,1,1,1,1,1,1,1,1,1,1,1,1,1,1,1,1,1,1,1,1,1,1,1,1,
1,1,1,1,1,1,1,1,1,1,1,1,1,1,1,1,1,1,1,1,1,1,1,1,1,1,1,1,1,1,1,1,1,1,1,1,
1,1,1,1,1,1,1,1,1,1,1,1,1,1,1,1,1,1,1,1,1,1,1,1,1,1,1,1,1,1,1,1,1,1,1,1,
1,1,1,1,1,1,1,1,1,1,1,1,1,1,1,1,1,1,1,1,1,1,1,1,1,1,1,1,1,1,1,1,1,1,1,1,
1,1,1,1,1,1,1,1,1,1,1,1,1,1,1,1,1,1,1,1,1,1,1,1,1,1,1,1,1,1,1,1,1,1,1,1,
1,1,1,1,1,1,1,1,1,1,1,1,1,1,1,1,1,1,1,1,1,1,1,1,1,1,1,1,1,1,1,1,1,1,1,1,
1,1,1,1,1,1,1,1,1,1,1,1,1,1,1,1,1,1,1,1,1,1,1,1,1,1,1,1,1,1,1,1,1,1,1,1,
1,1,1,1,1,1,1,1,1,1,1,1,1,1,1,1,1,1,1,1,1,1,1,1,1,1,1,1,1,1,1,1,1,1,1,1,
1,1,1,1,1,1,1,1,1,1,1,1,1,1,1,1,1,1,1,1,1,1,1,1,1,1,1,1,1,1,1,1,1,1,1,1,
1,1,1,1,1,1,1,1,1,1,1,1,1,1,1,1,1,1,1,1,1,1,1,1,1,1,1,1,1,1,1,1,1,1,1,1,
1,1,1,1,1,1,1,1,1,1,1,1,1,1,1,1,1,1,1,1,1,1,1,1,1,1,1,1,1,1,1,1,1,1,1,1,
1,1,1,1,1,1,1,1,1,1,1,1,1,1,1,1,1,1,1,1,1,1,1,1,1,1,1,1,1,1,1,1,1,1,1,1,
1,1,1,1,1,1,1,1,1,1,1,1,1,1,1,1,1,1,1,1,1,1,1,1,1,1,1,1,1,1,1,1,1,1,1,1,
1,4),(0.,0.23619826056056),(12.0433050839651,12.5431859047334,13.0430667255018,
14.0428283670385,15.0425900085752,16.0423516501119,17.0421132916487,18.0418749331854,
18.5417557539537,19.0416365747221,20.0413982162588,21.0411598577955,22.0409214993322,
23.040683140869,24.0404447824057,25.0402064239424,25.5400872447107,26.0399680654791,
27.0397297070158,28.0394913485525,29.0392529900893,30.039014631626,31.0387762731627,
32.0385379146994,32.5384187354678,33.0382995562361,34.0380611977728,35.0378228393096,
36.0375844808463,37.037346122383,38.0371077639197,39.0368694054564,39.5367502262248,
40.0366310469931,41.0363926885299,42.0361543300666,43.0359159716033,44.03567761314,
45.0354392546767,46.0352008962134,46.5350817169818,47.0349625377502,48.0347241792869,
49.0344858208236,50.0342474623603,51.034009103897,52.0337707454337,53.0335323869705,
53.5334132077388,54.0332940285072,55.0330556700439,56.0328173115806,57.0325789531173,
58.0323405946541,59.0321022361908,60.0318638777275,60.5317446984958,61.0316255192642,
62.0313871608009,63.0311488023376,64.0309104438743,65.0306720854111,66.0304337269478,
67.0301953684845,67.5300761892529,68.0299570100212,69.0297186515579,70.0294802930947,
71.0292419346314,72.0290035761681,73.0287652177048,74.0285268592415,74.5284076800099,
75.0282885007782,76.028050142315,77.0278117838517,78.0275734253884,79.0273350669251,
80.0270967084618,81.0268583499985,81.5267391707669,82.0266199915352,83.026381633072,
84.0261432746087,85.0259049161454,86.0256665576821,87.0254281992188,88.0251898407555,
88.5250706615239,89.0249514822923,90.024713123829,91.0244747653657,92.0242364069024,
93.0239980484391,94.0237596899758,95.0235213315126,95.5234021522809,96.0232829730493,
97.023044614586,98.0228062561227,99.0225678976594,100.022329539196,101.022091180733,
102.02185282227,102.521733643038,103.021614463806,104.021376105343,105.02113774688,
106.020899388416,107.020661029953,108.02042267149,109.020184313027,109.520065133795,
110.019945954563,111.0197075961,112.019469237637,113.019230879173,114.01899252071,
115.018754162247,116.018515803784,116.518396624552,117.01827744532,118.018039086857,
119.017800728394,120.01756236993,121.017324011467,122.017085653004,123.016847294541,
123.516728115309,124.016608936077,125.016370577614,126.016132219151,127.015893860688,
128.015655502224,129.015417143761,130.015178785298,130.515059606066,131.014940426834,
132.014702068371,133.014463709908,134.014225351445,135.013986992981,136.013748634518,
137.013510276055,137.513391096823,138.013271917591,139.013033559128,140.012795200665,
141.012556842202,142.012318483738,143.012080125275,144.011841766812,144.51172258758,
145.011603408348,146.011365049885,147.011126691422,148.010888332959,149.010649974495,
150.010411616032,151.010173257569,151.510054078337,152.009934899105,153.009696540642,
154.009458182179,155.009219823716,156.008981465252,157.008743106789,158.008504748326,
158.508385569094,159.008266389862,160.008028031399,161.007789672936,162.007551314473,
163.007312956009,164.007074597546,165.006836239083,165.506717059851,166.006597880619,
167.006359522156,168.006121163693,169.00588280523,170.005644446766,171.005406088303,
172.00516772984,172.505048550608,173.004929371376,174.004691012913,175.00445265445,
176.004214295987,177.003975937523,178.00373757906,179.003499220597,179.503380041365,
180.003260862133,181.00302250367,182.002784145207,183.002545786744,184.00230742828,
185.002069069817,186.001830711354,186.501711532122,187.001592352891,188.001353994427,
189.001115635964,190.000877277501,191.000638919037,192.000400560574,193.000162202111,
193.500043022879,193.999923843648,194.999685485184,195.999447126721,196.999208768258,
197.998970409794,198.998732051331,199.998493692868,200.498374513636,200.998255334405,
201.998016975941,202.997778617478,203.997540259015,204.997301900551,205.997063542088,
206.996825183625,207.496706004393,207.996586825162,208.996348466698,209.996110108235,
210.995871749772,211.995633391308,212.995395032845,213.995156674382,214.49503749515,
214.994918315919,215.994679957455,216.994441598992,217.994203240529,218.993964882065,
219.993726523602,220.993488165139,221.493368985907,221.993249806676,222.993011448212,
223.992773089749,224.992534731286,225.992296372822,226.992058014359,227.991819655896,
228.491700476664,228.991581297433,229.991342938969,230.991104580506,231.990866222043,
232.99062786358,233.990389505116,234.990151146653,235.490031967421,235.98991278819,
236.989674429726,237.989436071263,238.9891977128,239.988959354337,240.988720995873,
241.98848263741,242.488363458178,242.988244278947,243.988005920483,244.98776756202,
245.987529203557,246.987290845094,247.98705248663,248.986814128167,249.486694948935,
249.986575769704,250.98633741124,251.986099052777,252.985860694314,253.985622335851,
254.985383977387,255.985145618924,256.485026439692,256.984907260461,257.984668901997,
258.984430543534,259.984192185071,260.983953826608,261.983715468144,262.983477109681,
263.483357930449,263.983238751218,264.983000392754,265.982762034291,266.982523675828,
267.982285317365,268.982046958901,269.981808600438,270.481689421206,270.981570241975,
271.981331883511,272.981093525048,273.980855166585,274.980616808122,275.980378449658,
276.980140091195,277.480020911963,277.979901732732,278.979663374269,279.979425015805,
280.979186657342,281.978948298879,282.978709940415,283.978471581952,284.47835240272,
284.978233223489,285.977994865025,286.977756506562,287.977518148099,288.977279789636,
289.977041431172,290.976803072709,291.476683893477,291.976564714246,292.976326355783,
293.976087997319,294.975849638856,295.975611280393,296.975372921929,297.975134563466,
298.475015384234,298.974896205003,299.97465784654,300.974419488076,301.974181129613,
302.97394277115,303.973704412686,304.973466054223,305.473346874992,305.97322769576,
306.972989337297,307.972750978833,308.97251262037,309.972274261907,310.972035903443,
311.97179754498,312.471678365749,312.971559186517,313.971320828054,314.97108246959,
315.970844111127,316.970605752664,317.9703673942,318.970129035737,319.470009856505,
319.969890677274,320.969652318811,321.969413960347,322.969175601884,323.968937243421,
324.968698884957,325.968460526494,326.468341347263,326.968222168031,327.967983809568,
328.967745451104,329.967507092641,330.967268734178,331.967030375715,332.966792017251,
333.966553658788,334.966315300325,335.466196121093,335.966076941861,336.965838583398,
337.965600224935,338.965361866472,339.965123508008,340.964885149545,341.964646791082,
342.46452761185,342.964408432618,343.964170074155,344.963931715692,345.963693357229,
346.963454998765,347.963216640302,348.962978281839,349.462859102607,349.962739923375,
350.962501564912,351.962263206449,352.962024847986,353.961786489522,354.961548131059,
355.961309772596,356.461190593364,356.961071414132,357.960833055669,358.960594697206,
359.960356338743,360.960117980279,361.959879621816,362.959641263353,363.459522084121,
363.959402904889,364.959164546426,365.958926187963,366.9586878295,367.958449471036,
368.958211112573,369.95797275411,370.457853574878,370.957734395646,371.957496037183,
372.95725767872,373.957019320257,374.956780961793,375.95654260333,376.956304244867,
377.456185065635,377.956065886403,378.95582752794,379.955589169477,380.955350811014,
381.95511245255,382.954874094087,383.954635735624,384.454516556392,384.95439737716,
385.954159018697,386.953920660234,387.953682301771,388.953443943307,389.953205584844,
390.952967226381,391.452848047149,391.952728867918,392.952490509454,393.952252150991,
394.952013792528,395.951775434064,396.951537075601,397.951298717138,398.451179537906,
398.951060358675,399.950822000211,400.950583641748,401.950345283285,402.950106924821,
403.949868566358,404.949630207895,405.449511028663,405.949391849432,406.949153490968,
407.948915132505,408.948676774042,409.948438415578,410.948200057115,411.947961698652,
412.44784251942,412.947723340189,413.947484981725,414.947246623262,415.947008264799,
416.946769906335,417.946531547872,418.946293189409,419.446174010177,419.946054830946,
420.945816472482,421.945578114019,422.945339755556,423.945101397092,424.944863038629,
425.944624680166,426.444505500934,426.944386321703,427.944147963239,428.943909604776,
429.943671246313,430.943432887849,431.943194529386,432.942956170923,433.442836991691,
433.94271781246,434.942479453996,435.942241095533,436.94200273707,437.941764378606,
438.941526020143,439.94128766168,440.441168482448,440.941049303217,441.940810944753,
442.94057258629,443.940334227827,444.940095869364,445.9398575109,446.939619152437,
447.439499973205,447.939380793974,448.93914243551,449.938904077047,450.938665718584,
451.93842736012,452.938189001657,453.937950643194,454.437831463962,454.937712284731,
455.937473926267,456.937235567804,457.936997209341,458.936758850878,459.936520492414,
460.936282133951,461.436162954719,461.936043775488,462.935805417024,463.935567058561,
464.935328700098,465.935090341635,466.934851983171,467.934613624708,468.434494445476,
468.934375266245,469.934136907781,470.933898549318,471.933660190855,472.933421832392,
473.933183473928,474.932945115465,475.432825936233,475.932706757002,476.932468398538,
477.932230040075,478.931991681612,479.931753323149,480.931514964685,481.931276606222,
482.43115742699,482.931038247759,483.930799889295,484.930561530832,485.930323172369,
486.930084813906,487.929846455442,488.929608096979,489.429488917747,489.929369738516,
490.929131380052,491.928893021589,492.928654663126,493.928416304663,494.928177946199,
495.927939587736,496.427820408504,496.927701229273,497.92746287081,498.927224512346,
499.926986153883,500.92674779542,501.926509436956,502.926271078493,503.426151899261,
503.92603272003,504.925794361566,505.925556003103,506.92531764464,507.925079286177,
508.924840927713,509.92460256925,510.424483390018,510.924364210787,511.924125852324,
512.92388749386,513.923649135397,514.923410776934,515.92317241847,516.922934060007,
517.422814880775,517.922695701544,518.922457343081,519.922218984617,520.921980626154,
521.921742267691,522.921503909227,523.921265550764,524.421146371532,524.921027192301,
525.920788833837,526.920550475374,527.920312116911,528.920073758448,529.919835399984,
530.919597041521,531.419477862289,531.919358683058,532.919120324594,533.918881966131,
534.918643607668,535.918405249205,536.918166890741,537.917928532278,538.417809353046,
538.917690173815,539.917451815352,540.917213456888,541.916975098425,542.916736739962,
543.916498381498,544.916260023035,545.416140843804,545.916021664572,546.915783306109,
547.915544947645,548.915306589182,549.915068230719,550.914829872255,551.914591513792,
552.414472334561,552.914353155329,553.914114796866,554.913876438402,555.913638079939,
556.913399721476,557.913161363012,558.912923004549,559.412803825317,559.912684646086,
560.912446287623,561.912207929159,562.911969570696,563.911731212233,564.911492853769,
565.911254495306,566.411135316074,566.911016136843,567.91077777838,568.910539419916,
569.910301061453,570.91006270299,571.909824344526,572.909585986063,573.409466806832,
573.9093476276,574.909109269137,575.908870910673,576.90863255221,577.908394193747,
578.908155835284,579.90791747682,580.407798297589,580.907679118357,581.907440759894,
582.90720240143,583.906964042967,584.906725684504,585.906487326041,586.906248967577,
587.406129788346,587.906010609114,588.905772250651,589.905533892187,590.905295533724,
591.905057175261,592.904818816798,593.904580458334,594.404461279103,594.904342099871,
595.904103741408,596.903865382944,597.903627024481,598.903388666018,599.903150307555,
600.902911949091,601.40279276986,601.902673590628,602.902435232165,603.902196873701,
604.901958515238,605.901720156775,606.901481798312,607.901243439848,608.401124260617,
608.901005081385,609.900766722922,610.900528364458,611.900290005995,612.900051647532,
613.899813289069,614.899574930605,615.399455751374,615.899336572142,616.899098213679,
617.898859855216,618.898621496752,619.898383138289,620.898144779826,621.897906421362,
622.397787242131,622.897668062899,623.897429704436,624.897191345972,625.896952987509,
626.896714629046,627.896476270583,628.896237912119,629.396118732888,629.895999553656,
630.895761195193,631.895522836729,632.895284478266,633.895046119803,634.89480776134,
635.894569402876,636.394450223645,636.894331044413,637.89409268595,638.893854327487,
639.893615969023,640.89337761056,641.893139252097,642.393020072865,642.892900893633),
 .UNSPECIFIED.);
#68=B_SPLINE_SURFACE_WITH_KNOTS('',3,3,((#43587,#43588,#43589,#43590,#43591,
#43592,#43593,#43594,#43595,#43596,#43597,#43598,#43599,#43600,#43601,#43602,
#43603,#43604,#43605,#43606,#43607,#43608,#43609,#43610,#43611,#43612,#43613,
#43614,#43615,#43616,#43617,#43618,#43619,#43620,#43621,#43622,#43623,#43624,
#43625,#43626,#43627,#43628,#43629,#43630,#43631,#43632,#43633,#43634,#43635,
#43636,#43637,#43638,#43639,#43640,#43641,#43642,#43643,#43644,#43645,#43646,
#43647,#43648,#43649,#43650,#43651,#43652,#43653,#43654,#43655,#43656,#43657,
#43658,#43659,#43660,#43661,#43662,#43663,#43664,#43665,#43666,#43667,#43668,
#43669,#43670,#43671,#43672,#43673,#43674,#43675,#43676,#43677,#43678,#43679,
#43680,#43681,#43682,#43683,#43684,#43685,#43686,#43687,#43688,#43689,#43690,
#43691,#43692,#43693,#43694,#43695,#43696,#43697,#43698,#43699,#43700,#43701,
#43702,#43703,#43704,#43705,#43706,#43707,#43708,#43709,#43710,#43711,#43712,
#43713),(#43714,#43715,#43716,#43717,#43718,#43719,#43720,#43721,#43722,
#43723,#43724,#43725,#43726,#43727,#43728,#43729,#43730,#43731,#43732,#43733,
#43734,#43735,#43736,#43737,#43738,#43739,#43740,#43741,#43742,#43743,#43744,
#43745,#43746,#43747,#43748,#43749,#43750,#43751,#43752,#43753,#43754,#43755,
#43756,#43757,#43758,#43759,#43760,#43761,#43762,#43763,#43764,#43765,#43766,
#43767,#43768,#43769,#43770,#43771,#43772,#43773,#43774,#43775,#43776,#43777,
#43778,#43779,#43780,#43781,#43782,#43783,#43784,#43785,#43786,#43787,#43788,
#43789,#43790,#43791,#43792,#43793,#43794,#43795,#43796,#43797,#43798,#43799,
#43800,#43801,#43802,#43803,#43804,#43805,#43806,#43807,#43808,#43809,#43810,
#43811,#43812,#43813,#43814,#43815,#43816,#43817,#43818,#43819,#43820,#43821,
#43822,#43823,#43824,#43825,#43826,#43827,#43828,#43829,#43830,#43831,#43832,
#43833,#43834,#43835,#43836,#43837,#43838,#43839,#43840),(#43841,#43842,
#43843,#43844,#43845,#43846,#43847,#43848,#43849,#43850,#43851,#43852,#43853,
#43854,#43855,#43856,#43857,#43858,#43859,#43860,#43861,#43862,#43863,#43864,
#43865,#43866,#43867,#43868,#43869,#43870,#43871,#43872,#43873,#43874,#43875,
#43876,#43877,#43878,#43879,#43880,#43881,#43882,#43883,#43884,#43885,#43886,
#43887,#43888,#43889,#43890,#43891,#43892,#43893,#43894,#43895,#43896,#43897,
#43898,#43899,#43900,#43901,#43902,#43903,#43904,#43905,#43906,#43907,#43908,
#43909,#43910,#43911,#43912,#43913,#43914,#43915,#43916,#43917,#43918,#43919,
#43920,#43921,#43922,#43923,#43924,#43925,#43926,#43927,#43928,#43929,#43930,
#43931,#43932,#43933,#43934,#43935,#43936,#43937,#43938,#43939,#43940,#43941,
#43942,#43943,#43944,#43945,#43946,#43947,#43948,#43949,#43950,#43951,#43952,
#43953,#43954,#43955,#43956,#43957,#43958,#43959,#43960,#43961,#43962,#43963,
#43964,#43965,#43966,#43967),(#43968,#43969,#43970,#43971,#43972,#43973,
#43974,#43975,#43976,#43977,#43978,#43979,#43980,#43981,#43982,#43983,#43984,
#43985,#43986,#43987,#43988,#43989,#43990,#43991,#43992,#43993,#43994,#43995,
#43996,#43997,#43998,#43999,#44000,#44001,#44002,#44003,#44004,#44005,#44006,
#44007,#44008,#44009,#44010,#44011,#44012,#44013,#44014,#44015,#44016,#44017,
#44018,#44019,#44020,#44021,#44022,#44023,#44024,#44025,#44026,#44027,#44028,
#44029,#44030,#44031,#44032,#44033,#44034,#44035,#44036,#44037,#44038,#44039,
#44040,#44041,#44042,#44043,#44044,#44045,#44046,#44047,#44048,#44049,#44050,
#44051,#44052,#44053,#44054,#44055,#44056,#44057,#44058,#44059,#44060,#44061,
#44062,#44063,#44064,#44065,#44066,#44067,#44068,#44069,#44070,#44071,#44072,
#44073,#44074,#44075,#44076,#44077,#44078,#44079,#44080,#44081,#44082,#44083,
#44084,#44085,#44086,#44087,#44088,#44089,#44090,#44091,#44092,#44093,#44094)),
 .UNSPECIFIED.,.F.,.F.,.F.,(4,4),(4,1,1,1,1,1,1,1,1,1,1,1,1,1,1,1,1,1,1,
1,1,1,1,1,1,1,1,1,1,1,1,1,1,1,1,1,1,1,1,1,1,1,1,1,1,1,1,1,1,1,1,1,1,1,1,
1,1,1,1,1,1,1,1,1,1,1,1,1,1,1,1,1,1,1,1,1,1,1,1,1,1,1,1,1,1,1,1,1,1,1,1,
1,1,1,1,1,1,1,1,1,1,1,1,1,1,1,1,1,1,1,1,1,1,1,1,1,1,1,1,1,1,1,1,1,4),(-0.0117202104645729,
2.30765714068266E-14),(13.9661186601203,14.4600465471847,14.9539744342492,
15.4479023213137,15.9418302083782,16.4357580954427,16.9296859825072,17.4236138695716,
17.9175417566361,18.4114696437006,18.9053975307651,19.3993254178296,19.893253304894,
20.3871811919585,20.881109079023,21.3750369660875,21.868964853152,22.3628927402165,
22.8568206272809,23.3507485143454,23.8446764014099,24.3386042884744,24.8325321755389,
25.3264600626033,25.8203879496678,26.3143158367323,26.8082437237968,27.3021716108613,
27.7960994979258,28.2900273849902,28.7839552720547,29.2778831591192,29.7718110461837,
30.2657389332482,30.7596668203126,31.2535947073771,31.7475225944416,32.2414504815061,
32.7353783685706,33.2293062556351,33.7232341426995,34.217162029764,34.7110899168285,
35.205017803893,35.6989456909575,36.1928735780219,36.6868014650864,37.1807293521509,
37.6746572392154,38.1685851262799,38.6625130133444,39.1564409004088,39.6503687874733,
40.1442966745378,40.6382245616023,41.1321524486668,41.6260803357312,42.1200082227957,
42.6139361098602,43.1078639969247,43.6017918839892,44.0957197710537,44.5896476581181,
45.0835755451826,45.5775034322471,46.0714313193116,46.5653592063761,47.0592870934405,
47.553214980505,48.0471428675695,48.541070754634,49.0349986416985,49.528926528763,
50.0228544158274,50.5167823028919,51.0107101899564,51.5046380770209,51.9985659640854,
52.4924938511499,52.9864217382143,53.4803496252788,53.9742775123433,54.4682053994078,
54.9621332864723,55.4560611735367,55.9499890606012,56.4439169476657,56.9378448347302,
57.4317727217947,57.9257006088591,58.4196284959236,58.9135563829881,59.4074842700526,
59.9014121571171,60.3953400441816,60.889267931246,61.3831958183105,61.877123705375,
62.3710515924395,62.864979479504,63.3589073665685,63.8528352536329,64.3467631406974,
64.8406910277619,65.3346189148264,65.8285468018909,66.3224746889554,66.8164025760198,
67.3103304630843,67.8042583501488,68.2981862372133,68.7921141242778,69.2860420113422,
69.7799698984067,70.2738977854712,70.7678256725357,71.2617535596002,71.7556814466647,
72.2496093337291,72.7435372207936,73.2374651078581,73.7313929949226,74.2253208819871,
74.7192487690515,75.213176656116),.UNSPECIFIED.);
#69=B_SPLINE_SURFACE_WITH_KNOTS('',3,3,((#44151,#44152,#44153,#44154,#44155,
#44156,#44157,#44158,#44159,#44160,#44161,#44162,#44163,#44164,#44165,#44166,
#44167,#44168,#44169,#44170,#44171,#44172,#44173,#44174,#44175,#44176,#44177,
#44178,#44179,#44180,#44181,#44182,#44183,#44184,#44185,#44186,#44187,#44188,
#44189,#44190,#44191,#44192,#44193,#44194,#44195,#44196,#44197,#44198,#44199,
#44200,#44201,#44202,#44203,#44204,#44205,#44206,#44207,#44208,#44209,#44210,
#44211,#44212,#44213,#44214,#44215,#44216,#44217,#44218,#44219,#44220,#44221,
#44222,#44223,#44224,#44225,#44226,#44227,#44228,#44229,#44230,#44231,#44232,
#44233,#44234,#44235,#44236,#44237,#44238,#44239,#44240,#44241,#44242,#44243,
#44244,#44245,#44246,#44247,#44248,#44249,#44250,#44251,#44252,#44253,#44254,
#44255,#44256,#44257,#44258,#44259,#44260,#44261,#44262,#44263,#44264,#44265,
#44266,#44267,#44268,#44269,#44270,#44271,#44272,#44273,#44274,#44275,#44276,
#44277),(#44278,#44279,#44280,#44281,#44282,#44283,#44284,#44285,#44286,
#44287,#44288,#44289,#44290,#44291,#44292,#44293,#44294,#44295,#44296,#44297,
#44298,#44299,#44300,#44301,#44302,#44303,#44304,#44305,#44306,#44307,#44308,
#44309,#44310,#44311,#44312,#44313,#44314,#44315,#44316,#44317,#44318,#44319,
#44320,#44321,#44322,#44323,#44324,#44325,#44326,#44327,#44328,#44329,#44330,
#44331,#44332,#44333,#44334,#44335,#44336,#44337,#44338,#44339,#44340,#44341,
#44342,#44343,#44344,#44345,#44346,#44347,#44348,#44349,#44350,#44351,#44352,
#44353,#44354,#44355,#44356,#44357,#44358,#44359,#44360,#44361,#44362,#44363,
#44364,#44365,#44366,#44367,#44368,#44369,#44370,#44371,#44372,#44373,#44374,
#44375,#44376,#44377,#44378,#44379,#44380,#44381,#44382,#44383,#44384,#44385,
#44386,#44387,#44388,#44389,#44390,#44391,#44392,#44393,#44394,#44395,#44396,
#44397,#44398,#44399,#44400,#44401,#44402,#44403,#44404),(#44405,#44406,
#44407,#44408,#44409,#44410,#44411,#44412,#44413,#44414,#44415,#44416,#44417,
#44418,#44419,#44420,#44421,#44422,#44423,#44424,#44425,#44426,#44427,#44428,
#44429,#44430,#44431,#44432,#44433,#44434,#44435,#44436,#44437,#44438,#44439,
#44440,#44441,#44442,#44443,#44444,#44445,#44446,#44447,#44448,#44449,#44450,
#44451,#44452,#44453,#44454,#44455,#44456,#44457,#44458,#44459,#44460,#44461,
#44462,#44463,#44464,#44465,#44466,#44467,#44468,#44469,#44470,#44471,#44472,
#44473,#44474,#44475,#44476,#44477,#44478,#44479,#44480,#44481,#44482,#44483,
#44484,#44485,#44486,#44487,#44488,#44489,#44490,#44491,#44492,#44493,#44494,
#44495,#44496,#44497,#44498,#44499,#44500,#44501,#44502,#44503,#44504,#44505,
#44506,#44507,#44508,#44509,#44510,#44511,#44512,#44513,#44514,#44515,#44516,
#44517,#44518,#44519,#44520,#44521,#44522,#44523,#44524,#44525,#44526,#44527,
#44528,#44529,#44530,#44531),(#44532,#44533,#44534,#44535,#44536,#44537,
#44538,#44539,#44540,#44541,#44542,#44543,#44544,#44545,#44546,#44547,#44548,
#44549,#44550,#44551,#44552,#44553,#44554,#44555,#44556,#44557,#44558,#44559,
#44560,#44561,#44562,#44563,#44564,#44565,#44566,#44567,#44568,#44569,#44570,
#44571,#44572,#44573,#44574,#44575,#44576,#44577,#44578,#44579,#44580,#44581,
#44582,#44583,#44584,#44585,#44586,#44587,#44588,#44589,#44590,#44591,#44592,
#44593,#44594,#44595,#44596,#44597,#44598,#44599,#44600,#44601,#44602,#44603,
#44604,#44605,#44606,#44607,#44608,#44609,#44610,#44611,#44612,#44613,#44614,
#44615,#44616,#44617,#44618,#44619,#44620,#44621,#44622,#44623,#44624,#44625,
#44626,#44627,#44628,#44629,#44630,#44631,#44632,#44633,#44634,#44635,#44636,
#44637,#44638,#44639,#44640,#44641,#44642,#44643,#44644,#44645,#44646,#44647,
#44648,#44649,#44650,#44651,#44652,#44653,#44654,#44655,#44656,#44657,#44658)),
 .UNSPECIFIED.,.F.,.F.,.F.,(4,4),(4,1,1,1,1,1,1,1,1,1,1,1,1,1,1,1,1,1,1,
1,1,1,1,1,1,1,1,1,1,1,1,1,1,1,1,1,1,1,1,1,1,1,1,1,1,1,1,1,1,1,1,1,1,1,1,
1,1,1,1,1,1,1,1,1,1,1,1,1,1,1,1,1,1,1,1,1,1,1,1,1,1,1,1,1,1,1,1,1,1,1,1,
1,1,1,1,1,1,1,1,1,1,1,1,1,1,1,1,1,1,1,1,1,1,1,1,1,1,1,1,1,1,1,1,1,4),(0.115296848757141,
0.127017059221739),(14.9954123969612,15.4893404554446,15.9832685139281,
16.4771965724115,16.9711246308949,17.4650526893783,17.9589807478618,18.4529088063452,
18.9468368648286,19.440764923312,19.9346929817954,20.4286210402789,20.9225490987623,
21.4164771572457,21.9104052157291,22.4043332742125,22.898261332696,23.3921893911794,
23.8861174496628,24.3800455081462,24.8739735666297,25.3679016251131,25.8618296835965,
26.3557577420799,26.8496858005633,27.3436138590468,27.8375419175302,28.3314699760136,
28.825398034497,29.3193260929804,29.8132541514639,30.3071822099473,30.8011102684307,
31.2950383269141,31.7889663853976,32.282894443881,32.7768225023644,33.2707505608478,
33.7646786193312,34.2586066778147,34.7525347362981,35.2464627947815,35.7403908532649,
36.2343189117483,36.7282469702318,37.2221750287152,37.7161030871986,38.210031145682,
38.7039592041655,39.1978872626489,39.6918153211323,40.1857433796157,40.6796714380991,
41.1735994965826,41.667527555066,42.1614556135494,42.6553836720328,43.1493117305162,
43.6432397889997,44.1371678474831,44.6310959059665,45.1250239644499,45.6189520229333,
46.1128800814168,46.6068081399002,47.1007361983836,47.594664256867,48.0885923153505,
48.5825203738339,49.0764484323173,49.5703764908007,50.0643045492841,50.5582326077676,
51.052160666251,51.5460887247344,52.0400167832178,52.5339448417012,53.0278729001847,
53.5218009586681,54.0157290171515,54.5096570756349,55.0035851341184,55.4975131926018,
55.9914412510852,56.4853693095686,56.979297368052,57.4732254265355,57.9671534850189,
58.4610815435023,58.9550096019857,59.4489376604691,59.9428657189526,60.436793777436,
60.9307218359194,61.4246498944028,61.9185779528863,62.4125060113697,62.9064340698531,
63.4003621283365,63.8942901868199,64.3882182453034,64.8821463037868,65.3760743622702,
65.8700024207536,66.363930479237,66.8578585377205,67.3517865962039,67.8457146546873,
68.3396427131707,68.8335707716542,69.3274988301376,69.821426888621,70.3153549471044,
70.8092830055878,71.3032110640713,71.7971391225547,72.2910671810381,72.7849952395215,
73.2789232980049,73.7728513564884,74.2667794149718,74.7607074734552,75.2546355319386,
75.748563590422,76.2424916489055),.UNSPECIFIED.);
#70=B_SPLINE_SURFACE_WITH_KNOTS('',3,3,((#44719,#44720,#44721,#44722,#44723,
#44724,#44725,#44726,#44727,#44728,#44729,#44730,#44731,#44732,#44733,#44734,
#44735,#44736,#44737,#44738,#44739,#44740,#44741,#44742,#44743,#44744,#44745,
#44746,#44747,#44748,#44749,#44750,#44751,#44752,#44753,#44754,#44755,#44756,
#44757,#44758,#44759,#44760,#44761,#44762,#44763,#44764,#44765,#44766,#44767,
#44768,#44769,#44770,#44771,#44772,#44773,#44774,#44775,#44776,#44777,#44778,
#44779,#44780,#44781,#44782,#44783,#44784,#44785,#44786,#44787,#44788,#44789,
#44790,#44791,#44792,#44793,#44794,#44795,#44796,#44797,#44798,#44799,#44800,
#44801,#44802,#44803,#44804,#44805,#44806,#44807,#44808,#44809,#44810,#44811,
#44812,#44813,#44814,#44815,#44816,#44817,#44818,#44819,#44820,#44821,#44822,
#44823,#44824,#44825,#44826,#44827,#44828,#44829,#44830,#44831,#44832,#44833,
#44834,#44835,#44836,#44837,#44838,#44839,#44840,#44841,#44842,#44843,#44844,
#44845,#44846,#44847,#44848,#44849,#44850,#44851,#44852,#44853,#44854,#44855,
#44856,#44857,#44858,#44859,#44860,#44861,#44862,#44863,#44864,#44865,#44866,
#44867,#44868,#44869,#44870,#44871,#44872,#44873,#44874,#44875,#44876,#44877,
#44878,#44879,#44880,#44881,#44882,#44883,#44884,#44885,#44886,#44887,#44888,
#44889,#44890,#44891,#44892,#44893,#44894,#44895,#44896,#44897,#44898,#44899,
#44900,#44901,#44902,#44903,#44904,#44905,#44906,#44907,#44908,#44909,#44910,
#44911,#44912,#44913,#44914,#44915,#44916,#44917,#44918,#44919,#44920,#44921,
#44922,#44923,#44924,#44925,#44926,#44927,#44928,#44929,#44930,#44931,#44932,
#44933,#44934,#44935,#44936,#44937,#44938,#44939,#44940,#44941,#44942,#44943,
#44944,#44945,#44946,#44947,#44948,#44949,#44950,#44951,#44952,#44953,#44954,
#44955,#44956,#44957,#44958,#44959,#44960,#44961,#44962,#44963,#44964,#44965,
#44966,#44967,#44968,#44969,#44970,#44971,#44972,#44973,#44974,#44975,#44976,
#44977,#44978,#44979,#44980,#44981,#44982,#44983,#44984,#44985,#44986,#44987,
#44988,#44989,#44990,#44991,#44992,#44993,#44994,#44995,#44996,#44997,#44998,
#44999,#45000,#45001,#45002,#45003,#45004,#45005,#45006,#45007,#45008,#45009,
#45010,#45011,#45012,#45013,#45014,#45015,#45016,#45017,#45018,#45019,#45020,
#45021,#45022,#45023,#45024,#45025,#45026,#45027,#45028,#45029,#45030,#45031,
#45032,#45033,#45034,#45035,#45036,#45037,#45038,#45039,#45040,#45041,#45042,
#45043,#45044,#45045,#45046,#45047,#45048,#45049,#45050,#45051,#45052,#45053,
#45054,#45055,#45056,#45057,#45058,#45059,#45060,#45061,#45062,#45063,#45064,
#45065,#45066,#45067,#45068,#45069,#45070,#45071,#45072,#45073,#45074,#45075,
#45076,#45077,#45078,#45079,#45080,#45081,#45082,#45083,#45084,#45085,#45086,
#45087,#45088,#45089,#45090,#45091,#45092,#45093,#45094,#45095,#45096,#45097,
#45098,#45099,#45100,#45101,#45102,#45103,#45104,#45105,#45106,#45107,#45108,
#45109,#45110,#45111,#45112,#45113,#45114,#45115,#45116,#45117,#45118,#45119,
#45120,#45121,#45122,#45123,#45124,#45125,#45126,#45127,#45128,#45129,#45130,
#45131,#45132,#45133,#45134,#45135,#45136,#45137,#45138,#45139,#45140,#45141,
#45142,#45143,#45144,#45145,#45146,#45147,#45148,#45149,#45150,#45151,#45152,
#45153,#45154,#45155,#45156,#45157,#45158,#45159,#45160,#45161,#45162,#45163,
#45164,#45165,#45166,#45167,#45168,#45169,#45170,#45171,#45172,#45173,#45174,
#45175,#45176,#45177,#45178,#45179,#45180,#45181,#45182,#45183,#45184,#45185,
#45186,#45187,#45188,#45189,#45190,#45191,#45192,#45193,#45194,#45195,#45196,
#45197,#45198,#45199,#45200,#45201,#45202,#45203,#45204,#45205,#45206,#45207,
#45208,#45209,#45210,#45211,#45212,#45213,#45214,#45215,#45216,#45217,#45218,
#45219,#45220,#45221,#45222,#45223,#45224,#45225,#45226,#45227,#45228,#45229,
#45230,#45231,#45232,#45233,#45234,#45235,#45236,#45237,#45238,#45239,#45240,
#45241,#45242,#45243,#45244,#45245,#45246,#45247,#45248,#45249,#45250,#45251,
#45252,#45253,#45254,#45255,#45256,#45257,#45258,#45259,#45260,#45261,#45262,
#45263,#45264,#45265,#45266,#45267,#45268,#45269,#45270,#45271,#45272,#45273,
#45274,#45275,#45276,#45277,#45278,#45279,#45280,#45281,#45282,#45283,#45284,
#45285,#45286,#45287,#45288,#45289,#45290,#45291,#45292,#45293,#45294,#45295,
#45296,#45297,#45298,#45299,#45300,#45301,#45302,#45303,#45304,#45305,#45306,
#45307,#45308,#45309,#45310,#45311,#45312,#45313,#45314,#45315,#45316,#45317,
#45318,#45319,#45320,#45321,#45322,#45323,#45324,#45325,#45326,#45327,#45328,
#45329,#45330,#45331,#45332,#45333,#45334,#45335,#45336,#45337,#45338,#45339,
#45340,#45341,#45342,#45343,#45344,#45345,#45346,#45347,#45348,#45349,#45350,
#45351,#45352,#45353,#45354,#45355,#45356,#45357,#45358,#45359,#45360,#45361,
#45362,#45363,#45364,#45365,#45366,#45367,#45368,#45369,#45370,#45371,#45372,
#45373,#45374,#45375,#45376,#45377,#45378,#45379,#45380,#45381,#45382,#45383,
#45384,#45385,#45386,#45387,#45388,#45389,#45390,#45391,#45392,#45393,#45394,
#45395,#45396,#45397,#45398,#45399,#45400,#45401,#45402,#45403,#45404,#45405,
#45406,#45407,#45408,#45409,#45410,#45411,#45412,#45413,#45414,#45415,#45416,
#45417,#45418,#45419,#45420,#45421,#45422,#45423,#45424,#45425,#45426,#45427,
#45428,#45429,#45430,#45431,#45432,#45433,#45434,#45435,#45436,#45437,#45438,
#45439,#45440,#45441,#45442,#45443),(#45444,#45445,#45446,#45447,#45448,
#45449,#45450,#45451,#45452,#45453,#45454,#45455,#45456,#45457,#45458,#45459,
#45460,#45461,#45462,#45463,#45464,#45465,#45466,#45467,#45468,#45469,#45470,
#45471,#45472,#45473,#45474,#45475,#45476,#45477,#45478,#45479,#45480,#45481,
#45482,#45483,#45484,#45485,#45486,#45487,#45488,#45489,#45490,#45491,#45492,
#45493,#45494,#45495,#45496,#45497,#45498,#45499,#45500,#45501,#45502,#45503,
#45504,#45505,#45506,#45507,#45508,#45509,#45510,#45511,#45512,#45513,#45514,
#45515,#45516,#45517,#45518,#45519,#45520,#45521,#45522,#45523,#45524,#45525,
#45526,#45527,#45528,#45529,#45530,#45531,#45532,#45533,#45534,#45535,#45536,
#45537,#45538,#45539,#45540,#45541,#45542,#45543,#45544,#45545,#45546,#45547,
#45548,#45549,#45550,#45551,#45552,#45553,#45554,#45555,#45556,#45557,#45558,
#45559,#45560,#45561,#45562,#45563,#45564,#45565,#45566,#45567,#45568,#45569,
#45570,#45571,#45572,#45573,#45574,#45575,#45576,#45577,#45578,#45579,#45580,
#45581,#45582,#45583,#45584,#45585,#45586,#45587,#45588,#45589,#45590,#45591,
#45592,#45593,#45594,#45595,#45596,#45597,#45598,#45599,#45600,#45601,#45602,
#45603,#45604,#45605,#45606,#45607,#45608,#45609,#45610,#45611,#45612,#45613,
#45614,#45615,#45616,#45617,#45618,#45619,#45620,#45621,#45622,#45623,#45624,
#45625,#45626,#45627,#45628,#45629,#45630,#45631,#45632,#45633,#45634,#45635,
#45636,#45637,#45638,#45639,#45640,#45641,#45642,#45643,#45644,#45645,#45646,
#45647,#45648,#45649,#45650,#45651,#45652,#45653,#45654,#45655,#45656,#45657,
#45658,#45659,#45660,#45661,#45662,#45663,#45664,#45665,#45666,#45667,#45668,
#45669,#45670,#45671,#45672,#45673,#45674,#45675,#45676,#45677,#45678,#45679,
#45680,#45681,#45682,#45683,#45684,#45685,#45686,#45687,#45688,#45689,#45690,
#45691,#45692,#45693,#45694,#45695,#45696,#45697,#45698,#45699,#45700,#45701,
#45702,#45703,#45704,#45705,#45706,#45707,#45708,#45709,#45710,#45711,#45712,
#45713,#45714,#45715,#45716,#45717,#45718,#45719,#45720,#45721,#45722,#45723,
#45724,#45725,#45726,#45727,#45728,#45729,#45730,#45731,#45732,#45733,#45734,
#45735,#45736,#45737,#45738,#45739,#45740,#45741,#45742,#45743,#45744,#45745,
#45746,#45747,#45748,#45749,#45750,#45751,#45752,#45753,#45754,#45755,#45756,
#45757,#45758,#45759,#45760,#45761,#45762,#45763,#45764,#45765,#45766,#45767,
#45768,#45769,#45770,#45771,#45772,#45773,#45774,#45775,#45776,#45777,#45778,
#45779,#45780,#45781,#45782,#45783,#45784,#45785,#45786,#45787,#45788,#45789,
#45790,#45791,#45792,#45793,#45794,#45795,#45796,#45797,#45798,#45799,#45800,
#45801,#45802,#45803,#45804,#45805,#45806,#45807,#45808,#45809,#45810,#45811,
#45812,#45813,#45814,#45815,#45816,#45817,#45818,#45819,#45820,#45821,#45822,
#45823,#45824,#45825,#45826,#45827,#45828,#45829,#45830,#45831,#45832,#45833,
#45834,#45835,#45836,#45837,#45838,#45839,#45840,#45841,#45842,#45843,#45844,
#45845,#45846,#45847,#45848,#45849,#45850,#45851,#45852,#45853,#45854,#45855,
#45856,#45857,#45858,#45859,#45860,#45861,#45862,#45863,#45864,#45865,#45866,
#45867,#45868,#45869,#45870,#45871,#45872,#45873,#45874,#45875,#45876,#45877,
#45878,#45879,#45880,#45881,#45882,#45883,#45884,#45885,#45886,#45887,#45888,
#45889,#45890,#45891,#45892,#45893,#45894,#45895,#45896,#45897,#45898,#45899,
#45900,#45901,#45902,#45903,#45904,#45905,#45906,#45907,#45908,#45909,#45910,
#45911,#45912,#45913,#45914,#45915,#45916,#45917,#45918,#45919,#45920,#45921,
#45922,#45923,#45924,#45925,#45926,#45927,#45928,#45929,#45930,#45931,#45932,
#45933,#45934,#45935,#45936,#45937,#45938,#45939,#45940,#45941,#45942,#45943,
#45944,#45945,#45946,#45947,#45948,#45949,#45950,#45951,#45952,#45953,#45954,
#45955,#45956,#45957,#45958,#45959,#45960,#45961,#45962,#45963,#45964,#45965,
#45966,#45967,#45968,#45969,#45970,#45971,#45972,#45973,#45974,#45975,#45976,
#45977,#45978,#45979,#45980,#45981,#45982,#45983,#45984,#45985,#45986,#45987,
#45988,#45989,#45990,#45991,#45992,#45993,#45994,#45995,#45996,#45997,#45998,
#45999,#46000,#46001,#46002,#46003,#46004,#46005,#46006,#46007,#46008,#46009,
#46010,#46011,#46012,#46013,#46014,#46015,#46016,#46017,#46018,#46019,#46020,
#46021,#46022,#46023,#46024,#46025,#46026,#46027,#46028,#46029,#46030,#46031,
#46032,#46033,#46034,#46035,#46036,#46037,#46038,#46039,#46040,#46041,#46042,
#46043,#46044,#46045,#46046,#46047,#46048,#46049,#46050,#46051,#46052,#46053,
#46054,#46055,#46056,#46057,#46058,#46059,#46060,#46061,#46062,#46063,#46064,
#46065,#46066,#46067,#46068,#46069,#46070,#46071,#46072,#46073,#46074,#46075,
#46076,#46077,#46078,#46079,#46080,#46081,#46082,#46083,#46084,#46085,#46086,
#46087,#46088,#46089,#46090,#46091,#46092,#46093,#46094,#46095,#46096,#46097,
#46098,#46099,#46100,#46101,#46102,#46103,#46104,#46105,#46106,#46107,#46108,
#46109,#46110,#46111,#46112,#46113,#46114,#46115,#46116,#46117,#46118,#46119,
#46120,#46121,#46122,#46123,#46124,#46125,#46126,#46127,#46128,#46129,#46130,
#46131,#46132,#46133,#46134,#46135,#46136,#46137,#46138,#46139,#46140,#46141,
#46142,#46143,#46144,#46145,#46146,#46147,#46148,#46149,#46150,#46151,#46152,
#46153,#46154,#46155,#46156,#46157,#46158,#46159,#46160,#46161,#46162,#46163,
#46164,#46165,#46166,#46167,#46168),(#46169,#46170,#46171,#46172,#46173,
#46174,#46175,#46176,#46177,#46178,#46179,#46180,#46181,#46182,#46183,#46184,
#46185,#46186,#46187,#46188,#46189,#46190,#46191,#46192,#46193,#46194,#46195,
#46196,#46197,#46198,#46199,#46200,#46201,#46202,#46203,#46204,#46205,#46206,
#46207,#46208,#46209,#46210,#46211,#46212,#46213,#46214,#46215,#46216,#46217,
#46218,#46219,#46220,#46221,#46222,#46223,#46224,#46225,#46226,#46227,#46228,
#46229,#46230,#46231,#46232,#46233,#46234,#46235,#46236,#46237,#46238,#46239,
#46240,#46241,#46242,#46243,#46244,#46245,#46246,#46247,#46248,#46249,#46250,
#46251,#46252,#46253,#46254,#46255,#46256,#46257,#46258,#46259,#46260,#46261,
#46262,#46263,#46264,#46265,#46266,#46267,#46268,#46269,#46270,#46271,#46272,
#46273,#46274,#46275,#46276,#46277,#46278,#46279,#46280,#46281,#46282,#46283,
#46284,#46285,#46286,#46287,#46288,#46289,#46290,#46291,#46292,#46293,#46294,
#46295,#46296,#46297,#46298,#46299,#46300,#46301,#46302,#46303,#46304,#46305,
#46306,#46307,#46308,#46309,#46310,#46311,#46312,#46313,#46314,#46315,#46316,
#46317,#46318,#46319,#46320,#46321,#46322,#46323,#46324,#46325,#46326,#46327,
#46328,#46329,#46330,#46331,#46332,#46333,#46334,#46335,#46336,#46337,#46338,
#46339,#46340,#46341,#46342,#46343,#46344,#46345,#46346,#46347,#46348,#46349,
#46350,#46351,#46352,#46353,#46354,#46355,#46356,#46357,#46358,#46359,#46360,
#46361,#46362,#46363,#46364,#46365,#46366,#46367,#46368,#46369,#46370,#46371,
#46372,#46373,#46374,#46375,#46376,#46377,#46378,#46379,#46380,#46381,#46382,
#46383,#46384,#46385,#46386,#46387,#46388,#46389,#46390,#46391,#46392,#46393,
#46394,#46395,#46396,#46397,#46398,#46399,#46400,#46401,#46402,#46403,#46404,
#46405,#46406,#46407,#46408,#46409,#46410,#46411,#46412,#46413,#46414,#46415,
#46416,#46417,#46418,#46419,#46420,#46421,#46422,#46423,#46424,#46425,#46426,
#46427,#46428,#46429,#46430,#46431,#46432,#46433,#46434,#46435,#46436,#46437,
#46438,#46439,#46440,#46441,#46442,#46443,#46444,#46445,#46446,#46447,#46448,
#46449,#46450,#46451,#46452,#46453,#46454,#46455,#46456,#46457,#46458,#46459,
#46460,#46461,#46462,#46463,#46464,#46465,#46466,#46467,#46468,#46469,#46470,
#46471,#46472,#46473,#46474,#46475,#46476,#46477,#46478,#46479,#46480,#46481,
#46482,#46483,#46484,#46485,#46486,#46487,#46488,#46489,#46490,#46491,#46492,
#46493,#46494,#46495,#46496,#46497,#46498,#46499,#46500,#46501,#46502,#46503,
#46504,#46505,#46506,#46507,#46508,#46509,#46510,#46511,#46512,#46513,#46514,
#46515,#46516,#46517,#46518,#46519,#46520,#46521,#46522,#46523,#46524,#46525,
#46526,#46527,#46528,#46529,#46530,#46531,#46532,#46533,#46534,#46535,#46536,
#46537,#46538,#46539,#46540,#46541,#46542,#46543,#46544,#46545,#46546,#46547,
#46548,#46549,#46550,#46551,#46552,#46553,#46554,#46555,#46556,#46557,#46558,
#46559,#46560,#46561,#46562,#46563,#46564,#46565,#46566,#46567,#46568,#46569,
#46570,#46571,#46572,#46573,#46574,#46575,#46576,#46577,#46578,#46579,#46580,
#46581,#46582,#46583,#46584,#46585,#46586,#46587,#46588,#46589,#46590,#46591,
#46592,#46593,#46594,#46595,#46596,#46597,#46598,#46599,#46600,#46601,#46602,
#46603,#46604,#46605,#46606,#46607,#46608,#46609,#46610,#46611,#46612,#46613,
#46614,#46615,#46616,#46617,#46618,#46619,#46620,#46621,#46622,#46623,#46624,
#46625,#46626,#46627,#46628,#46629,#46630,#46631,#46632,#46633,#46634,#46635,
#46636,#46637,#46638,#46639,#46640,#46641,#46642,#46643,#46644,#46645,#46646,
#46647,#46648,#46649,#46650,#46651,#46652,#46653,#46654,#46655,#46656,#46657,
#46658,#46659,#46660,#46661,#46662,#46663,#46664,#46665,#46666,#46667,#46668,
#46669,#46670,#46671,#46672,#46673,#46674,#46675,#46676,#46677,#46678,#46679,
#46680,#46681,#46682,#46683,#46684,#46685,#46686,#46687,#46688,#46689,#46690,
#46691,#46692,#46693,#46694,#46695,#46696,#46697,#46698,#46699,#46700,#46701,
#46702,#46703,#46704,#46705,#46706,#46707,#46708,#46709,#46710,#46711,#46712,
#46713,#46714,#46715,#46716,#46717,#46718,#46719,#46720,#46721,#46722,#46723,
#46724,#46725,#46726,#46727,#46728,#46729,#46730,#46731,#46732,#46733,#46734,
#46735,#46736,#46737,#46738,#46739,#46740,#46741,#46742,#46743,#46744,#46745,
#46746,#46747,#46748,#46749,#46750,#46751,#46752,#46753,#46754,#46755,#46756,
#46757,#46758,#46759,#46760,#46761,#46762,#46763,#46764,#46765,#46766,#46767,
#46768,#46769,#46770,#46771,#46772,#46773,#46774,#46775,#46776,#46777,#46778,
#46779,#46780,#46781,#46782,#46783,#46784,#46785,#46786,#46787,#46788,#46789,
#46790,#46791,#46792,#46793,#46794,#46795,#46796,#46797,#46798,#46799,#46800,
#46801,#46802,#46803,#46804,#46805,#46806,#46807,#46808,#46809,#46810,#46811,
#46812,#46813,#46814,#46815,#46816,#46817,#46818,#46819,#46820,#46821,#46822,
#46823,#46824,#46825,#46826,#46827,#46828,#46829,#46830,#46831,#46832,#46833,
#46834,#46835,#46836,#46837,#46838,#46839,#46840,#46841,#46842,#46843,#46844,
#46845,#46846,#46847,#46848,#46849,#46850,#46851,#46852,#46853,#46854,#46855,
#46856,#46857,#46858,#46859,#46860,#46861,#46862,#46863,#46864,#46865,#46866,
#46867,#46868,#46869,#46870,#46871,#46872,#46873,#46874,#46875,#46876,#46877,
#46878,#46879,#46880,#46881,#46882,#46883,#46884,#46885,#46886,#46887,#46888,
#46889,#46890,#46891,#46892,#46893),(#46894,#46895,#46896,#46897,#46898,
#46899,#46900,#46901,#46902,#46903,#46904,#46905,#46906,#46907,#46908,#46909,
#46910,#46911,#46912,#46913,#46914,#46915,#46916,#46917,#46918,#46919,#46920,
#46921,#46922,#46923,#46924,#46925,#46926,#46927,#46928,#46929,#46930,#46931,
#46932,#46933,#46934,#46935,#46936,#46937,#46938,#46939,#46940,#46941,#46942,
#46943,#46944,#46945,#46946,#46947,#46948,#46949,#46950,#46951,#46952,#46953,
#46954,#46955,#46956,#46957,#46958,#46959,#46960,#46961,#46962,#46963,#46964,
#46965,#46966,#46967,#46968,#46969,#46970,#46971,#46972,#46973,#46974,#46975,
#46976,#46977,#46978,#46979,#46980,#46981,#46982,#46983,#46984,#46985,#46986,
#46987,#46988,#46989,#46990,#46991,#46992,#46993,#46994,#46995,#46996,#46997,
#46998,#46999,#47000,#47001,#47002,#47003,#47004,#47005,#47006,#47007,#47008,
#47009,#47010,#47011,#47012,#47013,#47014,#47015,#47016,#47017,#47018,#47019,
#47020,#47021,#47022,#47023,#47024,#47025,#47026,#47027,#47028,#47029,#47030,
#47031,#47032,#47033,#47034,#47035,#47036,#47037,#47038,#47039,#47040,#47041,
#47042,#47043,#47044,#47045,#47046,#47047,#47048,#47049,#47050,#47051,#47052,
#47053,#47054,#47055,#47056,#47057,#47058,#47059,#47060,#47061,#47062,#47063,
#47064,#47065,#47066,#47067,#47068,#47069,#47070,#47071,#47072,#47073,#47074,
#47075,#47076,#47077,#47078,#47079,#47080,#47081,#47082,#47083,#47084,#47085,
#47086,#47087,#47088,#47089,#47090,#47091,#47092,#47093,#47094,#47095,#47096,
#47097,#47098,#47099,#47100,#47101,#47102,#47103,#47104,#47105,#47106,#47107,
#47108,#47109,#47110,#47111,#47112,#47113,#47114,#47115,#47116,#47117,#47118,
#47119,#47120,#47121,#47122,#47123,#47124,#47125,#47126,#47127,#47128,#47129,
#47130,#47131,#47132,#47133,#47134,#47135,#47136,#47137,#47138,#47139,#47140,
#47141,#47142,#47143,#47144,#47145,#47146,#47147,#47148,#47149,#47150,#47151,
#47152,#47153,#47154,#47155,#47156,#47157,#47158,#47159,#47160,#47161,#47162,
#47163,#47164,#47165,#47166,#47167,#47168,#47169,#47170,#47171,#47172,#47173,
#47174,#47175,#47176,#47177,#47178,#47179,#47180,#47181,#47182,#47183,#47184,
#47185,#47186,#47187,#47188,#47189,#47190,#47191,#47192,#47193,#47194,#47195,
#47196,#47197,#47198,#47199,#47200,#47201,#47202,#47203,#47204,#47205,#47206,
#47207,#47208,#47209,#47210,#47211,#47212,#47213,#47214,#47215,#47216,#47217,
#47218,#47219,#47220,#47221,#47222,#47223,#47224,#47225,#47226,#47227,#47228,
#47229,#47230,#47231,#47232,#47233,#47234,#47235,#47236,#47237,#47238,#47239,
#47240,#47241,#47242,#47243,#47244,#47245,#47246,#47247,#47248,#47249,#47250,
#47251,#47252,#47253,#47254,#47255,#47256,#47257,#47258,#47259,#47260,#47261,
#47262,#47263,#47264,#47265,#47266,#47267,#47268,#47269,#47270,#47271,#47272,
#47273,#47274,#47275,#47276,#47277,#47278,#47279,#47280,#47281,#47282,#47283,
#47284,#47285,#47286,#47287,#47288,#47289,#47290,#47291,#47292,#47293,#47294,
#47295,#47296,#47297,#47298,#47299,#47300,#47301,#47302,#47303,#47304,#47305,
#47306,#47307,#47308,#47309,#47310,#47311,#47312,#47313,#47314,#47315,#47316,
#47317,#47318,#47319,#47320,#47321,#47322,#47323,#47324,#47325,#47326,#47327,
#47328,#47329,#47330,#47331,#47332,#47333,#47334,#47335,#47336,#47337,#47338,
#47339,#47340,#47341,#47342,#47343,#47344,#47345,#47346,#47347,#47348,#47349,
#47350,#47351,#47352,#47353,#47354,#47355,#47356,#47357,#47358,#47359,#47360,
#47361,#47362,#47363,#47364,#47365,#47366,#47367,#47368,#47369,#47370,#47371,
#47372,#47373,#47374,#47375,#47376,#47377,#47378,#47379,#47380,#47381,#47382,
#47383,#47384,#47385,#47386,#47387,#47388,#47389,#47390,#47391,#47392,#47393,
#47394,#47395,#47396,#47397,#47398,#47399,#47400,#47401,#47402,#47403,#47404,
#47405,#47406,#47407,#47408,#47409,#47410,#47411,#47412,#47413,#47414,#47415,
#47416,#47417,#47418,#47419,#47420,#47421,#47422,#47423,#47424,#47425,#47426,
#47427,#47428,#47429,#47430,#47431,#47432,#47433,#47434,#47435,#47436,#47437,
#47438,#47439,#47440,#47441,#47442,#47443,#47444,#47445,#47446,#47447,#47448,
#47449,#47450,#47451,#47452,#47453,#47454,#47455,#47456,#47457,#47458,#47459,
#47460,#47461,#47462,#47463,#47464,#47465,#47466,#47467,#47468,#47469,#47470,
#47471,#47472,#47473,#47474,#47475,#47476,#47477,#47478,#47479,#47480,#47481,
#47482,#47483,#47484,#47485,#47486,#47487,#47488,#47489,#47490,#47491,#47492,
#47493,#47494,#47495,#47496,#47497,#47498,#47499,#47500,#47501,#47502,#47503,
#47504,#47505,#47506,#47507,#47508,#47509,#47510,#47511,#47512,#47513,#47514,
#47515,#47516,#47517,#47518,#47519,#47520,#47521,#47522,#47523,#47524,#47525,
#47526,#47527,#47528,#47529,#47530,#47531,#47532,#47533,#47534,#47535,#47536,
#47537,#47538,#47539,#47540,#47541,#47542,#47543,#47544,#47545,#47546,#47547,
#47548,#47549,#47550,#47551,#47552,#47553,#47554,#47555,#47556,#47557,#47558,
#47559,#47560,#47561,#47562,#47563,#47564,#47565,#47566,#47567,#47568,#47569,
#47570,#47571,#47572,#47573,#47574,#47575,#47576,#47577,#47578,#47579,#47580,
#47581,#47582,#47583,#47584,#47585,#47586,#47587,#47588,#47589,#47590,#47591,
#47592,#47593,#47594,#47595,#47596,#47597,#47598,#47599,#47600,#47601,#47602,
#47603,#47604,#47605,#47606,#47607,#47608,#47609,#47610,#47611,#47612,#47613,
#47614,#47615,#47616,#47617,#47618)),.UNSPECIFIED.,.F.,.F.,.F.,(4,4),(4,
1,1,1,1,1,1,1,1,1,1,1,1,1,1,1,1,1,1,1,1,1,1,1,1,1,1,1,1,1,1,1,1,1,1,1,1,
1,1,1,1,1,1,1,1,1,1,1,1,1,1,1,1,1,1,1,1,1,1,1,1,1,1,1,1,1,1,1,1,1,1,1,1,
1,1,1,1,1,1,1,1,1,1,1,1,1,1,1,1,1,1,1,1,1,1,1,1,1,1,1,1,1,1,1,1,1,1,1,1,
1,1,1,1,1,1,1,1,1,1,1,1,1,1,1,1,1,1,1,1,1,1,1,1,1,1,1,1,1,1,1,1,1,1,1,1,
1,1,1,1,1,1,1,1,1,1,1,1,1,1,1,1,1,1,1,1,1,1,1,1,1,1,1,1,1,1,1,1,1,1,1,1,
1,1,1,1,1,1,1,1,1,1,1,1,1,1,1,1,1,1,1,1,1,1,1,1,1,1,1,1,1,1,1,1,1,1,1,1,
1,1,1,1,1,1,1,1,1,1,1,1,1,1,1,1,1,1,1,1,1,1,1,1,1,1,1,1,1,1,1,1,1,1,1,1,
1,1,1,1,1,1,1,1,1,1,1,1,1,1,1,1,1,1,1,1,1,1,1,1,1,1,1,1,1,1,1,1,1,1,1,1,
1,1,1,1,1,1,1,1,1,1,1,1,1,1,1,1,1,1,1,1,1,1,1,1,1,1,1,1,1,1,1,1,1,1,1,1,
1,1,1,1,1,1,1,1,1,1,1,1,1,1,1,1,1,1,1,1,1,1,1,1,1,1,1,1,1,1,1,1,1,1,1,1,
1,1,1,1,1,1,1,1,1,1,1,1,1,1,1,1,1,1,1,1,1,1,1,1,1,1,1,1,1,1,1,1,1,1,1,1,
1,1,1,1,1,1,1,1,1,1,1,1,1,1,1,1,1,1,1,1,1,1,1,1,1,1,1,1,1,1,1,1,1,1,1,1,
1,1,1,1,1,1,1,1,1,1,1,1,1,1,1,1,1,1,1,1,1,1,1,1,1,1,1,1,1,1,1,1,1,1,1,1,
1,1,1,1,1,1,1,1,1,1,1,1,1,1,1,1,1,1,1,1,1,1,1,1,1,1,1,1,1,1,1,1,1,1,1,1,
1,1,1,1,1,1,1,1,1,1,1,1,1,1,1,1,1,1,1,1,1,1,1,1,1,1,1,1,1,1,1,1,1,1,1,1,
1,1,1,1,1,1,1,1,1,1,1,1,1,1,1,1,1,1,1,1,1,1,1,1,1,1,1,1,1,1,1,1,1,1,1,1,
1,1,1,1,1,1,1,1,1,1,1,1,1,1,1,1,1,1,1,1,1,1,1,1,1,1,1,1,1,1,1,1,1,1,1,1,
1,1,1,1,1,1,1,1,1,1,1,1,1,1,1,1,1,1,1,1,1,1,1,1,1,1,1,1,1,1,1,1,1,1,1,1,
1,1,1,1,1,1,1,1,1,1,1,1,1,1,1,1,1,1,1,1,1,1,1,1,1,1,1,1,1,1,1,1,1,1,1,1,
1,1,1,1,1,1,1,1,1,1,1,1,1,1,1,1,1,1,1,1,1,1,1,1,1,1,1,1,1,1,1,1,1,1,1,1,
1,4),(0.,0.23619826056056),(8.98757472625123,9.48745554701959,9.98733636778795,
10.9870980093247,11.9868596508614,12.9866212923981,13.9863829339348,14.9861445754715,
15.4860253962399,15.9859062170083,16.985667858545,17.9854295000817,18.9851911416184,
19.9849527831551,20.9847144246918,21.9844760662286,22.4843568869969,22.9842377077653,
23.983999349302,24.9837609908387,25.9835226323754,26.9832842739122,27.9830459154489,
28.9828075569856,29.4826883777539,29.9825691985223,30.982330840059,31.9820924815957,
32.9818541231325,33.9816157646692,34.9813774062059,35.9811390477426,36.481019868511,
36.9809006892793,37.980662330816,38.9804239723528,39.9801856138895,40.9799472554262,
41.9797088969629,42.9794705384996,43.479351359268,43.9792321800364,44.9789938215731,
45.9787554631098,46.9785171046465,47.9782787461832,48.9780403877199,49.9778020292567,
50.477682850025,50.9775636707934,51.9773253123301,52.9770869538668,53.9768485954035,
54.9766102369402,55.976371878477,56.9761335200137,57.476014340782,57.9758951615504,
58.9756568030871,59.9754184446238,60.9751800861606,61.9749417276973,62.974703369234,
63.9744650107707,64.4743458315391,64.9742266523074,65.9739882938441,66.9737499353809,
67.9735115769176,68.9732732184543,69.973034859991,70.9727965015277,71.4726773222961,
71.9725581430645,72.9723197846012,73.9720814261379,74.9718430676746,75.9716047092113,
76.971366350748,77.9711279922848,78.4710088130531,78.9708896338215,79.9706512753582,
80.9704129168949,81.9701745584316,82.9699361999684,83.9696978415051,84.9694594830418,
85.4693403038102,85.9692211245785,86.9689827661152,87.9687444076519,88.9685060491887,
89.9682676907254,90.9680293322621,91.9677909737988,92.4676717945672,92.9675526153355,
93.9673142568722,94.967075898409,95.9668375399457,96.9665991814824,97.9663608230191,
98.9661224645558,99.4660032853242,99.9658841060926,100.965645747629,101.965407389166,
102.965169030703,103.964930672239,104.964692313776,105.964453955313,106.464334776081,
106.96421559685,107.963977238386,108.963738879923,109.96350052146,110.963262162996,
111.963023804533,112.96278544607,113.462666266838,113.962547087607,114.962308729143,
115.96207037068,116.961832012217,117.961593653753,118.96135529529,119.961116936827,
120.460997757595,120.960878578364,121.9606402199,122.960401861437,123.960163502974,
124.95992514451,125.959686786047,126.959448427584,127.459329248352,127.959210069121,
128.958971710657,129.958733352194,130.958494993731,131.958256635268,132.958018276804,
133.957779918341,134.457660739109,134.957541559878,135.957303201414,136.957064842951,
137.956826484488,138.956588126025,139.956349767561,140.956111409098,141.455992229866,
141.955873050635,142.955634692171,143.955396333708,144.955157975245,145.954919616782,
146.954681258318,147.954442899855,148.454323720623,148.954204541392,149.953966182928,
150.953727824465,151.953489466002,152.953251107539,153.953012749075,154.952774390612,
155.45265521138,155.952536032149,156.952297673685,157.952059315222,158.951820956759,
159.951582598296,160.951344239832,161.951105881369,162.450986702137,162.950867522906,
163.950629164442,164.950390805979,165.950152447516,166.949914089053,167.949675730589,
168.949437372126,169.449318192894,169.949199013663,170.9489606552,171.948722296736,
172.948483938273,173.94824557981,174.948007221346,175.947768862883,176.447649683651,
176.94753050442,177.947292145957,178.947053787493,179.94681542903,180.946577070567,
181.946338712103,182.94610035364,183.445981174408,183.945861995177,184.945623636714,
185.94538527825,186.945146919787,187.944908561324,188.94467020286,189.944431844397,
190.444312665166,190.944193485934,191.943955127471,192.943716769007,193.943478410544,
194.943240052081,195.943001693617,196.942763335154,197.442644155923,197.942524976691,
198.942286618228,199.942048259764,200.941809901301,201.941571542838,202.941333184374,
203.941094825911,204.44097564668,204.940856467448,205.940618108985,206.940379750521,
207.940141392058,208.939903033595,209.939664675131,210.939426316668,211.439307137437,
211.939187958205,212.938949599742,213.938711241278,214.938472882815,215.938234524352,
216.937996165889,217.937757807425,218.437638628194,218.937519448962,219.937281090499,
220.937042732035,221.936804373572,222.936566015109,223.936327656646,224.936089298182,
225.435970118951,225.935850939719,226.935612581256,227.935374222792,228.935135864329,
229.934897505866,230.934659147403,231.934420788939,232.434301609708,232.934182430476,
233.933944072013,234.933705713549,235.933467355086,236.933228996623,237.93299063816,
238.932752279696,239.432633100465,239.932513921233,240.93227556277,241.932037204306,
242.931798845843,243.93156048738,244.931322128917,245.931083770453,246.430964591222,
246.93084541199,247.930607053527,248.930368695063,249.9301303366,250.929891978137,
251.929653619674,252.92941526121,253.429296081979,253.929176902747,254.928938544284,
255.928700185821,256.928461827357,257.928223468894,258.927985110431,259.927746751967,
260.427627572736,260.927508393504,261.927270035041,262.927031676578,263.926793318114,
264.926554959651,265.926316601188,266.926078242724,267.425959063493,267.925839884261,
268.925601525798,269.925363167335,270.925124808871,271.924886450408,272.924648091945,
273.924409733481,274.42429055425,274.924171375018,275.923933016555,276.923694658092,
277.923456299628,278.923217941165,279.922979582702,280.922741224238,281.422622045007,
281.922502865775,282.922264507312,283.922026148849,284.921787790385,285.921549431922,
286.921311073459,287.921072714995,288.420953535764,288.920834356532,289.920595998069,
290.920357639606,291.920119281142,292.919880922679,293.919642564216,294.919404205753,
295.419285026521,295.919165847289,296.918927488826,297.918689130363,298.918450771899,
299.918212413436,300.917974054973,301.91773569651,302.417616517278,302.917497338046,
303.917258979583,304.91702062112,305.916782262656,306.916543904193,307.91630554573,
308.916067187267,309.415948008035,309.915828828803,310.91559047034,311.915352111877,
312.915113753413,313.91487539495,314.914637036487,315.914398678024,316.414279498792,
316.91416031956,317.913921961097,318.913683602634,319.91344524417,320.913206885707,
321.912968527244,322.912730168781,323.412610989549,323.912491810317,324.912253451854,
325.912015093391,326.911776734928,327.911538376464,328.911300018001,329.911061659538,
330.910823301074,331.910584942611,332.410465763379,332.910346584148,333.910108225684,
334.909869867221,335.909631508758,336.909393150295,337.909154791831,338.908916433368,
339.408797254136,339.908678074905,340.908439716442,341.908201357978,342.907962999515,
343.907724641052,344.907486282588,345.907247924125,346.407128744893,346.907009565662,
347.906771207199,348.906532848735,349.906294490272,350.906056131809,351.905817773345,
352.905579414882,353.40546023565,353.905341056419,354.905102697956,355.904864339492,
356.904625981029,357.904387622566,358.904149264102,359.903910905639,360.403791726408,
360.903672547176,361.903434188713,362.903195830249,363.902957471786,364.902719113323,
365.902480754859,366.902242396396,367.402123217165,367.902004037933,368.90176567947,
369.901527321006,370.901288962543,371.90105060408,372.900812245617,373.900573887153,
374.400454707922,374.90033552869,375.900097170227,376.899858811763,377.8996204533,
378.899382094837,379.899143736374,380.89890537791,381.398786198679,381.898667019447,
382.898428660984,383.89819030252,384.897951944057,385.897713585594,386.897475227131,
387.897236868667,388.397117689436,388.896998510204,389.896760151741,390.896521793277,
391.896283434814,392.896045076351,393.895806717888,394.895568359424,395.395449180193,
395.895330000961,396.895091642498,397.894853284034,398.894614925571,399.894376567108,
400.894138208645,401.893899850181,402.39378067095,402.893661491718,403.893423133255,
404.893184774791,405.892946416328,406.892708057865,407.892469699402,408.892231340938,
409.392112161707,409.891992982475,410.891754624012,411.891516265548,412.891277907085,
413.891039548622,414.890801190159,415.890562831695,416.390443652464,416.890324473232,
417.890086114769,418.889847756306,419.889609397842,420.889371039379,421.889132680916,
422.888894322452,423.388775143221,423.888655963989,424.888417605526,425.888179247063,
426.887940888599,427.887702530136,428.887464171673,429.887225813209,430.387106633978,
430.886987454746,431.886749096283,432.88651073782,433.886272379356,434.886034020893,
435.88579566243,436.885557303966,437.385438124735,437.885318945503,438.88508058704,
439.884842228577,440.884603870113,441.88436551165,442.884127153187,443.883888794723,
444.383769615492,444.88365043626,445.883412077797,446.883173719334,447.88293536087,
448.882697002407,449.882458643944,450.882220285481,451.382101106249,451.881981927017,
452.881743568554,453.881505210091,454.881266851627,455.881028493164,456.880790134701,
457.880551776237,458.380432597006,458.880313417774,459.880075059311,460.879836700848,
461.879598342384,462.879359983921,463.879121625458,464.878883266995,465.378764087763,
465.878644908531,466.878406550068,467.878168191605,468.877929833141,469.877691474678,
470.877453116215,471.877214757752,472.37709557852,472.876976399288,473.876738040825,
474.876499682362,475.876261323898,476.876022965435,477.875784606972,478.875546248509,
479.375427069277,479.875307890045,480.875069531582,481.874831173119,482.874592814655,
483.874354456192,484.874116097729,485.873877739266,486.373758560034,486.873639380802,
487.873401022339,488.873162663876,489.872924305412,490.872685946949,491.872447588486,
492.872209230023,493.372090050791,493.871970871559,494.871732513096,495.871494154633,
496.87125579617,497.871017437706,498.870779079243,499.87054072078,500.370421541548,
500.870302362316,501.870064003853,502.86982564539,503.869587286927,504.869348928463,
505.86911057,506.868872211537,507.368753032305,507.868633853073,508.86839549461,
509.868157136147,510.867918777684,511.86768041922,512.867442060757,513.867203702294,
514.367084523062,514.86696534383,515.866726985367,516.866488626904,517.866250268441,
518.866011909977,519.865773551514,520.865535193051,521.365416013819,521.865296834587,
522.865058476124,523.864820117661,524.864581759198,525.864343400734,526.864105042271,
527.863866683808,528.363747504576,528.863628325344,529.863389966881,530.863151608418,
531.862913249955,532.862674891491,533.862436533028,534.862198174565,535.362078995333,
535.861959816101,536.861721457638,537.861483099175,538.861244740712,539.861006382248,
540.860768023785,541.860529665322,542.36041048609,542.860291306858,543.860052948395,
544.859814589932,545.859576231469,546.859337873005,547.859099514542,548.858861156079,
549.358741976847,549.858622797615,550.858384439152,551.858146080689,552.857907722226,
553.857669363762,554.857431005299,555.857192646836,556.357073467604,556.856954288373,
557.856715929909,558.856477571446,559.856239212983,560.856000854519,561.855762496056,
562.855524137593,563.355404958361,563.85528577913,564.855047420666,565.854809062203,
566.85457070374,567.854332345276,568.854093986813,569.85385562835,570.353736449118,
570.853617269887,571.853378911423,572.85314055296,573.852902194497,574.852663836033,
575.85242547757,576.852187119107,577.352067939875,577.851948760644,578.85171040218,
579.851472043717,580.851233685254,581.85099532679,582.850756968327,583.850518609864,
584.350399430632,584.850280251401,585.850041892937,586.849803534474,587.849565176011,
588.849326817548,589.849088459084,590.848850100621,591.348730921389,591.848611742158,
592.848373383694,593.848135025231,594.847896666768,595.847658308305,596.847419949841,
597.847181591378,598.347062412146,598.846943232915,599.846704874451,600.846466515988,
601.846228157525,602.845989799061,603.845751440598,604.845513082135,605.345393902903,
605.845274723672,606.845036365208,607.844798006745,608.844559648282,609.844321289819,
610.844082931355,611.843844572892,612.34372539366,612.843606214429,613.843367855965,
614.843129497502,615.842891139039,616.842652780576,617.842414422112,618.842176063649,
619.342056884417,619.841937705186,620.841699346722,621.841460988259,622.841222629796,
623.840984271333,624.840745912869,625.840507554406,626.340388375174,626.840269195943,
627.84003083748,628.839792479016,629.839554120553,630.83931576209,631.839077403626,
632.838839045163,633.338719865931,633.8386006867,634.838362328236,635.838123969773,
636.83788561131,637.837647252847,638.837408894383,639.337289715152,639.83717053592),
 .UNSPECIFIED.);
#71=B_SPLINE_CURVE_WITH_KNOTS('',3,(#30996,#30997,#30998,#30999,#31000,
#31001,#31002,#31003,#31004,#31005,#31006,#31007,#31008),.UNSPECIFIED.,
 .F.,.F.,(4,3,3,3,4),(-3.66465818398557,-2.83011024963485,-1.99556231528413,
-1.16101438093341,-0.960268764914558),.UNSPECIFIED.);
#72=B_SPLINE_CURVE_WITH_KNOTS('',3,(#31011,#31012,#31013,#31014),
 .UNSPECIFIED.,.F.,.F.,(4,4),(0.,0.437203234522177),.UNSPECIFIED.);
#73=B_SPLINE_CURVE_WITH_KNOTS('',3,(#31019,#31020,#31021,#31022,#31023,
#31024,#31025,#31026,#31027,#31028,#31029,#31030,#31031,#31032,#31033,#31034,
#31035,#31036,#31037,#31038,#31039,#31040,#31041,#31042,#31043),
 .UNSPECIFIED.,.F.,.F.,(4,3,3,3,3,3,3,3,4),(-9.94784349116513,-8.99785477383045,
-7.99809313229373,-6.99833149075702,-6.49845066998866,-5.9985698492203,
-4.99880820768358,-3.99904656614687,-3.66465818398557),.UNSPECIFIED.);
#74=B_SPLINE_CURVE_WITH_KNOTS('',3,(#31044,#31045,#31046,#31047,#31048,
#31049,#31050,#31051,#31052,#31053,#31054,#31055,#31056,#31057,#31058,#31059,
#31060,#31061,#31062,#31063,#31064,#31065,#31066,#31067,#31068),
 .UNSPECIFIED.,.F.,.F.,(4,3,3,3,3,3,3,3,4),(0.437203234522177,1.27175116887288,
2.10629910322359,2.9408470375743,3.775394971925,4.60994290627571,5.44449084062642,
6.27903877497713,6.72038854170174),.UNSPECIFIED.);
#75=B_SPLINE_CURVE_WITH_KNOTS('',3,(#31073,#31074,#31075,#31076,#31077,
#31078,#31079,#31080,#31081,#31082,#31083,#31084,#31085,#31086,#31087,#31088,
#31089,#31090,#31091,#31092,#31093,#31094,#31095,#31096,#31097,#31098,#31099,
#31100),.UNSPECIFIED.,.F.,.F.,(4,3,3,3,3,3,3,3,3,4),(-16.2310287983448,
-15.9961862645875,-14.9964246230508,-13.996662981514,-13.4967821607457,
-12.9969013399773,-11.9971396984406,-10.9973780569039,-9.99761641536717,
-9.94784349116513),.UNSPECIFIED.);
#76=B_SPLINE_CURVE_WITH_KNOTS('',3,(#31101,#31102,#31103,#31104,#31105,
#31106,#31107,#31108,#31109,#31110,#31111,#31112,#31113,#31114,#31115,#31116,
#31117,#31118,#31119,#31120,#31121,#31122,#31123,#31124,#31125),
 .UNSPECIFIED.,.F.,.F.,(4,3,3,3,3,3,3,3,4),(6.72038854170174,6.99833149075699,
7.99809313229371,8.99785477383043,9.99761641536715,10.9973780569039,11.9971396984406,
12.9969013399773,13.0035738488813),.UNSPECIFIED.);
#77=B_SPLINE_CURVE_WITH_KNOTS('',3,(#31130,#31131,#31132,#31133,#31134,
#31135,#31136,#31137,#31138,#31139,#31140,#31141,#31142,#31143,#31144,#31145,
#31146,#31147,#31148,#31149,#31150,#31151,#31152,#31153,#31154),
 .UNSPECIFIED.,.F.,.F.,(4,3,3,3,3,3,3,3,4),(-22.5142141055244,-21.6796661711737,
-20.845118236823,-20.0105703024723,-19.1760223681216,-18.3414744337709,
-17.5069264994202,-16.6723785650695,-16.2310287983448),.UNSPECIFIED.);
#78=B_SPLINE_CURVE_WITH_KNOTS('',3,(#31155,#31156,#31157,#31158,#31159,
#31160,#31161,#31162,#31163,#31164,#31165,#31166,#31167,#31168,#31169,#31170,
#31171,#31172,#31173,#31174,#31175,#31176,#31177,#31178,#31179),
 .UNSPECIFIED.,.F.,.F.,(4,3,3,3,3,3,3,3,4),(13.0035738488813,13.4967821607457,
13.996662981514,14.9964246230507,15.9961862645875,16.9959479061242,17.9957095476609,
18.9954711891976,19.286759156061),.UNSPECIFIED.);
#79=B_SPLINE_CURVE_WITH_KNOTS('',3,(#31184,#31185,#31186,#31187,#31188,
#31189,#31190,#31191,#31192,#31193,#31194,#31195,#31196,#31197,#31198,#31199,
#31200,#31201,#31202,#31203,#31204,#31205,#31206,#31207,#31208),
 .UNSPECIFIED.,.F.,.F.,(4,3,3,3,3,3,3,3,4),(-28.7973994127039,-27.9628514783532,
-27.1283035440025,-26.2937556096518,-25.459207675301,-24.6246597409503,
-23.7901118065996,-22.9555638722489,-22.5142141055244),.UNSPECIFIED.);
#80=B_SPLINE_CURVE_WITH_KNOTS('',3,(#31209,#31210,#31211,#31212,#31213,
#31214,#31215,#31216,#31217,#31218,#31219,#31220,#31221,#31222,#31223,#31224,
#31225,#31226,#31227,#31228,#31229,#31230,#31231,#31232,#31233),
 .UNSPECIFIED.,.F.,.F.,(4,3,3,3,3,3,3,3,4),(19.286759156061,20.1213070904117,
20.9558550247624,21.7904029591131,22.6249508934638,23.4594988278145,24.2940467621652,
25.1285946965159,25.5699444632405),.UNSPECIFIED.);
#81=B_SPLINE_CURVE_WITH_KNOTS('',3,(#31238,#31239,#31240,#31241,#31242,
#31243,#31244,#31245,#31246,#31247,#31248,#31249,#31250,#31251,#31252,#31253,
#31254,#31255,#31256,#31257,#31258,#31259,#31260,#31261,#31262),
 .UNSPECIFIED.,.F.,.F.,(4,3,3,3,3,3,3,3,4),(-35.0805847198835,-34.2460367855328,
-33.4114888511821,-32.5769409168313,-31.7423929824806,-30.9078450481299,
-30.0732971137792,-29.2387491794285,-28.7973994127039),.UNSPECIFIED.);
#82=B_SPLINE_CURVE_WITH_KNOTS('',3,(#31263,#31264,#31265,#31266,#31267,
#31268,#31269,#31270,#31271,#31272,#31273,#31274,#31275,#31276,#31277,#31278,
#31279,#31280,#31281,#31282,#31283,#31284,#31285,#31286,#31287),
 .UNSPECIFIED.,.F.,.F.,(4,3,3,3,3,3,3,3,4),(25.5699444632405,25.9938026799547,
26.9935643214914,27.4934451422597,27.9933259630281,28.9930876045648,29.9928492461015,
30.9926108876382,31.8531297704201),.UNSPECIFIED.);
#83=B_SPLINE_CURVE_WITH_KNOTS('',3,(#31292,#31293,#31294,#31295,#31296,
#31297,#31298,#31299,#31300,#31301,#31302,#31303,#31304,#31305,#31306,#31307,
#31308,#31309,#31310,#31311,#31312,#31313),.UNSPECIFIED.,.F.,.F.,(4,3,3,
3,3,3,3,4),(-41.3637700270631,-40.9902273030054,-39.9904656614687,-38.990704019932,
-37.9909423783952,-36.9911807368585,-35.9914190953218,-35.0805847198835),
 .UNSPECIFIED.);
#84=B_SPLINE_CURVE_WITH_KNOTS('',3,(#31314,#31315,#31316,#31317,#31318,
#31319,#31320,#31321,#31322,#31323,#31324,#31325,#31326,#31327,#31328,#31329,
#31330,#31331,#31332,#31333,#31334,#31335,#31336,#31337,#31338),
 .UNSPECIFIED.,.F.,.F.,(4,3,3,3,3,3,3,3,4),(31.8531297704201,32.6876777047708,
33.5222256391215,34.3567735734723,35.191321507823,36.0258694421737,36.8604173765244,
37.6949653108752,38.1363150775997),.UNSPECIFIED.);
#85=B_SPLINE_CURVE_WITH_KNOTS('',3,(#31343,#31344,#31345,#31346,#31347,
#31348,#31349,#31350,#31351,#31352,#31353,#31354,#31355,#31356,#31357,#31358,
#31359,#31360,#31361,#31362,#31363,#31364,#31365,#31366,#31367),
 .UNSPECIFIED.,.F.,.F.,(4,3,3,3,3,3,3,3,4),(-47.6469553342427,-46.812407399892,
-45.9778594655413,-45.1433115311906,-44.3087635968399,-43.4742156624892,
-42.6396677281384,-41.8051197937877,-41.3637700270631),.UNSPECIFIED.);
#86=B_SPLINE_CURVE_WITH_KNOTS('',3,(#31368,#31369,#31370,#31371,#31372,
#31373,#31374,#31375,#31376,#31377,#31378,#31379,#31380,#31381,#31382,#31383,
#31384,#31385,#31386,#31387,#31388,#31389,#31390,#31391,#31392),
 .UNSPECIFIED.,.F.,.F.,(4,3,3,3,3,3,3,3,4),(38.1363150775997,38.990704019932,
39.9904656614687,40.9902273030054,41.4901081237738,41.9899889445422,42.9897505860789,
43.9895122276156,44.4195003847792),.UNSPECIFIED.);
#87=B_SPLINE_CURVE_WITH_KNOTS('',3,(#31397,#31398,#31399,#31400,#31401,
#31402,#31403,#31404,#31405,#31406,#31407,#31408,#31409,#31410,#31411,#31412,
#31413,#31414,#31415,#31416,#31417,#31418,#31419,#31420,#31421),
 .UNSPECIFIED.,.F.,.F.,(4,3,3,3,3,3,3,3,4),(-53.9301406414223,-52.987367001446,
-51.9876053599093,-50.9878437183726,-49.9880820768358,-48.9883204352991,
-48.4884396145308,-47.9885587937624,-47.6469553342427),.UNSPECIFIED.);
#88=B_SPLINE_CURVE_WITH_KNOTS('',3,(#31422,#31423,#31424,#31425,#31426,
#31427,#31428,#31429,#31430,#31431,#31432,#31433,#31434,#31435,#31436,#31437,
#31438,#31439,#31440,#31441,#31442,#31443,#31444,#31445,#31446),
 .UNSPECIFIED.,.F.,.F.,(4,3,3,3,3,3,3,3,4),(44.4195003847792,45.25404831913,
46.0885962534807,46.9231441878314,47.7576921221821,48.5922400565329,49.4267879908836,
50.2613359252343,50.7026856919589),.UNSPECIFIED.);
#89=B_SPLINE_CURVE_WITH_KNOTS('',3,(#31451,#31452,#31453,#31454,#31455,
#31456,#31457,#31458,#31459,#31460,#31461,#31462,#31463,#31464,#31465,#31466,
#31467,#31468,#31469,#31470,#31471,#31472,#31473,#31474,#31475),
 .UNSPECIFIED.,.F.,.F.,(4,3,3,3,3,3,3,3,4),(-60.2133259486019,-59.3787780142511,
-58.5442300799004,-57.7096821455496,-56.8751342111989,-56.0405862768482,
-55.2060383424974,-54.3714904081467,-53.9301406414223),.UNSPECIFIED.);
#90=B_SPLINE_CURVE_WITH_KNOTS('',3,(#31476,#31477,#31478,#31479,#31480,
#31481,#31482,#31483,#31484,#31485,#31486,#31487,#31488,#31489,#31490,#31491,
#31492,#31493,#31494,#31495,#31496,#31497,#31498,#31499,#31500),
 .UNSPECIFIED.,.F.,.F.,(4,3,3,3,3,3,3,3,4),(50.7026856919589,51.5372336263096,
52.3717815606603,53.206329495011,54.0408774293617,54.8754253637125,55.7099732980632,
56.5445212324139,56.9858709991385),.UNSPECIFIED.);
#91=B_SPLINE_CURVE_WITH_KNOTS('',3,(#31505,#31506,#31507,#31508,#31509,
#31510,#31511,#31512,#31513,#31514,#31515,#31516,#31517,#31518,#31519,#31520,
#31521,#31522,#31523,#31524,#31525,#31526,#31527,#31528,#31529),
 .UNSPECIFIED.,.F.,.F.,(4,3,3,3,3,3,3,3,4),(-66.4965112557814,-65.6619633214307,
-64.82741538708,-63.9928674527293,-63.1583195183786,-62.323771584028,-61.4892236496773,
-60.6546757153266,-60.2133259486019),.UNSPECIFIED.);
#92=B_SPLINE_CURVE_WITH_KNOTS('',3,(#31530,#31531,#31532,#31533,#31534,
#31535,#31536,#31537,#31538,#31539,#31540,#31541,#31542,#31543,#31544,#31545,
#31546,#31547,#31548,#31549,#31550,#31551,#31552,#31553,#31554),
 .UNSPECIFIED.,.F.,.F.,(4,3,3,3,3,3,3,3,4),(56.9858709991385,57.9861752091296,
58.9859368506664,59.9856984922031,60.9854601337398,61.9852217752765,62.4851025960449,
62.9849834168133,63.269056306318),.UNSPECIFIED.);
#93=B_SPLINE_CURVE_WITH_KNOTS('',3,(#31559,#31560,#31561,#31562,#31563,
#31564,#31565,#31566,#31567,#31568,#31569,#31570,#31571,#31572,#31573,#31574,
#31575,#31576,#31577,#31578,#31579,#31580,#31581,#31582,#31583),
 .UNSPECIFIED.,.F.,.F.,(4,3,3,3,3,3,3,3,4),(-72.7796965629611,-71.9828381906436,
-70.9830765491069,-69.9833149075702,-69.4834340868018,-68.9835532660335,
-67.9837916244967,-66.98402998296,-66.4965112557814),.UNSPECIFIED.);
#94=B_SPLINE_CURVE_WITH_KNOTS('',3,(#31584,#31585,#31586,#31587,#31588,
#31589,#31590,#31591,#31592,#31593,#31594,#31595,#31596,#31597,#31598,#31599,
#31600,#31601,#31602,#31603,#31604,#31605,#31606,#31607,#31608),
 .UNSPECIFIED.,.F.,.F.,(4,3,3,3,3,3,3,3,4),(63.269056306318,64.1036042406688,
64.9381521750195,65.7727001093702,66.6072480437209,67.4417959780717,68.2763439124224,
69.1108918467731,69.5522416134976),.UNSPECIFIED.);
#95=B_SPLINE_CURVE_WITH_KNOTS('',3,(#31613,#31614,#31615,#31616,#31617,
#31618,#31619,#31620,#31621,#31622,#31623,#31624,#31625,#31626,#31627,#31628,
#31629,#31630,#31631,#31632,#31633,#31634,#31635,#31636,#31637,#31638,#31639,
#31640),.UNSPECIFIED.,.F.,.F.,(4,3,3,3,3,3,3,3,3,4),(-79.0628818701407,
-78.9811696814006,-77.9814080398639,-76.9816463983272,-76.4817655775588,
-75.9818847567905,-74.9821231152538,-73.982361473717,-72.9825998321803,
-72.7796965629611),.UNSPECIFIED.);
#96=B_SPLINE_CURVE_WITH_KNOTS('',3,(#31641,#31642,#31643,#31644,#31645,
#31646,#31647,#31648,#31649,#31650,#31651,#31652,#31653,#31654,#31655,#31656,
#31657,#31658,#31659,#31660,#31661,#31662),.UNSPECIFIED.,.F.,.F.,(4,3,3,
3,3,3,3,4),(69.5522416134976,69.9833149075702,70.983076549107,71.9828381906437,
72.9825998321804,73.9823614737171,74.9821231152538,75.8354269206773),
 .UNSPECIFIED.);
#97=B_SPLINE_CURVE_WITH_KNOTS('',3,(#31667,#31668,#31669,#31670,#31671,
#31672,#31673,#31674,#31675,#31676,#31677,#31678,#31679,#31680,#31681,#31682,
#31683,#31684,#31685,#31686,#31687,#31688,#31689,#31690,#31691),
 .UNSPECIFIED.,.F.,.F.,(4,3,3,3,3,3,3,3,4),(-85.3460671773202,-84.9797395306209,
-83.9799778890842,-83.4800970683159,-82.9802162475475,-81.9804546060108,
-80.9806929644741,-79.9809313229374,-79.0628818701407),.UNSPECIFIED.);
#98=B_SPLINE_CURVE_WITH_KNOTS('',3,(#31692,#31693,#31694,#31695,#31696,
#31697,#31698,#31699,#31700,#31701,#31702,#31703,#31704,#31705,#31706,#31707,
#31708,#31709,#31710,#31711,#31712,#31713,#31714,#31715,#31716),
 .UNSPECIFIED.,.F.,.F.,(4,3,3,3,3,3,3,3,4),(75.8354269206773,76.669974855028,
77.5045227893787,78.3390707237294,79.1736186580801,80.0081665924308,80.8427145267815,
81.6772624611322,82.1186122278568),.UNSPECIFIED.);
#99=B_SPLINE_CURVE_WITH_KNOTS('',3,(#31721,#31722,#31723,#31724,#31725,
#31726,#31727,#31728,#31729,#31730,#31731,#31732,#31733,#31734,#31735,#31736,
#31737,#31738,#31739,#31740,#31741,#31742,#31743,#31744,#31745),
 .UNSPECIFIED.,.F.,.F.,(4,3,3,3,3,3,3,3,4),(-91.6292524844998,-90.794704550149,
-89.9601566157983,-89.1256086814476,-88.2910607470968,-87.4565128127461,
-86.6219648783954,-85.7874169440446,-85.3460671773202),.UNSPECIFIED.);
#100=B_SPLINE_CURVE_WITH_KNOTS('',3,(#31746,#31747,#31748,#31749,#31750,
#31751,#31752,#31753,#31754,#31755,#31756,#31757,#31758,#31759,#31760,#31761,
#31762,#31763,#31764,#31765,#31766,#31767,#31768,#31769,#31770),
 .UNSPECIFIED.,.F.,.F.,(4,3,3,3,3,3,3,3,4),(82.1186122278568,82.9802162475476,
83.4800970683159,83.9799778890843,84.979739530621,85.9795011721578,86.9792628136945,
87.9790244552312,88.4017975350364),.UNSPECIFIED.);
#101=B_SPLINE_CURVE_WITH_KNOTS('',3,(#31775,#31776,#31777,#31778,#31779,
#31780,#31781,#31782,#31783,#31784,#31785,#31786,#31787,#31788,#31789,#31790,
#31791,#31792,#31793,#31794,#31795,#31796,#31797,#31798,#31799),
 .UNSPECIFIED.,.F.,.F.,(4,3,3,3,3,3,3,3,4),(-97.9124377916795,-97.4767600498299,
-96.9768792290615,-95.9771175875248,-94.9773559459881,-93.9775943044514,
-92.9778326629147,-91.9780710213779,-91.6292524844998),.UNSPECIFIED.);
#102=B_SPLINE_CURVE_WITH_KNOTS('',3,(#31800,#31801,#31802,#31803,#31804,
#31805,#31806,#31807,#31808,#31809,#31810,#31811,#31812,#31813,#31814,#31815,
#31816,#31817,#31818,#31819,#31820,#31821,#31822,#31823,#31824),
 .UNSPECIFIED.,.F.,.F.,(4,3,3,3,3,3,3,3,4),(88.4017975350364,89.2363454693871,
90.0708934037379,90.9054413380886,91.7399892724394,92.5745372067901,93.4090851411408,
94.2436330754916,94.6849828422161),.UNSPECIFIED.);
#103=B_SPLINE_CURVE_WITH_KNOTS('',3,(#31829,#31830,#31831,#31832,#31833,
#31834,#31835,#31836,#31837,#31838,#31839,#31840,#31841,#31842,#31843,#31844,
#31845,#31846,#31847,#31848,#31849,#31850,#31851,#31852,#31853),
 .UNSPECIFIED.,.F.,.F.,(4,3,3,3,3,3,3,3,4),(-104.195623098859,-103.361075164508,
-102.526527230158,-101.691979295807,-100.857431361456,-100.022883427105,
-99.1883354927548,-98.3537875584041,-97.9124377916795),.UNSPECIFIED.);
#104=B_SPLINE_CURVE_WITH_KNOTS('',3,(#31854,#31855,#31856,#31857,#31858,
#31859,#31860,#31861,#31862,#31863,#31864,#31865,#31866,#31867,#31868,#31869,
#31870,#31871,#31872,#31873,#31874,#31875,#31876,#31877,#31878),
 .UNSPECIFIED.,.F.,.F.,(4,3,3,3,3,3,3,3,4),(94.6849828422161,94.9773559459882,
95.9771175875249,96.9768792290616,97.47676004983,97.9766408705983,98.976402512135,
99.9761641536718,100.968168149396),.UNSPECIFIED.);
#105=B_SPLINE_CURVE_WITH_KNOTS('',3,(#31883,#31884,#31885,#31886,#31887,
#31888,#31889,#31890,#31891,#31892,#31893,#31894,#31895,#31896,#31897,#31898,
#31899,#31900,#31901,#31902,#31903,#31904,#31905,#31906,#31907),
 .UNSPECIFIED.,.F.,.F.,(4,3,3,3,3,3,3,3,4),(-110.478808406039,-109.973780569039,
-108.974018927502,-107.974257285965,-106.974495644429,-105.974734002892,
-104.974972361355,-104.475091540587,-104.195623098859),.UNSPECIFIED.);
#106=B_SPLINE_CURVE_WITH_KNOTS('',3,(#31908,#31909,#31910,#31911,#31912,
#31913,#31914,#31915,#31916,#31917,#31918,#31919,#31920,#31921,#31922,#31923,
#31924,#31925,#31926,#31927,#31928,#31929,#31930,#31931,#31932,#31933,#31934,
#31935),.UNSPECIFIED.,.F.,.F.,(4,3,3,3,3,3,3,3,3,4),(100.968168149396,100.975925795209,
101.975687436745,102.975449078282,103.975210719819,104.475091540587,104.974972361355,
105.974734002892,106.974495644429,107.251353456575),.UNSPECIFIED.);
#107=B_SPLINE_CURVE_WITH_KNOTS('',3,(#31940,#31941,#31942,#31943,#31944,
#31945,#31946,#31947,#31948,#31949,#31950,#31951,#31952,#31953,#31954,#31955,
#31956,#31957,#31958,#31959,#31960,#31961,#31962,#31963,#31964),
 .UNSPECIFIED.,.F.,.F.,(4,3,3,3,3,3,3,3,4),(-116.761993713218,-115.927445778868,
-115.092897844517,-114.258349910166,-113.423801975815,-112.589254041465,
-111.754706107114,-110.920158172763,-110.478808406039),.UNSPECIFIED.);
#108=B_SPLINE_CURVE_WITH_KNOTS('',3,(#31965,#31966,#31967,#31968,#31969,
#31970,#31971,#31972,#31973,#31974,#31975,#31976,#31977,#31978,#31979,#31980,
#31981,#31982,#31983,#31984,#31985,#31986,#31987,#31988,#31989),
 .UNSPECIFIED.,.F.,.F.,(4,3,3,3,3,3,3,3,4),(107.251353456575,108.085901390926,
108.920449325277,109.754997259627,110.589545193978,111.424093128329,112.258641062679,
113.09318899703,113.534538763755),.UNSPECIFIED.);
#109=B_SPLINE_CURVE_WITH_KNOTS('',3,(#31994,#31995,#31996,#31997,#31998,
#31999,#32000,#32001,#32002,#32003,#32004,#32005,#32006,#32007,#32008,#32009,
#32010,#32011,#32012,#32013,#32014,#32015,#32016,#32017,#32018),
 .UNSPECIFIED.,.F.,.F.,(4,3,3,3,3,3,3,3,4),(-123.045179020398,-122.210631086047,
-121.376083151696,-120.541535217346,-119.706987282995,-118.872439348644,
-118.037891414293,-117.203343479943,-116.761993713218),.UNSPECIFIED.);
#110=B_SPLINE_CURVE_WITH_KNOTS('',3,(#32019,#32020,#32021,#32022,#32023,
#32024,#32025,#32026,#32027,#32028,#32029,#32030,#32031,#32032,#32033,#32034,
#32035,#32036,#32037,#32038,#32039,#32040,#32041,#32042,#32043),
 .UNSPECIFIED.,.F.,.F.,(4,3,3,3,3,3,3,3,4),(113.534538763755,114.369086698105,
115.203634632456,116.038182566807,116.872730501158,117.707278435508,118.541826369859,
119.37637430421,119.817724070934),.UNSPECIFIED.);
#111=B_SPLINE_CURVE_WITH_KNOTS('',3,(#32048,#32049,#32050,#32051,#32052,
#32053,#32054,#32055,#32056,#32057,#32058,#32059,#32060,#32061,#32062,#32063,
#32064,#32065,#32066,#32067,#32068,#32069,#32070,#32071,#32072),
 .UNSPECIFIED.,.F.,.F.,(4,3,3,3,3,3,3,3,4),(-129.328364327577,-128.969251758236,
-127.9694901167,-126.969728475163,-125.969966833626,-125.470086012858,-124.97020519209,
-123.970443550553,-123.045179020398),.UNSPECIFIED.);
#112=B_SPLINE_CURVE_WITH_KNOTS('',3,(#32073,#32074,#32075,#32076,#32077,
#32078,#32079,#32080,#32081,#32082,#32083,#32084,#32085,#32086,#32087,#32088,
#32089,#32090,#32091,#32092,#32093,#32094,#32095,#32096,#32097),
 .UNSPECIFIED.,.F.,.F.,(4,3,3,3,3,3,3,3,4),(119.817724070934,120.652272005285,
121.486819939636,122.321367873986,123.155915808337,123.990463742688,124.825011677039,
125.659559611389,126.100909378114),.UNSPECIFIED.);
#113=B_SPLINE_CURVE_WITH_KNOTS('',3,(#32102,#32103,#32104,#32105,#32106,
#32107,#32108,#32109,#32110,#32111,#32112,#32113,#32114,#32115,#32116,#32117,
#32118,#32119,#32120,#32121,#32122,#32123,#32124,#32125,#32126),
 .UNSPECIFIED.,.F.,.F.,(4,3,3,3,3,3,3,3,4),(-135.611549634757,-134.967821607457,
-133.96805996592,-132.968298324383,-132.468417503615,-131.968536682847,
-130.96877504131,-129.969013399773,-129.328364327577),.UNSPECIFIED.);
#114=B_SPLINE_CURVE_WITH_KNOTS('',3,(#32127,#32128,#32129,#32130,#32131,
#32132,#32133,#32134,#32135,#32136,#32137,#32138,#32139,#32140,#32141,#32142,
#32143,#32144,#32145,#32146,#32147,#32148),.UNSPECIFIED.,.F.,.F.,(4,3,3,
3,3,3,3,4),(126.100909378114,126.969728475163,127.9694901167,128.969251758237,
129.969013399773,130.96877504131,131.968536682847,132.384094685294),
 .UNSPECIFIED.);
#115=B_SPLINE_CURVE_WITH_KNOTS('',3,(#32153,#32154,#32155,#32156,#32157,
#32158,#32159,#32160,#32161,#32162,#32163,#32164,#32165,#32166,#32167,#32168,
#32169,#32170,#32171,#32172,#32173,#32174,#32175,#32176,#32177),
 .UNSPECIFIED.,.F.,.F.,(4,3,3,3,3,3,3,3,4),(-141.894734941937,-140.966391456677,
-139.96662981514,-139.466748994372,-138.966868173604,-137.967106532067,
-136.96734489053,-135.967583248994,-135.611549634757),.UNSPECIFIED.);
#116=B_SPLINE_CURVE_WITH_KNOTS('',3,(#32178,#32179,#32180,#32181,#32182,
#32183,#32184,#32185,#32186,#32187,#32188,#32189,#32190,#32191,#32192,#32193,
#32194,#32195,#32196,#32197,#32198,#32199,#32200,#32201,#32202),
 .UNSPECIFIED.,.F.,.F.,(4,3,3,3,3,3,3,3,4),(132.384094685294,133.218642619644,
134.053190553995,134.887738488346,135.722286422696,136.556834357047,137.391382291398,
138.225930225748,138.667279992473),.UNSPECIFIED.);
#117=B_SPLINE_CURVE_WITH_KNOTS('',3,(#32207,#32208,#32209,#32210,#32211,
#32212,#32213,#32214,#32215,#32216,#32217,#32218,#32219,#32220,#32221,#32222,
#32223,#32224,#32225,#32226,#32227,#32228,#32229,#32230,#32231),
 .UNSPECIFIED.,.F.,.F.,(4,3,3,3,3,3,3,3,4),(-148.177920249116,-147.343372314765,
-146.508824380415,-145.674276446064,-144.839728511713,-144.005180577363,
-143.170632643012,-142.336084708661,-141.894734941937),.UNSPECIFIED.);
#118=B_SPLINE_CURVE_WITH_KNOTS('',3,(#32232,#32233,#32234,#32235,#32236,
#32237,#32238,#32239,#32240,#32241,#32242,#32243,#32244,#32245,#32246,#32247,
#32248,#32249,#32250,#32251,#32252,#32253,#32254,#32255,#32256),
 .UNSPECIFIED.,.F.,.F.,(4,3,3,3,3,3,3,3,4),(138.667279992473,138.966868173604,
139.466748994372,139.96662981514,140.966391456677,141.966153098214,142.965914739751,
143.965676381287,144.950465299653),.UNSPECIFIED.);
#119=B_SPLINE_CURVE_WITH_KNOTS('',3,(#32261,#32262,#32263,#32264,#32265,
#32266,#32267,#32268,#32269,#32270,#32271,#32272,#32273,#32274,#32275,#32276,
#32277,#32278,#32279,#32280,#32281,#32282,#32283,#32284,#32285),
 .UNSPECIFIED.,.F.,.F.,(4,3,3,3,3,3,3,3,4),(-154.461105556296,-153.626557621945,
-152.792009687594,-151.957461753244,-151.122913818893,-150.288365884542,
-149.453817950192,-148.619270015841,-148.177920249116),.UNSPECIFIED.);
#120=B_SPLINE_CURVE_WITH_KNOTS('',3,(#32286,#32287,#32288,#32289,#32290,
#32291,#32292,#32293,#32294,#32295,#32296,#32297,#32298,#32299,#32300,#32301,
#32302,#32303,#32304,#32305,#32306,#32307,#32308,#32309,#32310),
 .UNSPECIFIED.,.F.,.F.,(4,3,3,3,3,3,3,3,4),(144.950465299653,145.785013234003,
146.619561168354,147.454109102705,148.288657037055,149.123204971406,149.957752905757,
150.792300840108,151.233650606832),.UNSPECIFIED.);
#121=B_SPLINE_CURVE_WITH_KNOTS('',3,(#32315,#32316,#32317,#32318,#32319,
#32320,#32321,#32322,#32323,#32324,#32325,#32326,#32327,#32328,#32329,#32330,
#32331,#32332,#32333,#32334,#32335,#32336,#32337,#32338,#32339),
 .UNSPECIFIED.,.F.,.F.,(4,3,3,3,3,3,3,3,4),(-160.744290863475,-160.461743466643,
-159.961862645875,-158.962101004338,-157.962339362801,-156.962577721265,
-155.962816079728,-154.963054438191,-154.461105556296),.UNSPECIFIED.);
#122=B_SPLINE_CURVE_WITH_KNOTS('',3,(#32340,#32341,#32342,#32343,#32344,
#32345,#32346,#32347,#32348,#32349,#32350,#32351,#32352,#32353,#32354,#32355,
#32356,#32357,#32358,#32359,#32360,#32361,#32362,#32363,#32364),
 .UNSPECIFIED.,.F.,.F.,(4,3,3,3,3,3,3,3,4),(151.233650606832,152.068198541183,
152.902746475534,153.737294409884,154.571842344235,155.406390278586,156.240938212937,
157.075486147287,157.516835914012),.UNSPECIFIED.);
#123=B_SPLINE_CURVE_WITH_KNOTS('',3,(#32369,#32370,#32371,#32372,#32373,
#32374,#32375,#32376,#32377,#32378,#32379,#32380,#32381,#32382,#32383,#32384,
#32385,#32386,#32387,#32388,#32389,#32390,#32391,#32392,#32393),
 .UNSPECIFIED.,.F.,.F.,(4,3,3,3,3,3,3,3,4),(-167.027476170655,-166.192928236304,
-165.358380301953,-164.523832367603,-163.689284433252,-162.854736498901,
-162.02018856455,-161.1856406302,-160.744290863475),.UNSPECIFIED.);
#124=B_SPLINE_CURVE_WITH_KNOTS('',3,(#32394,#32395,#32396,#32397,#32398,
#32399,#32400,#32401,#32402,#32403,#32404,#32405,#32406,#32407,#32408,#32409,
#32410,#32411,#32412,#32413,#32414,#32415,#32416,#32417,#32418),
 .UNSPECIFIED.,.F.,.F.,(4,3,3,3,3,3,3,3,4),(157.516835914012,157.962339362801,
158.962101004338,159.961862645875,160.461743466643,160.961624287412,161.961385928948,
162.961147570485,163.800021221191),.UNSPECIFIED.);
#125=B_SPLINE_CURVE_WITH_KNOTS('',3,(#32423,#32424,#32425,#32426,#32427,
#32428,#32429,#32430,#32431,#32432,#32433,#32434,#32435,#32436,#32437,#32438,
#32439,#32440,#32441,#32442,#32443,#32444,#32445,#32446,#32447),
 .UNSPECIFIED.,.F.,.F.,(4,3,3,3,3,3,3,3,4),(-173.310661477834,-172.958763985852,
-171.959002344315,-170.959240702779,-169.959479061242,-168.959717419705,
-167.959955778168,-167.4600749574,-167.027476170655),.UNSPECIFIED.);
#126=B_SPLINE_CURVE_WITH_KNOTS('',3,(#32448,#32449,#32450,#32451,#32452,
#32453,#32454,#32455,#32456,#32457,#32458,#32459,#32460,#32461,#32462,#32463,
#32464,#32465,#32466,#32467,#32468,#32469,#32470,#32471,#32472,#32473,#32474,
#32475),.UNSPECIFIED.,.F.,.F.,(4,3,3,3,3,3,3,3,3,4),(163.800021221191,163.960909212022,
164.960670853558,165.960432495095,166.960194136632,167.4600749574,167.959955778169,
168.959717419705,169.959479061242,170.083206528371),.UNSPECIFIED.);
#127=B_SPLINE_CURVE_WITH_KNOTS('',3,(#32480,#32481,#32482,#32483,#32484,
#32485,#32486,#32487,#32488,#32489,#32490,#32491,#32492,#32493,#32494,#32495,
#32496,#32497,#32498,#32499,#32500,#32501,#32502,#32503,#32504),
 .UNSPECIFIED.,.F.,.F.,(4,3,3,3,3,3,3,3,4),(-179.593846785014,-178.759298850663,
-177.924750916312,-177.090202981962,-176.255655047611,-175.42110711326,
-174.586559178909,-173.752011244559,-173.310661477834),.UNSPECIFIED.);
#128=B_SPLINE_CURVE_WITH_KNOTS('',3,(#32505,#32506,#32507,#32508,#32509,
#32510,#32511,#32512,#32513,#32514,#32515,#32516,#32517,#32518,#32519,#32520,
#32521,#32522,#32523,#32524,#32525,#32526,#32527,#32528,#32529),
 .UNSPECIFIED.,.F.,.F.,(4,3,3,3,3,3,3,3,4),(170.083206528371,170.959240702779,
171.959002344316,172.958763985852,173.958525627389,174.458406448157,174.958287268926,
175.958048910462,176.366391835551),.UNSPECIFIED.);
#129=B_SPLINE_CURVE_WITH_KNOTS('',3,(#32534,#32535,#32536,#32537,#32538,
#32539,#32540,#32541,#32542,#32543,#32544,#32545,#32546,#32547,#32548,#32549,
#32550,#32551,#32552,#32553,#32554,#32555,#32556,#32557,#32558),
 .UNSPECIFIED.,.F.,.F.,(4,3,3,3,3,3,3,3,4),(-185.877032092193,-184.955903684293,
-183.956142042756,-182.956380401219,-181.956618759682,-181.456737938914,
-180.956857118146,-179.957095476609,-179.593846785014),.UNSPECIFIED.);
#130=B_SPLINE_CURVE_WITH_KNOTS('',3,(#32559,#32560,#32561,#32562,#32563,
#32564,#32565,#32566,#32567,#32568,#32569,#32570,#32571,#32572,#32573,#32574,
#32575,#32576,#32577,#32578,#32579,#32580,#32581,#32582,#32583),
 .UNSPECIFIED.,.F.,.F.,(4,3,3,3,3,3,3,3,4),(176.366391835551,177.200939769901,
178.035487704252,178.870035638603,179.704583572953,180.539131507304,181.373679441655,
182.208227376006,182.64957714273),.UNSPECIFIED.);
#131=B_SPLINE_CURVE_WITH_KNOTS('',3,(#32588,#32589,#32590,#32591,#32592,
#32593,#32594,#32595,#32596,#32597,#32598,#32599,#32600,#32601,#32602,#32603,
#32604,#32605,#32606,#32607,#32608,#32609,#32610,#32611,#32612,#32613,#32614,
#32615),.UNSPECIFIED.,.F.,.F.,(4,3,3,3,3,3,3,3,3,4),(-192.160217399373,
-191.95423517505,-190.954473533513,-189.954711891976,-188.954950250439,
-188.455069429671,-187.955188608903,-186.955426967366,-185.955665325829,
-185.877032092193),.UNSPECIFIED.);
#132=B_SPLINE_CURVE_WITH_KNOTS('',3,(#32616,#32617,#32618,#32619,#32620,
#32621,#32622,#32623,#32624,#32625,#32626,#32627,#32628,#32629,#32630,#32631,
#32632,#32633,#32634,#32635,#32636,#32637,#32638,#32639,#32640),
 .UNSPECIFIED.,.F.,.F.,(4,3,3,3,3,3,3,3,4),(182.64957714273,182.956380401219,
183.956142042756,184.955903684293,185.95566532583,186.955426967366,187.955188608903,
188.455069429671,188.93276244991),.UNSPECIFIED.);
#133=B_SPLINE_CURVE_WITH_KNOTS('',3,(#32645,#32646,#32647,#32648,#32649,
#32650,#32651,#32652,#32653,#32654,#32655,#32656,#32657,#32658,#32659,#32660,
#32661,#32662,#32663,#32664,#32665,#32666,#32667,#32668,#32669),
 .UNSPECIFIED.,.F.,.F.,(4,3,3,3,3,3,3,3,4),(-198.443402706553,-197.95280502427,
-196.953043382733,-195.953281741197,-195.453400920428,-194.95352009966,
-193.953758458123,-192.953996816586,-192.160217399373),.UNSPECIFIED.);
#134=B_SPLINE_CURVE_WITH_KNOTS('',3,(#32670,#32671,#32672,#32673,#32674,
#32675,#32676,#32677,#32678,#32679,#32680,#32681,#32682,#32683,#32684,#32685,
#32686,#32687,#32688,#32689,#32690,#32691,#32692,#32693,#32694),
 .UNSPECIFIED.,.F.,.F.,(4,3,3,3,3,3,3,3,4),(188.93276244991,188.95495025044,
189.954711891976,190.954473533513,191.95423517505,192.953996816587,193.953758458123,
194.95352009966,195.215947757089),.UNSPECIFIED.);
#135=B_SPLINE_CURVE_WITH_KNOTS('',3,(#32699,#32700,#32701,#32702,#32703,
#32704,#32705,#32706,#32707,#32708,#32709,#32710,#32711,#32712,#32713,#32714,
#32715,#32716,#32717,#32718,#32719,#32720,#32721,#32722,#32723),
 .UNSPECIFIED.,.F.,.F.,(4,3,3,3,3,3,3,3,4),(-204.726588013732,-203.892040079381,
-203.057492145031,-202.22294421068,-201.388396276329,-200.553848341979,
-199.719300407628,-198.884752473277,-198.443402706553),.UNSPECIFIED.);
#136=B_SPLINE_CURVE_WITH_KNOTS('',3,(#32724,#32725,#32726,#32727,#32728,
#32729,#32730,#32731,#32732,#32733,#32734,#32735,#32736,#32737,#32738,#32739,
#32740,#32741,#32742,#32743,#32744,#32745,#32746,#32747,#32748),
 .UNSPECIFIED.,.F.,.F.,(4,3,3,3,3,3,3,3,4),(195.215947757089,196.05049569144,
196.885043625791,197.719591560141,198.554139494492,199.388687428843,200.223235363194,
201.057783297544,201.499133064269),.UNSPECIFIED.);
#137=B_SPLINE_CURVE_WITH_KNOTS('',3,(#32753,#32754,#32755,#32756,#32757,
#32758,#32759,#32760,#32761,#32762,#32763,#32764,#32765,#32766,#32767,#32768,
#32769,#32770,#32771,#32772,#32773,#32774,#32775,#32776,#32777),
 .UNSPECIFIED.,.F.,.F.,(4,3,3,3,3,3,3,3,4),(-211.009773320912,-210.175225386561,
-209.34067745221,-208.506129517859,-207.671581583509,-206.837033649158,
-206.002485714807,-205.167937780456,-204.726588013732),.UNSPECIFIED.);
#138=B_SPLINE_CURVE_WITH_KNOTS('',3,(#32778,#32779,#32780,#32781,#32782,
#32783,#32784,#32785,#32786,#32787,#32788,#32789,#32790,#32791,#32792,#32793,
#32794,#32795,#32796,#32797,#32798,#32799,#32800,#32801,#32802),
 .UNSPECIFIED.,.F.,.F.,(4,3,3,3,3,3,3,3,4),(201.499133064269,201.951851590417,
202.451732411185,202.951613231954,203.95137487349,204.951136515027,205.950898156564,
206.950659798101,207.782318371448),.UNSPECIFIED.);
#139=B_SPLINE_CURVE_WITH_KNOTS('',3,(#32807,#32808,#32809,#32810,#32811,
#32812,#32813,#32814,#32815,#32816,#32817,#32818,#32819,#32820,#32821,#32822,
#32823,#32824,#32825,#32826,#32827,#32828,#32829,#32830,#32831),
 .UNSPECIFIED.,.F.,.F.,(4,3,3,3,3,3,3,3,4),(-217.292958628091,-216.948276213468,
-216.448395392699,-215.948514571931,-214.948752930394,-213.948991288857,
-212.949229647321,-211.949468005784,-211.009773320912),.UNSPECIFIED.);
#140=B_SPLINE_CURVE_WITH_KNOTS('',3,(#32832,#32833,#32834,#32835,#32836,
#32837,#32838,#32839,#32840,#32841,#32842,#32843,#32844,#32845,#32846,#32847,
#32848,#32849,#32850,#32851,#32852,#32853,#32854,#32855,#32856),
 .UNSPECIFIED.,.F.,.F.,(4,3,3,3,3,3,3,3,4),(207.782318371448,208.616866305799,
209.45141424015,210.285962174501,211.120510108851,211.955058043202,212.789605977553,
213.624153911904,214.065503678628),.UNSPECIFIED.);
#141=B_SPLINE_CURVE_WITH_KNOTS('',3,(#32861,#32862,#32863,#32864,#32865,
#32866,#32867,#32868,#32869,#32870,#32871,#32872,#32873,#32874,#32875,#32876,
#32877,#32878,#32879,#32880,#32881,#32882,#32883,#32884,#32885),
 .UNSPECIFIED.,.F.,.F.,(4,3,3,3,3,3,3,3,4),(-223.576143935271,-222.74159600092,
-221.907048066569,-221.072500132219,-220.237952197868,-219.403404263517,
-218.568856329166,-217.734308394816,-217.292958628091),.UNSPECIFIED.);
#142=B_SPLINE_CURVE_WITH_KNOTS('',3,(#32886,#32887,#32888,#32889,#32890,
#32891,#32892,#32893,#32894,#32895,#32896,#32897,#32898,#32899,#32900,#32901,
#32902,#32903,#32904,#32905,#32906,#32907,#32908,#32909,#32910),
 .UNSPECIFIED.,.F.,.F.,(4,3,3,3,3,3,3,3,4),(214.065503678628,214.948752930394,
215.948514571931,216.448395392699,216.948276213468,217.948037855004,218.947799496541,
219.947561138078,220.348688985807),.UNSPECIFIED.);
#143=B_SPLINE_CURVE_WITH_KNOTS('',3,(#32915,#32916,#32917,#32918,#32919,
#32920,#32921,#32922,#32923,#32924,#32925,#32926,#32927,#32928,#32929,#32930,
#32931,#32932,#32933,#32934,#32935,#32936),.UNSPECIFIED.,.F.,.F.,(4,3,3,
3,3,3,3,4),(-229.85932924245,-228.945415911908,-227.945654270371,-226.945892628835,
-225.946130987298,-224.946369345761,-223.946607704225,-223.576143935271),
 .UNSPECIFIED.);
#144=B_SPLINE_CURVE_WITH_KNOTS('',3,(#32937,#32938,#32939,#32940,#32941,
#32942,#32943,#32944,#32945,#32946,#32947,#32948,#32949,#32950,#32951,#32952,
#32953,#32954,#32955,#32956,#32957,#32958,#32959,#32960,#32961),
 .UNSPECIFIED.,.F.,.F.,(4,3,3,3,3,3,3,3,4),(220.348688985807,220.947322779615,
221.947084421151,222.946846062688,223.446726883456,223.946607704225,224.946369345762,
225.946130987298,226.631874292987),.UNSPECIFIED.);
#145=B_SPLINE_CURVE_WITH_KNOTS('',3,(#32966,#32967,#32968,#32969,#32970,
#32971,#32972,#32973,#32974,#32975,#32976,#32977,#32978,#32979,#32980,#32981,
#32982,#32983,#32984,#32985,#32986,#32987,#32988,#32989,#32990),
 .UNSPECIFIED.,.F.,.F.,(4,3,3,3,3,3,3,3,4),(-236.14251454963,-235.307966615279,
-234.473418680928,-233.638870746578,-232.804322812227,-231.969774877876,
-231.135226943525,-230.300679009175,-229.85932924245),.UNSPECIFIED.);
#146=B_SPLINE_CURVE_WITH_KNOTS('',3,(#32991,#32992,#32993,#32994,#32995,
#32996,#32997,#32998,#32999,#33000,#33001,#33002,#33003,#33004,#33005,#33006,
#33007,#33008,#33009,#33010,#33011,#33012,#33013,#33014,#33015),
 .UNSPECIFIED.,.F.,.F.,(4,3,3,3,3,3,3,3,4),(226.631874292987,226.945892628835,
227.945654270372,228.945415911908,229.945177553445,230.445058374213,230.944939194982,
231.944700836519,232.915059600167),.UNSPECIFIED.);
#147=B_SPLINE_CURVE_WITH_KNOTS('',3,(#33020,#33021,#33022,#33023,#33024,
#33025,#33026,#33027,#33028,#33029,#33030,#33031,#33032,#33033,#33034,#33035,
#33036,#33037,#33038,#33039,#33040,#33041,#33042,#33043,#33044),
 .UNSPECIFIED.,.F.,.F.,(4,3,3,3,3,3,3,3,4),(-242.42569985681,-241.591151922459,
-240.756603988108,-239.922056053757,-239.087508119407,-238.252960185056,
-237.418412250705,-236.583864316354,-236.14251454963),.UNSPECIFIED.);
#148=B_SPLINE_CURVE_WITH_KNOTS('',3,(#33045,#33046,#33047,#33048,#33049,
#33050,#33051,#33052,#33053,#33054,#33055,#33056,#33057,#33058,#33059,#33060,
#33061,#33062,#33063,#33064,#33065,#33066,#33067,#33068,#33069),
 .UNSPECIFIED.,.F.,.F.,(4,3,3,3,3,3,3,3,4),(232.915059600167,233.749607534517,
234.584155468868,235.418703403219,236.253251337569,237.08779927192,237.922347206271,
238.756895140621,239.198244907346),.UNSPECIFIED.);
#149=B_SPLINE_CURVE_WITH_KNOTS('',3,(#33074,#33075,#33076,#33077,#33078,
#33079,#33080,#33081,#33082,#33083,#33084,#33085,#33086,#33087,#33088,#33089,
#33090,#33091,#33092,#33093,#33094,#33095,#33096,#33097,#33098),
 .UNSPECIFIED.,.F.,.F.,(4,3,3,3,3,3,3,3,4),(-248.708885163989,-247.874337229638,
-247.039789295288,-246.205241360937,-245.370693426586,-244.536145492235,
-243.701597557885,-242.867049623534,-242.42569985681),.UNSPECIFIED.);
#150=B_SPLINE_CURVE_WITH_KNOTS('',3,(#33099,#33100,#33101,#33102,#33103,
#33104,#33105,#33106,#33107,#33108,#33109,#33110,#33111,#33112,#33113,#33114,
#33115,#33116,#33117,#33118,#33119,#33120,#33121,#33122,#33123),
 .UNSPECIFIED.,.F.,.F.,(4,3,3,3,3,3,3,3,4),(239.198244907346,240.032792841697,
240.867340776048,241.701888710398,242.536436644749,243.3709845791,244.20553251345,
245.040080447801,245.481430214526),.UNSPECIFIED.);
#151=B_SPLINE_CURVE_WITH_KNOTS('',3,(#33128,#33129,#33130,#33131,#33132,
#33133,#33134,#33135,#33136,#33137,#33138,#33139,#33140,#33141,#33142,#33143,
#33144,#33145,#33146,#33147,#33148,#33149,#33150,#33151,#33152,#33153,#33154,
#33155),.UNSPECIFIED.,.F.,.F.,(4,3,3,3,3,3,3,3,3,4),(-254.992070471169,
-254.939218591863,-253.939456950326,-252.939695308789,-251.939933667253,
-251.440052846484,-250.940172025716,-249.940410384179,-248.940648742643,
-248.708885163989),.UNSPECIFIED.);
#152=B_SPLINE_CURVE_WITH_KNOTS('',3,(#33156,#33157,#33158,#33159,#33160,
#33161,#33162,#33163,#33164,#33165,#33166,#33167,#33168,#33169,#33170,#33171,
#33172,#33173,#33174,#33175,#33176,#33177,#33178,#33179,#33180),
 .UNSPECIFIED.,.F.,.F.,(4,3,3,3,3,3,3,3,4),(245.481430214526,245.941363818033,
246.941125459569,247.940887101106,248.940648742643,249.940410384179,250.940172025716,
251.440052846485,251.764615521705),.UNSPECIFIED.);
#153=B_SPLINE_CURVE_WITH_KNOTS('',3,(#33185,#33186,#33187,#33188,#33189,
#33190,#33191,#33192,#33193,#33194,#33195,#33196,#33197,#33198,#33199,#33200,
#33201,#33202,#33203,#33204,#33205,#33206,#33207,#33208,#33209),
 .UNSPECIFIED.,.F.,.F.,(4,3,3,3,3,3,3,3,4),(-261.275255778348,-260.937788441083,
-259.938026799546,-258.93826515801,-258.438384337241,-257.938503516473,
-256.938741874936,-255.9389802334,-254.992070471169),.UNSPECIFIED.);
#154=B_SPLINE_CURVE_WITH_KNOTS('',3,(#33210,#33211,#33212,#33213,#33214,
#33215,#33216,#33217,#33218,#33219,#33220,#33221,#33222,#33223,#33224,#33225,
#33226,#33227,#33228,#33229,#33230,#33231,#33232,#33233,#33234),
 .UNSPECIFIED.,.F.,.F.,(4,3,3,3,3,3,3,3,4),(251.764615521705,252.599163456056,
253.433711390407,254.268259324758,255.102807259108,255.937355193459,256.77190312781,
257.606451062161,258.047800828885),.UNSPECIFIED.);
#155=B_SPLINE_CURVE_WITH_KNOTS('',3,(#33239,#33240,#33241,#33242,#33243,
#33244,#33245,#33246,#33247,#33248,#33249,#33250,#33251,#33252,#33253,#33254,
#33255,#33256,#33257,#33258,#33259,#33260,#33261,#33262,#33263),
 .UNSPECIFIED.,.F.,.F.,(4,3,3,3,3,3,3,3,4),(-267.558441085528,-266.723893151177,
-265.889345216826,-265.054797282476,-264.220249348125,-263.385701413774,
-262.551153479423,-261.716605545073,-261.275255778348),.UNSPECIFIED.);
#156=B_SPLINE_CURVE_WITH_KNOTS('',3,(#33264,#33265,#33266,#33267,#33268,
#33269,#33270,#33271,#33272,#33273,#33274,#33275,#33276,#33277,#33278,#33279,
#33280,#33281,#33282,#33283,#33284,#33285,#33286,#33287,#33288),
 .UNSPECIFIED.,.F.,.F.,(4,3,3,3,3,3,3,3,4),(258.047800828885,258.438384337242,
258.93826515801,259.938026799547,260.937788441083,261.93755008262,262.937311724157,
263.937073365694,264.330986136064),.UNSPECIFIED.);
#157=B_SPLINE_CURVE_WITH_KNOTS('',3,(#33293,#33294,#33295,#33296,#33297,
#33298,#33299,#33300,#33301,#33302,#33303,#33304,#33305,#33306,#33307,#33308,
#33309,#33310,#33311,#33312,#33313,#33314,#33315,#33316,#33317),
 .UNSPECIFIED.,.F.,.F.,(4,3,3,3,3,3,3,3,4),(-273.841626392707,-272.934928139524,
-272.435047318755,-271.935166497987,-270.93540485645,-269.935643214914,
-268.935881573377,-267.93611993184,-267.558441085528),.UNSPECIFIED.);
#158=B_SPLINE_CURVE_WITH_KNOTS('',3,(#33318,#33319,#33320,#33321,#33322,
#33323,#33324,#33325,#33326,#33327,#33328,#33329,#33330,#33331,#33332,#33333,
#33334,#33335,#33336,#33337,#33338,#33339,#33340,#33341,#33342),
 .UNSPECIFIED.,.F.,.F.,(4,3,3,3,3,3,3,3,4),(264.330986136064,265.165534070415,
266.000082004766,266.834629939117,267.669177873467,268.503725807818,269.338273742169,
270.17282167652,270.614171443244),.UNSPECIFIED.);
#159=B_SPLINE_CURVE_WITH_KNOTS('',3,(#33347,#33348,#33349,#33350,#33351,
#33352,#33353,#33354,#33355,#33356,#33357,#33358,#33359,#33360,#33361,#33362,
#33363,#33364,#33365,#33366,#33367,#33368,#33369,#33370,#33371),
 .UNSPECIFIED.,.F.,.F.,(4,3,3,3,3,3,3,3,4),(-280.124811699887,-279.290263765536,
-278.455715831186,-277.621167896835,-276.786619962484,-275.952072028133,
-275.117524093783,-274.282976159432,-273.841626392707),.UNSPECIFIED.);
#160=B_SPLINE_CURVE_WITH_KNOTS('',3,(#33372,#33373,#33374,#33375,#33376,
#33377,#33378,#33379,#33380,#33381,#33382,#33383,#33384,#33385,#33386,#33387,
#33388,#33389,#33390,#33391,#33392,#33393,#33394,#33395,#33396),
 .UNSPECIFIED.,.F.,.F.,(4,3,3,3,3,3,3,3,4),(270.614171443244,270.935404856451,
271.935166497987,272.435047318756,272.934928139524,273.934689781061,274.934451422597,
275.934213064134,276.897356750424),.UNSPECIFIED.);
#161=B_SPLINE_CURVE_WITH_KNOTS('',3,(#33401,#33402,#33403,#33404,#33405,
#33406,#33407,#33408,#33409,#33410,#33411,#33412,#33413,#33414,#33415,#33416,
#33417,#33418,#33419,#33420,#33421,#33422),.UNSPECIFIED.,.F.,.F.,(4,3,3,
3,3,3,3,4),(-286.407997007067,-285.931829479501,-284.932067837964,-283.932306196428,
-282.932544554891,-281.932782913354,-280.933021271817,-280.124811699887),
 .UNSPECIFIED.);
#162=B_SPLINE_CURVE_WITH_KNOTS('',3,(#33423,#33424,#33425,#33426,#33427,
#33428,#33429,#33430,#33431,#33432,#33433,#33434,#33435,#33436,#33437,#33438,
#33439,#33440,#33441,#33442,#33443,#33444,#33445,#33446,#33447,#33448,#33449,
#33450),.UNSPECIFIED.,.F.,.F.,(4,3,3,3,3,3,3,3,3,4),(276.897356750424,276.933974705671,
277.933736347208,278.933497988744,279.433378809513,279.933259630281,280.933021271818,
281.932782913354,282.932544554891,283.180542057603),.UNSPECIFIED.);
#163=B_SPLINE_CURVE_WITH_KNOTS('',3,(#33455,#33456,#33457,#33458,#33459,
#33460,#33461,#33462,#33463,#33464,#33465,#33466,#33467,#33468,#33469,#33470,
#33471,#33472,#33473,#33474,#33475,#33476,#33477,#33478,#33479),
 .UNSPECIFIED.,.F.,.F.,(4,3,3,3,3,3,3,3,4),(-292.691182314246,-291.856634379895,
-291.022086445545,-290.187538511194,-289.352990576843,-288.518442642492,
-287.683894708141,-286.849346773791,-286.407997007067),.UNSPECIFIED.);
#164=B_SPLINE_CURVE_WITH_KNOTS('',3,(#33480,#33481,#33482,#33483,#33484,
#33485,#33486,#33487,#33488,#33489,#33490,#33491,#33492,#33493,#33494,#33495,
#33496,#33497,#33498,#33499,#33500,#33501,#33502,#33503,#33504),
 .UNSPECIFIED.,.F.,.F.,(4,3,3,3,3,3,3,3,4),(283.180542057603,283.932306196428,
284.932067837965,285.931829479501,286.43171030027,286.931591121038,287.931352762575,
288.931114404111,289.463727364783),.UNSPECIFIED.);
#165=B_SPLINE_CURVE_WITH_KNOTS('',3,(#33509,#33510,#33511,#33512,#33513,
#33514,#33515,#33516,#33517,#33518,#33519,#33520,#33521,#33522,#33523,#33524,
#33525,#33526,#33527,#33528,#33529,#33530,#33531,#33532,#33533),
 .UNSPECIFIED.,.F.,.F.,(4,3,3,3,3,3,3,3,4),(-298.974367621426,-298.139819687075,
-297.305271752724,-296.470723818374,-295.636175884023,-294.801627949672,
-293.967080015322,-293.132532080971,-292.691182314246),.UNSPECIFIED.);
#166=B_SPLINE_CURVE_WITH_KNOTS('',3,(#33534,#33535,#33536,#33537,#33538,
#33539,#33540,#33541,#33542,#33543,#33544,#33545,#33546,#33547,#33548,#33549,
#33550,#33551,#33552,#33553,#33554,#33555,#33556,#33557,#33558),
 .UNSPECIFIED.,.F.,.F.,(4,3,3,3,3,3,3,3,4),(289.463727364783,290.298275299133,
291.132823233484,291.967371167835,292.801919102186,293.636467036536,294.471014970887,
295.305562905238,295.746912671962),.UNSPECIFIED.);
#167=B_SPLINE_CURVE_WITH_KNOTS('',3,(#33563,#33564,#33565,#33566,#33567,
#33568,#33569,#33570,#33571,#33572,#33573,#33574,#33575,#33576,#33577,#33578,
#33579,#33580,#33581,#33582,#33583,#33584,#33585,#33586,#33587),
 .UNSPECIFIED.,.F.,.F.,(4,3,3,3,3,3,3,3,4),(-305.257552928605,-304.423004994254,
-303.588457059904,-302.753909125553,-301.919361191202,-301.084813256852,
-300.250265322501,-299.41571738815,-298.974367621426),.UNSPECIFIED.);
#168=B_SPLINE_CURVE_WITH_KNOTS('',3,(#33588,#33589,#33590,#33591,#33592,
#33593,#33594,#33595,#33596,#33597,#33598,#33599,#33600,#33601,#33602,#33603,
#33604,#33605,#33606,#33607,#33608,#33609,#33610,#33611,#33612),
 .UNSPECIFIED.,.F.,.F.,(4,3,3,3,3,3,3,3,4),(295.746912671962,296.581460606313,
297.416008540664,298.250556475015,299.085104409365,299.919652343716,300.754200278067,
301.588748212418,302.030097979142),.UNSPECIFIED.);
#169=B_SPLINE_CURVE_WITH_KNOTS('',3,(#33617,#33618,#33619,#33620,#33621,
#33622,#33623,#33624,#33625,#33626,#33627,#33628,#33629,#33630,#33631,#33632,
#33633,#33634,#33635,#33636,#33637,#33638,#33639,#33640,#33641),
 .UNSPECIFIED.,.F.,.F.,(4,3,3,3,3,3,3,3,4),(-311.540738235785,-310.706190301434,
-309.871642367083,-309.037094432733,-308.202546498382,-307.367998564031,
-306.533450629681,-305.69890269533,-305.257552928605),.UNSPECIFIED.);
#170=B_SPLINE_CURVE_WITH_KNOTS('',3,(#33642,#33643,#33644,#33645,#33646,
#33647,#33648,#33649,#33650,#33651,#33652,#33653,#33654,#33655,#33656,#33657,
#33658,#33659,#33660,#33661,#33662,#33663,#33664,#33665,#33666),
 .UNSPECIFIED.,.F.,.F.,(4,3,3,3,3,3,3,3,4),(302.030097979142,302.927777385626,
303.927539027162,304.927300668699,305.927062310236,306.926823951772,307.426704772541,
307.926585593309,308.313283286321),.UNSPECIFIED.);
#171=B_SPLINE_CURVE_WITH_KNOTS('',3,(#33671,#33672,#33673,#33674,#33675,
#33676,#33677,#33678,#33679,#33680,#33681,#33682,#33683,#33684,#33685,#33686,
#33687,#33688,#33689,#33690,#33691,#33692,#33693,#33694,#33695),
 .UNSPECIFIED.,.F.,.F.,(4,3,3,3,3,3,3,3,4),(-317.823923542964,-316.924440367139,
-315.924678725603,-314.924917084066,-314.425036263297,-313.925155442529,
-312.925393800992,-311.925632159456,-311.540738235785),.UNSPECIFIED.);
#172=B_SPLINE_CURVE_WITH_KNOTS('',3,(#33696,#33697,#33698,#33699,#33700,
#33701,#33702,#33703,#33704,#33705,#33706,#33707,#33708,#33709,#33710,#33711,
#33712,#33713,#33714,#33715,#33716,#33717,#33718,#33719,#33720),
 .UNSPECIFIED.,.F.,.F.,(4,3,3,3,3,3,3,3,4),(308.313283286321,309.147831220672,
309.982379155023,310.816927089373,311.651475023724,312.486022958075,313.320570892425,
314.155118826776,314.596468593501),.UNSPECIFIED.);
#173=B_SPLINE_CURVE_WITH_KNOTS('',3,(#33725,#33726,#33727,#33728,#33729,
#33730,#33731,#33732,#33733,#33734,#33735,#33736,#33737,#33738,#33739,#33740,
#33741,#33742,#33743,#33744,#33745,#33746,#33747,#33748,#33749),
 .UNSPECIFIED.,.F.,.F.,(4,3,3,3,3,3,3,3,4),(-324.107108850144,-323.272560915793,
-322.438012981442,-321.603465047092,-320.768917112741,-319.93436917839,
-319.09982124404,-318.265273309689,-317.823923542964),.UNSPECIFIED.);
#174=B_SPLINE_CURVE_WITH_KNOTS('',3,(#33750,#33751,#33752,#33753,#33754,
#33755,#33756,#33757,#33758,#33759,#33760,#33761,#33762,#33763,#33764,#33765,
#33766,#33767,#33768,#33769,#33770,#33771),.UNSPECIFIED.,.F.,.F.,(4,3,3,
3,3,3,3,4),(314.596468593501,314.924917084066,315.924678725603,316.92444036714,
317.924202008676,318.923963650213,319.92372529175,320.87965390068),
 .UNSPECIFIED.);
#175=B_SPLINE_CURVE_WITH_KNOTS('',3,(#33776,#33777,#33778,#33779,#33780,
#33781,#33782,#33783,#33784,#33785,#33786,#33787,#33788,#33789,#33790,#33791,
#33792,#33793,#33794,#33795,#33796,#33797),.UNSPECIFIED.,.F.,.F.,(4,3,3,
3,3,3,3,4),(-330.390294157323,-329.921341707117,-328.92158006558,-327.921818424043,
-326.922056782507,-325.92229514097,-324.922533499433,-324.107108850144),
 .UNSPECIFIED.);
#176=B_SPLINE_CURVE_WITH_KNOTS('',3,(#33798,#33799,#33800,#33801,#33802,
#33803,#33804,#33805,#33806,#33807,#33808,#33809,#33810,#33811,#33812,#33813,
#33814,#33815,#33816,#33817,#33818,#33819,#33820,#33821,#33822,#33823,#33824,
#33825),.UNSPECIFIED.,.F.,.F.,(4,3,3,3,3,3,3,3,3,4),(320.87965390068,320.923486933286,
321.923248574823,322.92301021636,323.422891037128,323.922771857897,324.922533499433,
325.92229514097,326.922056782507,327.16283920786),.UNSPECIFIED.);
#177=B_SPLINE_CURVE_WITH_KNOTS('',3,(#33830,#33831,#33832,#33833,#33834,
#33835,#33836,#33837,#33838,#33839,#33840,#33841,#33842,#33843,#33844,#33845,
#33846,#33847,#33848,#33849,#33850,#33851,#33852,#33853,#33854),
 .UNSPECIFIED.,.F.,.F.,(4,3,3,3,3,3,3,3,4),(-336.673479464503,-335.838931530152,
-335.004383595801,-334.169835661451,-333.3352877271,-332.500739792749,-331.666191858398,
-330.831643924048,-330.390294157323),.UNSPECIFIED.);
#178=B_SPLINE_CURVE_WITH_KNOTS('',3,(#33855,#33856,#33857,#33858,#33859,
#33860,#33861,#33862,#33863,#33864,#33865,#33866,#33867,#33868,#33869,#33870,
#33871,#33872,#33873,#33874,#33875,#33876,#33877,#33878,#33879),
 .UNSPECIFIED.,.F.,.F.,(4,3,3,3,3,3,3,3,4),(327.16283920786,327.921818424043,
328.92158006558,329.921341707117,330.421222527885,330.921103348654,331.92086499019,
332.920626631727,333.44602451504),.UNSPECIFIED.);
#179=B_SPLINE_CURVE_WITH_KNOTS('',3,(#33884,#33885,#33886,#33887,#33888,
#33889,#33890,#33891,#33892,#33893,#33894,#33895,#33896,#33897,#33898,#33899,
#33900,#33901,#33902,#33903,#33904,#33905,#33906,#33907,#33908),
 .UNSPECIFIED.,.F.,.F.,(4,3,3,3,3,3,3,3,4),(-342.956664771683,-342.122116837332,
-341.287568902981,-340.45302096863,-339.61847303428,-338.783925099929,-337.949377165578,
-337.114829231228,-336.673479464503),.UNSPECIFIED.);
#180=B_SPLINE_CURVE_WITH_KNOTS('',3,(#33909,#33910,#33911,#33912,#33913,
#33914,#33915,#33916,#33917,#33918,#33919,#33920,#33921,#33922,#33923,#33924,
#33925,#33926,#33927,#33928,#33929,#33930,#33931,#33932,#33933),
 .UNSPECIFIED.,.F.,.F.,(4,3,3,3,3,3,3,3,4),(333.44602451504,334.28057244939,
335.115120383741,335.949668318092,336.784216252443,337.618764186793,338.453312121144,
339.287860055495,339.729209822219),.UNSPECIFIED.);
#181=B_SPLINE_CURVE_WITH_KNOTS('',3,(#33938,#33939,#33940,#33941,#33942,
#33943,#33944,#33945,#33946,#33947,#33948,#33949,#33950,#33951,#33952,#33953,
#33954,#33955,#33956,#33957,#33958,#33959,#33960,#33961,#33962),
 .UNSPECIFIED.,.F.,.F.,(4,3,3,3,3,3,3,3,4),(-349.239850078862,-348.405302144511,
-347.570754210161,-346.73620627581,-345.901658341459,-345.067110407109,
-344.232562472758,-343.398014538407,-342.956664771683),.UNSPECIFIED.);
#182=B_SPLINE_CURVE_WITH_KNOTS('',3,(#33963,#33964,#33965,#33966,#33967,
#33968,#33969,#33970,#33971,#33972,#33973,#33974,#33975,#33976,#33977,#33978,
#33979,#33980,#33981,#33982,#33983,#33984,#33985,#33986,#33987),
 .UNSPECIFIED.,.F.,.F.,(4,3,3,3,3,3,3,3,4),(339.729209822219,340.56375775657,
341.398305690921,342.232853625271,343.067401559622,343.901949493973,344.736497428324,
345.571045362674,346.012395129399),.UNSPECIFIED.);
#183=B_SPLINE_CURVE_WITH_KNOTS('',3,(#33992,#33993,#33994,#33995,#33996,
#33997,#33998,#33999,#34000,#34001,#34002,#34003,#34004,#34005,#34006,#34007,
#34008,#34009,#34010,#34011,#34012,#34013,#34014,#34015,#34016),
 .UNSPECIFIED.,.F.,.F.,(4,3,3,3,3,3,3,3,4),(-355.523035386042,-354.688487451691,
-353.85393951734,-353.019391582989,-352.184843648639,-351.350295714288,
-350.515747779937,-349.681199845586,-349.239850078862),.UNSPECIFIED.);
#184=B_SPLINE_CURVE_WITH_KNOTS('',3,(#34017,#34018,#34019,#34020,#34021,
#34022,#34023,#34024,#34025,#34026,#34027,#34028,#34029,#34030,#34031,#34032,
#34033,#34034,#34035,#34036,#34037,#34038,#34039,#34040,#34041),
 .UNSPECIFIED.,.F.,.F.,(4,3,3,3,3,3,3,3,4),(346.012395129399,346.917289613241,
347.917051254778,348.916812896315,349.916574537851,350.916336179388,351.416217000156,
351.916097820925,352.295580436578),.UNSPECIFIED.);
#185=B_SPLINE_CURVE_WITH_KNOTS('',3,(#34046,#34047,#34048,#34049,#34050,
#34051,#34052,#34053,#34054,#34055,#34056,#34057,#34058,#34059,#34060,#34061,
#34062,#34063,#34064,#34065,#34066,#34067,#34068,#34069,#34070),
 .UNSPECIFIED.,.F.,.F.,(4,3,3,3,3,3,3,3,4),(-361.806220693221,-360.913952594755,
-359.914190953218,-358.914429311681,-358.414548490913,-357.914667670145,
-356.914906028608,-355.915144387071,-355.523035386042),.UNSPECIFIED.);
#186=B_SPLINE_CURVE_WITH_KNOTS('',3,(#34071,#34072,#34073,#34074,#34075,
#34076,#34077,#34078,#34079,#34080,#34081,#34082,#34083,#34084,#34085,#34086,
#34087,#34088,#34089,#34090,#34091,#34092,#34093,#34094,#34095),
 .UNSPECIFIED.,.F.,.F.,(4,3,3,3,3,3,3,3,4),(352.295580436578,353.130128370929,
353.96467630528,354.79922423963,355.633772173981,356.468320108332,357.302868042682,
358.137415977033,358.578765743758),.UNSPECIFIED.);
#187=B_SPLINE_CURVE_WITH_KNOTS('',3,(#34100,#34101,#34102,#34103,#34104,
#34105,#34106,#34107,#34108,#34109,#34110,#34111,#34112,#34113,#34114,#34115,
#34116,#34117,#34118,#34119,#34120,#34121,#34122,#34123,#34124),
 .UNSPECIFIED.,.F.,.F.,(4,3,3,3,3,3,3,3,4),(-368.089406000401,-367.25485806605,
-366.4203101317,-365.585762197349,-364.751214262998,-363.916666328648,-363.082118394297,
-362.247570459947,-361.806220693221),.UNSPECIFIED.);
#188=B_SPLINE_CURVE_WITH_KNOTS('',3,(#34125,#34126,#34127,#34128,#34129,
#34130,#34131,#34132,#34133,#34134,#34135,#34136,#34137,#34138,#34139,#34140,
#34141,#34142,#34143,#34144,#34145,#34146),.UNSPECIFIED.,.F.,.F.,(4,3,3,
3,3,3,3,4),(358.578765743758,358.914429311682,359.914190953219,360.913952594755,
361.913714236292,362.913475877829,363.913237519365,364.861951050937),
 .UNSPECIFIED.);
#189=B_SPLINE_CURVE_WITH_KNOTS('',3,(#34151,#34152,#34153,#34154,#34155,
#34156,#34157,#34158,#34159,#34160,#34161,#34162,#34163,#34164,#34165,#34166,
#34167,#34168,#34169,#34170,#34171,#34172,#34173,#34174,#34175),
 .UNSPECIFIED.,.F.,.F.,(4,3,3,3,3,3,3,3,4),(-374.37259130758,-373.53804337323,
-372.703495438879,-371.868947504528,-371.034399570178,-370.199851635827,
-369.365303701476,-368.530755767125,-368.089406000401),.UNSPECIFIED.);
#190=B_SPLINE_CURVE_WITH_KNOTS('',3,(#34176,#34177,#34178,#34179,#34180,
#34181,#34182,#34183,#34184,#34185,#34186,#34187,#34188,#34189,#34190,#34191,
#34192,#34193,#34194,#34195,#34196,#34197,#34198,#34199,#34200),
 .UNSPECIFIED.,.F.,.F.,(4,3,3,3,3,3,3,3,4),(364.861951050937,365.696498985288,
366.531046919639,367.36559485399,368.200142788341,369.034690722691,369.869238657042,
370.703786591393,371.145136358117),.UNSPECIFIED.);
#191=B_SPLINE_CURVE_WITH_KNOTS('',3,(#34205,#34206,#34207,#34208,#34209,
#34210,#34211,#34212,#34213,#34214,#34215,#34216,#34217,#34218,#34219,#34220,
#34221,#34222,#34223,#34224,#34225,#34226,#34227,#34228,#34229),
 .UNSPECIFIED.,.F.,.F.,(4,3,3,3,3,3,3,3,4),(-380.65577661476,-379.821228680409,
-378.986680746059,-378.152132811708,-377.317584877357,-376.483036943007,
-375.648489008656,-374.813941074305,-374.37259130758),.UNSPECIFIED.);
#192=B_SPLINE_CURVE_WITH_KNOTS('',3,(#34230,#34231,#34232,#34233,#34234,
#34235,#34236,#34237,#34238,#34239,#34240,#34241,#34242,#34243,#34244,#34245,
#34246,#34247,#34248,#34249,#34250,#34251,#34252,#34253,#34254),
 .UNSPECIFIED.,.F.,.F.,(4,3,3,3,3,3,3,3,4),(371.145136358117,371.979684292468,
372.814232226818,373.648780161169,374.48332809552,375.31787602987,376.152423964221,
376.986971898572,377.428321665297),.UNSPECIFIED.);
#193=B_SPLINE_CURVE_WITH_KNOTS('',3,(#34259,#34260,#34261,#34262,#34263,
#34264,#34265,#34266,#34267,#34268,#34269,#34270,#34271,#34272,#34273,#34274,
#34275,#34276,#34277,#34278,#34279,#34280,#34281,#34282,#34283),
 .UNSPECIFIED.,.F.,.F.,(4,3,3,3,3,3,3,3,4),(-386.938961921939,-386.104413987589,
-385.269866053238,-384.435318118887,-383.600770184537,-382.766222250186,
-381.931674315835,-381.097126381484,-380.65577661476),.UNSPECIFIED.);
#194=B_SPLINE_CURVE_WITH_KNOTS('',3,(#34284,#34285,#34286,#34287,#34288,
#34289,#34290,#34291,#34292,#34293,#34294,#34295,#34296,#34297,#34298,#34299,
#34300,#34301,#34302,#34303,#34304,#34305,#34306,#34307,#34308),
 .UNSPECIFIED.,.F.,.F.,(4,3,3,3,3,3,3,3,4),(377.428321665297,378.262869599647,
379.097417533998,379.931965468349,380.7665134027,381.601061337051,382.435609271401,
383.270157205752,383.711506972476),.UNSPECIFIED.);
#195=B_SPLINE_CURVE_WITH_KNOTS('',3,(#34313,#34314,#34315,#34316,#34317,
#34318,#34319,#34320,#34321,#34322,#34323,#34324,#34325,#34326,#34327,#34328,
#34329,#34330,#34331,#34332,#34333,#34334),.UNSPECIFIED.,.F.,.F.,(4,3,3,
3,3,3,3,4),(-393.222147229119,-392.90632512393,-391.906563482393,-390.906801840856,
-389.90704019932,-388.907278557783,-387.907516916246,-386.938961921939),
 .UNSPECIFIED.);
#196=B_SPLINE_CURVE_WITH_KNOTS('',3,(#34335,#34336,#34337,#34338,#34339,
#34340,#34341,#34342,#34343,#34344,#34345,#34346,#34347,#34348,#34349,#34350,
#34351,#34352,#34353,#34354,#34355,#34356,#34357,#34358,#34359),
 .UNSPECIFIED.,.F.,.F.,(4,3,3,3,3,3,3,3,4),(383.711506972476,384.546054906827,
385.380602841178,386.215150775528,387.049698709879,387.88424664423,388.718794578581,
389.553342512931,389.994692279656),.UNSPECIFIED.);
#197=B_SPLINE_CURVE_WITH_KNOTS('',3,(#34364,#34365,#34366,#34367,#34368,
#34369,#34370,#34371,#34372,#34373,#34374,#34375,#34376,#34377,#34378,#34379,
#34380,#34381,#34382,#34383,#34384,#34385,#34386,#34387,#34388),
 .UNSPECIFIED.,.F.,.F.,(4,3,3,3,3,3,3,3,4),(-399.505332536299,-398.670784601948,
-397.836236667597,-397.001688733247,-396.167140798896,-395.332592864546,
-394.498044930195,-393.663496995844,-393.222147229119),.UNSPECIFIED.);
#198=B_SPLINE_CURVE_WITH_KNOTS('',3,(#34389,#34390,#34391,#34392,#34393,
#34394,#34395,#34396,#34397,#34398,#34399,#34400,#34401,#34402,#34403,#34404,
#34405,#34406,#34407,#34408,#34409,#34410,#34411,#34412,#34413),
 .UNSPECIFIED.,.F.,.F.,(4,3,3,3,3,3,3,3,4),(389.994692279656,390.906801840857,
391.906563482393,392.90632512393,393.406205944699,393.906086765467,394.905848407004,
395.90561004854,396.277877586835),.UNSPECIFIED.);
#199=B_SPLINE_CURVE_WITH_KNOTS('',3,(#34418,#34419,#34420,#34421,#34422,
#34423,#34424,#34425,#34426,#34427,#34428,#34429,#34430,#34431,#34432,#34433,
#34434,#34435,#34436,#34437,#34438,#34439,#34440,#34441,#34442),
 .UNSPECIFIED.,.F.,.F.,(4,3,3,3,3,3,3,3,4),(-405.788517843478,-404.90346482237,
-403.903703180834,-402.903941539297,-401.90417989776,-400.904418256223,
-400.404537435455,-399.904656614687,-399.505332536299),.UNSPECIFIED.);
#200=B_SPLINE_CURVE_WITH_KNOTS('',3,(#34443,#34444,#34445,#34446,#34447,
#34448,#34449,#34450,#34451,#34452,#34453,#34454,#34455,#34456,#34457,#34458,
#34459,#34460,#34461,#34462,#34463,#34464,#34465,#34466,#34467),
 .UNSPECIFIED.,.F.,.F.,(4,3,3,3,3,3,3,3,4),(396.277877586835,397.112425521186,
397.946973455537,398.781521389887,399.616069324238,400.450617258589,401.285165192939,
402.11971312729,402.561062894015),.UNSPECIFIED.);
#201=B_SPLINE_CURVE_WITH_KNOTS('',3,(#34472,#34473,#34474,#34475,#34476,
#34477,#34478,#34479,#34480,#34481,#34482,#34483,#34484,#34485,#34486,#34487,
#34488,#34489,#34490,#34491,#34492,#34493,#34494,#34495,#34496),
 .UNSPECIFIED.,.F.,.F.,(4,3,3,3,3,3,3,3,4),(-412.071703150658,-411.237155216307,
-410.402607281956,-409.568059347606,-408.733511413255,-407.898963478904,
-407.064415544553,-406.229867610203,-405.788517843478),.UNSPECIFIED.);
#202=B_SPLINE_CURVE_WITH_KNOTS('',3,(#34497,#34498,#34499,#34500,#34501,
#34502,#34503,#34504,#34505,#34506,#34507,#34508,#34509,#34510,#34511,#34512,
#34513,#34514,#34515,#34516,#34517,#34518,#34519,#34520,#34521),
 .UNSPECIFIED.,.F.,.F.,(4,3,3,3,3,3,3,3,4),(402.561062894015,402.903941539297,
403.903703180834,404.903464822371,405.903226463907,406.902988105444,407.402868926213,
407.902749746981,408.844248201194),.UNSPECIFIED.);
#203=B_SPLINE_CURVE_WITH_KNOTS('',3,(#34526,#34527,#34528,#34529,#34530,
#34531,#34532,#34533,#34534,#34535,#34536,#34537,#34538,#34539,#34540,#34541,
#34542,#34543,#34544,#34545,#34546,#34547,#34548,#34549,#34550),
 .UNSPECIFIED.,.F.,.F.,(4,3,3,3,3,3,3,3,4),(-418.354888457837,-417.520340523487,
-416.685792589136,-415.851244654785,-415.016696720434,-414.182148786084,
-413.347600851733,-412.513052917382,-412.071703150658),.UNSPECIFIED.);
#204=B_SPLINE_CURVE_WITH_KNOTS('',3,(#34551,#34552,#34553,#34554,#34555,
#34556,#34557,#34558,#34559,#34560,#34561,#34562,#34563,#34564,#34565,#34566,
#34567,#34568,#34569,#34570,#34571,#34572,#34573,#34574,#34575),
 .UNSPECIFIED.,.F.,.F.,(4,3,3,3,3,3,3,3,4),(408.844248201194,409.678796135545,
410.513344069896,411.347892004246,412.182439938597,413.016987872948,413.851535807298,
414.686083741649,415.127433508374),.UNSPECIFIED.);
#205=B_SPLINE_CURVE_WITH_KNOTS('',3,(#34580,#34581,#34582,#34583,#34584,
#34585,#34586,#34587,#34588,#34589,#34590,#34591,#34592,#34593,#34594,#34595,
#34596,#34597,#34598,#34599,#34600,#34601,#34602,#34603,#34604),
 .UNSPECIFIED.,.F.,.F.,(4,3,3,3,3,3,3,3,4),(-424.638073765017,-423.898936011568,
-422.899174370031,-421.899412728495,-421.399531907726,-420.899651086958,
-419.899889445421,-418.900127803884,-418.354888457837),.UNSPECIFIED.);
#206=B_SPLINE_CURVE_WITH_KNOTS('',3,(#34605,#34606,#34607,#34608,#34609,
#34610,#34611,#34612,#34613,#34614,#34615,#34616,#34617,#34618,#34619,#34620,
#34621,#34622,#34623,#34624,#34625,#34626,#34627,#34628,#34629),
 .UNSPECIFIED.,.F.,.F.,(4,3,3,3,3,3,3,3,4),(415.127433508374,415.961981442725,
416.796529377076,417.631077311426,418.465625245777,419.300173180128,420.134721114479,
420.969269048829,421.410618815554),.UNSPECIFIED.);
#207=B_SPLINE_CURVE_WITH_KNOTS('',3,(#34634,#34635,#34636,#34637,#34638,
#34639,#34640,#34641,#34642,#34643,#34644,#34645,#34646,#34647,#34648,#34649,
#34650,#34651,#34652,#34653,#34654,#34655,#34656,#34657,#34658,#34659,#34660,
#34661),.UNSPECIFIED.,.F.,.F.,(4,3,3,3,3,3,3,3,3,4),(-430.921259072197,
-430.897267502325,-429.897505860788,-428.897744219252,-428.397863398483,
-427.897982577715,-426.898220936178,-425.898459294641,-424.898697653105,
-424.638073765017),.UNSPECIFIED.);
#208=B_SPLINE_CURVE_WITH_KNOTS('',3,(#34662,#34663,#34664,#34665,#34666,
#34667,#34668,#34669,#34670,#34671,#34672,#34673,#34674,#34675,#34676,#34677,
#34678,#34679,#34680,#34681,#34682,#34683,#34684,#34685,#34686),
 .UNSPECIFIED.,.F.,.F.,(4,3,3,3,3,3,3,3,4),(421.410618815554,422.245166749904,
423.079714684255,423.914262618605,424.748810552956,425.583358487307,426.417906421657,
427.252454356008,427.693804122733),.UNSPECIFIED.);
#209=B_SPLINE_CURVE_WITH_KNOTS('',3,(#34691,#34692,#34693,#34694,#34695,
#34696,#34697,#34698,#34699,#34700,#34701,#34702,#34703,#34704,#34705,#34706,
#34707,#34708,#34709,#34710,#34711,#34712,#34713,#34714,#34715),
 .UNSPECIFIED.,.F.,.F.,(4,3,3,3,3,3,3,3,4),(-437.204444379376,-436.895837351545,
-435.896075710009,-435.39619488924,-434.896314068472,-433.896552426935,
-432.896790785398,-431.897029143862,-430.921259072197),.UNSPECIFIED.);
#210=B_SPLINE_CURVE_WITH_KNOTS('',3,(#34716,#34717,#34718,#34719,#34720,
#34721,#34722,#34723,#34724,#34725,#34726,#34727,#34728,#34729,#34730,#34731,
#34732,#34733,#34734,#34735,#34736,#34737,#34738,#34739,#34740),
 .UNSPECIFIED.,.F.,.F.,(4,3,3,3,3,3,3,3,4),(427.693804122733,428.528352057084,
429.362899991434,430.197447925785,431.031995860136,431.866543794486,432.701091728837,
433.535639663188,433.976989429913),.UNSPECIFIED.);
#211=B_SPLINE_CURVE_WITH_KNOTS('',3,(#34745,#34746,#34747,#34748,#34749,
#34750,#34751,#34752,#34753,#34754,#34755,#34756,#34757,#34758,#34759,#34760,
#34761,#34762,#34763,#34764,#34765,#34766,#34767,#34768,#34769),
 .UNSPECIFIED.,.F.,.F.,(4,3,3,3,3,3,3,3,4),(-443.487629686556,-442.653081752205,
-441.818533817854,-440.983985883503,-440.149437949153,-439.314890014802,
-438.480342080451,-437.645794146101,-437.204444379376),.UNSPECIFIED.);
#212=B_SPLINE_CURVE_WITH_KNOTS('',3,(#34770,#34771,#34772,#34773,#34774,
#34775,#34776,#34777,#34778,#34779,#34780,#34781,#34782,#34783,#34784,#34785,
#34786,#34787,#34788,#34789,#34790,#34791,#34792,#34793,#34794),
 .UNSPECIFIED.,.F.,.F.,(4,3,3,3,3,3,3,3,4),(433.976989429913,434.896314068472,
435.396194889241,435.896075710009,436.895837351546,437.895598993082,438.895360634619,
439.895122276156,440.260174737092),.UNSPECIFIED.);
#213=B_SPLINE_CURVE_WITH_KNOTS('',3,(#34799,#34800,#34801,#34802,#34803,
#34804,#34805,#34806,#34807,#34808,#34809,#34810,#34811,#34812,#34813,#34814,
#34815,#34816,#34817,#34818,#34819,#34820,#34821,#34822,#34823),
 .UNSPECIFIED.,.F.,.F.,(4,3,3,3,3,3,3,3,4),(-449.770814993735,-449.392857870754,
-448.892977049986,-447.893215408449,-446.893453766913,-445.893692125376,
-444.893930483839,-443.894168842302,-443.487629686556),.UNSPECIFIED.);
#214=B_SPLINE_CURVE_WITH_KNOTS('',3,(#34824,#34825,#34826,#34827,#34828,
#34829,#34830,#34831,#34832,#34833,#34834,#34835,#34836,#34837,#34838,#34839,
#34840,#34841,#34842,#34843,#34844,#34845,#34846,#34847,#34848),
 .UNSPECIFIED.,.F.,.F.,(4,3,3,3,3,3,3,3,4),(440.260174737092,441.094722671443,
441.929270605794,442.763818540144,443.598366474495,444.432914408846,445.267462343196,
446.102010277547,446.543360044272),.UNSPECIFIED.);
#215=B_SPLINE_CURVE_WITH_KNOTS('',3,(#34853,#34854,#34855,#34856,#34857,
#34858,#34859,#34860,#34861,#34862,#34863,#34864,#34865,#34866,#34867,#34868,
#34869,#34870,#34871,#34872,#34873,#34874,#34875,#34876,#34877),
 .UNSPECIFIED.,.F.,.F.,(4,3,3,3,3,3,3,3,4),(-456.054000300915,-455.219452366564,
-454.384904432213,-453.550356497862,-452.715808563511,-451.881260629161,
-451.04671269481,-450.212164760459,-449.770814993735),.UNSPECIFIED.);
#216=B_SPLINE_CURVE_WITH_KNOTS('',3,(#34878,#34879,#34880,#34881,#34882,
#34883,#34884,#34885,#34886,#34887,#34888,#34889,#34890,#34891,#34892,#34893,
#34894,#34895,#34896,#34897,#34898,#34899,#34900,#34901,#34902),
 .UNSPECIFIED.,.F.,.F.,(4,3,3,3,3,3,3,3,4),(446.543360044272,446.893453766913,
447.89321540845,448.892977049986,449.392857870755,449.892738691523,450.89250033306,
451.892261974596,452.826545351451),.UNSPECIFIED.);
#217=B_SPLINE_CURVE_WITH_KNOTS('',3,(#34907,#34908,#34909,#34910,#34911,
#34912,#34913,#34914,#34915,#34916,#34917,#34918,#34919,#34920,#34921,#34922,
#34923,#34924,#34925,#34926,#34927,#34928,#34929,#34930,#34931),
 .UNSPECIFIED.,.F.,.F.,(4,3,3,3,3,3,3,3,4),(-462.337185608094,-461.889878389963,
-460.890116748427,-459.89035510689,-458.890593465353,-457.890831823816,
-456.89107018228,-456.391189361511,-456.054000300915),.UNSPECIFIED.);
#218=B_SPLINE_CURVE_WITH_KNOTS('',3,(#34932,#34933,#34934,#34935,#34936,
#34937,#34938,#34939,#34940,#34941,#34942,#34943,#34944,#34945,#34946,#34947,
#34948,#34949,#34950,#34951,#34952,#34953,#34954,#34955,#34956,#34957,#34958,
#34959),.UNSPECIFIED.,.F.,.F.,(4,3,3,3,3,3,3,3,3,4),(452.826545351451,452.892023616133,
453.89178525767,454.891546899207,455.891308540743,456.391189361512,456.89107018228,
457.890831823817,458.890593465354,459.109730658631),.UNSPECIFIED.);
#219=B_SPLINE_CURVE_WITH_KNOTS('',3,(#34964,#34965,#34966,#34967,#34968,
#34969,#34970,#34971,#34972,#34973,#34974,#34975,#34976,#34977,#34978,#34979,
#34980,#34981,#34982,#34983,#34984,#34985,#34986,#34987,#34988),
 .UNSPECIFIED.,.F.,.F.,(4,3,3,3,3,3,3,3,4),(-468.620370915274,-467.785822980923,
-466.951275046573,-466.116727112222,-465.282179177871,-464.447631243521,
-463.61308330917,-462.778535374819,-462.337185608094),.UNSPECIFIED.);
#220=B_SPLINE_CURVE_WITH_KNOTS('',3,(#34989,#34990,#34991,#34992,#34993,
#34994,#34995,#34996,#34997,#34998,#34999,#35000,#35001,#35002,#35003,#35004,
#35005,#35006,#35007,#35008,#35009,#35010,#35011,#35012,#35013),
 .UNSPECIFIED.,.F.,.F.,(4,3,3,3,3,3,3,3,4),(459.109730658631,459.944278592982,
460.778826527332,461.613374461683,462.447922396034,463.282470330384,464.117018264735,
464.951566199086,465.392915965811),.UNSPECIFIED.);
#221=B_SPLINE_CURVE_WITH_KNOTS('',3,(#35018,#35019,#35020,#35021,#35022,
#35023,#35024,#35025,#35026,#35027,#35028,#35029,#35030,#35031,#35032,#35033,
#35034,#35035,#35036,#35037,#35038,#35039,#35040,#35041,#35042,#35043,#35044,
#35045),.UNSPECIFIED.,.F.,.F.,(4,3,3,3,3,3,3,3,3,4),(-474.903556222453,
-474.886779729941,-473.887018088404,-472.887256446867,-471.88749480533,
-470.887733163794,-470.387852343025,-469.887971522257,-468.88820988072,
-468.620370915274),.UNSPECIFIED.);
#222=B_SPLINE_CURVE_WITH_KNOTS('',3,(#35046,#35047,#35048,#35049,#35050,
#35051,#35052,#35053,#35054,#35055,#35056,#35057,#35058,#35059,#35060,#35061,
#35062,#35063,#35064,#35065,#35066,#35067,#35068,#35069,#35070),
 .UNSPECIFIED.,.F.,.F.,(4,3,3,3,3,3,3,3,4),(465.392915965811,466.227463900161,
467.062011834512,467.896559768863,468.731107703214,469.565655637564,470.400203571915,
471.234751506266,471.67610127299),.UNSPECIFIED.);
#223=B_SPLINE_CURVE_WITH_KNOTS('',3,(#35075,#35076,#35077,#35078,#35079,
#35080,#35081,#35082,#35083,#35084,#35085,#35086,#35087,#35088,#35089,#35090,
#35091,#35092,#35093,#35094,#35095,#35096,#35097,#35098,#35099),
 .UNSPECIFIED.,.F.,.F.,(4,3,3,3,3,3,3,3,4),(-481.186741529633,-480.885349579161,
-479.885587937624,-478.885826296087,-477.886064654551,-477.386183833782,
-476.886303013014,-475.886541371477,-474.903556222453),.UNSPECIFIED.);
#224=B_SPLINE_CURVE_WITH_KNOTS('',3,(#35100,#35101,#35102,#35103,#35104,
#35105,#35106,#35107,#35108,#35109,#35110,#35111,#35112,#35113,#35114,#35115,
#35116,#35117,#35118,#35119,#35120,#35121,#35122,#35123,#35124),
 .UNSPECIFIED.,.F.,.F.,(4,3,3,3,3,3,3,3,4),(471.67610127299,472.510649207341,
473.345197141692,474.179745076042,475.014293010393,475.848840944744,476.683388879095,
477.517936813446,477.95928658017),.UNSPECIFIED.);
#225=B_SPLINE_CURVE_WITH_KNOTS('',3,(#35129,#35130,#35131,#35132,#35133,
#35134,#35135,#35136,#35137,#35138,#35139,#35140,#35141,#35142,#35143,#35144,
#35145,#35146,#35147,#35148,#35149,#35150,#35151,#35152,#35153),
 .UNSPECIFIED.,.F.,.F.,(4,3,3,3,3,3,3,3,4),(-487.469926836813,-486.883919428381,
-485.884157786844,-484.884396145308,-484.384515324539,-483.884634503771,
-482.884872862234,-481.885111220698,-481.186741529633),.UNSPECIFIED.);
#226=B_SPLINE_CURVE_WITH_KNOTS('',3,(#35154,#35155,#35156,#35157,#35158,
#35159,#35160,#35161,#35162,#35163,#35164,#35165,#35166,#35167,#35168,#35169,
#35170,#35171,#35172,#35173,#35174,#35175),.UNSPECIFIED.,.F.,.F.,(4,3,3,
3,3,3,3,4),(477.95928658017,478.885826296088,479.885587937625,480.885349579161,
481.885111220698,482.884872862235,483.884634503771,484.242471887349),
 .UNSPECIFIED.);
#227=B_SPLINE_CURVE_WITH_KNOTS('',3,(#35180,#35181,#35182,#35183,#35184,
#35185,#35186,#35187,#35188,#35189,#35190,#35191,#35192,#35193,#35194,#35195,
#35196,#35197,#35198,#35199,#35200,#35201,#35202,#35203,#35204),
 .UNSPECIFIED.,.F.,.F.,(4,3,3,3,3,3,3,3,4),(-493.753112143992,-492.882489277601,
-491.882727636065,-491.382846815296,-490.882965994528,-489.883204352991,
-488.883442711455,-487.883681069918,-487.469926836813),.UNSPECIFIED.);
#228=B_SPLINE_CURVE_WITH_KNOTS('',3,(#35205,#35206,#35207,#35208,#35209,
#35210,#35211,#35212,#35213,#35214,#35215,#35216,#35217,#35218,#35219,#35220,
#35221,#35222,#35223,#35224,#35225,#35226,#35227,#35228,#35229),
 .UNSPECIFIED.,.F.,.F.,(4,3,3,3,3,3,3,3,4),(484.242471887349,485.0770198217,
485.91156775605,486.746115690401,487.580663624752,488.415211559102,489.249759493453,
490.084307427803,490.525657194529),.UNSPECIFIED.);
#229=B_SPLINE_CURVE_WITH_KNOTS('',3,(#35234,#35235,#35236,#35237,#35238,
#35239,#35240,#35241,#35242,#35243,#35244,#35245,#35246,#35247,#35248,#35249,
#35250,#35251,#35252,#35253,#35254,#35255,#35256,#35257,#35258),
 .UNSPECIFIED.,.F.,.F.,(4,3,3,3,3,3,3,3,4),(-500.036297451172,-499.201749516821,
-498.36720158247,-497.53265364812,-496.698105713769,-495.863557779418,-495.029009845068,
-494.194461910717,-493.753112143992),.UNSPECIFIED.);
#230=B_SPLINE_CURVE_WITH_KNOTS('',3,(#35259,#35260,#35261,#35262,#35263,
#35264,#35265,#35266,#35267,#35268,#35269,#35270,#35271,#35272,#35273,#35274,
#35275,#35276,#35277,#35278,#35279,#35280,#35281,#35282,#35283),
 .UNSPECIFIED.,.F.,.F.,(4,3,3,3,3,3,3,3,4),(490.525657194529,490.882965994528,
491.382846815297,491.882727636065,492.882489277602,493.882250919139,494.882012560675,
495.881774202212,496.808842501708),.UNSPECIFIED.);
#231=B_SPLINE_CURVE_WITH_KNOTS('',3,(#35288,#35289,#35290,#35291,#35292,
#35293,#35294,#35295,#35296,#35297,#35298,#35299,#35300,#35301,#35302,#35303,
#35304,#35305,#35306,#35307,#35308,#35309,#35310,#35311,#35312),
 .UNSPECIFIED.,.F.,.F.,(4,3,3,3,3,3,3,3,4),(-506.319482758351,-505.879390617579,
-505.37950979681,-504.879628976042,-503.879867334505,-502.880105692969,
-501.880344051432,-500.880582409895,-500.036297451172),.UNSPECIFIED.);
#232=B_SPLINE_CURVE_WITH_KNOTS('',3,(#35313,#35314,#35315,#35316,#35317,
#35318,#35319,#35320,#35321,#35322,#35323,#35324,#35325,#35326,#35327,#35328,
#35329,#35330,#35331,#35332,#35333,#35334,#35335,#35336,#35337),
 .UNSPECIFIED.,.F.,.F.,(4,3,3,3,3,3,3,3,4),(496.808842501708,497.643390436059,
498.47793837041,499.312486304761,500.147034239112,500.981582173463,501.816130107813,
502.650678042164,503.092027808888),.UNSPECIFIED.);
#233=B_SPLINE_CURVE_WITH_KNOTS('',3,(#35342,#35343,#35344,#35345,#35346,
#35347,#35348,#35349,#35350,#35351,#35352,#35353,#35354,#35355,#35356,#35357,
#35358,#35359,#35360,#35361,#35362,#35363,#35364,#35365,#35366),
 .UNSPECIFIED.,.F.,.F.,(4,3,3,3,3,3,3,3,4),(-512.602668065531,-511.76812013118,
-510.933572196829,-510.099024262479,-509.264476328128,-508.429928393777,
-507.595380459427,-506.760832525076,-506.319482758351),.UNSPECIFIED.);
#234=B_SPLINE_CURVE_WITH_KNOTS('',3,(#35367,#35368,#35369,#35370,#35371,
#35372,#35373,#35374,#35375,#35376,#35377,#35378,#35379,#35380,#35381,#35382,
#35383,#35384,#35385,#35386,#35387,#35388,#35389,#35390,#35391),
 .UNSPECIFIED.,.F.,.F.,(4,3,3,3,3,3,3,3,4),(503.092027808888,503.926575743239,
504.761123677589,505.59567161194,506.430219546291,507.264767480641,508.099315414992,
508.933863349343,509.375213116067),.UNSPECIFIED.);
#235=B_SPLINE_CURVE_WITH_KNOTS('',3,(#35396,#35397,#35398,#35399,#35400,
#35401,#35402,#35403,#35404,#35405,#35406,#35407,#35408,#35409,#35410,#35411,
#35412,#35413,#35414,#35415,#35416,#35417,#35418,#35419,#35420),
 .UNSPECIFIED.,.F.,.F.,(4,3,3,3,3,3,3,3,4),(-518.88585337271,-518.876291957556,
-517.876530316019,-516.876768674483,-515.877007032946,-514.877245391409,
-513.877483749872,-512.877722108336,-512.602668065531),.UNSPECIFIED.);
#236=B_SPLINE_CURVE_WITH_KNOTS('',3,(#35421,#35422,#35423,#35424,#35425,
#35426,#35427,#35428,#35429,#35430,#35431,#35432,#35433,#35434,#35435,#35436,
#35437,#35438,#35439,#35440,#35441,#35442,#35443,#35444,#35445),
 .UNSPECIFIED.,.F.,.F.,(4,3,3,3,3,3,3,3,4),(509.375213116067,509.878437183726,
510.878198825263,511.877960466799,512.377841287568,512.877722108336,513.877483749873,
514.87724539141,515.658398423247),.UNSPECIFIED.);
#237=B_SPLINE_CURVE_WITH_KNOTS('',3,(#35450,#35451,#35452,#35453,#35454,
#35455,#35456,#35457,#35458,#35459,#35460,#35461,#35462,#35463,#35464,#35465,
#35466,#35467,#35468,#35469,#35470,#35471,#35472,#35473,#35474),
 .UNSPECIFIED.,.F.,.F.,(4,3,3,3,3,3,3,3,4),(-525.16903867989,-524.874861806776,
-523.87510016524,-522.875338523703,-521.875576882166,-520.875815240629,
-519.876053599093,-519.376172778324,-518.88585337271),.UNSPECIFIED.);
#238=B_SPLINE_CURVE_WITH_KNOTS('',3,(#35475,#35476,#35477,#35478,#35479,
#35480,#35481,#35482,#35483,#35484,#35485,#35486,#35487,#35488,#35489,#35490,
#35491,#35492,#35493,#35494,#35495,#35496,#35497,#35498,#35499,#35500,#35501,
#35502),.UNSPECIFIED.,.F.,.F.,(4,3,3,3,3,3,3,3,3,4),(515.658398423247,515.877007032946,
516.876768674483,517.87653031602,518.876291957556,519.376172778325,519.876053599093,
520.87581524063,521.875576882167,521.941583730426),.UNSPECIFIED.);
#239=B_SPLINE_CURVE_WITH_KNOTS('',3,(#35507,#35508,#35509,#35510,#35511,
#35512,#35513,#35514,#35515,#35516,#35517,#35518,#35519,#35520,#35521,#35522,
#35523,#35524,#35525,#35526,#35527,#35528,#35529,#35530,#35531),
 .UNSPECIFIED.,.F.,.F.,(4,3,3,3,3,3,3,3,4),(-531.45222398707,-530.617676052719,
-529.783128118368,-528.948580184017,-528.114032249666,-527.279484315316,
-526.444936380965,-525.610388446614,-525.16903867989),.UNSPECIFIED.);
#240=B_SPLINE_CURVE_WITH_KNOTS('',3,(#35532,#35533,#35534,#35535,#35536,
#35537,#35538,#35539,#35540,#35541,#35542,#35543,#35544,#35545,#35546,#35547,
#35548,#35549,#35550,#35551,#35552,#35553,#35554,#35555,#35556),
 .UNSPECIFIED.,.F.,.F.,(4,3,3,3,3,3,3,3,4),(521.941583730426,522.875338523703,
523.87510016524,524.874861806777,525.874623448314,526.374504269082,526.87438508985,
527.874146731387,528.224769037606),.UNSPECIFIED.);
#241=B_SPLINE_CURVE_WITH_KNOTS('',3,(#35561,#35562,#35563,#35564,#35565,
#35566,#35567,#35568,#35569,#35570,#35571,#35572,#35573,#35574,#35575,#35576,
#35577,#35578,#35579,#35580,#35581,#35582,#35583,#35584,#35585),
 .UNSPECIFIED.,.F.,.F.,(4,3,3,3,3,3,3,3,4),(-537.735409294249,-536.872001505217,
-535.87223986368,-534.872478222144,-533.872716580607,-533.372835759838,
-532.87295493907,-531.873193297533,-531.45222398707),.UNSPECIFIED.);
#242=B_SPLINE_CURVE_WITH_KNOTS('',3,(#35586,#35587,#35588,#35589,#35590,
#35591,#35592,#35593,#35594,#35595,#35596,#35597,#35598,#35599,#35600,#35601,
#35602,#35603,#35604,#35605,#35606,#35607,#35608,#35609,#35610),
 .UNSPECIFIED.,.F.,.F.,(4,3,3,3,3,3,3,3,4),(528.224769037606,529.059316971957,
529.893864906308,530.728412840658,531.562960775009,532.39750870936,533.232056643711,
534.066604578062,534.507954344786),.UNSPECIFIED.);
#243=B_SPLINE_CURVE_WITH_KNOTS('',3,(#35615,#35616,#35617,#35618,#35619,
#35620,#35621,#35622,#35623,#35624,#35625,#35626,#35627,#35628,#35629,#35630,
#35631,#35632,#35633,#35634,#35635,#35636,#35637,#35638,#35639),
 .UNSPECIFIED.,.F.,.F.,(4,3,3,3,3,3,3,3,4),(-544.018594601429,-543.184046667078,
-542.349498732727,-541.514950798377,-540.680402864026,-539.845854929675,
-539.011306995325,-538.176759060974,-537.735409294249),.UNSPECIFIED.);
#244=B_SPLINE_CURVE_WITH_KNOTS('',3,(#35640,#35641,#35642,#35643,#35644,
#35645,#35646,#35647,#35648,#35649,#35650,#35651,#35652,#35653,#35654,#35655,
#35656,#35657,#35658,#35659,#35660,#35661,#35662,#35663,#35664),
 .UNSPECIFIED.,.F.,.F.,(4,3,3,3,3,3,3,3,4),(534.507954344786,534.872478222144,
535.872239863681,536.872001505217,537.871763146754,538.871524788291,539.871286429828,
540.371167250596,540.791139651965),.UNSPECIFIED.);
#245=B_SPLINE_CURVE_WITH_KNOTS('',3,(#35669,#35670,#35671,#35672,#35673,
#35674,#35675,#35676,#35677,#35678,#35679,#35680,#35681,#35682,#35683,#35684,
#35685,#35686,#35687,#35688,#35689,#35690,#35691,#35692,#35693),
 .UNSPECIFIED.,.F.,.F.,(4,3,3,3,3,3,3,3,4),(-550.301779908608,-549.868902845194,
-548.869141203658,-547.869379562121,-547.369498741352,-546.869617920584,
-545.869856279047,-544.870094637511,-544.018594601429),.UNSPECIFIED.);
#246=B_SPLINE_CURVE_WITH_KNOTS('',3,(#35694,#35695,#35696,#35697,#35698,
#35699,#35700,#35701,#35702,#35703,#35704,#35705,#35706,#35707,#35708,#35709,
#35710,#35711,#35712,#35713,#35714,#35715,#35716,#35717,#35718),
 .UNSPECIFIED.,.F.,.F.,(4,3,3,3,3,3,3,3,4),(540.791139651965,541.625687586316,
542.460235520667,543.294783455017,544.129331389368,544.963879323719,545.798427258069,
546.63297519242,547.074324959145),.UNSPECIFIED.);
#247=B_SPLINE_CURVE_WITH_KNOTS('',3,(#35723,#35724,#35725,#35726,#35727,
#35728,#35729,#35730,#35731,#35732,#35733,#35734,#35735,#35736,#35737,#35738,
#35739,#35740,#35741,#35742,#35743,#35744,#35745,#35746,#35747),
 .UNSPECIFIED.,.F.,.F.,(4,3,3,3,3,3,3,3,4),(-556.584965215788,-555.750417281437,
-554.915869347087,-554.081321412736,-553.246773478385,-552.412225544035,
-551.577677609684,-550.743129675333,-550.301779908608),.UNSPECIFIED.);
#248=B_SPLINE_CURVE_WITH_KNOTS('',3,(#35748,#35749,#35750,#35751,#35752,
#35753,#35754,#35755,#35756,#35757,#35758,#35759,#35760,#35761,#35762,#35763,
#35764,#35765,#35766,#35767,#35768,#35769,#35770,#35771,#35772),
 .UNSPECIFIED.,.F.,.F.,(4,3,3,3,3,3,3,3,4),(547.074324959145,547.369498741353,
547.869379562121,548.869141203658,549.868902845195,550.868664486731,551.868426128268,
552.868187769805,553.357510266324),.UNSPECIFIED.);
#249=B_SPLINE_CURVE_WITH_KNOTS('',3,(#35777,#35778,#35779,#35780,#35781,
#35782,#35783,#35784,#35785,#35786,#35787,#35788,#35789,#35790,#35791,#35792,
#35793,#35794,#35795,#35796,#35797,#35798,#35799,#35800,#35801),
 .UNSPECIFIED.,.F.,.F.,(4,3,3,3,3,3,3,3,4),(-562.868150522967,-562.033602588617,
-561.199054654266,-560.364506719915,-559.529958785564,-558.695410851214,
-557.860862916863,-557.026314982512,-556.584965215788),.UNSPECIFIED.);
#250=B_SPLINE_CURVE_WITH_KNOTS('',3,(#35802,#35803,#35804,#35805,#35806,
#35807,#35808,#35809,#35810,#35811,#35812,#35813,#35814,#35815,#35816,#35817,
#35818,#35819,#35820,#35821,#35822,#35823,#35824,#35825,#35826),
 .UNSPECIFIED.,.F.,.F.,(4,3,3,3,3,3,3,3,4),(553.357510266324,554.192058200675,
555.026606135026,555.861154069376,556.695702003727,557.530249938078,558.364797872428,
559.199345806779,559.640695573504),.UNSPECIFIED.);
#251=B_SPLINE_CURVE_WITH_KNOTS('',3,(#35831,#35832,#35833,#35834,#35835,
#35836,#35837,#35838,#35839,#35840,#35841,#35842,#35843,#35844,#35845,#35846,
#35847,#35848,#35849,#35850,#35851,#35852,#35853,#35854,#35855),
 .UNSPECIFIED.,.F.,.F.,(4,3,3,3,3,3,3,3,4),(-569.151335830147,-568.864374034392,
-568.364493213624,-567.864612392855,-566.864850751318,-565.865089109782,
-564.865327468245,-563.865565826708,-562.868150522967),.UNSPECIFIED.);
#252=B_SPLINE_CURVE_WITH_KNOTS('',3,(#35856,#35857,#35858,#35859,#35860,
#35861,#35862,#35863,#35864,#35865,#35866,#35867,#35868,#35869,#35870,#35871,
#35872,#35873,#35874,#35875,#35876,#35877,#35878,#35879,#35880),
 .UNSPECIFIED.,.F.,.F.,(4,3,3,3,3,3,3,3,4),(559.640695573504,560.475243507855,
561.309791442206,562.144339376557,562.978887310907,563.813435245258,564.647983179609,
565.48253111396,565.923880880684),.UNSPECIFIED.);
#253=B_SPLINE_CURVE_WITH_KNOTS('',3,(#35885,#35886,#35887,#35888,#35889,
#35890,#35891,#35892,#35893,#35894,#35895,#35896,#35897,#35898,#35899,#35900,
#35901,#35902,#35903,#35904,#35905,#35906,#35907,#35908,#35909),
 .UNSPECIFIED.,.F.,.F.,(4,3,3,3,3,3,3,3,4),(-575.434521137327,-574.599973202976,
-573.765425268625,-572.930877334275,-572.096329399924,-571.261781465573,
-570.427233531223,-569.592685596872,-569.151335830147),.UNSPECIFIED.);
#254=B_SPLINE_CURVE_WITH_KNOTS('',3,(#35910,#35911,#35912,#35913,#35914,
#35915,#35916,#35917,#35918,#35919,#35920,#35921,#35922,#35923,#35924,#35925,
#35926,#35927,#35928,#35929,#35930,#35931,#35932,#35933,#35934),
 .UNSPECIFIED.,.F.,.F.,(4,3,3,3,3,3,3,3,4),(565.923880880684,566.864850751319,
567.864612392856,568.364493213624,568.864374034392,569.864135675929,570.863897317466,
571.863658959003,572.207066187863),.UNSPECIFIED.);
#255=B_SPLINE_CURVE_WITH_KNOTS('',3,(#35939,#35940,#35941,#35942,#35943,
#35944,#35945,#35946,#35947,#35948,#35949,#35950,#35951,#35952,#35953,#35954,
#35955,#35956,#35957,#35958,#35959,#35960),.UNSPECIFIED.,.F.,.F.,(4,3,3,
3,3,3,3,4),(-581.717706444506,-580.861513732832,-579.861752091296,-578.861990449759,
-577.862228808222,-576.862467166686,-575.862705525149,-575.434521137327),
 .UNSPECIFIED.);
#256=B_SPLINE_CURVE_WITH_KNOTS('',3,(#35961,#35962,#35963,#35964,#35965,
#35966,#35967,#35968,#35969,#35970,#35971,#35972,#35973,#35974,#35975,#35976,
#35977,#35978,#35979,#35980,#35981,#35982,#35983,#35984,#35985),
 .UNSPECIFIED.,.F.,.F.,(4,3,3,3,3,3,3,3,4),(572.207066187863,572.863420600539,
573.863182242076,574.862943883613,575.362824704381,575.862705525149,576.862467166686,
577.862228808223,578.490251495043),.UNSPECIFIED.);
#257=B_SPLINE_CURVE_WITH_KNOTS('',3,(#35990,#35991,#35992,#35993,#35994,
#35995,#35996,#35997,#35998,#35999,#36000,#36001,#36002,#36003,#36004,#36005,
#36006,#36007,#36008,#36009,#36010,#36011,#36012,#36013,#36014),
 .UNSPECIFIED.,.F.,.F.,(4,3,3,3,3,3,3,3,4),(-588.000891751686,-587.166343817335,
-586.331795882984,-585.497247948633,-584.662700014282,-583.828152079931,
-582.99360414558,-582.159056211229,-581.717706444506),.UNSPECIFIED.);
#258=B_SPLINE_CURVE_WITH_KNOTS('',3,(#36015,#36016,#36017,#36018,#36019,
#36020,#36021,#36022,#36023,#36024,#36025,#36026,#36027,#36028,#36029,#36030,
#36031,#36032,#36033,#36034,#36035,#36036,#36037,#36038,#36039),
 .UNSPECIFIED.,.F.,.F.,(4,3,3,3,3,3,3,3,4),(578.490251495043,578.861990449759,
579.861752091296,580.861513732833,581.86127537437,582.361156195138,582.861037015906,
583.860798657443,584.773436802222),.UNSPECIFIED.);
#259=B_SPLINE_CURVE_WITH_KNOTS('',3,(#36044,#36045,#36046,#36047,#36048,
#36049,#36050,#36051,#36052,#36053,#36054,#36055,#36056,#36057,#36058,#36059,
#36060,#36061,#36062,#36063,#36064,#36065,#36066,#36067,#36068),
 .UNSPECIFIED.,.F.,.F.,(4,3,3,3,3,3,3,3,4),(-594.284077058865,-593.85841507281,
-592.858653431273,-591.858891789736,-590.8591301482,-589.859368506663,-589.359487685895,
-588.859606865126,-588.000891751686),.UNSPECIFIED.);
#260=B_SPLINE_CURVE_WITH_KNOTS('',3,(#36069,#36070,#36071,#36072,#36073,
#36074,#36075,#36076,#36077,#36078,#36079,#36080,#36081,#36082,#36083,#36084,
#36085,#36086,#36087,#36088,#36089,#36090,#36091,#36092,#36093),
 .UNSPECIFIED.,.F.,.F.,(4,3,3,3,3,3,3,3,4),(584.773436802222,585.607984736573,
586.442532670923,587.277080605274,588.111628539624,588.946176473975,589.780724408326,
590.615272342676,591.056622109402),.UNSPECIFIED.);
#261=B_SPLINE_CURVE_WITH_KNOTS('',3,(#36098,#36099,#36100,#36101,#36102,
#36103,#36104,#36105,#36106,#36107,#36108,#36109,#36110,#36111,#36112,#36113,
#36114,#36115,#36116,#36117,#36118,#36119,#36120,#36121,#36122),
 .UNSPECIFIED.,.F.,.F.,(4,3,3,3,3,3,3,3,4),(-600.567262366045,-599.732714431694,
-598.898166497343,-598.063618562993,-597.229070628642,-596.394522694291,
-595.559974759941,-594.72542682559,-594.284077058865),.UNSPECIFIED.);
#262=B_SPLINE_CURVE_WITH_KNOTS('',3,(#36123,#36124,#36125,#36126,#36127,
#36128,#36129,#36130,#36131,#36132,#36133,#36134,#36135,#36136,#36137,#36138,
#36139,#36140,#36141,#36142,#36143,#36144,#36145,#36146,#36147),
 .UNSPECIFIED.,.F.,.F.,(4,3,3,3,3,3,3,3,4),(591.056622109402,591.858891789737,
592.858653431274,593.85841507281,594.858176714347,595.857938355884,596.357819176652,
596.85769999742,597.339807416581),.UNSPECIFIED.);
#263=B_SPLINE_CURVE_WITH_KNOTS('',3,(#36152,#36153,#36154,#36155,#36156,
#36157,#36158,#36159,#36160,#36161,#36162,#36163,#36164,#36165,#36166,#36167,
#36168,#36169,#36170,#36171,#36172,#36173,#36174,#36175,#36176),
 .UNSPECIFIED.,.F.,.F.,(4,3,3,3,3,3,3,3,4),(-606.850447673224,-605.85555477125,
-604.855793129714,-603.856031488177,-603.356150667409,-602.85626984664,
-601.856508205104,-600.856746563567,-600.567262366045),.UNSPECIFIED.);
#264=B_SPLINE_CURVE_WITH_KNOTS('',3,(#36177,#36178,#36179,#36180,#36181,
#36182,#36183,#36184,#36185,#36186,#36187,#36188,#36189,#36190,#36191,#36192,
#36193,#36194,#36195,#36196,#36197,#36198,#36199,#36200,#36201),
 .UNSPECIFIED.,.F.,.F.,(4,3,3,3,3,3,3,3,4),(597.339807416581,598.174355350932,
599.008903285283,599.843451219633,600.677999153984,601.512547088335,602.347095022685,
603.181642957036,603.622992723761),.UNSPECIFIED.);
#265=B_SPLINE_CURVE_WITH_KNOTS('',3,(#36206,#36207,#36208,#36209,#36210,
#36211,#36212,#36213,#36214,#36215,#36216,#36217,#36218,#36219,#36220,#36221,
#36222,#36223,#36224,#36225,#36226,#36227,#36228,#36229,#36230,#36231,#36232,
#36233),.UNSPECIFIED.,.F.,.F.,(4,3,3,3,3,3,3,3,3,4),(-613.133632980404,
-612.853886262007,-611.854124620471,-610.854362978934,-610.354482158166,
-609.854601337397,-608.854839695861,-607.855078054324,-606.855316412787,
-606.850447673224),.UNSPECIFIED.);
#266=B_SPLINE_CURVE_WITH_KNOTS('',3,(#36234,#36235,#36236,#36237,#36238,
#36239,#36240,#36241,#36242,#36243,#36244,#36245,#36246,#36247,#36248,#36249,
#36250,#36251,#36252,#36253,#36254,#36255,#36256,#36257,#36258),
 .UNSPECIFIED.,.F.,.F.,(4,3,3,3,3,3,3,3,4),(603.622992723761,604.457540658112,
605.292088592463,606.126636526814,606.961184461165,607.795732395515,608.630280329866,
609.464828264217,609.906178030941),.UNSPECIFIED.);
#267=B_SPLINE_CURVE_WITH_KNOTS('',3,(#36263,#36264,#36265,#36266,#36267,
#36268,#36269,#36270,#36271,#36272,#36273,#36274,#36275,#36276,#36277,#36278,
#36279,#36280,#36281,#36282,#36283,#36284,#36285,#36286,#36287),
 .UNSPECIFIED.,.F.,.F.,(4,3,3,3,3,3,3,3,4),(-619.416818287584,-618.582270353233,
-617.747722418882,-616.913174484532,-616.078626550181,-615.24407861583,
-614.40953068148,-613.574982747129,-613.133632980404),.UNSPECIFIED.);
#268=B_SPLINE_CURVE_WITH_KNOTS('',3,(#36288,#36289,#36290,#36291,#36292,
#36293,#36294,#36295,#36296,#36297,#36298,#36299,#36300,#36301,#36302,#36303,
#36304,#36305,#36306,#36307,#36308,#36309,#36310,#36311,#36312),
 .UNSPECIFIED.,.F.,.F.,(4,3,3,3,3,3,3,3,4),(609.906178030941,610.354482158166,
610.854362978934,611.854124620471,612.853886262008,613.853647903545,614.853409545081,
615.853171186618,616.18936333812),.UNSPECIFIED.);
#269=B_SPLINE_CURVE_WITH_KNOTS('',3,(#36317,#36318,#36319,#36320,#36321,
#36322,#36323,#36324,#36325,#36326,#36327,#36328,#36329,#36330,#36331,#36332,
#36333,#36334,#36335,#36336,#36337,#36338,#36339,#36340,#36341),
 .UNSPECIFIED.,.F.,.F.,(4,3,3,3,3,3,3,3,4),(-625.700003594763,-624.865455660412,
-624.030907726062,-623.196359791711,-622.36181185736,-621.527263923009,
-620.692715988658,-619.858168054308,-619.416818287584),.UNSPECIFIED.);
#270=B_SPLINE_CURVE_WITH_KNOTS('',3,(#36342,#36343,#36344,#36345,#36346,
#36347,#36348,#36349,#36350,#36351,#36352,#36353,#36354,#36355,#36356,#36357,
#36358,#36359,#36360,#36361,#36362,#36363,#36364,#36365,#36366),
 .UNSPECIFIED.,.F.,.F.,(4,3,3,3,3,3,3,3,4),(616.18936333812,617.023911272471,
617.858459206821,618.693007141172,619.527555075523,620.362103009873,621.196650944224,
622.031198878575,622.4725486453),.UNSPECIFIED.);
#271=B_SPLINE_CURVE_WITH_KNOTS('',3,(#36373,#36374,#36375,#36376,#36377,
#36378,#36379,#36380,#36381,#36382,#36383,#36384,#36385,#36386,#36387,#36388,
#36389,#36390,#36391,#36392,#36393,#36394),.UNSPECIFIED.,.F.,.F.,(4,3,3,
3,3,3,3,4),(-630.849595809668,-630.015047875317,-629.180499940967,-628.345952006616,
-627.511404072265,-626.676856137915,-625.842308203564,-625.700003594763),
 .UNSPECIFIED.);
#272=B_SPLINE_CURVE_WITH_KNOTS('',3,(#36395,#36396,#36397,#36398,#36399,
#36400,#36401,#36402,#36403,#36404,#36405,#36406,#36407,#36408,#36409,#36410,
#36411,#36412,#36413,#36414,#36415,#36416,#36417,#36418,#36419),
 .UNSPECIFIED.,.F.,.F.,(4,3,3,3,3,3,3,3,4),(622.4725486453,622.851502677375,
623.851264318912,624.35114513968,624.851025960449,625.850787601985,626.850549243522,
627.850310885059,628.755733952479),.UNSPECIFIED.);
#273=B_SPLINE_CURVE_WITH_KNOTS('',3,(#36425,#36426,#36427,#36428,#36429,
#36430,#36431,#36432,#36433,#36434,#36435,#36436,#36437,#36438,#36439,#36440,
#36441),.UNSPECIFIED.,.F.,.F.,(4,1,1,1,1,1,1,1,1,1,1,1,1,1,4),(15.707963267949,
15.9832685139281,16.4771965724115,16.9711246308949,17.4650526893783,17.9589807478618,
18.4529088063452,18.9468368648286,19.440764923312,19.9346929817954,20.4286210402789,
20.9225490987623,21.4164771572457,21.9104052157291,21.9911485751284),
 .UNSPECIFIED.);
#274=B_SPLINE_CURVE_WITH_KNOTS('',3,(#36446,#36447,#36448,#36449,#36450),
 .UNSPECIFIED.,.F.,.F.,(4,1,4),(14.9954123969612,15.4893404554446,15.707963267949),
 .UNSPECIFIED.);
#275=B_SPLINE_CURVE_WITH_KNOTS('',3,(#36453,#36454,#36455,#36456,#36457,
#36458,#36459,#36460,#36461,#36462,#36463,#36464,#36465),.UNSPECIFIED.,
 .F.,.F.,(4,3,3,3,4),(-15.707963267949,-15.4479023213137,-14.9539744342492,
-14.4600465471847,-14.1765193863714),.UNSPECIFIED.);
#276=B_SPLINE_CURVE_WITH_KNOTS('',3,(#36470,#36471,#36472,#36473,#36474,
#36475,#36476,#36477,#36478,#36479,#36480,#36481,#36482,#36483,#36484,#36485),
 .UNSPECIFIED.,.F.,.F.,(4,1,1,1,1,1,1,1,1,1,1,1,1,4),(21.9911485751284,
22.4043332742125,22.898261332696,23.3921893911794,23.8861174496628,24.3800455081462,
24.8739735666297,25.3679016251131,25.8618296835965,26.3557577420799,26.8496858005633,
27.3436138590468,27.8375419175302,28.2743338823082),.UNSPECIFIED.);
#277=B_SPLINE_CURVE_WITH_KNOTS('',3,(#36486,#36487,#36488,#36489,#36490,
#36491,#36492,#36493,#36494,#36495,#36496,#36497,#36498,#36499,#36500,#36501,
#36502,#36503,#36504,#36505,#36506,#36507,#36508,#36509,#36510,#36511,#36512,
#36513,#36514,#36515,#36516,#36517,#36518,#36519,#36520,#36521,#36522,#36523,
#36524,#36525,#36526,#36527,#36528),.UNSPECIFIED.,.F.,.F.,(4,3,3,3,3,3,
3,3,3,3,3,3,3,3,4),(-21.9911485751284,-21.868964853152,-21.3750369660875,
-20.881109079023,-20.3871811919585,-19.893253304894,-19.3993254178296,-18.9053975307651,
-18.4114696437006,-17.9175417566361,-17.4236138695716,-16.9296859825071,
-16.4357580954427,-15.9418302083782,-15.707963267949),.UNSPECIFIED.);
#278=B_SPLINE_CURVE_WITH_KNOTS('',3,(#36533,#36534,#36535,#36536,#36537,
#36538,#36539,#36540,#36541,#36542,#36543,#36544,#36545,#36546,#36547,#36548,
#36549),.UNSPECIFIED.,.F.,.F.,(4,1,1,1,1,1,1,1,1,1,1,1,1,1,4),(28.2743338823082,
28.3314699760136,28.825398034497,29.3193260929804,29.8132541514639,30.3071822099473,
30.8011102684307,31.2950383269141,31.7889663853976,32.282894443881,32.7768225023644,
33.2707505608478,33.7646786193312,34.2586066778147,34.5575191894877),
 .UNSPECIFIED.);
#279=B_SPLINE_CURVE_WITH_KNOTS('',3,(#36550,#36551,#36552,#36553,#36554,
#36555,#36556,#36557,#36558,#36559,#36560,#36561,#36562,#36563,#36564,#36565,
#36566,#36567,#36568,#36569,#36570,#36571,#36572,#36573,#36574,#36575,#36576,
#36577,#36578,#36579,#36580,#36581,#36582,#36583,#36584,#36585,#36586,#36587,
#36588,#36589),.UNSPECIFIED.,.F.,.F.,(4,3,3,3,3,3,3,3,3,3,3,3,3,4),(-28.2743338823079,
-27.7960994979258,-27.3021716108613,-26.8082437237968,-26.3143158367323,
-25.8203879496678,-25.3264600626034,-24.8325321755389,-24.3386042884744,
-23.8446764014099,-23.3507485143454,-22.8568206272809,-22.3628927402165,
-21.9911485751284),.UNSPECIFIED.);
#280=B_SPLINE_CURVE_WITH_KNOTS('',3,(#36594,#36595,#36596,#36597,#36598,
#36599,#36600,#36601,#36602,#36603,#36604,#36605,#36606,#36607,#36608,#36609,
#36610),.UNSPECIFIED.,.F.,.F.,(4,1,1,1,1,1,1,1,1,1,1,1,1,1,4),(34.5575191894877,
34.7525347362981,35.2464627947815,35.7403908532649,36.2343189117483,36.7282469702318,
37.2221750287152,37.7161030871986,38.210031145682,38.7039592041655,39.1978872626489,
39.6918153211323,40.1857433796157,40.6796714380991,40.8407044966672),
 .UNSPECIFIED.);
#281=B_SPLINE_CURVE_WITH_KNOTS('',3,(#36611,#36612,#36613,#36614,#36615,
#36616,#36617,#36618,#36619,#36620,#36621,#36622,#36623,#36624,#36625,#36626,
#36627,#36628,#36629,#36630,#36631,#36632,#36633,#36634,#36635,#36636,#36637,
#36638,#36639,#36640,#36641,#36642,#36643,#36644,#36645,#36646,#36647,#36648,
#36649,#36650,#36651,#36652,#36653),.UNSPECIFIED.,.F.,.F.,(4,3,3,3,3,3,
3,3,3,3,3,3,3,3,4),(-34.5575191894877,-34.217162029764,-33.7232341426995,
-33.2293062556351,-32.7353783685706,-32.2414504815061,-31.7475225944416,
-31.2535947073771,-30.7596668203126,-30.2657389332482,-29.7718110461837,
-29.2778831591192,-28.7839552720547,-28.2900273849902,-28.2743338823079),
 .UNSPECIFIED.);
#282=B_SPLINE_CURVE_WITH_KNOTS('',3,(#36658,#36659,#36660,#36661,#36662,
#36663,#36664,#36665,#36666,#36667,#36668,#36669,#36670,#36671,#36672,#36673,
#36674),.UNSPECIFIED.,.F.,.F.,(4,1,1,1,1,1,1,1,1,1,1,1,1,1,4),(40.8407044966672,
41.1735994965826,41.667527555066,42.1614556135494,42.6553836720328,43.1493117305162,
43.6432397889997,44.1371678474831,44.6310959059665,45.1250239644499,45.6189520229333,
46.1128800814168,46.6068081399002,47.1007361983836,47.1238898038469),
 .UNSPECIFIED.);
#283=B_SPLINE_CURVE_WITH_KNOTS('',3,(#36675,#36676,#36677,#36678,#36679,
#36680,#36681,#36682,#36683,#36684,#36685,#36686,#36687,#36688,#36689,#36690,
#36691,#36692,#36693,#36694,#36695,#36696,#36697,#36698,#36699,#36700,#36701,
#36702,#36703,#36704,#36705,#36706,#36707,#36708,#36709,#36710,#36711,#36712,
#36713,#36714,#36715,#36716,#36717),.UNSPECIFIED.,.F.,.F.,(4,3,3,3,3,3,
3,3,3,3,3,3,3,3,4),(-40.8407044966672,-40.6382245616023,-40.1442966745378,
-39.6503687874733,-39.1564409004088,-38.6625130133444,-38.1685851262799,
-37.6746572392154,-37.1807293521509,-36.6868014650864,-36.1928735780219,
-35.6989456909575,-35.205017803893,-34.7110899168285,-34.5575191894877),
 .UNSPECIFIED.);
#284=B_SPLINE_CURVE_WITH_KNOTS('',3,(#36722,#36723,#36724,#36725,#36726,
#36727,#36728,#36729,#36730,#36731,#36732,#36733,#36734,#36735,#36736,#36737),
 .UNSPECIFIED.,.F.,.F.,(4,1,1,1,1,1,1,1,1,1,1,1,1,4),(47.1238898038469,
47.594664256867,48.0885923153505,48.5825203738339,49.0764484323173,49.5703764908007,
50.0643045492841,50.5582326077676,51.052160666251,51.5460887247344,52.0400167832178,
52.5339448417012,53.0278729001847,53.4070751110264),.UNSPECIFIED.);
#285=B_SPLINE_CURVE_WITH_KNOTS('',3,(#36738,#36739,#36740,#36741,#36742,
#36743,#36744,#36745,#36746,#36747,#36748,#36749,#36750,#36751,#36752,#36753,
#36754,#36755,#36756,#36757,#36758,#36759,#36760,#36761,#36762,#36763,#36764,
#36765,#36766,#36767,#36768,#36769,#36770,#36771,#36772,#36773,#36774,#36775,
#36776,#36777,#36778,#36779,#36780),.UNSPECIFIED.,.F.,.F.,(4,3,3,3,3,3,
3,3,3,3,3,3,3,3,4),(-47.1238898038469,-47.0592870934406,-46.5653592063761,
-46.0714313193116,-45.5775034322471,-45.0835755451826,-44.5896476581181,
-44.0957197710537,-43.6017918839892,-43.1078639969247,-42.6139361098602,
-42.1200082227957,-41.6260803357312,-41.1321524486668,-40.8407044966672),
 .UNSPECIFIED.);
#286=B_SPLINE_CURVE_WITH_KNOTS('',3,(#36785,#36786,#36787,#36788,#36789,
#36790,#36791,#36792,#36793,#36794,#36795,#36796,#36797,#36798,#36799,#36800,
#36801),.UNSPECIFIED.,.F.,.F.,(4,1,1,1,1,1,1,1,1,1,1,1,1,1,4),(53.4070751110264,
53.5218009586681,54.0157290171515,54.5096570756349,55.0035851341184,55.4975131926018,
55.9914412510852,56.4853693095686,56.979297368052,57.4732254265355,57.9671534850189,
58.4610815435023,58.9550096019857,59.4489376604691,59.6902604182061),
 .UNSPECIFIED.);
#287=B_SPLINE_CURVE_WITH_KNOTS('',3,(#36802,#36803,#36804,#36805,#36806,
#36807,#36808,#36809,#36810,#36811,#36812,#36813,#36814,#36815,#36816,#36817,
#36818,#36819,#36820,#36821,#36822,#36823,#36824,#36825,#36826,#36827,#36828,
#36829,#36830,#36831,#36832,#36833,#36834,#36835,#36836,#36837,#36838,#36839,
#36840,#36841),.UNSPECIFIED.,.F.,.F.,(4,3,3,3,3,3,3,3,3,3,3,3,3,4),(-53.4070751110264,
-52.9864217382143,-52.4924938511499,-51.9985659640854,-51.5046380770209,
-51.0107101899564,-50.5167823028919,-50.0228544158274,-49.528926528763,
-49.0349986416985,-48.541070754634,-48.0471428675695,-47.553214980505,-47.1238898038469),
 .UNSPECIFIED.);
#288=B_SPLINE_CURVE_WITH_KNOTS('',3,(#36846,#36847,#36848,#36849,#36850,
#36851,#36852,#36853,#36854,#36855,#36856,#36857,#36858,#36859,#36860,#36861,
#36862),.UNSPECIFIED.,.F.,.F.,(4,1,1,1,1,1,1,1,1,1,1,1,1,1,4),(59.6902604182061,
59.9428657189526,60.436793777436,60.9307218359194,61.4246498944028,61.9185779528863,
62.4125060113697,62.9064340698531,63.4003621283365,63.8942901868199,64.3882182453034,
64.8821463037868,65.3760743622702,65.8700024207536,65.9734457253856),
 .UNSPECIFIED.);
#289=B_SPLINE_CURVE_WITH_KNOTS('',3,(#36863,#36864,#36865,#36866,#36867,
#36868,#36869,#36870,#36871,#36872,#36873,#36874,#36875,#36876,#36877,#36878,
#36879,#36880,#36881,#36882,#36883,#36884,#36885,#36886,#36887,#36888,#36889,
#36890,#36891,#36892,#36893,#36894,#36895,#36896,#36897,#36898,#36899,#36900,
#36901,#36902,#36903,#36904,#36905),.UNSPECIFIED.,.F.,.F.,(4,3,3,3,3,3,
3,3,3,3,3,3,3,3,4),(-59.6902604182059,-59.4074842700526,-58.9135563829881,
-58.4196284959236,-57.9257006088591,-57.4317727217947,-56.9378448347302,
-56.4439169476657,-55.9499890606012,-55.4560611735367,-54.9621332864723,
-54.4682053994078,-53.9742775123433,-53.4803496252788,-53.4070751110264),
 .UNSPECIFIED.);
#290=B_SPLINE_CURVE_WITH_KNOTS('',3,(#36910,#36911,#36912,#36913,#36914,
#36915,#36916,#36917,#36918,#36919,#36920,#36921,#36922,#36923,#36924,#36925),
 .UNSPECIFIED.,.F.,.F.,(4,1,1,1,1,1,1,1,1,1,1,1,1,4),(65.9734457253856,
66.363930479237,66.8578585377205,67.3517865962039,67.8457146546873,68.3396427131707,
68.8335707716542,69.3274988301376,69.821426888621,70.3153549471044,70.8092830055878,
71.3032110640713,71.7971391225547,72.2566310325653),.UNSPECIFIED.);
#291=B_SPLINE_CURVE_WITH_KNOTS('',3,(#36926,#36927,#36928,#36929,#36930,
#36931,#36932,#36933,#36934,#36935,#36936,#36937,#36938,#36939,#36940,#36941,
#36942,#36943,#36944,#36945,#36946,#36947,#36948,#36949,#36950,#36951,#36952,
#36953,#36954,#36955,#36956,#36957,#36958,#36959,#36960,#36961,#36962,#36963,
#36964,#36965,#36966,#36967,#36968),.UNSPECIFIED.,.F.,.F.,(4,3,3,3,3,3,
3,3,3,3,3,3,3,3,4),(-65.9734457253856,-65.8285468018909,-65.3346189148264,
-64.8406910277619,-64.3467631406974,-63.8528352536329,-63.3589073665684,
-62.864979479504,-62.3710515924395,-61.877123705375,-61.3831958183105,-60.889267931246,
-60.3953400441816,-59.9014121571171,-59.6902604182059),.UNSPECIFIED.);
#292=B_SPLINE_CURVE_WITH_KNOTS('',3,(#36975,#36976,#36977,#36978,#36979,
#36980,#36981,#36982,#36983,#36984,#36985,#36986),.UNSPECIFIED.,.F.,.F.,
(4,1,1,1,1,1,1,1,1,4),(72.2566310325653,72.2910671810381,72.7849952395215,
73.2789232980049,73.7728513564884,74.2667794149718,74.7607074734552,75.2546355319386,
75.748563590422,76.0320696667063),.UNSPECIFIED.);
#293=B_SPLINE_CURVE_WITH_KNOTS('',3,(#36987,#36988,#36989,#36990,#36991,
#36992,#36993,#36994,#36995,#36996,#36997,#36998,#36999,#37000,#37001,#37002,
#37003,#37004,#37005,#37006,#37007,#37008,#37009,#37010,#37011,#37012,#37013,
#37014,#37015,#37016,#37017,#37018,#37019,#37020,#37021,#37022,#37023,#37024,
#37025,#37026,#37027,#37028,#37029),.UNSPECIFIED.,.F.,.F.,(4,3,3,3,3,3,
3,3,3,3,3,3,3,3,4),(-72.2566310325651,-72.2496093337291,-71.7556814466647,
-71.2617535596002,-70.7678256725357,-70.2738977854712,-69.7799698984067,
-69.2860420113422,-68.7921141242778,-68.2981862372133,-67.8042583501488,
-67.3103304630843,-66.8164025760198,-66.3224746889554,-65.9734457253856),
 .UNSPECIFIED.);
#294=B_SPLINE_CURVE_WITH_KNOTS('',3,(#37035,#37036,#37037,#37038,#37039,
#37040,#37041,#37042,#37043,#37044,#37045,#37046),.UNSPECIFIED.,.F.,.F.,
(4,1,1,1,1,1,1,1,1,4),(72.2566310325653,72.2910671810381,72.7849952395215,
73.2789232980049,73.7728513564884,74.2667794149718,74.7607074734552,75.2546355319386,
75.748563590422,76.2424703929574),.UNSPECIFIED.);
#295=B_SPLINE_CURVE_WITH_KNOTS('',3,(#37049,#37050,#37051,#37052,#37053,
#37054,#37055,#37056,#37057),.UNSPECIFIED.,.F.,.F.,(4,1,1,1,1,1,4),(72.2566310325653,
72.7435372207936,73.2374651078581,73.7313929949226,74.2253208819871,74.7192487690515,
75.0027759298649),.UNSPECIFIED.);
#296=B_SPLINE_CURVE_WITH_KNOTS('',3,(#37062,#37063,#37064,#37065,#37066,
#37067,#37068,#37069,#37070,#37071,#37072,#37073,#37074,#37075,#37076,#37077),
 .UNSPECIFIED.,.F.,.F.,(4,1,1,1,1,1,1,1,1,1,1,1,1,4),(65.9734457253856,
66.363930479237,66.8578585377205,67.3517865962039,67.8457146546873,68.3396427131707,
68.8335707716542,69.3274988301376,69.821426888621,70.3153549471044,70.8092830055878,
71.3032110640713,71.7971391225547,72.2566310325653),.UNSPECIFIED.);
#297=B_SPLINE_CURVE_WITH_KNOTS('',3,(#37078,#37079,#37080,#37081,#37082,
#37083,#37084,#37085,#37086,#37087,#37088,#37089,#37090,#37091,#37092,#37093,
#37094),.UNSPECIFIED.,.F.,.F.,(4,1,1,1,1,1,1,1,1,1,1,1,1,1,4),(65.9734457253856,
66.3224746889554,66.8164025760198,67.3103304630843,67.8042583501488,68.2981862372133,
68.7921141242778,69.2860420113422,69.7799698984067,70.2738977854712,70.7678256725357,
71.2617535596002,71.7556814466647,72.2496093337291,72.2566310325653),
 .UNSPECIFIED.);
#298=B_SPLINE_CURVE_WITH_KNOTS('',3,(#37099,#37100,#37101,#37102,#37103,
#37104,#37105,#37106,#37107,#37108,#37109,#37110,#37111,#37112,#37113,#37114,
#37115),.UNSPECIFIED.,.F.,.F.,(4,1,1,1,1,1,1,1,1,1,1,1,1,1,4),(59.6902604182061,
59.9428657189526,60.436793777436,60.9307218359194,61.4246498944028,61.9185779528863,
62.4125060113697,62.9064340698531,63.4003621283365,63.8942901868199,64.3882182453034,
64.8821463037868,65.3760743622702,65.8700024207536,65.9734457253856),
 .UNSPECIFIED.);
#299=B_SPLINE_CURVE_WITH_KNOTS('',3,(#37116,#37117,#37118,#37119,#37120,
#37121,#37122,#37123,#37124,#37125,#37126,#37127,#37128,#37129,#37130,#37131,
#37132),.UNSPECIFIED.,.F.,.F.,(4,1,1,1,1,1,1,1,1,1,1,1,1,1,4),(59.6902604182061,
59.9014121571171,60.3953400441816,60.889267931246,61.3831958183105,61.877123705375,
62.3710515924395,62.864979479504,63.3589073665685,63.8528352536329,64.3467631406974,
64.8406910277619,65.3346189148264,65.8285468018909,65.9734457253856),
 .UNSPECIFIED.);
#300=B_SPLINE_CURVE_WITH_KNOTS('',3,(#37137,#37138,#37139,#37140,#37141,
#37142,#37143,#37144,#37145,#37146,#37147,#37148,#37149,#37150,#37151,#37152,
#37153),.UNSPECIFIED.,.F.,.F.,(4,1,1,1,1,1,1,1,1,1,1,1,1,1,4),(53.4070751110264,
53.5218009586681,54.0157290171515,54.5096570756349,55.0035851341184,55.4975131926018,
55.9914412510852,56.4853693095686,56.979297368052,57.4732254265355,57.9671534850189,
58.4610815435023,58.9550096019857,59.4489376604691,59.6902604182061),
 .UNSPECIFIED.);
#301=B_SPLINE_CURVE_WITH_KNOTS('',3,(#37154,#37155,#37156,#37157,#37158,
#37159,#37160,#37161,#37162,#37163,#37164,#37165,#37166,#37167,#37168,#37169,
#37170),.UNSPECIFIED.,.F.,.F.,(4,1,1,1,1,1,1,1,1,1,1,1,1,1,4),(53.4070751110264,
53.4803496252788,53.9742775123433,54.4682053994078,54.9621332864723,55.4560611735367,
55.9499890606012,56.4439169476657,56.9378448347302,57.4317727217947,57.9257006088591,
58.4196284959236,58.9135563829881,59.4074842700526,59.6902604182061),
 .UNSPECIFIED.);
#302=B_SPLINE_CURVE_WITH_KNOTS('',3,(#37175,#37176,#37177,#37178,#37179,
#37180,#37181,#37182,#37183,#37184,#37185,#37186,#37187,#37188,#37189,#37190),
 .UNSPECIFIED.,.F.,.F.,(4,1,1,1,1,1,1,1,1,1,1,1,1,4),(47.1238898038469,
47.594664256867,48.0885923153505,48.5825203738339,49.0764484323173,49.5703764908007,
50.0643045492841,50.5582326077676,51.052160666251,51.5460887247344,52.0400167832178,
52.5339448417012,53.0278729001847,53.4070751110264),.UNSPECIFIED.);
#303=B_SPLINE_CURVE_WITH_KNOTS('',3,(#37191,#37192,#37193,#37194,#37195,
#37196,#37197,#37198,#37199,#37200,#37201,#37202,#37203,#37204,#37205,#37206),
 .UNSPECIFIED.,.F.,.F.,(4,1,1,1,1,1,1,1,1,1,1,1,1,4),(47.1238898038469,
47.553214980505,48.0471428675695,48.541070754634,49.0349986416985,49.528926528763,
50.0228544158274,50.5167823028919,51.0107101899564,51.5046380770209,51.9985659640854,
52.4924938511499,52.9864217382143,53.4070751110264),.UNSPECIFIED.);
#304=B_SPLINE_CURVE_WITH_KNOTS('',3,(#37211,#37212,#37213,#37214,#37215,
#37216,#37217,#37218,#37219,#37220,#37221,#37222,#37223,#37224,#37225,#37226,
#37227),.UNSPECIFIED.,.F.,.F.,(4,1,1,1,1,1,1,1,1,1,1,1,1,1,4),(40.8407044966672,
41.1735994965826,41.667527555066,42.1614556135494,42.6553836720328,43.1493117305162,
43.6432397889997,44.1371678474831,44.6310959059665,45.1250239644499,45.6189520229333,
46.1128800814168,46.6068081399002,47.1007361983836,47.1238898038469),
 .UNSPECIFIED.);
#305=B_SPLINE_CURVE_WITH_KNOTS('',3,(#37228,#37229,#37230,#37231,#37232,
#37233,#37234,#37235,#37236,#37237,#37238,#37239,#37240,#37241,#37242,#37243,
#37244),.UNSPECIFIED.,.F.,.F.,(4,1,1,1,1,1,1,1,1,1,1,1,1,1,4),(40.8407044966672,
41.1321524486668,41.6260803357312,42.1200082227957,42.6139361098602,43.1078639969247,
43.6017918839892,44.0957197710537,44.5896476581181,45.0835755451826,45.5775034322471,
46.0714313193116,46.5653592063761,47.0592870934405,47.1238898038469),
 .UNSPECIFIED.);
#306=B_SPLINE_CURVE_WITH_KNOTS('',3,(#37249,#37250,#37251,#37252,#37253,
#37254,#37255,#37256,#37257,#37258,#37259,#37260,#37261,#37262,#37263,#37264,
#37265),.UNSPECIFIED.,.F.,.F.,(4,1,1,1,1,1,1,1,1,1,1,1,1,1,4),(34.5575191894877,
34.7525347362981,35.2464627947815,35.7403908532649,36.2343189117483,36.7282469702318,
37.2221750287152,37.7161030871986,38.210031145682,38.7039592041655,39.1978872626489,
39.6918153211323,40.1857433796157,40.6796714380991,40.8407044966672),
 .UNSPECIFIED.);
#307=B_SPLINE_CURVE_WITH_KNOTS('',3,(#37266,#37267,#37268,#37269,#37270,
#37271,#37272,#37273,#37274,#37275,#37276,#37277,#37278,#37279,#37280,#37281,
#37282),.UNSPECIFIED.,.F.,.F.,(4,1,1,1,1,1,1,1,1,1,1,1,1,1,4),(34.5575191894877,
34.7110899168285,35.205017803893,35.6989456909575,36.1928735780219,36.6868014650864,
37.1807293521509,37.6746572392154,38.1685851262799,38.6625130133444,39.1564409004088,
39.6503687874733,40.1442966745378,40.6382245616023,40.8407044966672),
 .UNSPECIFIED.);
#308=B_SPLINE_CURVE_WITH_KNOTS('',3,(#37287,#37288,#37289,#37290,#37291,
#37292,#37293,#37294,#37295,#37296,#37297,#37298,#37299,#37300,#37301,#37302,
#37303),.UNSPECIFIED.,.F.,.F.,(4,1,1,1,1,1,1,1,1,1,1,1,1,1,4),(28.2743338823082,
28.3314699760136,28.825398034497,29.3193260929804,29.8132541514639,30.3071822099473,
30.8011102684307,31.2950383269141,31.7889663853976,32.282894443881,32.7768225023644,
33.2707505608478,33.7646786193312,34.2586066778147,34.5575191894877),
 .UNSPECIFIED.);
#309=B_SPLINE_CURVE_WITH_KNOTS('',3,(#37304,#37305,#37306,#37307,#37308,
#37309,#37310,#37311,#37312,#37313,#37314,#37315,#37316,#37317,#37318,#37319,
#37320),.UNSPECIFIED.,.F.,.F.,(4,1,1,1,1,1,1,1,1,1,1,1,1,1,4),(28.2743338823082,
28.2900273849902,28.7839552720547,29.2778831591192,29.7718110461837,30.2657389332482,
30.7596668203126,31.2535947073771,31.7475225944416,32.2414504815061,32.7353783685706,
33.2293062556351,33.7232341426995,34.217162029764,34.5575191894877),
 .UNSPECIFIED.);
#310=B_SPLINE_CURVE_WITH_KNOTS('',3,(#37325,#37326,#37327,#37328,#37329,
#37330,#37331,#37332,#37333,#37334,#37335,#37336,#37337,#37338,#37339,#37340),
 .UNSPECIFIED.,.F.,.F.,(4,1,1,1,1,1,1,1,1,1,1,1,1,4),(21.9911485751284,
22.4043332742125,22.898261332696,23.3921893911794,23.8861174496628,24.3800455081462,
24.8739735666297,25.3679016251131,25.8618296835965,26.3557577420799,26.8496858005633,
27.3436138590468,27.8375419175302,28.2743338823082),.UNSPECIFIED.);
#311=B_SPLINE_CURVE_WITH_KNOTS('',3,(#37341,#37342,#37343,#37344,#37345,
#37346,#37347,#37348,#37349,#37350,#37351,#37352,#37353,#37354,#37355,#37356),
 .UNSPECIFIED.,.F.,.F.,(4,1,1,1,1,1,1,1,1,1,1,1,1,4),(21.9911485751284,
22.3628927402165,22.8568206272809,23.3507485143454,23.8446764014099,24.3386042884744,
24.8325321755389,25.3264600626033,25.8203879496678,26.3143158367323,26.8082437237968,
27.3021716108613,27.7960994979258,28.2743338823082),.UNSPECIFIED.);
#312=B_SPLINE_CURVE_WITH_KNOTS('',3,(#37361,#37362,#37363,#37364,#37365,
#37366,#37367,#37368,#37369,#37370,#37371,#37372,#37373,#37374,#37375,#37376,
#37377),.UNSPECIFIED.,.F.,.F.,(4,1,1,1,1,1,1,1,1,1,1,1,1,1,4),(15.707963267949,
15.9832685139281,16.4771965724115,16.9711246308949,17.4650526893783,17.9589807478618,
18.4529088063452,18.9468368648286,19.440764923312,19.9346929817954,20.4286210402789,
20.9225490987623,21.4164771572457,21.9104052157291,21.9911485751284),
 .UNSPECIFIED.);
#313=B_SPLINE_CURVE_WITH_KNOTS('',3,(#37378,#37379,#37380,#37381,#37382,
#37383,#37384,#37385,#37386,#37387,#37388,#37389,#37390,#37391,#37392,#37393,
#37394),.UNSPECIFIED.,.F.,.F.,(4,1,1,1,1,1,1,1,1,1,1,1,1,1,4),(15.707963267949,
15.9418302083782,16.4357580954427,16.9296859825072,17.4236138695716,17.9175417566361,
18.4114696437006,18.9053975307651,19.3993254178296,19.893253304894,20.3871811919585,
20.881109079023,21.3750369660875,21.868964853152,21.9911485751284),
 .UNSPECIFIED.);
#314=B_SPLINE_CURVE_WITH_KNOTS('',3,(#37400,#37401,#37402,#37403,#37404,
#37405,#37406,#37407,#37408),.UNSPECIFIED.,.F.,.F.,(4,1,1,1,1,1,4),(637.743308678727,
637.89409268595,638.893854327487,639.893615969023,640.89337761056,641.893139252097,
641.932632128719),.UNSPECIFIED.);
#315=B_SPLINE_CURVE_WITH_KNOTS('',3,(#37411,#37412,#37413,#37414,#37415,
#37416,#37417),.UNSPECIFIED.,.F.,.F.,(4,1,1,1,4),(637.743308678728,637.837647252847,
638.837408894383,639.337289715152,639.83717053592),.UNSPECIFIED.);
#316=B_SPLINE_CURVE_WITH_KNOTS('',3,(#37422,#37423,#37424,#37425,#37426,
#37427,#37428,#37429,#37430,#37431,#37432),.UNSPECIFIED.,.F.,.F.,(4,1,1,
1,1,1,1,1,4),(631.460123371548,631.895522836729,632.895284478266,633.895046119803,
634.89480776134,635.894569402876,636.394450223645,636.894331044413,637.743308678727),
 .UNSPECIFIED.);
#317=B_SPLINE_CURVE_WITH_KNOTS('',3,(#37433,#37434,#37435,#37436,#37437,
#37438,#37439,#37440,#37441,#37442,#37443),.UNSPECIFIED.,.F.,.F.,(4,1,1,
1,1,1,1,1,4),(631.460123371548,631.839077403626,632.838839045163,633.338719865931,
633.8386006867,634.838362328236,635.838123969773,636.83788561131,637.743308678728),
 .UNSPECIFIED.);
#318=B_SPLINE_CURVE_WITH_KNOTS('',3,(#37448,#37449,#37450,#37451,#37452,
#37453,#37454,#37455,#37456,#37457,#37458,#37459,#37460,#37461,#37462,#37463,
#37464,#37465,#37466,#37467,#37468,#37469),.UNSPECIFIED.,.F.,.F.,(4,3,3,
3,3,3,3,4),(625.176938064368,626.085415137985,626.993892211602,627.902369285219,
628.810846358836,629.719323432453,630.62780050607,631.460123371548),
 .UNSPECIFIED.);
#319=B_SPLINE_CURVE_WITH_KNOTS('',3,(#37470,#37471,#37472,#37473,#37474,
#37475,#37476,#37477,#37478,#37479,#37480),.UNSPECIFIED.,.F.,.F.,(4,1,1,
1,1,1,1,1,4),(625.176938064369,625.840507554406,626.340388375174,626.840269195943,
627.84003083748,628.839792479016,629.839554120553,630.83931576209,631.460123371548),
 .UNSPECIFIED.);
#320=B_SPLINE_CURVE_WITH_KNOTS('',3,(#37485,#37486,#37487,#37488,#37489,
#37490,#37491,#37492,#37493,#37494,#37495,#37496,#37497,#37498,#37499,#37500,
#37501,#37502,#37503,#37504,#37505,#37506,#37507,#37508,#37509,#37510,#37511,
#37512),.UNSPECIFIED.,.F.,.F.,(4,3,3,3,3,3,3,3,3,4),(618.893752757189,618.898621496752,
619.898383138289,620.898144779826,621.897906421362,622.397787242131,622.897668062899,
623.897429704436,624.897191345972,625.176938064368),.UNSPECIFIED.);
#321=B_SPLINE_CURVE_WITH_KNOTS('',3,(#37513,#37514,#37515,#37516,#37517,
#37518,#37519,#37520,#37521,#37522,#37523),.UNSPECIFIED.,.F.,.F.,(4,1,1,
1,1,1,1,1,4),(618.893752757189,619.342056884417,619.841937705186,620.841699346722,
621.841460988259,622.841222629796,623.840984271333,624.840745912869,625.176938064369),
 .UNSPECIFIED.);
#322=B_SPLINE_CURVE_WITH_KNOTS('',3,(#37528,#37529,#37530,#37531,#37532,
#37533,#37534,#37535,#37536,#37537,#37538,#37539,#37540,#37541,#37542,#37543,
#37544,#37545,#37546,#37547,#37548,#37549,#37550,#37551,#37552),
 .UNSPECIFIED.,.F.,.F.,(4,3,3,3,3,3,3,3,4),(612.610567450009,612.900051647532,
613.899813289069,614.899574930605,615.399455751374,615.899336572142,616.899098213679,
617.898859855216,618.893752757189),.UNSPECIFIED.);
#323=B_SPLINE_CURVE_WITH_KNOTS('',3,(#37553,#37554,#37555,#37556,#37557,
#37558,#37559,#37560,#37561,#37562,#37563,#37564,#37565,#37566,#37567,#37568,
#37569,#37570,#37571,#37572,#37573,#37574,#37575,#37576,#37577),
 .UNSPECIFIED.,.F.,.F.,(4,3,3,3,3,3,3,3,4),(612.61056745001,612.843606214429,
613.843367855966,614.843129497502,615.842891139039,616.842652780576,617.842414422112,
618.842176063649,618.893752757189),.UNSPECIFIED.);
#324=B_SPLINE_CURVE_WITH_KNOTS('',3,(#37582,#37583,#37584,#37585,#37586,
#37587,#37588,#37589,#37590,#37591,#37592,#37593,#37594,#37595,#37596,#37597,
#37598,#37599,#37600,#37601,#37602,#37603),.UNSPECIFIED.,.F.,.F.,(4,3,3,
3,3,3,3,4),(606.327382142829,607.235859216446,608.144336290063,609.05281336368,
609.961290437297,610.869767510914,611.778244584531,612.610567450009),
 .UNSPECIFIED.);
#325=B_SPLINE_CURVE_WITH_KNOTS('',3,(#37604,#37605,#37606,#37607,#37608,
#37609,#37610,#37611,#37612,#37613,#37614,#37615,#37616,#37617,#37618,#37619,
#37620,#37621,#37622,#37623,#37624,#37625,#37626,#37627,#37628),
 .UNSPECIFIED.,.F.,.F.,(4,3,3,3,3,3,3,3,4),(606.32738214283,606.845036365208,
607.844798006745,608.844559648282,609.844321289819,610.844082931355,611.843844572892,
612.343725393661,612.61056745001),.UNSPECIFIED.);
#326=B_SPLINE_CURVE_WITH_KNOTS('',3,(#37633,#37634,#37635,#37636,#37637,
#37638,#37639,#37640,#37641,#37642,#37643),.UNSPECIFIED.,.F.,.F.,(4,1,1,
1,1,1,1,1,4),(600.04419683565,600.902911949091,601.40279276986,601.902673590628,
602.902435232165,603.902196873701,604.901958515238,605.901720156775,606.327382142829),
 .UNSPECIFIED.);
#327=B_SPLINE_CURVE_WITH_KNOTS('',3,(#37644,#37645,#37646,#37647,#37648,
#37649,#37650,#37651,#37652,#37653,#37654),.UNSPECIFIED.,.F.,.F.,(4,1,1,
1,1,1,1,1,4),(600.044196835651,600.846466515988,601.846228157525,602.845989799061,
603.845751440598,604.845513082135,605.345393902903,605.845274723672,606.32738214283),
 .UNSPECIFIED.);
#328=B_SPLINE_CURVE_WITH_KNOTS('',3,(#37659,#37660,#37661,#37662,#37663,
#37664,#37665,#37666,#37667,#37668,#37669,#37670),.UNSPECIFIED.,.F.,.F.,
(4,1,1,1,1,1,1,1,1,4),(593.76101152847,593.904580458334,594.404461279103,
594.904342099871,595.904103741408,596.903865382944,597.903627024481,598.903388666018,
599.903150307555,600.04419683565),.UNSPECIFIED.);
#329=B_SPLINE_CURVE_WITH_KNOTS('',3,(#37671,#37672,#37673,#37674,#37675,
#37676,#37677,#37678,#37679,#37680,#37681,#37682),.UNSPECIFIED.,.F.,.F.,
(4,1,1,1,1,1,1,1,1,4),(593.761011528471,593.848135025231,594.847896666768,
595.847658308305,596.847419949841,597.847181591378,598.347062412146,598.846943232915,
599.846704874451,600.044196835651),.UNSPECIFIED.);
#330=B_SPLINE_CURVE_WITH_KNOTS('',3,(#37687,#37688,#37689,#37690,#37691,
#37692,#37693,#37694,#37695,#37696,#37697,#37698,#37699,#37700,#37701,#37702,
#37703,#37704,#37705,#37706,#37707,#37708),.UNSPECIFIED.,.F.,.F.,(4,3,3,
3,3,3,3,4),(587.477826221291,587.906010609114,588.905772250651,589.905533892187,
590.905295533724,591.905057175261,592.904818816798,593.76101152847),
 .UNSPECIFIED.);
#331=B_SPLINE_CURVE_WITH_KNOTS('',3,(#37709,#37710,#37711,#37712,#37713,
#37714,#37715,#37716,#37717,#37718,#37719),.UNSPECIFIED.,.F.,.F.,(4,1,1,
1,1,1,1,1,4),(587.477826221291,587.849565176011,588.849326817548,589.849088459084,
590.848850100621,591.348730921389,591.848611742158,592.848373383694,593.761011528471),
 .UNSPECIFIED.);
#332=B_SPLINE_CURVE_WITH_KNOTS('',3,(#37724,#37725,#37726,#37727,#37728,
#37729,#37730,#37731,#37732,#37733,#37734,#37735,#37736,#37737,#37738,#37739,
#37740,#37741,#37742,#37743,#37744,#37745,#37746,#37747,#37748),
 .UNSPECIFIED.,.F.,.F.,(4,3,3,3,3,3,3,3,4),(581.194640914111,581.907440759894,
582.90720240143,583.906964042967,584.906725684504,585.906487326041,586.906248967577,
587.406129788346,587.477826221291),.UNSPECIFIED.);
#333=B_SPLINE_CURVE_WITH_KNOTS('',3,(#37749,#37750,#37751,#37752,#37753,
#37754,#37755,#37756,#37757,#37758,#37759,#37760,#37761,#37762,#37763,#37764,
#37765,#37766,#37767,#37768,#37769,#37770,#37771,#37772,#37773),
 .UNSPECIFIED.,.F.,.F.,(4,3,3,3,3,3,3,3,4),(581.194640914112,581.850995326791,
582.850756968327,583.850518609864,584.350399430632,584.850280251401,585.850041892937,
586.849803534474,587.477826221291),.UNSPECIFIED.);
#334=B_SPLINE_CURVE_WITH_KNOTS('',3,(#37778,#37779,#37780,#37781,#37782,
#37783,#37784,#37785,#37786,#37787,#37788),.UNSPECIFIED.,.F.,.F.,(4,1,1,
1,1,1,1,1,4),(574.911455606932,575.908870910673,576.90863255221,577.908394193747,
578.908155835284,579.90791747682,580.407798297589,580.907679118357,581.194640914111),
 .UNSPECIFIED.);
#335=B_SPLINE_CURVE_WITH_KNOTS('',3,(#37789,#37790,#37791,#37792,#37793,
#37794,#37795,#37796,#37797,#37798,#37799,#37800,#37801,#37802,#37803,#37804,
#37805,#37806,#37807,#37808,#37809,#37810,#37811,#37812,#37813),
 .UNSPECIFIED.,.F.,.F.,(4,3,3,3,3,3,3,3,4),(574.911455606932,575.85242547757,
576.852187119107,577.352067939875,577.851948760644,578.85171040218,579.851472043717,
580.851233685254,581.194640914112),.UNSPECIFIED.);
#336=B_SPLINE_CURVE_WITH_KNOTS('',3,(#37818,#37819,#37820,#37821,#37822,
#37823,#37824,#37825,#37826,#37827,#37828,#37829),.UNSPECIFIED.,.F.,.F.,
(4,1,1,1,1,1,1,1,1,4),(568.628270299752,568.910539419916,569.910301061453,
570.91006270299,571.909824344526,572.909585986063,573.409466806832,573.9093476276,
574.909109269137,574.911455606932),.UNSPECIFIED.);
#337=B_SPLINE_CURVE_WITH_KNOTS('',3,(#37830,#37831,#37832,#37833,#37834,
#37835,#37836,#37837,#37838,#37839,#37840,#37841),.UNSPECIFIED.,.F.,.F.,
(4,1,1,1,1,1,1,1,1,4),(568.628270299753,568.854093986813,569.85385562835,
570.353736449118,570.853617269887,571.853378911423,572.85314055296,573.852902194497,
574.852663836033,574.911455606932),.UNSPECIFIED.);
#338=B_SPLINE_CURVE_WITH_KNOTS('',3,(#37846,#37847,#37848,#37849,#37850,
#37851,#37852,#37853,#37854,#37855,#37856,#37857,#37858,#37859,#37860,#37861,
#37862,#37863,#37864,#37865,#37866,#37867),.UNSPECIFIED.,.F.,.F.,(4,3,3,
3,3,3,3,4),(562.345084992572,563.253562066189,564.162039139807,565.070516213424,
565.978993287041,566.887470360658,567.795947434275,568.628270299752),
 .UNSPECIFIED.);
#339=B_SPLINE_CURVE_WITH_KNOTS('',3,(#37868,#37869,#37870,#37871,#37872,
#37873,#37874,#37875,#37876,#37877,#37878),.UNSPECIFIED.,.F.,.F.,(4,1,1,
1,1,1,1,1,4),(562.345084992573,562.855524137593,563.355404958361,563.85528577913,
564.855047420666,565.854809062203,566.85457070374,567.854332345276,568.628270299753),
 .UNSPECIFIED.);
#340=B_SPLINE_CURVE_WITH_KNOTS('',3,(#37883,#37884,#37885,#37886,#37887,
#37888,#37889,#37890,#37891,#37892,#37893,#37894,#37895,#37896,#37897,#37898,
#37899,#37900,#37901,#37902,#37903,#37904,#37905,#37906,#37907),
 .UNSPECIFIED.,.F.,.F.,(4,3,3,3,3,3,3,3,4),(556.061899685393,556.913399721476,
557.913161363013,558.912923004549,559.412803825317,559.912684646086,560.912446287623,
561.912207929159,562.345084992572),.UNSPECIFIED.);
#341=B_SPLINE_CURVE_WITH_KNOTS('',3,(#37908,#37909,#37910,#37911,#37912,
#37913,#37914,#37915,#37916,#37917,#37918),.UNSPECIFIED.,.F.,.F.,(4,1,1,
1,1,1,1,1,4),(556.061899685394,556.357073467604,556.856954288373,557.856715929909,
558.856477571446,559.856239212983,560.856000854519,561.855762496056,562.345084992573),
 .UNSPECIFIED.);
#342=B_SPLINE_CURVE_WITH_KNOTS('',3,(#37923,#37924,#37925,#37926,#37927,
#37928,#37929,#37930,#37931,#37932,#37933,#37934,#37935,#37936,#37937,#37938,
#37939,#37940,#37941,#37942,#37943,#37944,#37945,#37946,#37947,#37948,#37949,
#37950),.UNSPECIFIED.,.F.,.F.,(4,3,3,3,3,3,3,3,3,4),(549.778714378213,549.915068230719,
550.914829872255,551.914591513792,552.414472334561,552.914353155329,553.914114796866,
554.913876438402,555.913638079939,556.061899685393),.UNSPECIFIED.);
#343=B_SPLINE_CURVE_WITH_KNOTS('',3,(#37951,#37952,#37953,#37954,#37955,
#37956,#37957,#37958,#37959,#37960,#37961,#37962,#37963,#37964,#37965,#37966,
#37967,#37968,#37969,#37970,#37971,#37972,#37973,#37974,#37975),
 .UNSPECIFIED.,.F.,.F.,(4,3,3,3,3,3,3,3,4),(549.778714378214,549.858622797616,
550.858384439152,551.858146080689,552.857907722226,553.857669363763,554.857431005299,
555.857192646836,556.061899685394),.UNSPECIFIED.);
#344=B_SPLINE_CURVE_WITH_KNOTS('',3,(#37980,#37981,#37982,#37983,#37984,
#37985,#37986,#37987,#37988,#37989,#37990,#37991,#37992,#37993,#37994,#37995,
#37996,#37997,#37998,#37999,#38000,#38001,#38002,#38003,#38004),
 .UNSPECIFIED.,.F.,.F.,(4,3,3,3,3,3,3,3,4),(543.495529071034,543.916498381498,
544.916260023035,545.416140843804,545.916021664572,546.915783306109,547.915544947645,
548.915306589182,549.778714378213),.UNSPECIFIED.);
#345=B_SPLINE_CURVE_WITH_KNOTS('',3,(#38005,#38006,#38007,#38008,#38009,
#38010,#38011,#38012,#38013,#38014,#38015,#38016,#38017,#38018,#38019,#38020,
#38021,#38022,#38023,#38024,#38025,#38026,#38027,#38028,#38029),
 .UNSPECIFIED.,.F.,.F.,(4,3,3,3,3,3,3,3,4),(543.495529071035,543.860052948395,
544.859814589932,545.859576231469,546.859337873005,547.859099514542,548.858861156079,
549.358741976847,549.778714378214),.UNSPECIFIED.);
#346=B_SPLINE_CURVE_WITH_KNOTS('',3,(#38034,#38035,#38036,#38037,#38038,
#38039,#38040,#38041,#38042,#38043,#38044),.UNSPECIFIED.,.F.,.F.,(4,1,1,
1,1,1,1,1,4),(537.212343763854,537.917928532278,538.417809353046,538.917690173815,
539.917451815352,540.917213456888,541.916975098425,542.916736739962,543.495529071034),
 .UNSPECIFIED.);
#347=B_SPLINE_CURVE_WITH_KNOTS('',3,(#38045,#38046,#38047,#38048,#38049,
#38050,#38051,#38052,#38053,#38054,#38055,#38056,#38057,#38058,#38059,#38060,
#38061,#38062,#38063,#38064,#38065,#38066,#38067,#38068,#38069),
 .UNSPECIFIED.,.F.,.F.,(4,3,3,3,3,3,3,3,4),(537.212343763855,537.861483099175,
538.861244740712,539.861006382248,540.860768023785,541.860529665322,542.36041048609,
542.860291306859,543.495529071035),.UNSPECIFIED.);
#348=B_SPLINE_CURVE_WITH_KNOTS('',3,(#38074,#38075,#38076,#38077,#38078,
#38079,#38080,#38081,#38082,#38083,#38084),.UNSPECIFIED.,.F.,.F.,(4,1,1,
1,1,1,1,1,4),(530.929158456675,531.419477862289,531.919358683058,532.919120324594,
533.918881966131,534.918643607668,535.918405249205,536.918166890741,537.212343763854),
 .UNSPECIFIED.);
#349=B_SPLINE_CURVE_WITH_KNOTS('',3,(#38085,#38086,#38087,#38088,#38089,
#38090,#38091,#38092,#38093,#38094,#38095),.UNSPECIFIED.,.F.,.F.,(4,1,1,
1,1,1,1,1,4),(530.929158456675,531.862913249955,532.862674891491,533.862436533028,
534.862198174565,535.362078995333,535.861959816101,536.861721457638,537.212343763855),
 .UNSPECIFIED.);
#350=B_SPLINE_CURVE_WITH_KNOTS('',3,(#38100,#38101,#38102,#38103,#38104,
#38105,#38106,#38107,#38108,#38109,#38110),.UNSPECIFIED.,.F.,.F.,(4,1,1,
1,1,1,1,1,4),(524.645973149495,524.921027192301,525.920788833837,526.920550475374,
527.920312116911,528.920073758448,529.919835399984,530.919597041521,530.929158456675),
 .UNSPECIFIED.);
#351=B_SPLINE_CURVE_WITH_KNOTS('',3,(#38111,#38112,#38113,#38114,#38115,
#38116,#38117,#38118,#38119,#38120,#38121,#38122),.UNSPECIFIED.,.F.,.F.,
(4,1,1,1,1,1,1,1,1,4),(524.645973149496,524.864581759198,525.864343400734,
526.864105042271,527.863866683808,528.363747504576,528.863628325344,529.863389966881,
530.863151608418,530.929158456675),.UNSPECIFIED.);
#352=B_SPLINE_CURVE_WITH_KNOTS('',3,(#38127,#38128,#38129,#38130,#38131,
#38132,#38133,#38134,#38135,#38136,#38137,#38138,#38139,#38140,#38141,#38142,
#38143,#38144,#38145,#38146,#38147,#38148,#38149,#38150,#38151),
 .UNSPECIFIED.,.F.,.F.,(4,3,3,3,3,3,3,3,4),(518.362787842315,518.922457343081,
519.922218984617,520.921980626154,521.921742267691,522.921503909227,523.921265550764,
524.421146371532,524.645973149495),.UNSPECIFIED.);
#353=B_SPLINE_CURVE_WITH_KNOTS('',3,(#38152,#38153,#38154,#38155,#38156,
#38157,#38158,#38159,#38160,#38161,#38162),.UNSPECIFIED.,.F.,.F.,(4,1,1,
1,1,1,1,1,4),(518.362787842316,518.866011909977,519.865773551514,520.865535193051,
521.365416013819,521.865296834587,522.865058476124,523.864820117661,524.645973149496),
 .UNSPECIFIED.);
#354=B_SPLINE_CURVE_WITH_KNOTS('',3,(#38167,#38168,#38169,#38170,#38171,
#38172,#38173,#38174,#38175,#38176,#38177,#38178,#38179,#38180,#38181,#38182,
#38183,#38184,#38185,#38186,#38187,#38188,#38189,#38190,#38191),
 .UNSPECIFIED.,.F.,.F.,(4,3,3,3,3,3,3,3,4),(512.079602535136,512.92388749386,
513.923649135397,514.923410776934,515.92317241847,516.922934060007,517.422814880776,
517.922695701544,518.362787842315),.UNSPECIFIED.);
#355=B_SPLINE_CURVE_WITH_KNOTS('',3,(#38192,#38193,#38194,#38195,#38196,
#38197,#38198,#38199,#38200,#38201,#38202,#38203,#38204,#38205,#38206,#38207,
#38208,#38209,#38210,#38211,#38212,#38213,#38214,#38215,#38216),
 .UNSPECIFIED.,.F.,.F.,(4,3,3,3,3,3,3,3,4),(512.079602535137,512.867442060757,
513.867203702294,514.367084523062,514.86696534383,515.866726985367,516.866488626904,
517.866250268441,518.362787842316),.UNSPECIFIED.);
#356=B_SPLINE_CURVE_WITH_KNOTS('',3,(#38221,#38222,#38223,#38224,#38225,
#38226,#38227,#38228,#38229,#38230,#38231,#38232),.UNSPECIFIED.,.F.,.F.,
(4,1,1,1,1,1,1,1,1,4),(505.796417227956,505.925556003103,506.92531764464,
507.925079286177,508.924840927713,509.92460256925,510.424483390018,510.924364210787,
511.924125852324,512.079602535136),.UNSPECIFIED.);
#357=B_SPLINE_CURVE_WITH_KNOTS('',3,(#38233,#38234,#38235,#38236,#38237,
#38238,#38239,#38240,#38241,#38242,#38243,#38244,#38245,#38246,#38247,#38248,
#38249,#38250,#38251,#38252,#38253,#38254,#38255,#38256,#38257,#38258,#38259,
#38260),.UNSPECIFIED.,.F.,.F.,(4,3,3,3,3,3,3,3,3,4),(505.796417227957,505.86911057,
506.868872211537,507.368753032305,507.868633853074,508.86839549461,509.868157136147,
510.867918777684,511.86768041922,512.079602535137),.UNSPECIFIED.);
#358=B_SPLINE_CURVE_WITH_KNOTS('',3,(#38265,#38266,#38267,#38268,#38269,
#38270,#38271,#38272,#38273,#38274,#38275),.UNSPECIFIED.,.F.,.F.,(4,1,1,
1,1,1,1,1,4),(499.513231920777,499.926986153883,500.92674779542,501.926509436956,
502.926271078493,503.426151899261,503.92603272003,504.925794361566,505.796417227956),
 .UNSPECIFIED.);
#359=B_SPLINE_CURVE_WITH_KNOTS('',3,(#38276,#38277,#38278,#38279,#38280,
#38281,#38282,#38283,#38284,#38285,#38286),.UNSPECIFIED.,.F.,.F.,(4,1,1,
1,1,1,1,1,4),(499.513231920778,499.87054072078,500.370421541548,500.870302362316,
501.870064003853,502.86982564539,503.869587286927,504.869348928463,505.796417227957),
 .UNSPECIFIED.);
#360=B_SPLINE_CURVE_WITH_KNOTS('',3,(#38291,#38292,#38293,#38294,#38295,
#38296,#38297,#38298,#38299,#38300,#38301),.UNSPECIFIED.,.F.,.F.,(4,1,1,
1,1,1,1,1,4),(493.230046613597,493.928416304663,494.928177946199,495.927939587736,
496.427820408504,496.927701229273,497.92746287081,498.927224512346,499.513231920777),
 .UNSPECIFIED.);
#361=B_SPLINE_CURVE_WITH_KNOTS('',3,(#38302,#38303,#38304,#38305,#38306,
#38307,#38308,#38309,#38310,#38311,#38312),.UNSPECIFIED.,.F.,.F.,(4,1,1,
1,1,1,1,1,4),(493.230046613598,493.372090050791,493.871970871559,494.871732513096,
495.871494154633,496.87125579617,497.871017437706,498.870779079243,499.513231920778),
 .UNSPECIFIED.);
#362=B_SPLINE_CURVE_WITH_KNOTS('',3,(#38317,#38318,#38319,#38320,#38321,
#38322,#38323,#38324,#38325,#38326,#38327),.UNSPECIFIED.,.F.,.F.,(4,1,1,
1,1,1,1,1,4),(486.946861306418,487.929846455442,488.929608096979,489.429488917747,
489.929369738516,490.929131380052,491.928893021589,492.928654663126,493.230046613597),
 .UNSPECIFIED.);
#363=B_SPLINE_CURVE_WITH_KNOTS('',3,(#38328,#38329,#38330,#38331,#38332,
#38333,#38334,#38335,#38336,#38337),.UNSPECIFIED.,.F.,.F.,(4,1,1,1,1,1,
1,4),(486.946861306418,487.873401022339,488.873162663876,489.872924305412,
490.872685946949,491.872447588486,492.872209230023,493.230046613598),
 .UNSPECIFIED.);
#364=B_SPLINE_CURVE_WITH_KNOTS('',3,(#38342,#38343,#38344,#38345,#38346,
#38347,#38348,#38349,#38350,#38351,#38352,#38353),.UNSPECIFIED.,.F.,.F.,
(4,1,1,1,1,1,1,1,1,4),(480.663675999238,480.931514964685,481.931276606222,
482.43115742699,482.931038247759,483.930799889295,484.930561530832,485.930323172369,
486.930084813906,486.946861306418),.UNSPECIFIED.);
#365=B_SPLINE_CURVE_WITH_KNOTS('',3,(#38354,#38355,#38356,#38357,#38358,
#38359,#38360,#38361,#38362,#38363,#38364,#38365),.UNSPECIFIED.,.F.,.F.,
(4,1,1,1,1,1,1,1,1,4),(480.663675999239,480.875069531582,481.874831173119,
482.874592814655,483.874354456192,484.874116097729,485.873877739266,486.373758560034,
486.873639380802,486.946861306418),.UNSPECIFIED.);
#366=B_SPLINE_CURVE_WITH_KNOTS('',3,(#38370,#38371,#38372,#38373,#38374,
#38375,#38376,#38377,#38378,#38379,#38380),.UNSPECIFIED.,.F.,.F.,(4,1,1,
1,1,1,1,1,4),(474.380490692059,474.932945115465,475.432825936233,475.932706757002,
476.932468398538,477.932230040075,478.931991681612,479.931753323149,480.663675999238),
 .UNSPECIFIED.);
#367=B_SPLINE_CURVE_WITH_KNOTS('',3,(#38381,#38382,#38383,#38384,#38385,
#38386,#38387,#38388,#38389,#38390,#38391),.UNSPECIFIED.,.F.,.F.,(4,1,1,
1,1,1,1,1,4),(474.380490692059,474.876499682362,475.876261323898,476.876022965435,
477.875784606972,478.875546248509,479.375427069277,479.875307890045,480.663675999239),
 .UNSPECIFIED.);
#368=B_SPLINE_CURVE_WITH_KNOTS('',3,(#38396,#38397,#38398,#38399,#38400,
#38401,#38402,#38403,#38404,#38405,#38406),.UNSPECIFIED.,.F.,.F.,(4,1,1,
1,1,1,1,1,4),(468.097305384879,468.434494445476,468.934375266245,469.934136907781,
470.933898549318,471.933660190855,472.933421832392,473.933183473928,474.380490692059),
 .UNSPECIFIED.);
#369=B_SPLINE_CURVE_WITH_KNOTS('',3,(#38407,#38408,#38409,#38410,#38411,
#38412,#38413,#38414,#38415,#38416,#38417),.UNSPECIFIED.,.F.,.F.,(4,1,1,
1,1,1,1,1,4),(468.09730538488,468.877929833141,469.877691474678,470.877453116215,
471.877214757752,472.37709557852,472.876976399288,473.876738040825,474.380490692059),
 .UNSPECIFIED.);
#370=B_SPLINE_CURVE_WITH_KNOTS('',3,(#38422,#38423,#38424,#38425,#38426,
#38427,#38428,#38429,#38430,#38431,#38432),.UNSPECIFIED.,.F.,.F.,(4,1,1,
1,1,1,1,1,4),(461.814120077699,461.936043775488,462.935805417024,463.935567058561,
464.935328700098,465.935090341635,466.934851983171,467.934613624708,468.097305384879),
 .UNSPECIFIED.);
#371=B_SPLINE_CURVE_WITH_KNOTS('',3,(#38433,#38434,#38435,#38436,#38437,
#38438,#38439,#38440,#38441,#38442,#38443,#38444),.UNSPECIFIED.,.F.,.F.,
(4,1,1,1,1,1,1,1,1,4),(461.8141200777,461.879598342384,462.879359983921,
463.879121625458,464.878883266995,465.378764087763,465.878644908531,466.878406550068,
467.878168191605,468.09730538488),.UNSPECIFIED.);
#372=B_SPLINE_CURVE_WITH_KNOTS('',3,(#38449,#38450,#38451,#38452,#38453,
#38454,#38455,#38456,#38457,#38458,#38459),.UNSPECIFIED.,.F.,.F.,(4,1,1,
1,1,1,1,1,4),(455.53093477052,455.937473926267,456.937235567804,457.936997209341,
458.936758850878,459.936520492414,460.936282133951,461.436162954719,461.814120077699),
 .UNSPECIFIED.);
#373=B_SPLINE_CURVE_WITH_KNOTS('',3,(#38460,#38461,#38462,#38463,#38464,
#38465,#38466,#38467,#38468,#38469,#38470),.UNSPECIFIED.,.F.,.F.,(4,1,1,
1,1,1,1,1,4),(455.530934770521,455.881028493164,456.880790134701,457.880551776237,
458.380432597006,458.880313417774,459.880075059311,460.879836700848,461.8141200777),
 .UNSPECIFIED.);
#374=B_SPLINE_CURVE_WITH_KNOTS('',3,(#38475,#38476,#38477,#38478,#38479,
#38480,#38481,#38482,#38483,#38484,#38485),.UNSPECIFIED.,.F.,.F.,(4,1,1,
1,1,1,1,1,4),(449.24774946334,449.938904077047,450.938665718584,451.93842736012,
452.938189001657,453.937950643194,454.437831463962,454.937712284731,455.53093477052),
 .UNSPECIFIED.);
#375=B_SPLINE_CURVE_WITH_KNOTS('',3,(#38486,#38487,#38488,#38489,#38490,
#38491,#38492,#38493,#38494,#38495,#38496,#38497,#38498,#38499,#38500,#38501,
#38502,#38503,#38504,#38505,#38506,#38507),.UNSPECIFIED.,.F.,.F.,(4,3,3,
3,3,3,3,4),(449.247749463341,450.156226536958,451.064703610575,451.973180684192,
452.881657757809,453.790134831426,454.698611905043,455.530934770521),
 .UNSPECIFIED.);
#376=B_SPLINE_CURVE_WITH_KNOTS('',3,(#38512,#38513,#38514,#38515,#38516,
#38517,#38518,#38519,#38520,#38521,#38522,#38523,#38524,#38525,#38526,#38527,
#38528,#38529,#38530,#38531,#38532,#38533,#38534,#38535,#38536),
 .UNSPECIFIED.,.F.,.F.,(4,3,3,3,3,3,3,3,4),(442.964564156161,443.940334227827,
444.940095869364,445.9398575109,446.939619152437,447.439499973205,447.939380793974,
448.93914243551,449.24774946334),.UNSPECIFIED.);
#377=B_SPLINE_CURVE_WITH_KNOTS('',3,(#38537,#38538,#38539,#38540,#38541,
#38542,#38543,#38544,#38545,#38546,#38547),.UNSPECIFIED.,.F.,.F.,(4,1,1,
1,1,1,1,1,4),(442.964564156161,443.883888794723,444.383769615492,444.88365043626,
445.883412077797,446.883173719334,447.88293536087,448.882697002407,449.247749463341),
 .UNSPECIFIED.);
#378=B_SPLINE_CURVE_WITH_KNOTS('',3,(#38552,#38553,#38554,#38555,#38556,
#38557,#38558,#38559,#38560,#38561,#38562,#38563,#38564,#38565,#38566,#38567,
#38568,#38569,#38570,#38571,#38572,#38573,#38574,#38575,#38576,#38577,#38578,
#38579),.UNSPECIFIED.,.F.,.F.,(4,3,3,3,3,3,3,3,3,4),(436.681378848981,436.94200273707,
437.941764378607,438.941526020143,439.94128766168,440.441168482448,440.941049303217,
441.940810944753,442.94057258629,442.964564156161),.UNSPECIFIED.);
#379=B_SPLINE_CURVE_WITH_KNOTS('',3,(#38580,#38581,#38582,#38583,#38584,
#38585,#38586,#38587,#38588,#38589,#38590,#38591),.UNSPECIFIED.,.F.,.F.,
(4,1,1,1,1,1,1,1,1,4),(436.681378848982,436.885557303966,437.385438124735,
437.885318945503,438.88508058704,439.884842228577,440.884603870113,441.88436551165,
442.884127153187,442.964564156161),.UNSPECIFIED.);
#380=B_SPLINE_CURVE_WITH_KNOTS('',3,(#38596,#38597,#38598,#38599,#38600,
#38601,#38602,#38603,#38604,#38605,#38606),.UNSPECIFIED.,.F.,.F.,(4,1,1,
1,1,1,1,1,4),(430.398193541802,430.943432887849,431.943194529386,432.942956170923,
433.442836991691,433.94271781246,434.942479453996,435.942241095533,436.681378848981),
 .UNSPECIFIED.);
#381=B_SPLINE_CURVE_WITH_KNOTS('',3,(#38607,#38608,#38609,#38610,#38611,
#38612,#38613,#38614,#38615,#38616),.UNSPECIFIED.,.F.,.F.,(4,1,1,1,1,1,
1,4),(430.398193541802,430.886987454746,431.886749096283,432.88651073782,
433.886272379356,434.886034020893,435.88579566243,436.681378848982),
 .UNSPECIFIED.);
#382=B_SPLINE_CURVE_WITH_KNOTS('',3,(#38621,#38622,#38623,#38624,#38625,
#38626,#38627,#38628,#38629,#38630,#38631),.UNSPECIFIED.,.F.,.F.,(4,1,1,
1,1,1,1,1,4),(424.115008234622,424.944863038629,425.944624680166,426.444505500934,
426.944386321703,427.944147963239,428.943909604776,429.943671246313,430.398193541802),
 .UNSPECIFIED.);
#383=B_SPLINE_CURVE_WITH_KNOTS('',3,(#38632,#38633,#38634,#38635,#38636,
#38637,#38638,#38639,#38640,#38641,#38642),.UNSPECIFIED.,.F.,.F.,(4,1,1,
1,1,1,1,1,4),(424.115008234623,424.888417605526,425.888179247063,426.887940888599,
427.887702530136,428.887464171673,429.887225813209,430.387106633978,430.398193541802),
 .UNSPECIFIED.);
#384=B_SPLINE_CURVE_WITH_KNOTS('',3,(#38647,#38648,#38649,#38650,#38651,
#38652,#38653,#38654,#38655,#38656,#38657,#38658),.UNSPECIFIED.,.F.,.F.,
(4,1,1,1,1,1,1,1,1,4),(417.831822927443,417.946531547872,418.946293189409,
419.446174010177,419.946054830946,420.945816472482,421.945578114019,422.945339755556,
423.945101397092,424.115008234622),.UNSPECIFIED.);
#385=B_SPLINE_CURVE_WITH_KNOTS('',3,(#38659,#38660,#38661,#38662,#38663,
#38664,#38665,#38666,#38667,#38668,#38669,#38670),.UNSPECIFIED.,.F.,.F.,
(4,1,1,1,1,1,1,1,1,4),(417.831822927443,417.890086114769,418.889847756306,
419.889609397842,420.889371039379,421.889132680916,422.888894322452,423.388775143221,
423.888655963989,424.115008234623),.UNSPECIFIED.);
#386=B_SPLINE_CURVE_WITH_KNOTS('',3,(#38675,#38676,#38677,#38678,#38679,
#38680,#38681,#38682,#38683,#38684,#38685),.UNSPECIFIED.,.F.,.F.,(4,1,1,
1,1,1,1,1,4),(411.548637620263,411.947961698652,412.44784251942,412.947723340189,
413.947484981725,414.947246623262,415.947008264799,416.946769906335,417.831822927443),
 .UNSPECIFIED.);
#387=B_SPLINE_CURVE_WITH_KNOTS('',3,(#38686,#38687,#38688,#38689,#38690,
#38691,#38692,#38693,#38694,#38695,#38696),.UNSPECIFIED.,.F.,.F.,(4,1,1,
1,1,1,1,1,4),(411.548637620264,411.891516265548,412.891277907085,413.891039548622,
414.890801190159,415.890562831695,416.390443652464,416.890324473232,417.831822927443),
 .UNSPECIFIED.);
#388=B_SPLINE_CURVE_WITH_KNOTS('',3,(#38701,#38702,#38703,#38704,#38705,
#38706,#38707,#38708,#38709,#38710,#38711),.UNSPECIFIED.,.F.,.F.,(4,1,1,
1,1,1,1,1,4),(405.265452313083,405.449511028663,405.949391849432,406.949153490968,
407.948915132505,408.948676774042,409.948438415578,410.948200057115,411.548637620263),
 .UNSPECIFIED.);
#389=B_SPLINE_CURVE_WITH_KNOTS('',3,(#38712,#38713,#38714,#38715,#38716,
#38717,#38718,#38719,#38720,#38721,#38722,#38723,#38724,#38725,#38726,#38727,
#38728,#38729,#38730,#38731,#38732,#38733),.UNSPECIFIED.,.F.,.F.,(4,3,3,
3,3,3,3,4),(405.265452313084,406.173929386701,407.082406460318,407.990883533935,
408.899360607552,409.807837681169,410.716314754786,411.548637620264),
 .UNSPECIFIED.);
#390=B_SPLINE_CURVE_WITH_KNOTS('',3,(#38738,#38739,#38740,#38741,#38742,
#38743,#38744,#38745,#38746,#38747),.UNSPECIFIED.,.F.,.F.,(4,1,1,1,1,1,
1,4),(398.982267005904,399.950822000211,400.950583641748,401.950345283285,
402.950106924821,403.949868566358,404.949630207895,405.265452313083),
 .UNSPECIFIED.);
#391=B_SPLINE_CURVE_WITH_KNOTS('',3,(#38748,#38749,#38750,#38751,#38752,
#38753,#38754,#38755,#38756,#38757,#38758),.UNSPECIFIED.,.F.,.F.,(4,1,1,
1,1,1,1,1,4),(398.982267005905,399.894376567108,400.894138208645,401.893899850181,
402.39378067095,402.893661491718,403.893423133255,404.893184774791,405.265452313084),
 .UNSPECIFIED.);
#392=B_SPLINE_CURVE_WITH_KNOTS('',3,(#38763,#38764,#38765,#38766,#38767,
#38768,#38769,#38770,#38771,#38772,#38773,#38774),.UNSPECIFIED.,.F.,.F.,
(4,1,1,1,1,1,1,1,1,4),(392.699081698724,392.952490509454,393.952252150991,
394.952013792528,395.951775434064,396.951537075601,397.951298717138,398.451179537906,
398.951060358675,398.982267005904),.UNSPECIFIED.);
#393=B_SPLINE_CURVE_WITH_KNOTS('',3,(#38775,#38776,#38777,#38778,#38779,
#38780,#38781,#38782,#38783,#38784,#38785,#38786),.UNSPECIFIED.,.F.,.F.,
(4,1,1,1,1,1,1,1,1,4),(392.699081698725,392.896045076351,393.895806717888,
394.895568359424,395.395449180193,395.895330000961,396.895091642498,397.894853284034,
398.894614925571,398.982267005905),.UNSPECIFIED.);
#394=B_SPLINE_CURVE_WITH_KNOTS('',3,(#38791,#38792,#38793,#38794,#38795,
#38796,#38797,#38798,#38799,#38800,#38801),.UNSPECIFIED.,.F.,.F.,(4,1,1,
1,1,1,1,1,4),(386.415896391545,386.953920660234,387.953682301771,388.953443943307,
389.953205584844,390.952967226381,391.452848047149,391.952728867918,392.699081698724),
 .UNSPECIFIED.);
#395=B_SPLINE_CURVE_WITH_KNOTS('',3,(#38802,#38803,#38804,#38805,#38806,
#38807,#38808,#38809,#38810,#38811,#38812),.UNSPECIFIED.,.F.,.F.,(4,1,1,
1,1,1,1,1,4),(386.415896391545,386.897475227131,387.897236868667,388.397117689436,
388.896998510204,389.896760151741,390.896521793277,391.896283434814,392.699081698725),
 .UNSPECIFIED.);
#396=B_SPLINE_CURVE_WITH_KNOTS('',3,(#38817,#38818,#38819,#38820,#38821,
#38822,#38823,#38824,#38825,#38826,#38827),.UNSPECIFIED.,.F.,.F.,(4,1,1,
1,1,1,1,1,4),(380.132711084365,380.955350811014,381.95511245255,382.954874094087,
383.954635735624,384.454516556392,384.95439737716,385.954159018697,386.415896391545),
 .UNSPECIFIED.);
#397=B_SPLINE_CURVE_WITH_KNOTS('',3,(#38828,#38829,#38830,#38831,#38832,
#38833,#38834,#38835,#38836,#38837,#38838),.UNSPECIFIED.,.F.,.F.,(4,1,1,
1,1,1,1,1,4),(380.132711084366,380.89890537791,381.398786198679,381.898667019447,
382.898428660984,383.89819030252,384.897951944057,385.897713585594,386.415896391545),
 .UNSPECIFIED.);
#398=B_SPLINE_CURVE_WITH_KNOTS('',3,(#38843,#38844,#38845,#38846,#38847,
#38848,#38849,#38850,#38851,#38852,#38853,#38854),.UNSPECIFIED.,.F.,.F.,
(4,1,1,1,1,1,1,1,1,4),(373.849525777185,373.957019320257,374.956780961793,
375.95654260333,376.956304244867,377.456185065635,377.956065886403,378.95582752794,
379.955589169477,380.132711084365),.UNSPECIFIED.);
#399=B_SPLINE_CURVE_WITH_KNOTS('',3,(#38855,#38856,#38857,#38858,#38859,
#38860,#38861,#38862,#38863,#38864,#38865,#38866),.UNSPECIFIED.,.F.,.F.,
(4,1,1,1,1,1,1,1,1,4),(373.849525777186,373.900573887153,374.400454707922,
374.90033552869,375.900097170227,376.899858811763,377.8996204533,378.899382094837,
379.899143736374,380.132711084366),.UNSPECIFIED.);
#400=B_SPLINE_CURVE_WITH_KNOTS('',3,(#38871,#38872,#38873,#38874,#38875,
#38876,#38877,#38878,#38879,#38880,#38881),.UNSPECIFIED.,.F.,.F.,(4,1,1,
1,1,1,1,1,4),(367.566340470006,367.958449471036,368.958211112573,369.95797275411,
370.457853574878,370.957734395646,371.957496037183,372.95725767872,373.849525777185),
 .UNSPECIFIED.);
#401=B_SPLINE_CURVE_WITH_KNOTS('',3,(#38882,#38883,#38884,#38885,#38886,
#38887,#38888,#38889,#38890,#38891),.UNSPECIFIED.,.F.,.F.,(4,1,1,1,1,1,
1,4),(367.566340470007,367.902004037933,368.90176567947,369.901527321006,
370.901288962543,371.90105060408,372.900812245617,373.849525777186),
 .UNSPECIFIED.);
#402=B_SPLINE_CURVE_WITH_KNOTS('',3,(#38896,#38897,#38898,#38899,#38900,
#38901,#38902,#38903,#38904,#38905,#38906,#38907,#38908,#38909,#38910,#38911,
#38912,#38913,#38914,#38915,#38916,#38917),.UNSPECIFIED.,.F.,.F.,(4,3,3,
3,3,3,3,4),(361.283155162826,362.191632236443,363.10010931006,364.008586383677,
364.917063457294,365.825540530911,366.734017604529,367.566340470006),
 .UNSPECIFIED.);
#403=B_SPLINE_CURVE_WITH_KNOTS('',3,(#38918,#38919,#38920,#38921,#38922,
#38923,#38924,#38925,#38926,#38927,#38928),.UNSPECIFIED.,.F.,.F.,(4,1,1,
1,1,1,1,1,4),(361.283155162827,361.903434188713,362.903195830249,363.902957471786,
364.902719113323,365.902480754859,366.902242396396,367.402123217165,367.566340470007),
 .UNSPECIFIED.);
#404=B_SPLINE_CURVE_WITH_KNOTS('',3,(#38933,#38934,#38935,#38936,#38937,
#38938,#38939,#38940,#38941,#38942,#38943),.UNSPECIFIED.,.F.,.F.,(4,1,1,
1,1,1,1,1,4),(354.999969855647,355.961309772596,356.461190593364,356.961071414132,
357.960833055669,358.960594697206,359.960356338743,360.960117980279,361.283155162826),
 .UNSPECIFIED.);
#405=B_SPLINE_CURVE_WITH_KNOTS('',3,(#38944,#38945,#38946,#38947,#38948,
#38949,#38950,#38951,#38952,#38953,#38954),.UNSPECIFIED.,.F.,.F.,(4,1,1,
1,1,1,1,1,4),(354.999969855648,355.904864339492,356.904625981029,357.904387622566,
358.904149264102,359.903910905639,360.403791726408,360.903672547176,361.283155162827),
 .UNSPECIFIED.);
#406=B_SPLINE_CURVE_WITH_KNOTS('',3,(#38959,#38960,#38961,#38962,#38963,
#38964,#38965,#38966,#38967,#38968,#38969,#38970),.UNSPECIFIED.,.F.,.F.,
(4,1,1,1,1,1,1,1,1,4),(348.716784548467,348.962978281839,349.462859102607,
349.962739923375,350.962501564912,351.962263206449,352.962024847986,353.961786489522,
354.961548131059,354.999969855647),.UNSPECIFIED.);
#407=B_SPLINE_CURVE_WITH_KNOTS('',3,(#38971,#38972,#38973,#38974,#38975,
#38976,#38977,#38978,#38979,#38980,#38981,#38982),.UNSPECIFIED.,.F.,.F.,
(4,1,1,1,1,1,1,1,1,4),(348.716784548468,348.906532848735,349.906294490272,
350.906056131809,351.905817773345,352.905579414882,353.40546023565,353.905341056419,
354.905102697956,354.999969855648),.UNSPECIFIED.);
#408=B_SPLINE_CURVE_WITH_KNOTS('',3,(#38987,#38988,#38989,#38990,#38991,
#38992,#38993,#38994,#38995,#38996,#38997),.UNSPECIFIED.,.F.,.F.,(4,1,1,
1,1,1,1,1,4),(342.433599241288,342.46452761185,342.964408432618,343.964170074155,
344.963931715692,345.963693357229,346.963454998765,347.963216640302,348.716784548467),
 .UNSPECIFIED.);
#409=B_SPLINE_CURVE_WITH_KNOTS('',3,(#38998,#38999,#39000,#39001,#39002,
#39003,#39004,#39005,#39006,#39007,#39008),.UNSPECIFIED.,.F.,.F.,(4,1,1,
1,1,1,1,1,4),(342.433599241289,342.907962999515,343.907724641052,344.907486282588,
345.907247924125,346.407128744893,346.907009565662,347.906771207199,348.716784548468),
 .UNSPECIFIED.);
#410=B_SPLINE_CURVE_WITH_KNOTS('',3,(#39013,#39014,#39015,#39016,#39017,
#39018,#39019,#39020,#39021,#39022),.UNSPECIFIED.,.F.,.F.,(4,1,1,1,1,1,
1,4),(336.150413934108,336.965838583398,337.965600224935,338.965361866472,
339.965123508008,340.964885149545,341.964646791082,342.433599241288),
 .UNSPECIFIED.);
#411=B_SPLINE_CURVE_WITH_KNOTS('',3,(#39023,#39024,#39025,#39026,#39027,
#39028,#39029,#39030,#39031,#39032,#39033),.UNSPECIFIED.,.F.,.F.,(4,1,1,
1,1,1,1,1,4),(336.150413934109,336.909393150295,337.909154791831,338.908916433368,
339.408797254136,339.908678074905,340.908439716442,341.908201357978,342.433599241289),
 .UNSPECIFIED.);
#412=B_SPLINE_CURVE_WITH_KNOTS('',3,(#39038,#39039,#39040,#39041,#39042,
#39043,#39044,#39045,#39046,#39047,#39048,#39049),.UNSPECIFIED.,.F.,.F.,
(4,1,1,1,1,1,1,1,1,4),(329.867228626929,329.967507092641,330.967268734178,
331.967030375715,332.966792017251,333.966553658788,334.966315300325,335.466196121093,
335.966076941861,336.150413934108),.UNSPECIFIED.);
#413=B_SPLINE_CURVE_WITH_KNOTS('',3,(#39050,#39051,#39052,#39053,#39054,
#39055,#39056,#39057,#39058,#39059,#39060,#39061),.UNSPECIFIED.,.F.,.F.,
(4,1,1,1,1,1,1,1,1,4),(329.867228626929,329.911061659538,330.910823301074,
331.910584942611,332.410465763379,332.910346584148,333.910108225684,334.909869867221,
335.909631508758,336.150413934109),.UNSPECIFIED.);
#414=B_SPLINE_CURVE_WITH_KNOTS('',3,(#39066,#39067,#39068,#39069,#39070,
#39071,#39072,#39073,#39074,#39075,#39076),.UNSPECIFIED.,.F.,.F.,(4,1,1,
1,1,1,1,1,4),(323.584043319749,323.968937243421,324.968698884957,325.968460526494,
326.468341347263,326.968222168031,327.967983809568,328.967745451104,329.867228626929),
 .UNSPECIFIED.);
#415=B_SPLINE_CURVE_WITH_KNOTS('',3,(#39077,#39078,#39079,#39080,#39081,
#39082,#39083,#39084,#39085,#39086),.UNSPECIFIED.,.F.,.F.,(4,1,1,1,1,1,
1,4),(323.58404331975,323.912491810317,324.912253451854,325.912015093391,
326.911776734928,327.911538376464,328.911300018001,329.867228626929),
 .UNSPECIFIED.);
#416=B_SPLINE_CURVE_WITH_KNOTS('',3,(#39091,#39092,#39093,#39094,#39095,
#39096,#39097,#39098,#39099,#39100,#39101,#39102,#39103,#39104,#39105,#39106,
#39107,#39108,#39109,#39110,#39111,#39112),.UNSPECIFIED.,.F.,.F.,(4,3,3,
3,3,3,3,4),(317.300858012569,318.209335086186,319.117812159803,320.02628923342,
320.934766307037,321.843243380654,322.751720454271,323.584043319749),
 .UNSPECIFIED.);
#417=B_SPLINE_CURVE_WITH_KNOTS('',3,(#39113,#39114,#39115,#39116,#39117,
#39118,#39119,#39120,#39121,#39122,#39123),.UNSPECIFIED.,.F.,.F.,(4,1,1,
1,1,1,1,1,4),(317.30085801257,317.913921961097,318.913683602634,319.91344524417,
320.913206885707,321.912968527244,322.912730168781,323.412610989549,323.58404331975),
 .UNSPECIFIED.);
#418=B_SPLINE_CURVE_WITH_KNOTS('',3,(#39128,#39129,#39130,#39131,#39132,
#39133,#39134,#39135,#39136,#39137,#39138),.UNSPECIFIED.,.F.,.F.,(4,1,1,
1,1,1,1,1,4),(311.01767270539,311.97179754498,312.471678365749,312.971559186517,
313.971320828054,314.97108246959,315.970844111127,316.970605752664,317.300858012569),
 .UNSPECIFIED.);
#419=B_SPLINE_CURVE_WITH_KNOTS('',3,(#39139,#39140,#39141,#39142,#39143,
#39144,#39145,#39146,#39147,#39148,#39149),.UNSPECIFIED.,.F.,.F.,(4,1,1,
1,1,1,1,1,4),(311.017672705391,311.915352111877,312.915113753413,313.91487539495,
314.914637036487,315.914398678024,316.414279498792,316.91416031956,317.30085801257),
 .UNSPECIFIED.);
#420=B_SPLINE_CURVE_WITH_KNOTS('',3,(#39154,#39155,#39156,#39157,#39158,
#39159,#39160,#39161,#39162,#39163,#39164,#39165),.UNSPECIFIED.,.F.,.F.,
(4,1,1,1,1,1,1,1,1,4),(304.73448739821,304.973466054223,305.473346874992,
305.97322769576,306.972989337297,307.972750978833,308.97251262037,309.972274261907,
310.972035903443,311.01767270539),.UNSPECIFIED.);
#421=B_SPLINE_CURVE_WITH_KNOTS('',3,(#39166,#39167,#39168,#39169,#39170,
#39171,#39172,#39173,#39174,#39175,#39176,#39177),.UNSPECIFIED.,.F.,.F.,
(4,1,1,1,1,1,1,1,1,4),(304.734487398211,304.91702062112,305.916782262656,
306.916543904193,307.91630554573,308.916067187267,309.415948008035,309.915828828803,
310.91559047034,311.017672705391),.UNSPECIFIED.);
#422=B_SPLINE_CURVE_WITH_KNOTS('',3,(#39182,#39183,#39184,#39185,#39186,
#39187,#39188,#39189,#39190,#39191,#39192),.UNSPECIFIED.,.F.,.F.,(4,1,1,
1,1,1,1,1,4),(298.451302091031,298.475015384234,298.974896205003,299.97465784654,
300.974419488076,301.974181129613,302.97394277115,303.973704412686,304.73448739821),
 .UNSPECIFIED.);
#423=B_SPLINE_CURVE_WITH_KNOTS('',3,(#39193,#39194,#39195,#39196,#39197,
#39198,#39199,#39200,#39201,#39202,#39203),.UNSPECIFIED.,.F.,.F.,(4,1,1,
1,1,1,1,1,4),(298.451302091031,298.918450771899,299.918212413436,300.917974054973,
301.91773569651,302.417616517278,302.917497338046,303.917258979583,304.734487398211),
 .UNSPECIFIED.);
#424=B_SPLINE_CURVE_WITH_KNOTS('',3,(#39208,#39209,#39210,#39211,#39212,
#39213,#39214,#39215,#39216,#39217),.UNSPECIFIED.,.F.,.F.,(4,1,1,1,1,1,
1,4),(292.168116783851,292.976326355783,293.976087997319,294.975849638856,
295.975611280393,296.975372921929,297.975134563466,298.451302091031),
 .UNSPECIFIED.);
#425=B_SPLINE_CURVE_WITH_KNOTS('',3,(#39218,#39219,#39220,#39221,#39222,
#39223,#39224,#39225,#39226,#39227,#39228),.UNSPECIFIED.,.F.,.F.,(4,1,1,
1,1,1,1,1,4),(292.168116783852,292.919880922679,293.919642564216,294.919404205753,
295.419285026521,295.919165847289,296.918927488826,297.918689130363,298.451302091031),
 .UNSPECIFIED.);
#426=B_SPLINE_CURVE_WITH_KNOTS('',3,(#39233,#39234,#39235,#39236,#39237,
#39238,#39239,#39240,#39241,#39242,#39243,#39244),.UNSPECIFIED.,.F.,.F.,
(4,1,1,1,1,1,1,1,1,4),(285.884931476672,285.977994865025,286.977756506562,
287.977518148099,288.977279789636,289.977041431172,290.976803072709,291.476683893477,
291.976564714246,292.168116783851),.UNSPECIFIED.);
#427=B_SPLINE_CURVE_WITH_KNOTS('',3,(#39245,#39246,#39247,#39248,#39249,
#39250,#39251,#39252,#39253,#39254,#39255,#39256),.UNSPECIFIED.,.F.,.F.,
(4,1,1,1,1,1,1,1,1,4),(285.884931476672,285.921549431922,286.921311073459,
287.921072714995,288.420953535764,288.920834356532,289.920595998069,290.920357639606,
291.920119281142,292.168116783852),.UNSPECIFIED.);
#428=B_SPLINE_CURVE_WITH_KNOTS('',3,(#39261,#39262,#39263,#39264,#39265,
#39266,#39267,#39268,#39269,#39270,#39271),.UNSPECIFIED.,.F.,.F.,(4,1,1,
1,1,1,1,1,4),(279.601746169492,279.979425015805,280.979186657342,281.978948298879,
282.978709940415,283.978471581952,284.47835240272,284.978233223489,285.884931476672),
 .UNSPECIFIED.);
#429=B_SPLINE_CURVE_WITH_KNOTS('',3,(#39272,#39273,#39274,#39275,#39276,
#39277,#39278,#39279,#39280,#39281,#39282),.UNSPECIFIED.,.F.,.F.,(4,1,1,
1,1,1,1,1,4),(279.601746169493,279.922979582702,280.922741224238,281.422622045007,
281.922502865775,282.922264507312,283.922026148849,284.921787790385,285.884931476672),
 .UNSPECIFIED.);
#430=B_SPLINE_CURVE_WITH_KNOTS('',3,(#39287,#39288,#39289,#39290,#39291,
#39292,#39293,#39294,#39295,#39296,#39297,#39298,#39299,#39300,#39301,#39302,
#39303,#39304,#39305,#39306,#39307,#39308),.UNSPECIFIED.,.F.,.F.,(4,3,3,
3,3,3,3,4),(273.318560862313,274.227037935929,275.135515009546,276.043992083163,
276.95246915678,277.860946230397,278.769423304014,279.601746169492),
 .UNSPECIFIED.);
#431=B_SPLINE_CURVE_WITH_KNOTS('',3,(#39309,#39310,#39311,#39312,#39313,
#39314,#39315,#39316,#39317,#39318,#39319),.UNSPECIFIED.,.F.,.F.,(4,1,1,
1,1,1,1,1,4),(273.318560862313,273.924409733481,274.42429055425,274.924171375018,
275.923933016555,276.923694658092,277.923456299628,278.923217941165,279.601746169493),
 .UNSPECIFIED.);
#432=B_SPLINE_CURVE_WITH_KNOTS('',3,(#39324,#39325,#39326,#39327,#39328,
#39329,#39330,#39331,#39332,#39333,#39334),.UNSPECIFIED.,.F.,.F.,(4,1,1,
1,1,1,1,1,4),(267.035375555133,267.982285317365,268.982046958901,269.981808600438,
270.481689421206,270.981570241975,271.981331883511,272.981093525048,273.318560862312),
 .UNSPECIFIED.);
#433=B_SPLINE_CURVE_WITH_KNOTS('',3,(#39335,#39336,#39337,#39338,#39339,
#39340,#39341,#39342,#39343,#39344,#39345),.UNSPECIFIED.,.F.,.F.,(4,1,1,
1,1,1,1,1,4),(267.035375555134,267.425959063493,267.925839884261,268.925601525798,
269.925363167335,270.925124808871,271.924886450408,272.924648091945,273.318560862313),
 .UNSPECIFIED.);
#434=B_SPLINE_CURVE_WITH_KNOTS('',3,(#39350,#39351,#39352,#39353,#39354,
#39355,#39356,#39357,#39358,#39359,#39360,#39361),.UNSPECIFIED.,.F.,.F.,
(4,1,1,1,1,1,1,1,1,4),(260.752190247953,260.983953826608,261.983715468144,
262.983477109681,263.483357930449,263.983238751218,264.983000392754,265.982762034291,
266.982523675828,267.035375555133),.UNSPECIFIED.);
#435=B_SPLINE_CURVE_WITH_KNOTS('',3,(#39362,#39363,#39364,#39365,#39366,
#39367,#39368,#39369,#39370,#39371,#39372),.UNSPECIFIED.,.F.,.F.,(4,1,1,
1,1,1,1,1,4),(260.752190247954,260.927508393504,261.927270035041,262.927031676578,
263.926793318114,264.926554959651,265.926316601188,266.926078242724,267.035375555134),
 .UNSPECIFIED.);
#436=B_SPLINE_CURVE_WITH_KNOTS('',3,(#39377,#39378,#39379,#39380,#39381,
#39382,#39383,#39384,#39385,#39386,#39387),.UNSPECIFIED.,.F.,.F.,(4,1,1,
1,1,1,1,1,4),(254.469004940774,254.985383977387,255.985145618924,256.485026439692,
256.984907260461,257.984668901997,258.984430543534,259.984192185071,260.752190247953),
 .UNSPECIFIED.);
#437=B_SPLINE_CURVE_WITH_KNOTS('',3,(#39388,#39389,#39390,#39391,#39392,
#39393,#39394,#39395,#39396,#39397,#39398),.UNSPECIFIED.,.F.,.F.,(4,1,1,
1,1,1,1,1,4),(254.469004940774,254.928938544284,255.928700185821,256.928461827357,
257.928223468894,258.927985110431,259.927746751967,260.427627572736,260.752190247954),
 .UNSPECIFIED.);
#438=B_SPLINE_CURVE_WITH_KNOTS('',3,(#39403,#39404,#39405,#39406,#39407,
#39408,#39409,#39410,#39411,#39412,#39413),.UNSPECIFIED.,.F.,.F.,(4,1,1,
1,1,1,1,1,4),(248.185819633594,248.986814128167,249.486694948935,249.986575769704,
250.98633741124,251.986099052777,252.985860694314,253.985622335851,254.469004940774),
 .UNSPECIFIED.);
#439=B_SPLINE_CURVE_WITH_KNOTS('',3,(#39414,#39415,#39416,#39417,#39418,
#39419,#39420,#39421,#39422,#39423,#39424),.UNSPECIFIED.,.F.,.F.,(4,1,1,
1,1,1,1,1,4),(248.185819633595,248.930368695063,249.9301303366,250.929891978137,
251.929653619674,252.92941526121,253.429296081979,253.929176902747,254.469004940774),
 .UNSPECIFIED.);
#440=B_SPLINE_CURVE_WITH_KNOTS('',3,(#39429,#39430,#39431,#39432,#39433,
#39434,#39435,#39436,#39437,#39438,#39439,#39440),.UNSPECIFIED.,.F.,.F.,
(4,1,1,1,1,1,1,1,1,4),(241.902634326415,241.98848263741,242.488363458178,
242.988244278947,243.988005920483,244.98776756202,245.987529203557,246.987290845094,
247.98705248663,248.185819633594),.UNSPECIFIED.);
#441=B_SPLINE_CURVE_WITH_KNOTS('',3,(#39441,#39442,#39443,#39444,#39445,
#39446,#39447,#39448,#39449,#39450,#39451,#39452),.UNSPECIFIED.,.F.,.F.,
(4,1,1,1,1,1,1,1,1,4),(241.902634326415,241.932037204306,242.931798845843,
243.93156048738,244.931322128917,245.931083770453,246.430964591222,246.93084541199,
247.930607053527,248.185819633595),.UNSPECIFIED.);
#442=B_SPLINE_CURVE_WITH_KNOTS('',3,(#39457,#39458,#39459,#39460,#39461,
#39462,#39463,#39464,#39465,#39466),.UNSPECIFIED.,.F.,.F.,(4,1,1,1,1,1,
1,4),(235.619449019235,235.98991278819,236.989674429726,237.989436071263,
238.9891977128,239.988959354337,240.988720995873,241.902634326415),
 .UNSPECIFIED.);
#443=B_SPLINE_CURVE_WITH_KNOTS('',3,(#39467,#39468,#39469,#39470,#39471,
#39472,#39473,#39474,#39475,#39476,#39477),.UNSPECIFIED.,.F.,.F.,(4,1,1,
1,1,1,1,1,4),(235.619449019236,235.933467355086,236.933228996623,237.93299063816,
238.932752279696,239.432633100465,239.932513921233,240.93227556277,241.902634326415),
 .UNSPECIFIED.);
#444=B_SPLINE_CURVE_WITH_KNOTS('',3,(#39482,#39483,#39484,#39485,#39486,
#39487,#39488,#39489,#39490,#39491,#39492),.UNSPECIFIED.,.F.,.F.,(4,1,1,
1,1,1,1,1,4),(229.336263712056,229.991342938969,230.991104580506,231.990866222043,
232.99062786358,233.990389505116,234.990151146653,235.490031967421,235.619449019235),
 .UNSPECIFIED.);
#445=B_SPLINE_CURVE_WITH_KNOTS('',3,(#39493,#39494,#39495,#39496,#39497,
#39498,#39499,#39500,#39501,#39502,#39503),.UNSPECIFIED.,.F.,.F.,(4,1,1,
1,1,1,1,1,4),(229.336263712056,229.934897505866,230.934659147403,231.934420788939,
232.434301609708,232.934182430476,233.933944072013,234.933705713549,235.619449019236),
 .UNSPECIFIED.);
#446=B_SPLINE_CURVE_WITH_KNOTS('',3,(#39508,#39509,#39510,#39511,#39512,
#39513,#39514,#39515,#39516,#39517,#39518),.UNSPECIFIED.,.F.,.F.,(4,1,1,
1,1,1,1,1,4),(223.053078404876,223.992773089749,224.992534731286,225.992296372822,
226.992058014359,227.991819655896,228.491700476664,228.991581297433,229.336263712056),
 .UNSPECIFIED.);
#447=B_SPLINE_CURVE_WITH_KNOTS('',3,(#39519,#39520,#39521,#39522,#39523,
#39524,#39525,#39526,#39527,#39528,#39529),.UNSPECIFIED.,.F.,.F.,(4,1,1,
1,1,1,1,1,4),(223.053078404877,223.936327656646,224.936089298182,225.435970118951,
225.935850939719,226.935612581256,227.935374222792,228.935135864329,229.336263712056),
 .UNSPECIFIED.);
#448=B_SPLINE_CURVE_WITH_KNOTS('',3,(#39534,#39535,#39536,#39537,#39538,
#39539,#39540,#39541,#39542,#39543,#39544,#39545),.UNSPECIFIED.,.F.,.F.,
(4,1,1,1,1,1,1,1,1,4),(216.769893097696,216.994441598992,217.994203240529,
218.993964882065,219.993726523602,220.993488165139,221.493368985907,221.993249806676,
222.993011448212,223.053078404876),.UNSPECIFIED.);
#449=B_SPLINE_CURVE_WITH_KNOTS('',3,(#39546,#39547,#39548,#39549,#39550,
#39551,#39552,#39553,#39554,#39555,#39556,#39557),.UNSPECIFIED.,.F.,.F.,
(4,1,1,1,1,1,1,1,1,4),(216.769893097697,216.937996165889,217.937757807425,
218.437638628194,218.937519448962,219.937281090499,220.937042732035,221.936804373572,
222.936566015109,223.053078404877),.UNSPECIFIED.);
#450=B_SPLINE_CURVE_WITH_KNOTS('',3,(#39562,#39563,#39564,#39565,#39566,
#39567,#39568,#39569,#39570,#39571,#39572),.UNSPECIFIED.,.F.,.F.,(4,1,1,
1,1,1,1,1,4),(210.486707790517,210.995871749772,211.995633391308,212.995395032845,
213.995156674382,214.49503749515,214.994918315919,215.994679957455,216.769893097696),
 .UNSPECIFIED.);
#451=B_SPLINE_CURVE_WITH_KNOTS('',3,(#39573,#39574,#39575,#39576,#39577,
#39578,#39579,#39580,#39581,#39582,#39583),.UNSPECIFIED.,.F.,.F.,(4,1,1,
1,1,1,1,1,4),(210.486707790518,210.939426316668,211.439307137437,211.939187958205,
212.938949599742,213.938711241278,214.938472882815,215.938234524352,216.769893097697),
 .UNSPECIFIED.);
#452=B_SPLINE_CURVE_WITH_KNOTS('',3,(#39588,#39589,#39590,#39591,#39592,
#39593,#39594,#39595,#39596,#39597,#39598),.UNSPECIFIED.,.F.,.F.,(4,1,1,
1,1,1,1,1,4),(204.203522483337,204.997301900551,205.997063542088,206.996825183625,
207.496706004393,207.996586825162,208.996348466698,209.996110108235,210.486707790517),
 .UNSPECIFIED.);
#453=B_SPLINE_CURVE_WITH_KNOTS('',3,(#39599,#39600,#39601,#39602,#39603,
#39604,#39605,#39606,#39607,#39608,#39609),.UNSPECIFIED.,.F.,.F.,(4,1,1,
1,1,1,1,1,4),(204.203522483338,204.44097564668,204.940856467448,205.940618108985,
206.940379750521,207.940141392058,208.939903033595,209.939664675131,210.486707790518),
 .UNSPECIFIED.);
#454=B_SPLINE_CURVE_WITH_KNOTS('',3,(#39614,#39615,#39616,#39617,#39618,
#39619,#39620,#39621,#39622,#39623,#39624,#39625),.UNSPECIFIED.,.F.,.F.,
(4,1,1,1,1,1,1,1,1,4),(197.920337176158,197.998970409794,198.998732051331,
199.998493692868,200.498374513636,200.998255334405,201.998016975941,202.997778617478,
203.997540259015,204.203522483337),.UNSPECIFIED.);
#455=B_SPLINE_CURVE_WITH_KNOTS('',3,(#39626,#39627,#39628,#39629,#39630,
#39631,#39632,#39633,#39634,#39635,#39636),.UNSPECIFIED.,.F.,.F.,(4,1,1,
1,1,1,1,1,4),(197.920337176158,197.942524976691,198.942286618228,199.942048259764,
200.941809901301,201.941571542838,202.941333184374,203.941094825911,204.203522483338),
 .UNSPECIFIED.);
#456=B_SPLINE_CURVE_WITH_KNOTS('',3,(#39641,#39642,#39643,#39644,#39645,
#39646,#39647,#39648,#39649,#39650,#39651),.UNSPECIFIED.,.F.,.F.,(4,1,1,
1,1,1,1,1,4),(191.637151868978,192.000400560574,193.000162202111,193.500043022879,
193.999923843648,194.999685485184,195.999447126721,196.999208768258,197.920337176158),
 .UNSPECIFIED.);
#457=B_SPLINE_CURVE_WITH_KNOTS('',3,(#39652,#39653,#39654,#39655,#39656,
#39657,#39658,#39659,#39660,#39661,#39662),.UNSPECIFIED.,.F.,.F.,(4,1,1,
1,1,1,1,1,4),(191.637151868979,191.943955127471,192.943716769007,193.943478410544,
194.943240052081,195.943001693617,196.942763335154,197.442644155923,197.920337176158),
 .UNSPECIFIED.);
#458=B_SPLINE_CURVE_WITH_KNOTS('',3,(#39667,#39668,#39669,#39670,#39671,
#39672,#39673,#39674,#39675,#39676,#39677),.UNSPECIFIED.,.F.,.F.,(4,1,1,
1,1,1,1,1,4),(185.353966561799,186.001830711354,186.501711532122,187.001592352891,
188.001353994427,189.001115635964,190.000877277501,191.000638919037,191.637151868978),
 .UNSPECIFIED.);
#459=B_SPLINE_CURVE_WITH_KNOTS('',3,(#39678,#39679,#39680,#39681,#39682,
#39683,#39684,#39685,#39686,#39687,#39688),.UNSPECIFIED.,.F.,.F.,(4,1,1,
1,1,1,1,1,4),(185.353966561799,185.94538527825,186.945146919787,187.944908561324,
188.94467020286,189.944431844397,190.444312665166,190.944193485934,191.637151868979),
 .UNSPECIFIED.);
#460=B_SPLINE_CURVE_WITH_KNOTS('',3,(#39693,#39694,#39695,#39696,#39697,
#39698,#39699,#39700,#39701,#39702,#39703),.UNSPECIFIED.,.F.,.F.,(4,1,1,
1,1,1,1,1,4),(179.070781254619,179.503380041365,180.003260862133,181.00302250367,
182.002784145207,183.002545786744,184.00230742828,185.002069069817,185.353966561799),
 .UNSPECIFIED.);
#461=B_SPLINE_CURVE_WITH_KNOTS('',3,(#39704,#39705,#39706,#39707,#39708,
#39709,#39710,#39711,#39712,#39713,#39714),.UNSPECIFIED.,.F.,.F.,(4,1,1,
1,1,1,1,1,4),(179.07078125462,179.94681542903,180.946577070567,181.946338712103,
182.94610035364,183.445981174408,183.945861995177,184.945623636714,185.353966561799),
 .UNSPECIFIED.);
#462=B_SPLINE_CURVE_WITH_KNOTS('',3,(#39719,#39720,#39721,#39722,#39723,
#39724,#39725,#39726,#39727,#39728,#39729),.UNSPECIFIED.,.F.,.F.,(4,1,1,
1,1,1,1,1,4),(172.78759594744,173.004929371376,174.004691012913,175.00445265445,
176.004214295987,177.003975937523,178.00373757906,179.003499220597,179.070781254619),
 .UNSPECIFIED.);
#463=B_SPLINE_CURVE_WITH_KNOTS('',3,(#39730,#39731,#39732,#39733,#39734,
#39735,#39736,#39737,#39738,#39739,#39740,#39741),.UNSPECIFIED.,.F.,.F.,
(4,1,1,1,1,1,1,1,1,4),(172.78759594744,172.948483938273,173.94824557981,
174.948007221346,175.947768862883,176.447649683651,176.94753050442,177.947292145957,
178.947053787493,179.07078125462),.UNSPECIFIED.);
#464=B_SPLINE_CURVE_WITH_KNOTS('',3,(#39746,#39747,#39748,#39749,#39750,
#39751,#39752,#39753,#39754,#39755,#39756),.UNSPECIFIED.,.F.,.F.,(4,1,1,
1,1,1,1,1,4),(166.50441064026,167.006359522156,168.006121163693,169.00588280523,
170.005644446766,171.005406088303,172.00516772984,172.505048550608,172.78759594744),
 .UNSPECIFIED.);
#465=B_SPLINE_CURVE_WITH_KNOTS('',3,(#39757,#39758,#39759,#39760,#39761,
#39762,#39763,#39764,#39765,#39766,#39767),.UNSPECIFIED.,.F.,.F.,(4,1,1,
1,1,1,1,1,4),(166.504410640261,166.949914089053,167.949675730589,168.949437372126,
169.449318192894,169.949199013663,170.9489606552,171.948722296736,172.78759594744),
 .UNSPECIFIED.);
#466=B_SPLINE_CURVE_WITH_KNOTS('',3,(#39772,#39773,#39774,#39775,#39776,
#39777,#39778,#39779,#39780,#39781,#39782),.UNSPECIFIED.,.F.,.F.,(4,1,1,
1,1,1,1,1,4),(160.22122533308,161.007789672936,162.007551314473,163.007312956009,
164.007074597546,165.006836239083,165.506717059851,166.006597880619,166.50441064026),
 .UNSPECIFIED.);
#467=B_SPLINE_CURVE_WITH_KNOTS('',3,(#39783,#39784,#39785,#39786,#39787,
#39788,#39789,#39790,#39791,#39792,#39793,#39794,#39795,#39796,#39797,#39798,
#39799,#39800,#39801,#39802,#39803,#39804),.UNSPECIFIED.,.F.,.F.,(4,3,3,
3,3,3,3,4),(160.221225333081,161.129702406698,162.038179480315,162.946656553932,
163.855133627549,164.763610701166,165.672087774783,166.504410640261),
 .UNSPECIFIED.);
#468=B_SPLINE_CURVE_WITH_KNOTS('',3,(#39809,#39810,#39811,#39812,#39813,
#39814,#39815,#39816,#39817,#39818,#39819,#39820),.UNSPECIFIED.,.F.,.F.,
(4,1,1,1,1,1,1,1,1,4),(153.938040025901,154.009458182179,155.009219823716,
156.008981465252,157.008743106789,158.008504748326,158.508385569094,159.008266389862,
160.008028031399,160.22122533308),.UNSPECIFIED.);
#469=B_SPLINE_CURVE_WITH_KNOTS('',3,(#39821,#39822,#39823,#39824,#39825,
#39826,#39827,#39828,#39829,#39830,#39831,#39832),.UNSPECIFIED.,.F.,.F.,
(4,1,1,1,1,1,1,1,1,4),(153.938040025902,153.953012749075,154.952774390612,
155.45265521138,155.952536032149,156.952297673685,157.952059315222,158.951820956759,
159.951582598296,160.221225333081),.UNSPECIFIED.);
#470=B_SPLINE_CURVE_WITH_KNOTS('',3,(#39837,#39838,#39839,#39840,#39841,
#39842,#39843,#39844,#39845,#39846,#39847),.UNSPECIFIED.,.F.,.F.,(4,1,1,
1,1,1,1,1,4),(147.654854718721,148.010888332959,149.010649974495,150.010411616032,
151.010173257569,151.510054078337,152.009934899105,153.009696540642,153.938040025901),
 .UNSPECIFIED.);
#471=B_SPLINE_CURVE_WITH_KNOTS('',3,(#39848,#39849,#39850,#39851,#39852,
#39853,#39854,#39855,#39856,#39857,#39858),.UNSPECIFIED.,.F.,.F.,(4,1,1,
1,1,1,1,1,4),(147.654854718722,147.954442899855,148.454323720623,148.954204541392,
149.953966182928,150.953727824465,151.953489466002,152.953251107539,153.938040025902),
 .UNSPECIFIED.);
#472=B_SPLINE_CURVE_WITH_KNOTS('',3,(#39863,#39864,#39865,#39866,#39867,
#39868,#39869,#39870,#39871,#39872,#39873),.UNSPECIFIED.,.F.,.F.,(4,1,1,
1,1,1,1,1,4),(141.371669411542,142.012318483738,143.012080125275,144.011841766812,
144.51172258758,145.011603408348,146.011365049885,147.011126691422,147.654854718721),
 .UNSPECIFIED.);
#473=B_SPLINE_CURVE_WITH_KNOTS('',3,(#39874,#39875,#39876,#39877,#39878,
#39879,#39880,#39881,#39882,#39883,#39884),.UNSPECIFIED.,.F.,.F.,(4,1,1,
1,1,1,1,1,4),(141.371669411542,141.455992229866,141.955873050635,142.955634692171,
143.955396333708,144.955157975245,145.954919616782,146.954681258318,147.654854718722),
 .UNSPECIFIED.);
#474=B_SPLINE_CURVE_WITH_KNOTS('',3,(#39889,#39890,#39891,#39892,#39893,
#39894,#39895,#39896,#39897,#39898,#39899),.UNSPECIFIED.,.F.,.F.,(4,1,1,
1,1,1,1,1,4),(135.088484104362,136.013748634518,137.013510276055,137.513391096823,
138.013271917591,139.013033559128,140.012795200665,141.012556842202,141.371669411542),
 .UNSPECIFIED.);
#475=B_SPLINE_CURVE_WITH_KNOTS('',3,(#39900,#39901,#39902,#39903,#39904,
#39905,#39906,#39907,#39908,#39909),.UNSPECIFIED.,.F.,.F.,(4,1,1,1,1,1,
1,4),(135.088484104363,135.957303201414,136.957064842951,137.956826484488,
138.956588126025,139.956349767561,140.956111409098,141.371669411542),
 .UNSPECIFIED.);
#476=B_SPLINE_CURVE_WITH_KNOTS('',3,(#39914,#39915,#39916,#39917,#39918,
#39919,#39920,#39921,#39922,#39923,#39924,#39925),.UNSPECIFIED.,.F.,.F.,
(4,1,1,1,1,1,1,1,1,4),(128.805298797183,129.015417143761,130.015178785298,
130.515059606066,131.014940426834,132.014702068371,133.014463709908,134.014225351445,
135.013986992981,135.088484104362),.UNSPECIFIED.);
#477=B_SPLINE_CURVE_WITH_KNOTS('',3,(#39926,#39927,#39928,#39929,#39930,
#39931,#39932,#39933,#39934,#39935,#39936,#39937),.UNSPECIFIED.,.F.,.F.,
(4,1,1,1,1,1,1,1,1,4),(128.805298797183,128.958971710657,129.958733352194,
130.958494993731,131.958256635268,132.958018276804,133.957779918341,134.457660739109,
134.957541559878,135.088484104363),.UNSPECIFIED.);
#478=B_SPLINE_CURVE_WITH_KNOTS('',3,(#39942,#39943,#39944,#39945,#39946,
#39947,#39948,#39949,#39950,#39951,#39952),.UNSPECIFIED.,.F.,.F.,(4,1,1,
1,1,1,1,1,4),(122.522113490003,123.016847294541,123.516728115309,124.016608936077,
125.016370577614,126.016132219151,127.015893860688,128.015655502224,128.805298797183),
 .UNSPECIFIED.);
#479=B_SPLINE_CURVE_WITH_KNOTS('',3,(#39953,#39954,#39955,#39956,#39957,
#39958,#39959,#39960,#39961,#39962,#39963),.UNSPECIFIED.,.F.,.F.,(4,1,1,
1,1,1,1,1,4),(122.522113490004,122.960401861437,123.960163502974,124.95992514451,
125.959686786047,126.959448427584,127.459329248352,127.959210069121,128.805298797183),
 .UNSPECIFIED.);
#480=B_SPLINE_CURVE_WITH_KNOTS('',3,(#39968,#39969,#39970,#39971,#39972,
#39973,#39974,#39975,#39976,#39977,#39978),.UNSPECIFIED.,.F.,.F.,(4,1,1,
1,1,1,1,1,4),(116.238928182823,116.518396624552,117.01827744532,118.018039086857,
119.017800728394,120.01756236993,121.017324011467,122.017085653004,122.522113490003),
 .UNSPECIFIED.);
#481=B_SPLINE_CURVE_WITH_KNOTS('',3,(#39979,#39980,#39981,#39982,#39983,
#39984,#39985,#39986,#39987,#39988,#39989,#39990,#39991,#39992,#39993,#39994,
#39995,#39996,#39997,#39998,#39999,#40000),.UNSPECIFIED.,.F.,.F.,(4,3,3,
3,3,3,3,4),(116.238928182824,117.147405256441,118.055882330058,118.964359403675,
119.872836477292,120.781313550909,121.689790624526,122.522113490004),
 .UNSPECIFIED.);
#482=B_SPLINE_CURVE_WITH_KNOTS('',3,(#40005,#40006,#40007,#40008,#40009,
#40010,#40011,#40012,#40013,#40014,#40015),.UNSPECIFIED.,.F.,.F.,(4,1,1,
1,1,1,1,1,4),(109.955742875644,110.019945954563,111.0197075961,112.019469237637,
113.019230879173,114.01899252071,115.018754162247,116.018515803784,116.238928182823),
 .UNSPECIFIED.);
#483=B_SPLINE_CURVE_WITH_KNOTS('',3,(#40016,#40017,#40018,#40019,#40020,
#40021,#40022,#40023,#40024,#40025,#40026,#40027),.UNSPECIFIED.,.F.,.F.,
(4,1,1,1,1,1,1,1,1,4),(109.955742875644,109.96350052146,110.963262162996,
111.963023804533,112.96278544607,113.462666266838,113.962547087607,114.962308729143,
115.96207037068,116.238928182824),.UNSPECIFIED.);
#484=B_SPLINE_CURVE_WITH_KNOTS('',3,(#40032,#40033,#40034,#40035,#40036,
#40037,#40038,#40039,#40040,#40041,#40042),.UNSPECIFIED.,.F.,.F.,(4,1,1,
1,1,1,1,1,4),(103.672557568464,104.021376105343,105.02113774688,106.020899388416,
107.020661029953,108.02042267149,109.020184313027,109.520065133795,109.955742875644),
 .UNSPECIFIED.);
#485=B_SPLINE_CURVE_WITH_KNOTS('',3,(#40043,#40044,#40045,#40046,#40047,
#40048,#40049,#40050,#40051,#40052,#40053),.UNSPECIFIED.,.F.,.F.,(4,1,1,
1,1,1,1,1,4),(103.672557568465,103.964930672239,104.964692313776,105.964453955313,
106.464334776081,106.96421559685,107.963977238386,108.963738879923,109.955742875644),
 .UNSPECIFIED.);
#486=B_SPLINE_CURVE_WITH_KNOTS('',3,(#40058,#40059,#40060,#40061,#40062,
#40063,#40064,#40065,#40066,#40067,#40068),.UNSPECIFIED.,.F.,.F.,(4,1,1,
1,1,1,1,1,4),(97.3893722612846,98.0228062561227,99.0225678976594,100.022329539196,
101.022091180733,102.02185282227,102.521733643038,103.021614463806,103.672557568464),
 .UNSPECIFIED.);
#487=B_SPLINE_CURVE_WITH_KNOTS('',3,(#40069,#40070,#40071,#40072,#40073,
#40074,#40075,#40076,#40077,#40078,#40079,#40080,#40081,#40082,#40083,#40084,
#40085,#40086,#40087,#40088,#40089,#40090),.UNSPECIFIED.,.F.,.F.,(4,3,3,
3,3,3,3,4),(97.3893722612853,98.2978493349022,99.2063264085192,100.114803482136,
101.023280555753,101.93175762937,102.840234702987,103.672557568465),
 .UNSPECIFIED.);
#488=B_SPLINE_CURVE_WITH_KNOTS('',3,(#40095,#40096,#40097,#40098,#40099,
#40100,#40101,#40102,#40103,#40104,#40105),.UNSPECIFIED.,.F.,.F.,(4,1,1,
1,1,1,1,1,4),(91.1061869541049,92.0242364069024,93.0239980484391,94.0237596899758,
95.0235213315126,95.5234021522809,96.0232829730493,97.023044614586,97.3893722612846),
 .UNSPECIFIED.);
#489=B_SPLINE_CURVE_WITH_KNOTS('',3,(#40106,#40107,#40108,#40109,#40110,
#40111,#40112,#40113,#40114,#40115,#40116),.UNSPECIFIED.,.F.,.F.,(4,1,1,
1,1,1,1,1,4),(91.1061869541057,91.9677909737988,92.4676717945672,92.9675526153355,
93.9673142568722,94.967075898409,95.9668375399457,96.9665991814824,97.3893722612853),
 .UNSPECIFIED.);
#490=B_SPLINE_CURVE_WITH_KNOTS('',3,(#40121,#40122,#40123,#40124,#40125,
#40126,#40127,#40128,#40129,#40130,#40131,#40132),.UNSPECIFIED.,.F.,.F.,
(4,1,1,1,1,1,1,1,1,4),(84.8230016469254,85.0259049161454,86.0256665576821,
87.0254281992188,88.0251898407555,88.5250706615239,89.0249514822923,90.024713123829,
91.0244747653657,91.1061869541049),.UNSPECIFIED.);
#491=B_SPLINE_CURVE_WITH_KNOTS('',3,(#40133,#40134,#40135,#40136,#40137,
#40138,#40139,#40140,#40141,#40142,#40143,#40144),.UNSPECIFIED.,.F.,.F.,
(4,1,1,1,1,1,1,1,1,4),(84.8230016469261,84.9694594830418,85.4693403038102,
85.9692211245785,86.9689827661152,87.9687444076519,88.9685060491887,89.9682676907254,
90.9680293322621,91.1061869541057),.UNSPECIFIED.);
#492=B_SPLINE_CURVE_WITH_KNOTS('',3,(#40149,#40150,#40151,#40152,#40153,
#40154,#40155,#40156,#40157,#40158,#40159),.UNSPECIFIED.,.F.,.F.,(4,1,1,
1,1,1,1,1,4),(78.5398163397458,79.0273350669251,80.0270967084618,81.0268583499985,
81.5267391707669,82.0266199915352,83.026381633072,84.0261432746087,84.8230016469254),
 .UNSPECIFIED.);
#493=B_SPLINE_CURVE_WITH_KNOTS('',3,(#40160,#40161,#40162,#40163,#40164,
#40165,#40166,#40167,#40168,#40169),.UNSPECIFIED.,.F.,.F.,(4,1,1,1,1,1,
1,4),(78.5398163397465,78.9708896338215,79.9706512753582,80.9704129168949,
81.9701745584316,82.9699361999684,83.9696978415051,84.8230016469261),
 .UNSPECIFIED.);
#494=B_SPLINE_CURVE_WITH_KNOTS('',3,(#40174,#40175,#40176,#40177,#40178,
#40179,#40180,#40181,#40182,#40183,#40184),.UNSPECIFIED.,.F.,.F.,(4,1,1,
1,1,1,1,1,4),(72.2566310325663,73.0287652177048,74.0285268592415,74.5284076800099,
75.0282885007782,76.028050142315,77.0278117838517,78.0275734253884,78.5398163397458),
 .UNSPECIFIED.);
#495=B_SPLINE_CURVE_WITH_KNOTS('',3,(#40185,#40186,#40187,#40188,#40189,
#40190,#40191,#40192,#40193,#40194,#40195),.UNSPECIFIED.,.F.,.F.,(4,1,1,
1,1,1,1,1,4),(72.2566310325669,72.9723197846012,73.9720814261379,74.9718430676746,
75.9716047092113,76.971366350748,77.9711279922848,78.4710088130531,78.5398163397465),
 .UNSPECIFIED.);
#496=B_SPLINE_CURVE_WITH_KNOTS('',3,(#40200,#40201,#40202,#40203,#40204,
#40205,#40206,#40207,#40208,#40209,#40210,#40211),.UNSPECIFIED.,.F.,.F.,
(4,1,1,1,1,1,1,1,1,4),(65.9734457253866,66.0304337269478,67.0301953684845,
67.5300761892529,68.0299570100212,69.0297186515579,70.0294802930947,71.0292419346314,
72.0290035761681,72.2566310325663),.UNSPECIFIED.);
#497=B_SPLINE_CURVE_WITH_KNOTS('',3,(#40212,#40213,#40214,#40215,#40216,
#40217,#40218,#40219,#40220,#40221,#40222,#40223),.UNSPECIFIED.,.F.,.F.,
(4,1,1,1,1,1,1,1,1,4),(65.9734457253873,65.9739882938441,66.9737499353809,
67.9735115769176,68.9732732184543,69.973034859991,70.9727965015277,71.4726773222961,
71.9725581430645,72.2566310325669),.UNSPECIFIED.);
#498=B_SPLINE_CURVE_WITH_KNOTS('',3,(#40228,#40229,#40230,#40231,#40232,
#40233,#40234,#40235,#40236,#40237,#40238),.UNSPECIFIED.,.F.,.F.,(4,1,1,
1,1,1,1,1,4),(59.690260418207,60.0318638777275,60.5317446984958,61.0316255192642,
62.0313871608009,63.0311488023376,64.0309104438743,65.0306720854111,65.9734457253866),
 .UNSPECIFIED.);
#499=B_SPLINE_CURVE_WITH_KNOTS('',3,(#40239,#40240,#40241,#40242,#40243,
#40244,#40245,#40246,#40247,#40248,#40249),.UNSPECIFIED.,.F.,.F.,(4,1,1,
1,1,1,1,1,4),(59.6902604182077,59.9754184446238,60.9751800861606,61.9749417276973,
62.974703369234,63.9744650107707,64.4743458315391,64.9742266523074,65.9734457253873),
 .UNSPECIFIED.);
#500=B_SPLINE_CURVE_WITH_KNOTS('',3,(#40254,#40255,#40256,#40257,#40258,
#40259,#40260,#40261,#40262,#40263,#40264),.UNSPECIFIED.,.F.,.F.,(4,1,1,
1,1,1,1,1,4),(53.4070751110275,53.5334132077388,54.0332940285072,55.0330556700439,
56.0328173115806,57.0325789531173,58.0323405946541,59.0321022361908,59.690260418207),
 .UNSPECIFIED.);
#501=B_SPLINE_CURVE_WITH_KNOTS('',3,(#40265,#40266,#40267,#40268,#40269,
#40270,#40271,#40272,#40273,#40274,#40275,#40276,#40277,#40278,#40279,#40280,
#40281,#40282,#40283,#40284,#40285,#40286),.UNSPECIFIED.,.F.,.F.,(4,3,3,
3,3,3,3,4),(53.4070751110281,54.315552184645,55.224029258262,56.1325063318789,
57.0409834054958,57.9494604791127,58.8579375527296,59.6902604182077),
 .UNSPECIFIED.);
#502=B_SPLINE_CURVE_WITH_KNOTS('',3,(#40291,#40292,#40293,#40294,#40295,
#40296,#40297,#40298,#40299,#40300),.UNSPECIFIED.,.F.,.F.,(4,1,1,1,1,1,
1,4),(47.1238898038478,48.0347241792869,49.0344858208236,50.0342474623603,
51.034009103897,52.0337707454337,53.0335323869705,53.4070751110275),
 .UNSPECIFIED.);
#503=B_SPLINE_CURVE_WITH_KNOTS('',3,(#40301,#40302,#40303,#40304,#40305,
#40306,#40307,#40308,#40309,#40310,#40311),.UNSPECIFIED.,.F.,.F.,(4,1,1,
1,1,1,1,1,4),(47.1238898038486,47.9782787461832,48.9780403877199,49.9778020292567,
50.477682850025,50.9775636707934,51.9773253123301,52.9770869538668,53.4070751110281),
 .UNSPECIFIED.);
#504=B_SPLINE_CURVE_WITH_KNOTS('',3,(#40316,#40317,#40318,#40319,#40320,
#40321,#40322,#40323,#40324,#40325,#40326,#40327),.UNSPECIFIED.,.F.,.F.,
(4,1,1,1,1,1,1,1,1,4),(40.8407044966682,41.0363926885299,42.0361543300666,
43.0359159716033,44.03567761314,45.0354392546767,46.0352008962134,46.5350817169818,
47.0349625377502,47.1238898038478),.UNSPECIFIED.);
#505=B_SPLINE_CURVE_WITH_KNOTS('',3,(#40328,#40329,#40330,#40331,#40332,
#40333,#40334,#40335,#40336,#40337,#40338,#40339),.UNSPECIFIED.,.F.,.F.,
(4,1,1,1,1,1,1,1,1,4),(40.8407044966689,40.9799472554262,41.9797088969629,
42.9794705384996,43.479351359268,43.9792321800364,44.9789938215731,45.9787554631098,
46.9785171046465,47.1238898038486),.UNSPECIFIED.);
#506=B_SPLINE_CURVE_WITH_KNOTS('',3,(#40344,#40345,#40346,#40347,#40348,
#40349,#40350,#40351,#40352,#40353,#40354),.UNSPECIFIED.,.F.,.F.,(4,1,1,
1,1,1,1,1,4),(34.5575191894887,35.0378228393096,36.0375844808463,37.037346122383,
38.0371077639197,39.0368694054564,39.5367502262248,40.0366310469931,40.8407044966682),
 .UNSPECIFIED.);
#507=B_SPLINE_CURVE_WITH_KNOTS('',3,(#40355,#40356,#40357,#40358,#40359,
#40360,#40361,#40362,#40363,#40364,#40365),.UNSPECIFIED.,.F.,.F.,(4,1,1,
1,1,1,1,1,4),(34.5575191894893,34.9813774062059,35.9811390477426,36.481019868511,
36.9809006892793,37.980662330816,38.9804239723528,39.9801856138895,40.8407044966689),
 .UNSPECIFIED.);
#508=B_SPLINE_CURVE_WITH_KNOTS('',3,(#40370,#40371,#40372,#40373,#40374,
#40375,#40376,#40377,#40378,#40379,#40380),.UNSPECIFIED.,.F.,.F.,(4,1,1,
1,1,1,1,1,4),(28.2743338823091,29.0392529900893,30.039014631626,31.0387762731627,
32.0385379146994,32.5384187354678,33.0382995562361,34.0380611977728,34.5575191894887),
 .UNSPECIFIED.);
#509=B_SPLINE_CURVE_WITH_KNOTS('',3,(#40381,#40382,#40383,#40384,#40385,
#40386,#40387,#40388,#40389,#40390,#40391),.UNSPECIFIED.,.F.,.F.,(4,1,1,
1,1,1,1,1,4),(28.2743338823098,28.9828075569856,29.4826883777539,29.9825691985223,
30.982330840059,31.9820924815957,32.9818541231325,33.9816157646692,34.5575191894893),
 .UNSPECIFIED.);
#510=B_SPLINE_CURVE_WITH_KNOTS('',3,(#40396,#40397,#40398,#40399,#40400,
#40401,#40402,#40403,#40404,#40405,#40406,#40407),.UNSPECIFIED.,.F.,.F.,
(4,1,1,1,1,1,1,1,1,4),(21.9911485751295,22.0409214993322,23.040683140869,
24.0404447824057,25.0402064239424,25.5400872447107,26.0399680654791,27.0397297070158,
28.0394913485525,28.2743338823091),.UNSPECIFIED.);
#511=B_SPLINE_CURVE_WITH_KNOTS('',3,(#40408,#40409,#40410,#40411,#40412,
#40413,#40414,#40415,#40416,#40417,#40418),.UNSPECIFIED.,.F.,.F.,(4,1,1,
1,1,1,1,1,4),(21.9911485751302,22.4843568869969,22.9842377077653,23.983999349302,
24.9837609908387,25.9835226323754,26.9832842739122,27.9830459154489,28.2743338823098),
 .UNSPECIFIED.);
#512=B_SPLINE_CURVE_WITH_KNOTS('',3,(#40423,#40424,#40425,#40426,#40427,
#40428,#40429,#40430,#40431,#40432,#40433),.UNSPECIFIED.,.F.,.F.,(4,1,1,
1,1,1,1,1,4),(15.7079632679499,16.0423516501119,17.0421132916487,18.0418749331854,
18.5417557539537,19.0416365747221,20.0413982162588,21.0411598577955,21.9911485751295),
 .UNSPECIFIED.);
#513=B_SPLINE_CURVE_WITH_KNOTS('',3,(#40434,#40435,#40436,#40437,#40438,
#40439,#40440,#40441,#40442,#40443,#40444),.UNSPECIFIED.,.F.,.F.,(4,1,1,
1,1,1,1,1,4),(15.7079632679505,15.9859062170083,16.985667858545,17.9854295000817,
18.9851911416184,19.9849527831551,20.9847144246918,21.9844760662286,21.9911485751302),
 .UNSPECIFIED.);
#514=B_SPLINE_CURVE_WITH_KNOTS('',3,(#40469,#40470,#40471,#40472,#40473,
#40474,#40475,#40476,#40477,#40478,#40479,#40480,#40481,#40482,#40483,#40484,
#40485,#40486,#40487,#40488,#40489,#40490,#40491,#40492,#40493,#40494,#40495,
#40496,#40497,#40498,#40499,#40500,#40501,#40502,#40503,#40504,#40505,#40506,
#40507,#40508,#40509,#40510,#40511,#40512,#40513,#40514,#40515,#40516,#40517,
#40518,#40519,#40520,#40521,#40522,#40523,#40524,#40525,#40526),
 .UNSPECIFIED.,.F.,.F.,(4,3,3,3,3,3,3,3,3,3,3,3,3,3,3,3,3,3,3,4),(-0.694415684853046,
-0.651517903549149,-0.607914821239224,-0.56365275566676,-0.518801975968359,
-0.5037477542567,-0.493849355084242,-0.446277542502629,-0.397620428148984,
-0.35840958277914,-0.313608384931747,-0.294007860873513,-0.285041234230192,
-0.276619367837676,-0.224941839812129,-0.172301174308133,-0.118270567804678,
-0.0635860442762699,-0.00841504377438129,0.),.UNSPECIFIED.);
#515=B_SPLINE_CURVE_WITH_KNOTS('',3,(#40527,#40528,#40529,#40530,#40531,
#40532,#40533,#40534,#40535,#40536,#40537,#40538,#40539,#40540,#40541,#40542,
#40543,#40544,#40545,#40546,#40547,#40548,#40549,#40550,#40551,#40552,#40553,
#40554,#40555,#40556,#40557,#40558,#40559,#40560,#40561,#40562,#40563,#40564,
#40565,#40566,#40567,#40568,#40569,#40570,#40571,#40572,#40573,#40574,#40575,
#40576,#40577,#40578),.UNSPECIFIED.,.F.,.F.,(4,3,3,3,3,3,3,3,3,3,3,3,3,
3,3,3,3,4),(-0.689375724006324,-0.634260226335645,-0.579590449708639,-0.525633818728872,
-0.470565042052615,-0.44680280770273,-0.438973044842247,-0.388760986671672,
-0.339371186895675,-0.305358712023844,-0.25794484133391,-0.22489097506966,
-0.215263201343678,-0.170398777370464,-0.126568635661146,-0.0833490831487066,
-0.0410882702651496,0.),.UNSPECIFIED.);
#516=B_SPLINE_CURVE_WITH_KNOTS('',3,(#43481,#43482,#43483,#43484,#43485,
#43486,#43487,#43488),.UNSPECIFIED.,.F.,.F.,(4,1,1,1,1,4),(12.0433050839651,
12.5431859047334,13.0430667255018,14.0428283670385,15.0425900085752,15.7079632679499),
 .UNSPECIFIED.);
#517=B_SPLINE_CURVE_WITH_KNOTS('',3,(#43489,#43490,#43491,#43492,#43493,
#43494,#43495,#43496,#43497,#43498,#43499,#43500,#43501,#43502,#43503,#43504,
#43505,#43506,#43507,#43508,#43509,#43510,#43511,#43512,#43513,#43514,#43515,
#43516,#43517,#43518,#43519,#43520,#43521,#43522,#43523,#43524,#43525,#43526,
#43527,#43528,#43529,#43530,#43531,#43532,#43533,#43534,#43535,#43536,#43537,
#43538,#43539,#43540,#43541,#43542,#43543,#43544,#43545,#43546,#43547,#43548,
#43549),.UNSPECIFIED.,.F.,.F.,(4,3,3,3,3,3,3,3,3,3,3,3,3,3,3,3,3,3,3,3,
4),(0.,0.0551258591420952,0.109754210237386,0.163556354459871,0.21588036197585,
0.25151266717677,0.280554162019188,0.289557091917646,0.338951994283204,
0.35840958277953,0.407098532341802,0.454999930760489,0.484939548121938,
0.498910397309242,0.507155395896732,0.557573774787132,0.59180954850337,
0.613641770187594,0.63416209310979,0.680471724035206,0.694516869652084),
 .UNSPECIFIED.);
#518=B_SPLINE_CURVE_WITH_KNOTS('',3,(#43552,#43553,#43554,#43555,#43556,
#43557,#43558,#43559,#43560,#43561,#43562),.UNSPECIFIED.,.F.,.F.,(4,1,1,
1,1,1,1,1,4),(9.9478434911665,9.98733636778795,10.9870980093247,11.9868596508614,
12.9866212923981,13.9863829339348,14.9861445754715,15.4860253962399,15.7079632679505),
 .UNSPECIFIED.);
#519=B_SPLINE_CURVE_WITH_KNOTS('',3,(#43565,#43566,#43567,#43568,#43569,
#43570,#43571,#43572,#43573,#43574),.UNSPECIFIED.,.F.,.F.,(4,3,3,4),(-0.104077581167986,
-0.0617457737573955,-0.0189375188380278,-0.000362254369400641),
 .UNSPECIFIED.);
#520=B_SPLINE_CURVE_WITH_KNOTS('',3,(#43577,#43578,#43579,#43580,#43581,
#43582,#43583,#43584,#43585,#43586),.UNSPECIFIED.,.F.,.F.,(4,3,3,4),(1.13119827306084,
1.17364379143339,1.21521247145906,1.23499833094825),.UNSPECIFIED.);
#521=B_SPLINE_CURVE_WITH_KNOTS('',3,(#44096,#44097,#44098,#44099,#44100,
#44101,#44102),.UNSPECIFIED.,.F.,.F.,(4,1,1,1,4),(13.9661186601203,14.4600465471847,
14.9539744342492,15.4479023213137,15.707963267949),.UNSPECIFIED.);
#522=B_SPLINE_CURVE_WITH_KNOTS('',3,(#44103,#44104,#44105,#44106,#44107,
#44108,#44109,#44110,#44111,#44112,#44113,#44114,#44115,#44116,#44117,#44118,
#44119,#44120,#44121),.UNSPECIFIED.,.F.,.F.,(4,3,3,3,3,3,4),(-75.213176656116,
-74.7192487690515,-74.2253208819871,-73.7313929949226,-73.2374651078581,
-72.7435372207936,-72.2566310325651),.UNSPECIFIED.);
#523=B_SPLINE_CURVE_WITH_KNOTS('',3,(#44122,#44123,#44124,#44125,#44126,
#44127,#44128,#44129,#44130,#44131),.UNSPECIFIED.,.F.,.F.,(4,3,3,4),(-1.2345266614268,
-1.18927506134227,-1.14422754617811,-1.13094109509773),.UNSPECIFIED.);
#524=B_SPLINE_CURVE_WITH_KNOTS('',3,(#44134,#44135,#44136,#44137,#44138,
#44139,#44140,#44141,#44142,#44143),.UNSPECIFIED.,.F.,.F.,(4,3,3,4),(0.,
0.0450425198133127,0.0896231119338811,0.103234008807617),.UNSPECIFIED.);
#525=B_SPLINE_CURVE_WITH_KNOTS('',3,(#44146,#44147,#44148,#44149,#44150),
 .UNSPECIFIED.,.F.,.F.,(4,1,4),(15.2058131232128,15.4893404554446,15.707963267949),
 .UNSPECIFIED.);
#526=B_SPLINE_CURVE_WITH_KNOTS('',3,(#44661,#44662,#44663,#44664,#44665,
#44666,#44667,#44668,#44669,#44670,#44671,#44672,#44673,#44674,#44675,#44676,
#44677,#44678,#44679,#44680,#44681,#44682,#44683,#44684,#44685,#44686,#44687,
#44688,#44689,#44690,#44691,#44692,#44693,#44694,#44695,#44696,#44697,#44698,
#44699,#44700,#44701,#44702,#44703,#44704,#44705,#44706,#44707,#44708,#44709,
#44710,#44711,#44712,#44713,#44714,#44715,#44716,#44717,#44718),
 .UNSPECIFIED.,.F.,.F.,(4,3,3,3,3,3,3,3,3,3,3,3,3,3,3,3,3,3,3,4),(-0.000126486984424551,
0.0380591628916226,0.0717539043258247,0.087077502336768,0.108257623455665,
0.157532895597737,0.194489349704291,0.21378887858042,0.225593456009171,
0.272971435314458,0.305358712023953,0.354854209826148,0.404963477880151,
0.440515008646049,0.449592202308796,0.502330952057729,0.556359025569192,
0.610979682449441,0.666132005565916,0.689375724007338),.UNSPECIFIED.);
#527=B_SPLINE_CURVE_WITH_KNOTS('',3,(#47619,#47620,#47621,#47622,#47623,
#47624,#47625),.UNSPECIFIED.,.F.,.F.,(4,3,4),(628.755733952479,629.586155179399,
629.889327044754),.UNSPECIFIED.);
#592=CONICAL_SURFACE('',#21639,4.50000000000001,0.785398163397439);
#593=CONICAL_SURFACE('',#21645,4.5,0.785398163397447);
#617=SHAPE_REPRESENTATION_RELATIONSHIP('SRR','None',#48417,#628);
#628=ADVANCED_BREP_SHAPE_REPRESENTATION('',(#774),#48362);
#685=FACE_BOUND('',#3207,.T.);
#686=FACE_BOUND('',#3211,.T.);
#687=FACE_BOUND('',#3218,.T.);
#748=STYLED_ITEM('',(#48524),#774);
#774=MANIFOLD_SOLID_BREP('Screw',#20127);
#922=CYLINDRICAL_SURFACE('',#21411,7.925);
#923=CYLINDRICAL_SURFACE('',#21413,7.925);
#924=CYLINDRICAL_SURFACE('',#21414,7.925);
#925=CYLINDRICAL_SURFACE('',#21415,7.925);
#926=CYLINDRICAL_SURFACE('',#21416,7.925);
#927=CYLINDRICAL_SURFACE('',#21417,7.925);
#928=CYLINDRICAL_SURFACE('',#21418,7.925);
#929=CYLINDRICAL_SURFACE('',#21419,7.925);
#930=CYLINDRICAL_SURFACE('',#21420,7.925);
#931=CYLINDRICAL_SURFACE('',#21421,7.925);
#932=CYLINDRICAL_SURFACE('',#21422,7.925);
#933=CYLINDRICAL_SURFACE('',#21423,7.925);
#934=CYLINDRICAL_SURFACE('',#21424,7.925);
#935=CYLINDRICAL_SURFACE('',#21425,7.925);
#936=CYLINDRICAL_SURFACE('',#21426,7.925);
#937=CYLINDRICAL_SURFACE('',#21427,7.925);
#938=CYLINDRICAL_SURFACE('',#21428,7.925);
#939=CYLINDRICAL_SURFACE('',#21429,7.925);
#940=CYLINDRICAL_SURFACE('',#21430,7.925);
#941=CYLINDRICAL_SURFACE('',#21431,7.925);
#942=CYLINDRICAL_SURFACE('',#21432,7.925);
#943=CYLINDRICAL_SURFACE('',#21433,7.925);
#944=CYLINDRICAL_SURFACE('',#21434,7.925);
#945=CYLINDRICAL_SURFACE('',#21435,7.925);
#946=CYLINDRICAL_SURFACE('',#21436,7.925);
#947=CYLINDRICAL_SURFACE('',#21437,7.925);
#948=CYLINDRICAL_SURFACE('',#21438,7.925);
#949=CYLINDRICAL_SURFACE('',#21439,7.925);
#950=CYLINDRICAL_SURFACE('',#21440,7.925);
#951=CYLINDRICAL_SURFACE('',#21441,7.925);
#952=CYLINDRICAL_SURFACE('',#21442,7.925);
#953=CYLINDRICAL_SURFACE('',#21443,7.925);
#954=CYLINDRICAL_SURFACE('',#21444,7.925);
#955=CYLINDRICAL_SURFACE('',#21445,7.925);
#956=CYLINDRICAL_SURFACE('',#21446,7.925);
#957=CYLINDRICAL_SURFACE('',#21447,7.925);
#958=CYLINDRICAL_SURFACE('',#21448,7.925);
#959=CYLINDRICAL_SURFACE('',#21449,7.925);
#960=CYLINDRICAL_SURFACE('',#21450,7.925);
#961=CYLINDRICAL_SURFACE('',#21451,7.925);
#962=CYLINDRICAL_SURFACE('',#21452,7.925);
#963=CYLINDRICAL_SURFACE('',#21453,7.925);
#964=CYLINDRICAL_SURFACE('',#21454,7.925);
#965=CYLINDRICAL_SURFACE('',#21455,7.925);
#966=CYLINDRICAL_SURFACE('',#21456,7.925);
#967=CYLINDRICAL_SURFACE('',#21457,7.925);
#968=CYLINDRICAL_SURFACE('',#21458,7.925);
#969=CYLINDRICAL_SURFACE('',#21459,7.925);
#970=CYLINDRICAL_SURFACE('',#21460,7.925);
#971=CYLINDRICAL_SURFACE('',#21461,7.925);
#972=CYLINDRICAL_SURFACE('',#21462,7.925);
#973=CYLINDRICAL_SURFACE('',#21463,7.925);
#974=CYLINDRICAL_SURFACE('',#21464,7.925);
#975=CYLINDRICAL_SURFACE('',#21465,7.925);
#976=CYLINDRICAL_SURFACE('',#21466,7.925);
#977=CYLINDRICAL_SURFACE('',#21467,7.925);
#978=CYLINDRICAL_SURFACE('',#21468,7.925);
#979=CYLINDRICAL_SURFACE('',#21469,7.925);
#980=CYLINDRICAL_SURFACE('',#21470,7.925);
#981=CYLINDRICAL_SURFACE('',#21471,7.925);
#982=CYLINDRICAL_SURFACE('',#21472,7.925);
#983=CYLINDRICAL_SURFACE('',#21473,7.925);
#984=CYLINDRICAL_SURFACE('',#21474,7.925);
#985=CYLINDRICAL_SURFACE('',#21475,7.925);
#986=CYLINDRICAL_SURFACE('',#21476,7.925);
#987=CYLINDRICAL_SURFACE('',#21477,7.925);
#988=CYLINDRICAL_SURFACE('',#21478,7.925);
#989=CYLINDRICAL_SURFACE('',#21479,7.925);
#990=CYLINDRICAL_SURFACE('',#21480,7.925);
#991=CYLINDRICAL_SURFACE('',#21481,7.925);
#992=CYLINDRICAL_SURFACE('',#21482,7.925);
#993=CYLINDRICAL_SURFACE('',#21483,7.925);
#994=CYLINDRICAL_SURFACE('',#21484,7.925);
#995=CYLINDRICAL_SURFACE('',#21485,7.925);
#996=CYLINDRICAL_SURFACE('',#21486,7.925);
#997=CYLINDRICAL_SURFACE('',#21487,7.925);
#998=CYLINDRICAL_SURFACE('',#21488,7.925);
#999=CYLINDRICAL_SURFACE('',#21489,7.925);
#1000=CYLINDRICAL_SURFACE('',#21490,7.925);
#1001=CYLINDRICAL_SURFACE('',#21491,7.925);
#1002=CYLINDRICAL_SURFACE('',#21492,7.925);
#1003=CYLINDRICAL_SURFACE('',#21493,7.925);
#1004=CYLINDRICAL_SURFACE('',#21494,7.925);
#1005=CYLINDRICAL_SURFACE('',#21495,7.925);
#1006=CYLINDRICAL_SURFACE('',#21496,7.925);
#1007=CYLINDRICAL_SURFACE('',#21497,7.925);
#1008=CYLINDRICAL_SURFACE('',#21498,7.925);
#1009=CYLINDRICAL_SURFACE('',#21499,7.925);
#1010=CYLINDRICAL_SURFACE('',#21500,7.925);
#1011=CYLINDRICAL_SURFACE('',#21501,7.925);
#1012=CYLINDRICAL_SURFACE('',#21502,7.925);
#1013=CYLINDRICAL_SURFACE('',#21503,7.925);
#1014=CYLINDRICAL_SURFACE('',#21504,7.925);
#1015=CYLINDRICAL_SURFACE('',#21505,7.925);
#1016=CYLINDRICAL_SURFACE('',#21506,7.925);
#1017=CYLINDRICAL_SURFACE('',#21507,7.925);
#1018=CYLINDRICAL_SURFACE('',#21508,7.925);
#1019=CYLINDRICAL_SURFACE('',#21509,7.925);
#1020=CYLINDRICAL_SURFACE('',#21510,7.925);
#1021=CYLINDRICAL_SURFACE('',#21511,7.925);
#1022=CYLINDRICAL_SURFACE('',#21512,7.925);
#1023=CYLINDRICAL_SURFACE('',#21514,4.81675);
#1024=CYLINDRICAL_SURFACE('',#21517,4.81675);
#1025=CYLINDRICAL_SURFACE('',#21518,4.81675);
#1026=CYLINDRICAL_SURFACE('',#21519,4.81675);
#1027=CYLINDRICAL_SURFACE('',#21520,4.81675);
#1028=CYLINDRICAL_SURFACE('',#21521,4.81675);
#1029=CYLINDRICAL_SURFACE('',#21522,4.81675);
#1030=CYLINDRICAL_SURFACE('',#21523,4.81675);
#1031=CYLINDRICAL_SURFACE('',#21524,4.81675);
#1032=CYLINDRICAL_SURFACE('',#21525,4.81675);
#1033=CYLINDRICAL_SURFACE('',#21527,4.91825);
#1034=CYLINDRICAL_SURFACE('',#21529,4.91825);
#1035=CYLINDRICAL_SURFACE('',#21530,4.91825);
#1036=CYLINDRICAL_SURFACE('',#21531,4.91825);
#1037=CYLINDRICAL_SURFACE('',#21532,4.91825);
#1038=CYLINDRICAL_SURFACE('',#21533,4.91825);
#1039=CYLINDRICAL_SURFACE('',#21534,4.91825);
#1040=CYLINDRICAL_SURFACE('',#21535,4.91825);
#1041=CYLINDRICAL_SURFACE('',#21536,4.91825);
#1042=CYLINDRICAL_SURFACE('',#21537,4.91825);
#1043=CYLINDRICAL_SURFACE('',#21538,5.6435);
#1044=CYLINDRICAL_SURFACE('',#21540,5.6435);
#1045=CYLINDRICAL_SURFACE('',#21541,5.6435);
#1046=CYLINDRICAL_SURFACE('',#21542,5.6435);
#1047=CYLINDRICAL_SURFACE('',#21543,5.6435);
#1048=CYLINDRICAL_SURFACE('',#21544,5.6435);
#1049=CYLINDRICAL_SURFACE('',#21545,5.6435);
#1050=CYLINDRICAL_SURFACE('',#21546,5.6435);
#1051=CYLINDRICAL_SURFACE('',#21547,5.6435);
#1052=CYLINDRICAL_SURFACE('',#21548,5.6435);
#1053=CYLINDRICAL_SURFACE('',#21549,5.6435);
#1054=CYLINDRICAL_SURFACE('',#21550,5.6435);
#1055=CYLINDRICAL_SURFACE('',#21551,5.6435);
#1056=CYLINDRICAL_SURFACE('',#21552,5.6435);
#1057=CYLINDRICAL_SURFACE('',#21553,5.6435);
#1058=CYLINDRICAL_SURFACE('',#21554,5.6435);
#1059=CYLINDRICAL_SURFACE('',#21555,5.6435);
#1060=CYLINDRICAL_SURFACE('',#21556,5.6435);
#1061=CYLINDRICAL_SURFACE('',#21557,5.6435);
#1062=CYLINDRICAL_SURFACE('',#21558,5.6435);
#1063=CYLINDRICAL_SURFACE('',#21559,5.6435);
#1064=CYLINDRICAL_SURFACE('',#21560,5.6435);
#1065=CYLINDRICAL_SURFACE('',#21561,5.6435);
#1066=CYLINDRICAL_SURFACE('',#21562,5.6435);
#1067=CYLINDRICAL_SURFACE('',#21563,5.6435);
#1068=CYLINDRICAL_SURFACE('',#21564,5.6435);
#1069=CYLINDRICAL_SURFACE('',#21565,5.6435);
#1070=CYLINDRICAL_SURFACE('',#21566,5.6435);
#1071=CYLINDRICAL_SURFACE('',#21567,5.6435);
#1072=CYLINDRICAL_SURFACE('',#21568,5.6435);
#1073=CYLINDRICAL_SURFACE('',#21569,5.6435);
#1074=CYLINDRICAL_SURFACE('',#21570,5.6435);
#1075=CYLINDRICAL_SURFACE('',#21571,5.6435);
#1076=CYLINDRICAL_SURFACE('',#21572,5.6435);
#1077=CYLINDRICAL_SURFACE('',#21573,5.6435);
#1078=CYLINDRICAL_SURFACE('',#21574,5.6435);
#1079=CYLINDRICAL_SURFACE('',#21575,5.6435);
#1080=CYLINDRICAL_SURFACE('',#21576,5.6435);
#1081=CYLINDRICAL_SURFACE('',#21577,5.6435);
#1082=CYLINDRICAL_SURFACE('',#21578,5.6435);
#1083=CYLINDRICAL_SURFACE('',#21579,5.6435);
#1084=CYLINDRICAL_SURFACE('',#21580,5.6435);
#1085=CYLINDRICAL_SURFACE('',#21581,5.6435);
#1086=CYLINDRICAL_SURFACE('',#21582,5.6435);
#1087=CYLINDRICAL_SURFACE('',#21583,5.6435);
#1088=CYLINDRICAL_SURFACE('',#21584,5.6435);
#1089=CYLINDRICAL_SURFACE('',#21585,5.6435);
#1090=CYLINDRICAL_SURFACE('',#21586,5.6435);
#1091=CYLINDRICAL_SURFACE('',#21587,5.6435);
#1092=CYLINDRICAL_SURFACE('',#21588,5.6435);
#1093=CYLINDRICAL_SURFACE('',#21589,5.6435);
#1094=CYLINDRICAL_SURFACE('',#21590,5.6435);
#1095=CYLINDRICAL_SURFACE('',#21591,5.6435);
#1096=CYLINDRICAL_SURFACE('',#21592,5.6435);
#1097=CYLINDRICAL_SURFACE('',#21593,5.6435);
#1098=CYLINDRICAL_SURFACE('',#21594,5.6435);
#1099=CYLINDRICAL_SURFACE('',#21595,5.6435);
#1100=CYLINDRICAL_SURFACE('',#21596,5.6435);
#1101=CYLINDRICAL_SURFACE('',#21597,5.6435);
#1102=CYLINDRICAL_SURFACE('',#21598,5.6435);
#1103=CYLINDRICAL_SURFACE('',#21599,5.6435);
#1104=CYLINDRICAL_SURFACE('',#21600,5.6435);
#1105=CYLINDRICAL_SURFACE('',#21601,5.6435);
#1106=CYLINDRICAL_SURFACE('',#21602,5.6435);
#1107=CYLINDRICAL_SURFACE('',#21603,5.6435);
#1108=CYLINDRICAL_SURFACE('',#21604,5.6435);
#1109=CYLINDRICAL_SURFACE('',#21605,5.6435);
#1110=CYLINDRICAL_SURFACE('',#21606,5.6435);
#1111=CYLINDRICAL_SURFACE('',#21607,5.6435);
#1112=CYLINDRICAL_SURFACE('',#21608,5.6435);
#1113=CYLINDRICAL_SURFACE('',#21609,5.6435);
#1114=CYLINDRICAL_SURFACE('',#21610,5.6435);
#1115=CYLINDRICAL_SURFACE('',#21611,5.6435);
#1116=CYLINDRICAL_SURFACE('',#21612,5.6435);
#1117=CYLINDRICAL_SURFACE('',#21613,5.6435);
#1118=CYLINDRICAL_SURFACE('',#21614,5.6435);
#1119=CYLINDRICAL_SURFACE('',#21615,5.6435);
#1120=CYLINDRICAL_SURFACE('',#21616,5.6435);
#1121=CYLINDRICAL_SURFACE('',#21617,5.6435);
#1122=CYLINDRICAL_SURFACE('',#21618,5.6435);
#1123=CYLINDRICAL_SURFACE('',#21619,5.6435);
#1124=CYLINDRICAL_SURFACE('',#21620,5.6435);
#1125=CYLINDRICAL_SURFACE('',#21621,5.6435);
#1126=CYLINDRICAL_SURFACE('',#21622,5.6435);
#1127=CYLINDRICAL_SURFACE('',#21623,5.6435);
#1128=CYLINDRICAL_SURFACE('',#21624,5.6435);
#1129=CYLINDRICAL_SURFACE('',#21625,5.6435);
#1130=CYLINDRICAL_SURFACE('',#21626,5.6435);
#1131=CYLINDRICAL_SURFACE('',#21627,5.6435);
#1132=CYLINDRICAL_SURFACE('',#21628,5.6435);
#1133=CYLINDRICAL_SURFACE('',#21629,5.6435);
#1134=CYLINDRICAL_SURFACE('',#21630,5.6435);
#1135=CYLINDRICAL_SURFACE('',#21631,5.6435);
#1136=CYLINDRICAL_SURFACE('',#21632,5.6435);
#1137=CYLINDRICAL_SURFACE('',#21633,5.6435);
#1138=CYLINDRICAL_SURFACE('',#21634,5.6435);
#1139=CYLINDRICAL_SURFACE('',#21635,5.6435);
#1140=CYLINDRICAL_SURFACE('',#21636,5.6435);
#1141=CYLINDRICAL_SURFACE('',#21637,5.6435);
#1142=CYLINDRICAL_SURFACE('',#21638,5.6435);
#1143=CYLINDRICAL_SURFACE('',#21642,5.00000000000001);
#1144=CYLINDRICAL_SURFACE('',#21648,5.);
#1145=CYLINDRICAL_SURFACE('',#21653,5.6435);
#1146=CYLINDRICAL_SURFACE('',#21659,4.91825);
#1147=CYLINDRICAL_SURFACE('',#21660,4.81675);
#1148=CYLINDRICAL_SURFACE('',#21662,7.925);
#1885=FACE_OUTER_BOUND('',#2979,.T.);
#1886=FACE_OUTER_BOUND('',#2980,.T.);
#1887=FACE_OUTER_BOUND('',#2981,.T.);
#1888=FACE_OUTER_BOUND('',#2982,.T.);
#1889=FACE_OUTER_BOUND('',#2983,.T.);
#1890=FACE_OUTER_BOUND('',#2984,.T.);
#1891=FACE_OUTER_BOUND('',#2985,.T.);
#1892=FACE_OUTER_BOUND('',#2986,.T.);
#1893=FACE_OUTER_BOUND('',#2987,.T.);
#1894=FACE_OUTER_BOUND('',#2988,.T.);
#1895=FACE_OUTER_BOUND('',#2989,.T.);
#1896=FACE_OUTER_BOUND('',#2990,.T.);
#1897=FACE_OUTER_BOUND('',#2991,.T.);
#1898=FACE_OUTER_BOUND('',#2992,.T.);
#1899=FACE_OUTER_BOUND('',#2993,.T.);
#1900=FACE_OUTER_BOUND('',#2994,.T.);
#1901=FACE_OUTER_BOUND('',#2995,.T.);
#1902=FACE_OUTER_BOUND('',#2996,.T.);
#1903=FACE_OUTER_BOUND('',#2997,.T.);
#1904=FACE_OUTER_BOUND('',#2998,.T.);
#1905=FACE_OUTER_BOUND('',#2999,.T.);
#1906=FACE_OUTER_BOUND('',#3000,.T.);
#1907=FACE_OUTER_BOUND('',#3001,.T.);
#1908=FACE_OUTER_BOUND('',#3002,.T.);
#1909=FACE_OUTER_BOUND('',#3003,.T.);
#1910=FACE_OUTER_BOUND('',#3004,.T.);
#1911=FACE_OUTER_BOUND('',#3005,.T.);
#1912=FACE_OUTER_BOUND('',#3006,.T.);
#1913=FACE_OUTER_BOUND('',#3007,.T.);
#1914=FACE_OUTER_BOUND('',#3008,.T.);
#1915=FACE_OUTER_BOUND('',#3009,.T.);
#1916=FACE_OUTER_BOUND('',#3010,.T.);
#1917=FACE_OUTER_BOUND('',#3011,.T.);
#1918=FACE_OUTER_BOUND('',#3012,.T.);
#1919=FACE_OUTER_BOUND('',#3013,.T.);
#1920=FACE_OUTER_BOUND('',#3014,.T.);
#1921=FACE_OUTER_BOUND('',#3015,.T.);
#1922=FACE_OUTER_BOUND('',#3016,.T.);
#1923=FACE_OUTER_BOUND('',#3017,.T.);
#1924=FACE_OUTER_BOUND('',#3018,.T.);
#1925=FACE_OUTER_BOUND('',#3019,.T.);
#1926=FACE_OUTER_BOUND('',#3020,.T.);
#1927=FACE_OUTER_BOUND('',#3021,.T.);
#1928=FACE_OUTER_BOUND('',#3022,.T.);
#1929=FACE_OUTER_BOUND('',#3023,.T.);
#1930=FACE_OUTER_BOUND('',#3024,.T.);
#1931=FACE_OUTER_BOUND('',#3025,.T.);
#1932=FACE_OUTER_BOUND('',#3026,.T.);
#1933=FACE_OUTER_BOUND('',#3027,.T.);
#1934=FACE_OUTER_BOUND('',#3028,.T.);
#1935=FACE_OUTER_BOUND('',#3029,.T.);
#1936=FACE_OUTER_BOUND('',#3030,.T.);
#1937=FACE_OUTER_BOUND('',#3031,.T.);
#1938=FACE_OUTER_BOUND('',#3032,.T.);
#1939=FACE_OUTER_BOUND('',#3033,.T.);
#1940=FACE_OUTER_BOUND('',#3034,.T.);
#1941=FACE_OUTER_BOUND('',#3035,.T.);
#1942=FACE_OUTER_BOUND('',#3036,.T.);
#1943=FACE_OUTER_BOUND('',#3037,.T.);
#1944=FACE_OUTER_BOUND('',#3038,.T.);
#1945=FACE_OUTER_BOUND('',#3039,.T.);
#1946=FACE_OUTER_BOUND('',#3040,.T.);
#1947=FACE_OUTER_BOUND('',#3041,.T.);
#1948=FACE_OUTER_BOUND('',#3042,.T.);
#1949=FACE_OUTER_BOUND('',#3043,.T.);
#1950=FACE_OUTER_BOUND('',#3044,.T.);
#1951=FACE_OUTER_BOUND('',#3045,.T.);
#1952=FACE_OUTER_BOUND('',#3046,.T.);
#1953=FACE_OUTER_BOUND('',#3047,.T.);
#1954=FACE_OUTER_BOUND('',#3048,.T.);
#1955=FACE_OUTER_BOUND('',#3049,.T.);
#1956=FACE_OUTER_BOUND('',#3050,.T.);
#1957=FACE_OUTER_BOUND('',#3051,.T.);
#1958=FACE_OUTER_BOUND('',#3052,.T.);
#1959=FACE_OUTER_BOUND('',#3053,.T.);
#1960=FACE_OUTER_BOUND('',#3054,.T.);
#1961=FACE_OUTER_BOUND('',#3055,.T.);
#1962=FACE_OUTER_BOUND('',#3056,.T.);
#1963=FACE_OUTER_BOUND('',#3057,.T.);
#1964=FACE_OUTER_BOUND('',#3058,.T.);
#1965=FACE_OUTER_BOUND('',#3059,.T.);
#1966=FACE_OUTER_BOUND('',#3060,.T.);
#1967=FACE_OUTER_BOUND('',#3061,.T.);
#1968=FACE_OUTER_BOUND('',#3062,.T.);
#1969=FACE_OUTER_BOUND('',#3063,.T.);
#1970=FACE_OUTER_BOUND('',#3064,.T.);
#1971=FACE_OUTER_BOUND('',#3065,.T.);
#1972=FACE_OUTER_BOUND('',#3066,.T.);
#1973=FACE_OUTER_BOUND('',#3067,.T.);
#1974=FACE_OUTER_BOUND('',#3068,.T.);
#1975=FACE_OUTER_BOUND('',#3069,.T.);
#1976=FACE_OUTER_BOUND('',#3070,.T.);
#1977=FACE_OUTER_BOUND('',#3071,.T.);
#1978=FACE_OUTER_BOUND('',#3072,.T.);
#1979=FACE_OUTER_BOUND('',#3073,.T.);
#1980=FACE_OUTER_BOUND('',#3074,.T.);
#1981=FACE_OUTER_BOUND('',#3075,.T.);
#1982=FACE_OUTER_BOUND('',#3076,.T.);
#1983=FACE_OUTER_BOUND('',#3077,.T.);
#1984=FACE_OUTER_BOUND('',#3078,.T.);
#1985=FACE_OUTER_BOUND('',#3079,.T.);
#1986=FACE_OUTER_BOUND('',#3080,.T.);
#1987=FACE_OUTER_BOUND('',#3081,.T.);
#1988=FACE_OUTER_BOUND('',#3082,.T.);
#1989=FACE_OUTER_BOUND('',#3083,.T.);
#1990=FACE_OUTER_BOUND('',#3084,.T.);
#1991=FACE_OUTER_BOUND('',#3085,.T.);
#1992=FACE_OUTER_BOUND('',#3086,.T.);
#1993=FACE_OUTER_BOUND('',#3087,.T.);
#1994=FACE_OUTER_BOUND('',#3088,.T.);
#1995=FACE_OUTER_BOUND('',#3089,.T.);
#1996=FACE_OUTER_BOUND('',#3090,.T.);
#1997=FACE_OUTER_BOUND('',#3091,.T.);
#1998=FACE_OUTER_BOUND('',#3092,.T.);
#1999=FACE_OUTER_BOUND('',#3093,.T.);
#2000=FACE_OUTER_BOUND('',#3094,.T.);
#2001=FACE_OUTER_BOUND('',#3095,.T.);
#2002=FACE_OUTER_BOUND('',#3096,.T.);
#2003=FACE_OUTER_BOUND('',#3097,.T.);
#2004=FACE_OUTER_BOUND('',#3098,.T.);
#2005=FACE_OUTER_BOUND('',#3099,.T.);
#2006=FACE_OUTER_BOUND('',#3100,.T.);
#2007=FACE_OUTER_BOUND('',#3101,.T.);
#2008=FACE_OUTER_BOUND('',#3102,.T.);
#2009=FACE_OUTER_BOUND('',#3103,.T.);
#2010=FACE_OUTER_BOUND('',#3104,.T.);
#2011=FACE_OUTER_BOUND('',#3105,.T.);
#2012=FACE_OUTER_BOUND('',#3106,.T.);
#2013=FACE_OUTER_BOUND('',#3107,.T.);
#2014=FACE_OUTER_BOUND('',#3108,.T.);
#2015=FACE_OUTER_BOUND('',#3109,.T.);
#2016=FACE_OUTER_BOUND('',#3110,.T.);
#2017=FACE_OUTER_BOUND('',#3111,.T.);
#2018=FACE_OUTER_BOUND('',#3112,.T.);
#2019=FACE_OUTER_BOUND('',#3113,.T.);
#2020=FACE_OUTER_BOUND('',#3114,.T.);
#2021=FACE_OUTER_BOUND('',#3115,.T.);
#2022=FACE_OUTER_BOUND('',#3116,.T.);
#2023=FACE_OUTER_BOUND('',#3117,.T.);
#2024=FACE_OUTER_BOUND('',#3118,.T.);
#2025=FACE_OUTER_BOUND('',#3119,.T.);
#2026=FACE_OUTER_BOUND('',#3120,.T.);
#2027=FACE_OUTER_BOUND('',#3121,.T.);
#2028=FACE_OUTER_BOUND('',#3122,.T.);
#2029=FACE_OUTER_BOUND('',#3123,.T.);
#2030=FACE_OUTER_BOUND('',#3124,.T.);
#2031=FACE_OUTER_BOUND('',#3125,.T.);
#2032=FACE_OUTER_BOUND('',#3126,.T.);
#2033=FACE_OUTER_BOUND('',#3127,.T.);
#2034=FACE_OUTER_BOUND('',#3128,.T.);
#2035=FACE_OUTER_BOUND('',#3129,.T.);
#2036=FACE_OUTER_BOUND('',#3130,.T.);
#2037=FACE_OUTER_BOUND('',#3131,.T.);
#2038=FACE_OUTER_BOUND('',#3132,.T.);
#2039=FACE_OUTER_BOUND('',#3133,.T.);
#2040=FACE_OUTER_BOUND('',#3134,.T.);
#2041=FACE_OUTER_BOUND('',#3135,.T.);
#2042=FACE_OUTER_BOUND('',#3136,.T.);
#2043=FACE_OUTER_BOUND('',#3137,.T.);
#2044=FACE_OUTER_BOUND('',#3138,.T.);
#2045=FACE_OUTER_BOUND('',#3139,.T.);
#2046=FACE_OUTER_BOUND('',#3140,.T.);
#2047=FACE_OUTER_BOUND('',#3141,.T.);
#2048=FACE_OUTER_BOUND('',#3142,.T.);
#2049=FACE_OUTER_BOUND('',#3143,.T.);
#2050=FACE_OUTER_BOUND('',#3144,.T.);
#2051=FACE_OUTER_BOUND('',#3145,.T.);
#2052=FACE_OUTER_BOUND('',#3146,.T.);
#2053=FACE_OUTER_BOUND('',#3147,.T.);
#2054=FACE_OUTER_BOUND('',#3148,.T.);
#2055=FACE_OUTER_BOUND('',#3149,.T.);
#2056=FACE_OUTER_BOUND('',#3150,.T.);
#2057=FACE_OUTER_BOUND('',#3151,.T.);
#2058=FACE_OUTER_BOUND('',#3152,.T.);
#2059=FACE_OUTER_BOUND('',#3153,.T.);
#2060=FACE_OUTER_BOUND('',#3154,.T.);
#2061=FACE_OUTER_BOUND('',#3155,.T.);
#2062=FACE_OUTER_BOUND('',#3156,.T.);
#2063=FACE_OUTER_BOUND('',#3157,.T.);
#2064=FACE_OUTER_BOUND('',#3158,.T.);
#2065=FACE_OUTER_BOUND('',#3159,.T.);
#2066=FACE_OUTER_BOUND('',#3160,.T.);
#2067=FACE_OUTER_BOUND('',#3161,.T.);
#2068=FACE_OUTER_BOUND('',#3162,.T.);
#2069=FACE_OUTER_BOUND('',#3163,.T.);
#2070=FACE_OUTER_BOUND('',#3164,.T.);
#2071=FACE_OUTER_BOUND('',#3165,.T.);
#2072=FACE_OUTER_BOUND('',#3166,.T.);
#2073=FACE_OUTER_BOUND('',#3167,.T.);
#2074=FACE_OUTER_BOUND('',#3168,.T.);
#2075=FACE_OUTER_BOUND('',#3169,.T.);
#2076=FACE_OUTER_BOUND('',#3170,.T.);
#2077=FACE_OUTER_BOUND('',#3171,.T.);
#2078=FACE_OUTER_BOUND('',#3172,.T.);
#2079=FACE_OUTER_BOUND('',#3173,.T.);
#2080=FACE_OUTER_BOUND('',#3174,.T.);
#2081=FACE_OUTER_BOUND('',#3175,.T.);
#2082=FACE_OUTER_BOUND('',#3176,.T.);
#2083=FACE_OUTER_BOUND('',#3177,.T.);
#2084=FACE_OUTER_BOUND('',#3178,.T.);
#2085=FACE_OUTER_BOUND('',#3179,.T.);
#2086=FACE_OUTER_BOUND('',#3180,.T.);
#2087=FACE_OUTER_BOUND('',#3181,.T.);
#2088=FACE_OUTER_BOUND('',#3182,.T.);
#2089=FACE_OUTER_BOUND('',#3183,.T.);
#2090=FACE_OUTER_BOUND('',#3184,.T.);
#2091=FACE_OUTER_BOUND('',#3185,.T.);
#2092=FACE_OUTER_BOUND('',#3186,.T.);
#2093=FACE_OUTER_BOUND('',#3187,.T.);
#2094=FACE_OUTER_BOUND('',#3188,.T.);
#2095=FACE_OUTER_BOUND('',#3189,.T.);
#2096=FACE_OUTER_BOUND('',#3190,.T.);
#2097=FACE_OUTER_BOUND('',#3191,.T.);
#2098=FACE_OUTER_BOUND('',#3192,.T.);
#2099=FACE_OUTER_BOUND('',#3193,.T.);
#2100=FACE_OUTER_BOUND('',#3194,.T.);
#2101=FACE_OUTER_BOUND('',#3195,.T.);
#2102=FACE_OUTER_BOUND('',#3196,.T.);
#2103=FACE_OUTER_BOUND('',#3197,.T.);
#2104=FACE_OUTER_BOUND('',#3198,.T.);
#2105=FACE_OUTER_BOUND('',#3199,.T.);
#2106=FACE_OUTER_BOUND('',#3200,.T.);
#2107=FACE_OUTER_BOUND('',#3201,.T.);
#2108=FACE_OUTER_BOUND('',#3202,.T.);
#2109=FACE_OUTER_BOUND('',#3203,.T.);
#2110=FACE_OUTER_BOUND('',#3204,.T.);
#2111=FACE_OUTER_BOUND('',#3205,.T.);
#2112=FACE_OUTER_BOUND('',#3206,.T.);
#2113=FACE_OUTER_BOUND('',#3208,.T.);
#2114=FACE_OUTER_BOUND('',#3209,.T.);
#2115=FACE_OUTER_BOUND('',#3210,.T.);
#2116=FACE_OUTER_BOUND('',#3212,.T.);
#2117=FACE_OUTER_BOUND('',#3213,.T.);
#2118=FACE_OUTER_BOUND('',#3214,.T.);
#2119=FACE_OUTER_BOUND('',#3215,.T.);
#2120=FACE_OUTER_BOUND('',#3216,.T.);
#2121=FACE_OUTER_BOUND('',#3217,.T.);
#2122=FACE_OUTER_BOUND('',#3219,.T.);
#2123=FACE_OUTER_BOUND('',#3220,.T.);
#2979=EDGE_LOOP('',(#16451,#16452,#16453,#16454));
#2980=EDGE_LOOP('',(#16455,#16456,#16457,#16458));
#2981=EDGE_LOOP('',(#16459,#16460,#16461,#16462));
#2982=EDGE_LOOP('',(#16463,#16464,#16465,#16466));
#2983=EDGE_LOOP('',(#16467,#16468,#16469,#16470));
#2984=EDGE_LOOP('',(#16471,#16472,#16473,#16474));
#2985=EDGE_LOOP('',(#16475,#16476,#16477,#16478));
#2986=EDGE_LOOP('',(#16479,#16480,#16481,#16482));
#2987=EDGE_LOOP('',(#16483,#16484,#16485,#16486));
#2988=EDGE_LOOP('',(#16487,#16488,#16489,#16490));
#2989=EDGE_LOOP('',(#16491,#16492,#16493,#16494));
#2990=EDGE_LOOP('',(#16495,#16496,#16497,#16498));
#2991=EDGE_LOOP('',(#16499,#16500,#16501,#16502));
#2992=EDGE_LOOP('',(#16503,#16504,#16505,#16506));
#2993=EDGE_LOOP('',(#16507,#16508,#16509,#16510));
#2994=EDGE_LOOP('',(#16511,#16512,#16513,#16514));
#2995=EDGE_LOOP('',(#16515,#16516,#16517,#16518));
#2996=EDGE_LOOP('',(#16519,#16520,#16521,#16522));
#2997=EDGE_LOOP('',(#16523,#16524,#16525,#16526));
#2998=EDGE_LOOP('',(#16527,#16528,#16529,#16530));
#2999=EDGE_LOOP('',(#16531,#16532,#16533,#16534));
#3000=EDGE_LOOP('',(#16535,#16536,#16537,#16538));
#3001=EDGE_LOOP('',(#16539,#16540,#16541,#16542));
#3002=EDGE_LOOP('',(#16543,#16544,#16545,#16546));
#3003=EDGE_LOOP('',(#16547,#16548,#16549,#16550));
#3004=EDGE_LOOP('',(#16551,#16552,#16553,#16554));
#3005=EDGE_LOOP('',(#16555,#16556,#16557,#16558));
#3006=EDGE_LOOP('',(#16559,#16560,#16561,#16562));
#3007=EDGE_LOOP('',(#16563,#16564,#16565,#16566));
#3008=EDGE_LOOP('',(#16567,#16568,#16569,#16570));
#3009=EDGE_LOOP('',(#16571,#16572,#16573,#16574));
#3010=EDGE_LOOP('',(#16575,#16576,#16577,#16578));
#3011=EDGE_LOOP('',(#16579,#16580,#16581,#16582));
#3012=EDGE_LOOP('',(#16583,#16584,#16585,#16586));
#3013=EDGE_LOOP('',(#16587,#16588,#16589,#16590));
#3014=EDGE_LOOP('',(#16591,#16592,#16593,#16594));
#3015=EDGE_LOOP('',(#16595,#16596,#16597,#16598));
#3016=EDGE_LOOP('',(#16599,#16600,#16601,#16602));
#3017=EDGE_LOOP('',(#16603,#16604,#16605,#16606));
#3018=EDGE_LOOP('',(#16607,#16608,#16609,#16610));
#3019=EDGE_LOOP('',(#16611,#16612,#16613,#16614));
#3020=EDGE_LOOP('',(#16615,#16616,#16617,#16618));
#3021=EDGE_LOOP('',(#16619,#16620,#16621,#16622));
#3022=EDGE_LOOP('',(#16623,#16624,#16625,#16626));
#3023=EDGE_LOOP('',(#16627,#16628,#16629,#16630));
#3024=EDGE_LOOP('',(#16631,#16632,#16633,#16634));
#3025=EDGE_LOOP('',(#16635,#16636,#16637,#16638));
#3026=EDGE_LOOP('',(#16639,#16640,#16641,#16642));
#3027=EDGE_LOOP('',(#16643,#16644,#16645,#16646));
#3028=EDGE_LOOP('',(#16647,#16648,#16649,#16650));
#3029=EDGE_LOOP('',(#16651,#16652,#16653,#16654));
#3030=EDGE_LOOP('',(#16655,#16656,#16657,#16658));
#3031=EDGE_LOOP('',(#16659,#16660,#16661,#16662));
#3032=EDGE_LOOP('',(#16663,#16664,#16665,#16666));
#3033=EDGE_LOOP('',(#16667,#16668,#16669,#16670));
#3034=EDGE_LOOP('',(#16671,#16672,#16673,#16674));
#3035=EDGE_LOOP('',(#16675,#16676,#16677,#16678));
#3036=EDGE_LOOP('',(#16679,#16680,#16681,#16682));
#3037=EDGE_LOOP('',(#16683,#16684,#16685,#16686));
#3038=EDGE_LOOP('',(#16687,#16688,#16689,#16690));
#3039=EDGE_LOOP('',(#16691,#16692,#16693,#16694));
#3040=EDGE_LOOP('',(#16695,#16696,#16697,#16698));
#3041=EDGE_LOOP('',(#16699,#16700,#16701,#16702));
#3042=EDGE_LOOP('',(#16703,#16704,#16705,#16706));
#3043=EDGE_LOOP('',(#16707,#16708,#16709,#16710));
#3044=EDGE_LOOP('',(#16711,#16712,#16713,#16714));
#3045=EDGE_LOOP('',(#16715,#16716,#16717,#16718));
#3046=EDGE_LOOP('',(#16719,#16720,#16721,#16722));
#3047=EDGE_LOOP('',(#16723,#16724,#16725,#16726));
#3048=EDGE_LOOP('',(#16727,#16728,#16729,#16730));
#3049=EDGE_LOOP('',(#16731,#16732,#16733,#16734));
#3050=EDGE_LOOP('',(#16735,#16736,#16737,#16738));
#3051=EDGE_LOOP('',(#16739,#16740,#16741,#16742));
#3052=EDGE_LOOP('',(#16743,#16744,#16745,#16746));
#3053=EDGE_LOOP('',(#16747,#16748,#16749,#16750));
#3054=EDGE_LOOP('',(#16751,#16752,#16753,#16754));
#3055=EDGE_LOOP('',(#16755,#16756,#16757,#16758));
#3056=EDGE_LOOP('',(#16759,#16760,#16761,#16762));
#3057=EDGE_LOOP('',(#16763,#16764,#16765,#16766));
#3058=EDGE_LOOP('',(#16767,#16768,#16769,#16770));
#3059=EDGE_LOOP('',(#16771,#16772,#16773,#16774));
#3060=EDGE_LOOP('',(#16775,#16776,#16777,#16778));
#3061=EDGE_LOOP('',(#16779,#16780,#16781,#16782));
#3062=EDGE_LOOP('',(#16783,#16784,#16785,#16786));
#3063=EDGE_LOOP('',(#16787,#16788,#16789,#16790));
#3064=EDGE_LOOP('',(#16791,#16792,#16793,#16794));
#3065=EDGE_LOOP('',(#16795,#16796,#16797,#16798));
#3066=EDGE_LOOP('',(#16799,#16800,#16801,#16802));
#3067=EDGE_LOOP('',(#16803,#16804,#16805,#16806));
#3068=EDGE_LOOP('',(#16807,#16808,#16809,#16810));
#3069=EDGE_LOOP('',(#16811,#16812,#16813,#16814));
#3070=EDGE_LOOP('',(#16815,#16816,#16817,#16818));
#3071=EDGE_LOOP('',(#16819,#16820,#16821,#16822));
#3072=EDGE_LOOP('',(#16823,#16824,#16825,#16826));
#3073=EDGE_LOOP('',(#16827,#16828,#16829,#16830));
#3074=EDGE_LOOP('',(#16831,#16832,#16833,#16834));
#3075=EDGE_LOOP('',(#16835,#16836,#16837,#16838));
#3076=EDGE_LOOP('',(#16839,#16840,#16841,#16842));
#3077=EDGE_LOOP('',(#16843,#16844,#16845,#16846));
#3078=EDGE_LOOP('',(#16847,#16848,#16849,#16850));
#3079=EDGE_LOOP('',(#16851,#16852,#16853,#16854,#16855));
#3080=EDGE_LOOP('',(#16856,#16857,#16858,#16859,#16860,#16861,#16862,#16863));
#3081=EDGE_LOOP('',(#16864,#16865,#16866,#16867));
#3082=EDGE_LOOP('',(#16868,#16869,#16870,#16871));
#3083=EDGE_LOOP('',(#16872,#16873,#16874,#16875));
#3084=EDGE_LOOP('',(#16876,#16877,#16878,#16879));
#3085=EDGE_LOOP('',(#16880,#16881,#16882,#16883));
#3086=EDGE_LOOP('',(#16884,#16885,#16886,#16887));
#3087=EDGE_LOOP('',(#16888,#16889,#16890,#16891));
#3088=EDGE_LOOP('',(#16892,#16893,#16894,#16895));
#3089=EDGE_LOOP('',(#16896,#16897,#16898,#16899,#16900));
#3090=EDGE_LOOP('',(#16901,#16902,#16903,#16904));
#3091=EDGE_LOOP('',(#16905,#16906,#16907,#16908));
#3092=EDGE_LOOP('',(#16909,#16910,#16911,#16912));
#3093=EDGE_LOOP('',(#16913,#16914,#16915,#16916));
#3094=EDGE_LOOP('',(#16917,#16918,#16919,#16920));
#3095=EDGE_LOOP('',(#16921,#16922,#16923,#16924));
#3096=EDGE_LOOP('',(#16925,#16926,#16927,#16928));
#3097=EDGE_LOOP('',(#16929,#16930,#16931,#16932));
#3098=EDGE_LOOP('',(#16933,#16934,#16935,#16936));
#3099=EDGE_LOOP('',(#16937,#16938,#16939,#16940));
#3100=EDGE_LOOP('',(#16941,#16942,#16943,#16944));
#3101=EDGE_LOOP('',(#16945,#16946,#16947,#16948));
#3102=EDGE_LOOP('',(#16949,#16950,#16951,#16952));
#3103=EDGE_LOOP('',(#16953,#16954,#16955,#16956));
#3104=EDGE_LOOP('',(#16957,#16958,#16959,#16960));
#3105=EDGE_LOOP('',(#16961,#16962,#16963,#16964));
#3106=EDGE_LOOP('',(#16965,#16966,#16967,#16968));
#3107=EDGE_LOOP('',(#16969,#16970,#16971,#16972));
#3108=EDGE_LOOP('',(#16973,#16974,#16975,#16976));
#3109=EDGE_LOOP('',(#16977,#16978,#16979,#16980));
#3110=EDGE_LOOP('',(#16981,#16982,#16983,#16984));
#3111=EDGE_LOOP('',(#16985,#16986,#16987,#16988));
#3112=EDGE_LOOP('',(#16989,#16990,#16991,#16992));
#3113=EDGE_LOOP('',(#16993,#16994,#16995,#16996));
#3114=EDGE_LOOP('',(#16997,#16998,#16999,#17000));
#3115=EDGE_LOOP('',(#17001,#17002,#17003,#17004));
#3116=EDGE_LOOP('',(#17005,#17006,#17007,#17008));
#3117=EDGE_LOOP('',(#17009,#17010,#17011,#17012));
#3118=EDGE_LOOP('',(#17013,#17014,#17015,#17016));
#3119=EDGE_LOOP('',(#17017,#17018,#17019,#17020));
#3120=EDGE_LOOP('',(#17021,#17022,#17023,#17024));
#3121=EDGE_LOOP('',(#17025,#17026,#17027,#17028));
#3122=EDGE_LOOP('',(#17029,#17030,#17031,#17032));
#3123=EDGE_LOOP('',(#17033,#17034,#17035,#17036));
#3124=EDGE_LOOP('',(#17037,#17038,#17039,#17040));
#3125=EDGE_LOOP('',(#17041,#17042,#17043,#17044));
#3126=EDGE_LOOP('',(#17045,#17046,#17047,#17048));
#3127=EDGE_LOOP('',(#17049,#17050,#17051,#17052));
#3128=EDGE_LOOP('',(#17053,#17054,#17055,#17056));
#3129=EDGE_LOOP('',(#17057,#17058,#17059,#17060));
#3130=EDGE_LOOP('',(#17061,#17062,#17063,#17064));
#3131=EDGE_LOOP('',(#17065,#17066,#17067,#17068));
#3132=EDGE_LOOP('',(#17069,#17070,#17071,#17072));
#3133=EDGE_LOOP('',(#17073,#17074,#17075,#17076));
#3134=EDGE_LOOP('',(#17077,#17078,#17079,#17080));
#3135=EDGE_LOOP('',(#17081,#17082,#17083,#17084));
#3136=EDGE_LOOP('',(#17085,#17086,#17087,#17088));
#3137=EDGE_LOOP('',(#17089,#17090,#17091,#17092));
#3138=EDGE_LOOP('',(#17093,#17094,#17095,#17096));
#3139=EDGE_LOOP('',(#17097,#17098,#17099,#17100));
#3140=EDGE_LOOP('',(#17101,#17102,#17103,#17104));
#3141=EDGE_LOOP('',(#17105,#17106,#17107,#17108));
#3142=EDGE_LOOP('',(#17109,#17110,#17111,#17112));
#3143=EDGE_LOOP('',(#17113,#17114,#17115,#17116));
#3144=EDGE_LOOP('',(#17117,#17118,#17119,#17120));
#3145=EDGE_LOOP('',(#17121,#17122,#17123,#17124));
#3146=EDGE_LOOP('',(#17125,#17126,#17127,#17128));
#3147=EDGE_LOOP('',(#17129,#17130,#17131,#17132));
#3148=EDGE_LOOP('',(#17133,#17134,#17135,#17136));
#3149=EDGE_LOOP('',(#17137,#17138,#17139,#17140));
#3150=EDGE_LOOP('',(#17141,#17142,#17143,#17144));
#3151=EDGE_LOOP('',(#17145,#17146,#17147,#17148));
#3152=EDGE_LOOP('',(#17149,#17150,#17151,#17152));
#3153=EDGE_LOOP('',(#17153,#17154,#17155,#17156));
#3154=EDGE_LOOP('',(#17157,#17158,#17159,#17160));
#3155=EDGE_LOOP('',(#17161,#17162,#17163,#17164));
#3156=EDGE_LOOP('',(#17165,#17166,#17167,#17168));
#3157=EDGE_LOOP('',(#17169,#17170,#17171,#17172));
#3158=EDGE_LOOP('',(#17173,#17174,#17175,#17176));
#3159=EDGE_LOOP('',(#17177,#17178,#17179,#17180));
#3160=EDGE_LOOP('',(#17181,#17182,#17183,#17184));
#3161=EDGE_LOOP('',(#17185,#17186,#17187,#17188));
#3162=EDGE_LOOP('',(#17189,#17190,#17191,#17192));
#3163=EDGE_LOOP('',(#17193,#17194,#17195,#17196));
#3164=EDGE_LOOP('',(#17197,#17198,#17199,#17200));
#3165=EDGE_LOOP('',(#17201,#17202,#17203,#17204));
#3166=EDGE_LOOP('',(#17205,#17206,#17207,#17208));
#3167=EDGE_LOOP('',(#17209,#17210,#17211,#17212));
#3168=EDGE_LOOP('',(#17213,#17214,#17215,#17216));
#3169=EDGE_LOOP('',(#17217,#17218,#17219,#17220));
#3170=EDGE_LOOP('',(#17221,#17222,#17223,#17224));
#3171=EDGE_LOOP('',(#17225,#17226,#17227,#17228));
#3172=EDGE_LOOP('',(#17229,#17230,#17231,#17232));
#3173=EDGE_LOOP('',(#17233,#17234,#17235,#17236));
#3174=EDGE_LOOP('',(#17237,#17238,#17239,#17240));
#3175=EDGE_LOOP('',(#17241,#17242,#17243,#17244));
#3176=EDGE_LOOP('',(#17245,#17246,#17247,#17248));
#3177=EDGE_LOOP('',(#17249,#17250,#17251,#17252));
#3178=EDGE_LOOP('',(#17253,#17254,#17255,#17256));
#3179=EDGE_LOOP('',(#17257,#17258,#17259,#17260));
#3180=EDGE_LOOP('',(#17261,#17262,#17263,#17264));
#3181=EDGE_LOOP('',(#17265,#17266,#17267,#17268));
#3182=EDGE_LOOP('',(#17269,#17270,#17271,#17272));
#3183=EDGE_LOOP('',(#17273,#17274,#17275,#17276));
#3184=EDGE_LOOP('',(#17277,#17278,#17279,#17280));
#3185=EDGE_LOOP('',(#17281,#17282,#17283,#17284));
#3186=EDGE_LOOP('',(#17285,#17286,#17287,#17288));
#3187=EDGE_LOOP('',(#17289,#17290,#17291,#17292));
#3188=EDGE_LOOP('',(#17293,#17294,#17295,#17296));
#3189=EDGE_LOOP('',(#17297,#17298,#17299,#17300));
#3190=EDGE_LOOP('',(#17301,#17302,#17303,#17304));
#3191=EDGE_LOOP('',(#17305,#17306,#17307,#17308));
#3192=EDGE_LOOP('',(#17309,#17310,#17311,#17312));
#3193=EDGE_LOOP('',(#17313,#17314,#17315,#17316));
#3194=EDGE_LOOP('',(#17317,#17318,#17319,#17320));
#3195=EDGE_LOOP('',(#17321,#17322,#17323,#17324));
#3196=EDGE_LOOP('',(#17325,#17326,#17327,#17328));
#3197=EDGE_LOOP('',(#17329,#17330,#17331,#17332));
#3198=EDGE_LOOP('',(#17333,#17334,#17335,#17336));
#3199=EDGE_LOOP('',(#17337,#17338,#17339,#17340));
#3200=EDGE_LOOP('',(#17341,#17342,#17343,#17344));
#3201=EDGE_LOOP('',(#17345,#17346,#17347,#17348));
#3202=EDGE_LOOP('',(#17349));
#3203=EDGE_LOOP('',(#17350,#17351,#17352,#17353));
#3204=EDGE_LOOP('',(#17354,#17355,#17356,#17357));
#3205=EDGE_LOOP('',(#17358));
#3206=EDGE_LOOP('',(#17359,#17360,#17361,#17362,#17363));
#3207=EDGE_LOOP('',(#17364));
#3208=EDGE_LOOP('',(#17365,#17366,#17367,#17368,#17369,#17370,#17371,#17372,
#17373,#17374,#17375,#17376,#17377,#17378,#17379,#17380,#17381,#17382,#17383,
#17384,#17385,#17386,#17387,#17388,#17389,#17390,#17391,#17392,#17393,#17394,
#17395,#17396,#17397,#17398,#17399,#17400,#17401,#17402,#17403,#17404,#17405,
#17406,#17407,#17408,#17409,#17410,#17411,#17412,#17413,#17414,#17415,#17416,
#17417,#17418,#17419,#17420,#17421,#17422,#17423,#17424,#17425,#17426,#17427,
#17428,#17429,#17430,#17431,#17432,#17433,#17434,#17435,#17436,#17437,#17438,
#17439,#17440,#17441,#17442,#17443,#17444,#17445,#17446,#17447,#17448,#17449,
#17450,#17451,#17452,#17453,#17454,#17455,#17456,#17457,#17458,#17459,#17460,
#17461,#17462,#17463,#17464,#17465,#17466,#17467,#17468,#17469,#17470,#17471,
#17472,#17473,#17474,#17475,#17476,#17477,#17478,#17479,#17480,#17481,#17482,
#17483,#17484,#17485,#17486,#17487,#17488,#17489,#17490,#17491,#17492,#17493,
#17494,#17495,#17496,#17497,#17498,#17499,#17500,#17501,#17502,#17503,#17504,
#17505,#17506,#17507,#17508,#17509,#17510,#17511,#17512,#17513,#17514,#17515,
#17516,#17517,#17518,#17519,#17520,#17521,#17522,#17523,#17524,#17525,#17526,
#17527,#17528,#17529,#17530,#17531,#17532,#17533,#17534,#17535,#17536,#17537,
#17538,#17539,#17540,#17541,#17542,#17543,#17544,#17545,#17546,#17547,#17548,
#17549,#17550,#17551,#17552,#17553,#17554,#17555,#17556,#17557,#17558,#17559,
#17560,#17561,#17562,#17563,#17564,#17565,#17566,#17567,#17568));
#3209=EDGE_LOOP('',(#17569,#17570,#17571,#17572));
#3210=EDGE_LOOP('',(#17573));
#3211=EDGE_LOOP('',(#17574,#17575,#17576,#17577,#17578));
#3212=EDGE_LOOP('',(#17579,#17580,#17581,#17582,#17583,#17584,#17585,#17586,
#17587,#17588,#17589,#17590,#17591,#17592,#17593,#17594,#17595,#17596,#17597,
#17598,#17599,#17600,#17601,#17602));
#3213=EDGE_LOOP('',(#17603,#17604,#17605,#17606));
#3214=EDGE_LOOP('',(#17607,#17608,#17609,#17610));
#3215=EDGE_LOOP('',(#17611,#17612,#17613,#17614,#17615,#17616,#17617,#17618,
#17619,#17620,#17621,#17622,#17623,#17624,#17625,#17626,#17627,#17628,#17629,
#17630,#17631,#17632,#17633,#17634));
#3216=EDGE_LOOP('',(#17635,#17636,#17637));
#3217=EDGE_LOOP('',(#17638,#17639,#17640,#17641));
#3218=EDGE_LOOP('',(#17642));
#3219=EDGE_LOOP('',(#17643,#17644,#17645,#17646,#17647,#17648,#17649,#17650,
#17651,#17652,#17653,#17654,#17655,#17656,#17657,#17658,#17659,#17660,#17661,
#17662,#17663,#17664,#17665,#17666,#17667,#17668,#17669,#17670,#17671,#17672,
#17673,#17674,#17675,#17676,#17677,#17678,#17679,#17680,#17681,#17682,#17683,
#17684,#17685,#17686,#17687,#17688,#17689,#17690,#17691,#17692,#17693,#17694,
#17695,#17696,#17697,#17698,#17699,#17700,#17701,#17702,#17703,#17704,#17705,
#17706,#17707,#17708,#17709,#17710,#17711,#17712,#17713,#17714,#17715,#17716,
#17717,#17718,#17719,#17720,#17721,#17722,#17723,#17724,#17725,#17726,#17727,
#17728,#17729,#17730,#17731,#17732,#17733,#17734,#17735,#17736,#17737,#17738,
#17739,#17740,#17741,#17742,#17743,#17744,#17745,#17746,#17747,#17748,#17749,
#17750,#17751,#17752,#17753,#17754,#17755,#17756,#17757,#17758,#17759,#17760,
#17761,#17762,#17763,#17764,#17765,#17766,#17767,#17768,#17769,#17770,#17771,
#17772,#17773,#17774,#17775,#17776,#17777,#17778,#17779,#17780,#17781,#17782,
#17783,#17784,#17785,#17786,#17787,#17788,#17789,#17790,#17791,#17792,#17793,
#17794,#17795,#17796,#17797,#17798,#17799,#17800,#17801,#17802,#17803,#17804,
#17805,#17806,#17807,#17808,#17809,#17810,#17811,#17812,#17813,#17814,#17815,
#17816,#17817,#17818,#17819,#17820,#17821,#17822,#17823,#17824,#17825,#17826,
#17827,#17828,#17829,#17830,#17831,#17832,#17833,#17834,#17835,#17836,#17837,
#17838,#17839,#17840,#17841,#17842,#17843,#17844,#17845,#17846,#17847));
#3220=EDGE_LOOP('',(#17848,#17849,#17850));
#3860=CIRCLE('',#21412,7.925);
#3861=CIRCLE('',#21513,7.925);
#3862=CIRCLE('',#21515,4.81675);
#3863=CIRCLE('',#21516,4.81675);
#3864=CIRCLE('',#21526,4.81675);
#3865=CIRCLE('',#21528,4.91825);
#3866=CIRCLE('',#21539,5.6435);
#3867=CIRCLE('',#21640,5.00000000000001);
#3868=CIRCLE('',#21641,4.00000000000001);
#3869=CIRCLE('',#21643,5.00000000000001);
#3870=CIRCLE('',#21646,4.);
#3871=CIRCLE('',#21647,5.);
#3872=CIRCLE('',#21649,5.);
#3873=CIRCLE('',#21652,7.925);
#3874=CIRCLE('',#21654,5.6435);
#3875=CIRCLE('',#21656,4.81675);
#3876=CIRCLE('',#21658,4.91825);
#5422=LINE('',#30994,#7303);
#5423=LINE('',#31018,#7304);
#5424=LINE('',#31072,#7305);
#5425=LINE('',#31129,#7306);
#5426=LINE('',#31183,#7307);
#5427=LINE('',#31237,#7308);
#5428=LINE('',#31291,#7309);
#5429=LINE('',#31342,#7310);
#5430=LINE('',#31396,#7311);
#5431=LINE('',#31450,#7312);
#5432=LINE('',#31504,#7313);
#5433=LINE('',#31558,#7314);
#5434=LINE('',#31612,#7315);
#5435=LINE('',#31666,#7316);
#5436=LINE('',#31720,#7317);
#5437=LINE('',#31774,#7318);
#5438=LINE('',#31828,#7319);
#5439=LINE('',#31882,#7320);
#5440=LINE('',#31939,#7321);
#5441=LINE('',#31993,#7322);
#5442=LINE('',#32047,#7323);
#5443=LINE('',#32101,#7324);
#5444=LINE('',#32152,#7325);
#5445=LINE('',#32206,#7326);
#5446=LINE('',#32260,#7327);
#5447=LINE('',#32314,#7328);
#5448=LINE('',#32368,#7329);
#5449=LINE('',#32422,#7330);
#5450=LINE('',#32479,#7331);
#5451=LINE('',#32533,#7332);
#5452=LINE('',#32587,#7333);
#5453=LINE('',#32644,#7334);
#5454=LINE('',#32698,#7335);
#5455=LINE('',#32752,#7336);
#5456=LINE('',#32806,#7337);
#5457=LINE('',#32860,#7338);
#5458=LINE('',#32914,#7339);
#5459=LINE('',#32965,#7340);
#5460=LINE('',#33019,#7341);
#5461=LINE('',#33073,#7342);
#5462=LINE('',#33127,#7343);
#5463=LINE('',#33184,#7344);
#5464=LINE('',#33238,#7345);
#5465=LINE('',#33292,#7346);
#5466=LINE('',#33346,#7347);
#5467=LINE('',#33400,#7348);
#5468=LINE('',#33454,#7349);
#5469=LINE('',#33508,#7350);
#5470=LINE('',#33562,#7351);
#5471=LINE('',#33616,#7352);
#5472=LINE('',#33670,#7353);
#5473=LINE('',#33724,#7354);
#5474=LINE('',#33775,#7355);
#5475=LINE('',#33829,#7356);
#5476=LINE('',#33883,#7357);
#5477=LINE('',#33937,#7358);
#5478=LINE('',#33991,#7359);
#5479=LINE('',#34045,#7360);
#5480=LINE('',#34099,#7361);
#5481=LINE('',#34150,#7362);
#5482=LINE('',#34204,#7363);
#5483=LINE('',#34258,#7364);
#5484=LINE('',#34312,#7365);
#5485=LINE('',#34363,#7366);
#5486=LINE('',#34417,#7367);
#5487=LINE('',#34471,#7368);
#5488=LINE('',#34525,#7369);
#5489=LINE('',#34579,#7370);
#5490=LINE('',#34633,#7371);
#5491=LINE('',#34690,#7372);
#5492=LINE('',#34744,#7373);
#5493=LINE('',#34798,#7374);
#5494=LINE('',#34852,#7375);
#5495=LINE('',#34906,#7376);
#5496=LINE('',#34963,#7377);
#5497=LINE('',#35017,#7378);
#5498=LINE('',#35074,#7379);
#5499=LINE('',#35128,#7380);
#5500=LINE('',#35179,#7381);
#5501=LINE('',#35233,#7382);
#5502=LINE('',#35287,#7383);
#5503=LINE('',#35341,#7384);
#5504=LINE('',#35395,#7385);
#5505=LINE('',#35449,#7386);
#5506=LINE('',#35506,#7387);
#5507=LINE('',#35560,#7388);
#5508=LINE('',#35614,#7389);
#5509=LINE('',#35668,#7390);
#5510=LINE('',#35722,#7391);
#5511=LINE('',#35776,#7392);
#5512=LINE('',#35830,#7393);
#5513=LINE('',#35884,#7394);
#5514=LINE('',#35938,#7395);
#5515=LINE('',#35989,#7396);
#5516=LINE('',#36043,#7397);
#5517=LINE('',#36097,#7398);
#5518=LINE('',#36151,#7399);
#5519=LINE('',#36205,#7400);
#5520=LINE('',#36262,#7401);
#5521=LINE('',#36316,#7402);
#5522=LINE('',#36370,#7403);
#5523=LINE('',#36423,#7404);
#5524=LINE('',#36443,#7405);
#5525=LINE('',#36469,#7406);
#5526=LINE('',#36532,#7407);
#5527=LINE('',#36593,#7408);
#5528=LINE('',#36657,#7409);
#5529=LINE('',#36721,#7410);
#5530=LINE('',#36784,#7411);
#5531=LINE('',#36845,#7412);
#5532=LINE('',#36909,#7413);
#5533=LINE('',#36972,#7414);
#5534=LINE('',#37033,#7415);
#5535=LINE('',#37061,#7416);
#5536=LINE('',#37098,#7417);
#5537=LINE('',#37136,#7418);
#5538=LINE('',#37174,#7419);
#5539=LINE('',#37210,#7420);
#5540=LINE('',#37248,#7421);
#5541=LINE('',#37286,#7422);
#5542=LINE('',#37324,#7423);
#5543=LINE('',#37360,#7424);
#5544=LINE('',#37398,#7425);
#5545=LINE('',#37421,#7426);
#5546=LINE('',#37447,#7427);
#5547=LINE('',#37484,#7428);
#5548=LINE('',#37527,#7429);
#5549=LINE('',#37581,#7430);
#5550=LINE('',#37632,#7431);
#5551=LINE('',#37658,#7432);
#5552=LINE('',#37686,#7433);
#5553=LINE('',#37723,#7434);
#5554=LINE('',#37777,#7435);
#5555=LINE('',#37817,#7436);
#5556=LINE('',#37845,#7437);
#5557=LINE('',#37882,#7438);
#5558=LINE('',#37922,#7439);
#5559=LINE('',#37979,#7440);
#5560=LINE('',#38033,#7441);
#5561=LINE('',#38073,#7442);
#5562=LINE('',#38099,#7443);
#5563=LINE('',#38126,#7444);
#5564=LINE('',#38166,#7445);
#5565=LINE('',#38220,#7446);
#5566=LINE('',#38264,#7447);
#5567=LINE('',#38290,#7448);
#5568=LINE('',#38316,#7449);
#5569=LINE('',#38341,#7450);
#5570=LINE('',#38369,#7451);
#5571=LINE('',#38395,#7452);
#5572=LINE('',#38421,#7453);
#5573=LINE('',#38448,#7454);
#5574=LINE('',#38474,#7455);
#5575=LINE('',#38511,#7456);
#5576=LINE('',#38551,#7457);
#5577=LINE('',#38595,#7458);
#5578=LINE('',#38620,#7459);
#5579=LINE('',#38646,#7460);
#5580=LINE('',#38674,#7461);
#5581=LINE('',#38700,#7462);
#5582=LINE('',#38737,#7463);
#5583=LINE('',#38762,#7464);
#5584=LINE('',#38790,#7465);
#5585=LINE('',#38816,#7466);
#5586=LINE('',#38842,#7467);
#5587=LINE('',#38870,#7468);
#5588=LINE('',#38895,#7469);
#5589=LINE('',#38932,#7470);
#5590=LINE('',#38958,#7471);
#5591=LINE('',#38986,#7472);
#5592=LINE('',#39012,#7473);
#5593=LINE('',#39037,#7474);
#5594=LINE('',#39065,#7475);
#5595=LINE('',#39090,#7476);
#5596=LINE('',#39127,#7477);
#5597=LINE('',#39153,#7478);
#5598=LINE('',#39181,#7479);
#5599=LINE('',#39207,#7480);
#5600=LINE('',#39232,#7481);
#5601=LINE('',#39260,#7482);
#5602=LINE('',#39286,#7483);
#5603=LINE('',#39323,#7484);
#5604=LINE('',#39349,#7485);
#5605=LINE('',#39376,#7486);
#5606=LINE('',#39402,#7487);
#5607=LINE('',#39428,#7488);
#5608=LINE('',#39456,#7489);
#5609=LINE('',#39481,#7490);
#5610=LINE('',#39507,#7491);
#5611=LINE('',#39533,#7492);
#5612=LINE('',#39561,#7493);
#5613=LINE('',#39587,#7494);
#5614=LINE('',#39613,#7495);
#5615=LINE('',#39640,#7496);
#5616=LINE('',#39666,#7497);
#5617=LINE('',#39692,#7498);
#5618=LINE('',#39718,#7499);
#5619=LINE('',#39745,#7500);
#5620=LINE('',#39771,#7501);
#5621=LINE('',#39808,#7502);
#5622=LINE('',#39836,#7503);
#5623=LINE('',#39862,#7504);
#5624=LINE('',#39888,#7505);
#5625=LINE('',#39913,#7506);
#5626=LINE('',#39941,#7507);
#5627=LINE('',#39967,#7508);
#5628=LINE('',#40004,#7509);
#5629=LINE('',#40031,#7510);
#5630=LINE('',#40057,#7511);
#5631=LINE('',#40094,#7512);
#5632=LINE('',#40120,#7513);
#5633=LINE('',#40148,#7514);
#5634=LINE('',#40173,#7515);
#5635=LINE('',#40199,#7516);
#5636=LINE('',#40227,#7517);
#5637=LINE('',#40253,#7518);
#5638=LINE('',#40290,#7519);
#5639=LINE('',#40315,#7520);
#5640=LINE('',#40343,#7521);
#5641=LINE('',#40369,#7522);
#5642=LINE('',#40395,#7523);
#5643=LINE('',#40422,#7524);
#5644=LINE('',#40449,#7525);
#5645=LINE('',#40453,#7526);
#5646=LINE('',#40460,#7527);
#5647=LINE('',#40464,#7528);
#7303=VECTOR('',#25667,8.00000000000001);
#7304=VECTOR('',#25672,8.00000000000001);
#7305=VECTOR('',#25675,8.00000000000001);
#7306=VECTOR('',#25678,8.00000000000001);
#7307=VECTOR('',#25681,8.00000000000001);
#7308=VECTOR('',#25684,8.00000000000001);
#7309=VECTOR('',#25687,8.00000000000001);
#7310=VECTOR('',#25690,8.00000000000001);
#7311=VECTOR('',#25693,8.00000000000001);
#7312=VECTOR('',#25696,8.00000000000001);
#7313=VECTOR('',#25699,8.00000000000001);
#7314=VECTOR('',#25702,8.00000000000001);
#7315=VECTOR('',#25705,8.00000000000001);
#7316=VECTOR('',#25708,8.00000000000001);
#7317=VECTOR('',#25711,8.00000000000001);
#7318=VECTOR('',#25714,8.00000000000001);
#7319=VECTOR('',#25717,8.00000000000001);
#7320=VECTOR('',#25720,8.00000000000001);
#7321=VECTOR('',#25723,8.00000000000001);
#7322=VECTOR('',#25726,8.00000000000001);
#7323=VECTOR('',#25729,8.00000000000001);
#7324=VECTOR('',#25732,8.00000000000001);
#7325=VECTOR('',#25735,8.00000000000001);
#7326=VECTOR('',#25738,8.00000000000001);
#7327=VECTOR('',#25741,8.00000000000001);
#7328=VECTOR('',#25744,8.00000000000001);
#7329=VECTOR('',#25747,8.00000000000001);
#7330=VECTOR('',#25750,8.00000000000001);
#7331=VECTOR('',#25753,8.00000000000001);
#7332=VECTOR('',#25756,8.00000000000001);
#7333=VECTOR('',#25759,8.00000000000001);
#7334=VECTOR('',#25762,8.00000000000001);
#7335=VECTOR('',#25765,8.00000000000001);
#7336=VECTOR('',#25768,8.00000000000001);
#7337=VECTOR('',#25771,8.00000000000001);
#7338=VECTOR('',#25774,8.00000000000001);
#7339=VECTOR('',#25777,8.00000000000001);
#7340=VECTOR('',#25780,8.00000000000001);
#7341=VECTOR('',#25783,8.00000000000001);
#7342=VECTOR('',#25786,8.00000000000001);
#7343=VECTOR('',#25789,8.00000000000001);
#7344=VECTOR('',#25792,8.00000000000001);
#7345=VECTOR('',#25795,8.00000000000001);
#7346=VECTOR('',#25798,8.00000000000001);
#7347=VECTOR('',#25801,8.00000000000001);
#7348=VECTOR('',#25804,8.00000000000001);
#7349=VECTOR('',#25807,8.00000000000001);
#7350=VECTOR('',#25810,8.00000000000001);
#7351=VECTOR('',#25813,8.00000000000001);
#7352=VECTOR('',#25816,8.00000000000001);
#7353=VECTOR('',#25819,8.00000000000001);
#7354=VECTOR('',#25822,8.00000000000001);
#7355=VECTOR('',#25825,8.00000000000001);
#7356=VECTOR('',#25828,8.00000000000001);
#7357=VECTOR('',#25831,8.00000000000001);
#7358=VECTOR('',#25834,8.00000000000001);
#7359=VECTOR('',#25837,8.00000000000001);
#7360=VECTOR('',#25840,8.00000000000001);
#7361=VECTOR('',#25843,8.00000000000001);
#7362=VECTOR('',#25846,8.00000000000001);
#7363=VECTOR('',#25849,8.00000000000001);
#7364=VECTOR('',#25852,8.00000000000001);
#7365=VECTOR('',#25855,8.00000000000001);
#7366=VECTOR('',#25858,8.00000000000001);
#7367=VECTOR('',#25861,8.00000000000001);
#7368=VECTOR('',#25864,8.00000000000001);
#7369=VECTOR('',#25867,8.00000000000001);
#7370=VECTOR('',#25870,8.00000000000001);
#7371=VECTOR('',#25873,8.00000000000001);
#7372=VECTOR('',#25876,8.00000000000001);
#7373=VECTOR('',#25879,8.00000000000001);
#7374=VECTOR('',#25882,8.00000000000001);
#7375=VECTOR('',#25885,8.00000000000001);
#7376=VECTOR('',#25888,8.00000000000001);
#7377=VECTOR('',#25891,8.00000000000001);
#7378=VECTOR('',#25894,8.00000000000001);
#7379=VECTOR('',#25897,8.00000000000001);
#7380=VECTOR('',#25900,8.00000000000001);
#7381=VECTOR('',#25903,8.00000000000001);
#7382=VECTOR('',#25906,8.00000000000001);
#7383=VECTOR('',#25909,8.00000000000001);
#7384=VECTOR('',#25912,8.00000000000001);
#7385=VECTOR('',#25915,8.00000000000001);
#7386=VECTOR('',#25918,8.00000000000001);
#7387=VECTOR('',#25921,8.00000000000001);
#7388=VECTOR('',#25924,8.00000000000001);
#7389=VECTOR('',#25927,8.00000000000001);
#7390=VECTOR('',#25930,8.00000000000001);
#7391=VECTOR('',#25933,8.00000000000001);
#7392=VECTOR('',#25936,8.00000000000001);
#7393=VECTOR('',#25939,8.00000000000001);
#7394=VECTOR('',#25942,8.00000000000001);
#7395=VECTOR('',#25945,8.00000000000001);
#7396=VECTOR('',#25948,8.00000000000001);
#7397=VECTOR('',#25951,8.00000000000001);
#7398=VECTOR('',#25954,8.00000000000001);
#7399=VECTOR('',#25957,8.00000000000001);
#7400=VECTOR('',#25960,8.00000000000001);
#7401=VECTOR('',#25963,8.00000000000001);
#7402=VECTOR('',#25966,8.00000000000001);
#7403=VECTOR('',#25969,8.00000000000001);
#7404=VECTOR('',#25974,6.);
#7405=VECTOR('',#25975,6.);
#7406=VECTOR('',#25982,6.);
#7407=VECTOR('',#25985,6.);
#7408=VECTOR('',#25988,6.);
#7409=VECTOR('',#25991,6.);
#7410=VECTOR('',#25994,6.);
#7411=VECTOR('',#25997,6.);
#7412=VECTOR('',#26000,6.);
#7413=VECTOR('',#26003,6.);
#7414=VECTOR('',#26006,6.);
#7415=VECTOR('',#26011,4.91825);
#7416=VECTOR('',#26016,4.91825);
#7417=VECTOR('',#26019,4.91825);
#7418=VECTOR('',#26022,4.91825);
#7419=VECTOR('',#26025,4.91825);
#7420=VECTOR('',#26028,4.91825);
#7421=VECTOR('',#26031,4.91825);
#7422=VECTOR('',#26034,4.91825);
#7423=VECTOR('',#26037,4.91825);
#7424=VECTOR('',#26040,4.91825);
#7425=VECTOR('',#26043,5.6435);
#7426=VECTOR('',#26048,5.6435);
#7427=VECTOR('',#26051,5.6435);
#7428=VECTOR('',#26054,5.6435);
#7429=VECTOR('',#26057,5.6435);
#7430=VECTOR('',#26060,5.6435);
#7431=VECTOR('',#26063,5.6435);
#7432=VECTOR('',#26066,5.6435);
#7433=VECTOR('',#26069,5.6435);
#7434=VECTOR('',#26072,5.6435);
#7435=VECTOR('',#26075,5.6435);
#7436=VECTOR('',#26078,5.6435);
#7437=VECTOR('',#26081,5.6435);
#7438=VECTOR('',#26084,5.6435);
#7439=VECTOR('',#26087,5.6435);
#7440=VECTOR('',#26090,5.6435);
#7441=VECTOR('',#26093,5.6435);
#7442=VECTOR('',#26096,5.6435);
#7443=VECTOR('',#26099,5.6435);
#7444=VECTOR('',#26102,5.6435);
#7445=VECTOR('',#26105,5.6435);
#7446=VECTOR('',#26108,5.6435);
#7447=VECTOR('',#26111,5.6435);
#7448=VECTOR('',#26114,5.6435);
#7449=VECTOR('',#26117,5.6435);
#7450=VECTOR('',#26120,5.6435);
#7451=VECTOR('',#26123,5.6435);
#7452=VECTOR('',#26126,5.6435);
#7453=VECTOR('',#26129,5.6435);
#7454=VECTOR('',#26132,5.6435);
#7455=VECTOR('',#26135,5.6435);
#7456=VECTOR('',#26138,5.6435);
#7457=VECTOR('',#26141,5.6435);
#7458=VECTOR('',#26144,5.6435);
#7459=VECTOR('',#26147,5.6435);
#7460=VECTOR('',#26150,5.6435);
#7461=VECTOR('',#26153,5.6435);
#7462=VECTOR('',#26156,5.6435);
#7463=VECTOR('',#26159,5.6435);
#7464=VECTOR('',#26162,5.6435);
#7465=VECTOR('',#26165,5.6435);
#7466=VECTOR('',#26168,5.6435);
#7467=VECTOR('',#26171,5.6435);
#7468=VECTOR('',#26174,5.6435);
#7469=VECTOR('',#26177,5.6435);
#7470=VECTOR('',#26180,5.6435);
#7471=VECTOR('',#26183,5.6435);
#7472=VECTOR('',#26186,5.6435);
#7473=VECTOR('',#26189,5.6435);
#7474=VECTOR('',#26192,5.6435);
#7475=VECTOR('',#26195,5.6435);
#7476=VECTOR('',#26198,5.6435);
#7477=VECTOR('',#26201,5.6435);
#7478=VECTOR('',#26204,5.6435);
#7479=VECTOR('',#26207,5.6435);
#7480=VECTOR('',#26210,5.6435);
#7481=VECTOR('',#26213,5.6435);
#7482=VECTOR('',#26216,5.6435);
#7483=VECTOR('',#26219,5.6435);
#7484=VECTOR('',#26222,5.6435);
#7485=VECTOR('',#26225,5.6435);
#7486=VECTOR('',#26228,5.6435);
#7487=VECTOR('',#26231,5.6435);
#7488=VECTOR('',#26234,5.6435);
#7489=VECTOR('',#26237,5.6435);
#7490=VECTOR('',#26240,5.6435);
#7491=VECTOR('',#26243,5.6435);
#7492=VECTOR('',#26246,5.6435);
#7493=VECTOR('',#26249,5.6435);
#7494=VECTOR('',#26252,5.6435);
#7495=VECTOR('',#26255,5.6435);
#7496=VECTOR('',#26258,5.6435);
#7497=VECTOR('',#26261,5.6435);
#7498=VECTOR('',#26264,5.6435);
#7499=VECTOR('',#26267,5.6435);
#7500=VECTOR('',#26270,5.6435);
#7501=VECTOR('',#26273,5.6435);
#7502=VECTOR('',#26276,5.6435);
#7503=VECTOR('',#26279,5.6435);
#7504=VECTOR('',#26282,5.6435);
#7505=VECTOR('',#26285,5.6435);
#7506=VECTOR('',#26288,5.6435);
#7507=VECTOR('',#26291,5.6435);
#7508=VECTOR('',#26294,5.6435);
#7509=VECTOR('',#26297,5.6435);
#7510=VECTOR('',#26300,5.6435);
#7511=VECTOR('',#26303,5.6435);
#7512=VECTOR('',#26306,5.6435);
#7513=VECTOR('',#26309,5.6435);
#7514=VECTOR('',#26312,5.6435);
#7515=VECTOR('',#26315,5.6435);
#7516=VECTOR('',#26318,5.6435);
#7517=VECTOR('',#26321,5.6435);
#7518=VECTOR('',#26324,5.6435);
#7519=VECTOR('',#26327,5.6435);
#7520=VECTOR('',#26330,5.6435);
#7521=VECTOR('',#26333,5.6435);
#7522=VECTOR('',#26336,5.6435);
#7523=VECTOR('',#26339,5.6435);
#7524=VECTOR('',#26342,5.6435);
#7525=VECTOR('',#26347,4.50000000000001);
#7526=VECTOR('',#26352,5.00000000000001);
#7527=VECTOR('',#26361,4.5);
#7528=VECTOR('',#26366,5.);
#9015=VERTEX_POINT('',#30992);
#9016=VERTEX_POINT('',#30993);
#9017=VERTEX_POINT('',#30995);
#9018=VERTEX_POINT('',#31009);
#9019=VERTEX_POINT('',#31016);
#9020=VERTEX_POINT('',#31017);
#9021=VERTEX_POINT('',#31070);
#9022=VERTEX_POINT('',#31071);
#9023=VERTEX_POINT('',#31127);
#9024=VERTEX_POINT('',#31128);
#9025=VERTEX_POINT('',#31181);
#9026=VERTEX_POINT('',#31182);
#9027=VERTEX_POINT('',#31235);
#9028=VERTEX_POINT('',#31236);
#9029=VERTEX_POINT('',#31289);
#9030=VERTEX_POINT('',#31290);
#9031=VERTEX_POINT('',#31340);
#9032=VERTEX_POINT('',#31341);
#9033=VERTEX_POINT('',#31394);
#9034=VERTEX_POINT('',#31395);
#9035=VERTEX_POINT('',#31448);
#9036=VERTEX_POINT('',#31449);
#9037=VERTEX_POINT('',#31502);
#9038=VERTEX_POINT('',#31503);
#9039=VERTEX_POINT('',#31556);
#9040=VERTEX_POINT('',#31557);
#9041=VERTEX_POINT('',#31610);
#9042=VERTEX_POINT('',#31611);
#9043=VERTEX_POINT('',#31664);
#9044=VERTEX_POINT('',#31665);
#9045=VERTEX_POINT('',#31718);
#9046=VERTEX_POINT('',#31719);
#9047=VERTEX_POINT('',#31772);
#9048=VERTEX_POINT('',#31773);
#9049=VERTEX_POINT('',#31826);
#9050=VERTEX_POINT('',#31827);
#9051=VERTEX_POINT('',#31880);
#9052=VERTEX_POINT('',#31881);
#9053=VERTEX_POINT('',#31937);
#9054=VERTEX_POINT('',#31938);
#9055=VERTEX_POINT('',#31991);
#9056=VERTEX_POINT('',#31992);
#9057=VERTEX_POINT('',#32045);
#9058=VERTEX_POINT('',#32046);
#9059=VERTEX_POINT('',#32099);
#9060=VERTEX_POINT('',#32100);
#9061=VERTEX_POINT('',#32150);
#9062=VERTEX_POINT('',#32151);
#9063=VERTEX_POINT('',#32204);
#9064=VERTEX_POINT('',#32205);
#9065=VERTEX_POINT('',#32258);
#9066=VERTEX_POINT('',#32259);
#9067=VERTEX_POINT('',#32312);
#9068=VERTEX_POINT('',#32313);
#9069=VERTEX_POINT('',#32366);
#9070=VERTEX_POINT('',#32367);
#9071=VERTEX_POINT('',#32420);
#9072=VERTEX_POINT('',#32421);
#9073=VERTEX_POINT('',#32477);
#9074=VERTEX_POINT('',#32478);
#9075=VERTEX_POINT('',#32531);
#9076=VERTEX_POINT('',#32532);
#9077=VERTEX_POINT('',#32585);
#9078=VERTEX_POINT('',#32586);
#9079=VERTEX_POINT('',#32642);
#9080=VERTEX_POINT('',#32643);
#9081=VERTEX_POINT('',#32696);
#9082=VERTEX_POINT('',#32697);
#9083=VERTEX_POINT('',#32750);
#9084=VERTEX_POINT('',#32751);
#9085=VERTEX_POINT('',#32804);
#9086=VERTEX_POINT('',#32805);
#9087=VERTEX_POINT('',#32858);
#9088=VERTEX_POINT('',#32859);
#9089=VERTEX_POINT('',#32912);
#9090=VERTEX_POINT('',#32913);
#9091=VERTEX_POINT('',#32963);
#9092=VERTEX_POINT('',#32964);
#9093=VERTEX_POINT('',#33017);
#9094=VERTEX_POINT('',#33018);
#9095=VERTEX_POINT('',#33071);
#9096=VERTEX_POINT('',#33072);
#9097=VERTEX_POINT('',#33125);
#9098=VERTEX_POINT('',#33126);
#9099=VERTEX_POINT('',#33182);
#9100=VERTEX_POINT('',#33183);
#9101=VERTEX_POINT('',#33236);
#9102=VERTEX_POINT('',#33237);
#9103=VERTEX_POINT('',#33290);
#9104=VERTEX_POINT('',#33291);
#9105=VERTEX_POINT('',#33344);
#9106=VERTEX_POINT('',#33345);
#9107=VERTEX_POINT('',#33398);
#9108=VERTEX_POINT('',#33399);
#9109=VERTEX_POINT('',#33452);
#9110=VERTEX_POINT('',#33453);
#9111=VERTEX_POINT('',#33506);
#9112=VERTEX_POINT('',#33507);
#9113=VERTEX_POINT('',#33560);
#9114=VERTEX_POINT('',#33561);
#9115=VERTEX_POINT('',#33614);
#9116=VERTEX_POINT('',#33615);
#9117=VERTEX_POINT('',#33668);
#9118=VERTEX_POINT('',#33669);
#9119=VERTEX_POINT('',#33722);
#9120=VERTEX_POINT('',#33723);
#9121=VERTEX_POINT('',#33773);
#9122=VERTEX_POINT('',#33774);
#9123=VERTEX_POINT('',#33827);
#9124=VERTEX_POINT('',#33828);
#9125=VERTEX_POINT('',#33881);
#9126=VERTEX_POINT('',#33882);
#9127=VERTEX_POINT('',#33935);
#9128=VERTEX_POINT('',#33936);
#9129=VERTEX_POINT('',#33989);
#9130=VERTEX_POINT('',#33990);
#9131=VERTEX_POINT('',#34043);
#9132=VERTEX_POINT('',#34044);
#9133=VERTEX_POINT('',#34097);
#9134=VERTEX_POINT('',#34098);
#9135=VERTEX_POINT('',#34148);
#9136=VERTEX_POINT('',#34149);
#9137=VERTEX_POINT('',#34202);
#9138=VERTEX_POINT('',#34203);
#9139=VERTEX_POINT('',#34256);
#9140=VERTEX_POINT('',#34257);
#9141=VERTEX_POINT('',#34310);
#9142=VERTEX_POINT('',#34311);
#9143=VERTEX_POINT('',#34361);
#9144=VERTEX_POINT('',#34362);
#9145=VERTEX_POINT('',#34415);
#9146=VERTEX_POINT('',#34416);
#9147=VERTEX_POINT('',#34469);
#9148=VERTEX_POINT('',#34470);
#9149=VERTEX_POINT('',#34523);
#9150=VERTEX_POINT('',#34524);
#9151=VERTEX_POINT('',#34577);
#9152=VERTEX_POINT('',#34578);
#9153=VERTEX_POINT('',#34631);
#9154=VERTEX_POINT('',#34632);
#9155=VERTEX_POINT('',#34688);
#9156=VERTEX_POINT('',#34689);
#9157=VERTEX_POINT('',#34742);
#9158=VERTEX_POINT('',#34743);
#9159=VERTEX_POINT('',#34796);
#9160=VERTEX_POINT('',#34797);
#9161=VERTEX_POINT('',#34850);
#9162=VERTEX_POINT('',#34851);
#9163=VERTEX_POINT('',#34904);
#9164=VERTEX_POINT('',#34905);
#9165=VERTEX_POINT('',#34961);
#9166=VERTEX_POINT('',#34962);
#9167=VERTEX_POINT('',#35015);
#9168=VERTEX_POINT('',#35016);
#9169=VERTEX_POINT('',#35072);
#9170=VERTEX_POINT('',#35073);
#9171=VERTEX_POINT('',#35126);
#9172=VERTEX_POINT('',#35127);
#9173=VERTEX_POINT('',#35177);
#9174=VERTEX_POINT('',#35178);
#9175=VERTEX_POINT('',#35231);
#9176=VERTEX_POINT('',#35232);
#9177=VERTEX_POINT('',#35285);
#9178=VERTEX_POINT('',#35286);
#9179=VERTEX_POINT('',#35339);
#9180=VERTEX_POINT('',#35340);
#9181=VERTEX_POINT('',#35393);
#9182=VERTEX_POINT('',#35394);
#9183=VERTEX_POINT('',#35447);
#9184=VERTEX_POINT('',#35448);
#9185=VERTEX_POINT('',#35504);
#9186=VERTEX_POINT('',#35505);
#9187=VERTEX_POINT('',#35558);
#9188=VERTEX_POINT('',#35559);
#9189=VERTEX_POINT('',#35612);
#9190=VERTEX_POINT('',#35613);
#9191=VERTEX_POINT('',#35666);
#9192=VERTEX_POINT('',#35667);
#9193=VERTEX_POINT('',#35720);
#9194=VERTEX_POINT('',#35721);
#9195=VERTEX_POINT('',#35774);
#9196=VERTEX_POINT('',#35775);
#9197=VERTEX_POINT('',#35828);
#9198=VERTEX_POINT('',#35829);
#9199=VERTEX_POINT('',#35882);
#9200=VERTEX_POINT('',#35883);
#9201=VERTEX_POINT('',#35936);
#9202=VERTEX_POINT('',#35937);
#9203=VERTEX_POINT('',#35987);
#9204=VERTEX_POINT('',#35988);
#9205=VERTEX_POINT('',#36041);
#9206=VERTEX_POINT('',#36042);
#9207=VERTEX_POINT('',#36095);
#9208=VERTEX_POINT('',#36096);
#9209=VERTEX_POINT('',#36149);
#9210=VERTEX_POINT('',#36150);
#9211=VERTEX_POINT('',#36203);
#9212=VERTEX_POINT('',#36204);
#9213=VERTEX_POINT('',#36260);
#9214=VERTEX_POINT('',#36261);
#9215=VERTEX_POINT('',#36314);
#9216=VERTEX_POINT('',#36315);
#9217=VERTEX_POINT('',#36368);
#9218=VERTEX_POINT('',#36369);
#9219=VERTEX_POINT('',#36371);
#9220=VERTEX_POINT('',#36421);
#9221=VERTEX_POINT('',#36422);
#9222=VERTEX_POINT('',#36424);
#9223=VERTEX_POINT('',#36442);
#9224=VERTEX_POINT('',#36445);
#9225=VERTEX_POINT('',#36451);
#9226=VERTEX_POINT('',#36467);
#9227=VERTEX_POINT('',#36468);
#9228=VERTEX_POINT('',#36530);
#9229=VERTEX_POINT('',#36531);
#9230=VERTEX_POINT('',#36591);
#9231=VERTEX_POINT('',#36592);
#9232=VERTEX_POINT('',#36655);
#9233=VERTEX_POINT('',#36656);
#9234=VERTEX_POINT('',#36719);
#9235=VERTEX_POINT('',#36720);
#9236=VERTEX_POINT('',#36782);
#9237=VERTEX_POINT('',#36783);
#9238=VERTEX_POINT('',#36843);
#9239=VERTEX_POINT('',#36844);
#9240=VERTEX_POINT('',#36907);
#9241=VERTEX_POINT('',#36908);
#9242=VERTEX_POINT('',#36970);
#9243=VERTEX_POINT('',#36971);
#9244=VERTEX_POINT('',#36973);
#9245=VERTEX_POINT('',#37031);
#9246=VERTEX_POINT('',#37032);
#9247=VERTEX_POINT('',#37034);
#9248=VERTEX_POINT('',#37047);
#9249=VERTEX_POINT('',#37059);
#9250=VERTEX_POINT('',#37060);
#9251=VERTEX_POINT('',#37096);
#9252=VERTEX_POINT('',#37097);
#9253=VERTEX_POINT('',#37134);
#9254=VERTEX_POINT('',#37135);
#9255=VERTEX_POINT('',#37172);
#9256=VERTEX_POINT('',#37173);
#9257=VERTEX_POINT('',#37208);
#9258=VERTEX_POINT('',#37209);
#9259=VERTEX_POINT('',#37246);
#9260=VERTEX_POINT('',#37247);
#9261=VERTEX_POINT('',#37284);
#9262=VERTEX_POINT('',#37285);
#9263=VERTEX_POINT('',#37322);
#9264=VERTEX_POINT('',#37323);
#9265=VERTEX_POINT('',#37358);
#9266=VERTEX_POINT('',#37359);
#9267=VERTEX_POINT('',#37396);
#9268=VERTEX_POINT('',#37397);
#9269=VERTEX_POINT('',#37399);
#9270=VERTEX_POINT('',#37409);
#9271=VERTEX_POINT('',#37419);
#9272=VERTEX_POINT('',#37420);
#9273=VERTEX_POINT('',#37445);
#9274=VERTEX_POINT('',#37446);
#9275=VERTEX_POINT('',#37482);
#9276=VERTEX_POINT('',#37483);
#9277=VERTEX_POINT('',#37525);
#9278=VERTEX_POINT('',#37526);
#9279=VERTEX_POINT('',#37579);
#9280=VERTEX_POINT('',#37580);
#9281=VERTEX_POINT('',#37630);
#9282=VERTEX_POINT('',#37631);
#9283=VERTEX_POINT('',#37656);
#9284=VERTEX_POINT('',#37657);
#9285=VERTEX_POINT('',#37684);
#9286=VERTEX_POINT('',#37685);
#9287=VERTEX_POINT('',#37721);
#9288=VERTEX_POINT('',#37722);
#9289=VERTEX_POINT('',#37775);
#9290=VERTEX_POINT('',#37776);
#9291=VERTEX_POINT('',#37815);
#9292=VERTEX_POINT('',#37816);
#9293=VERTEX_POINT('',#37843);
#9294=VERTEX_POINT('',#37844);
#9295=VERTEX_POINT('',#37880);
#9296=VERTEX_POINT('',#37881);
#9297=VERTEX_POINT('',#37920);
#9298=VERTEX_POINT('',#37921);
#9299=VERTEX_POINT('',#37977);
#9300=VERTEX_POINT('',#37978);
#9301=VERTEX_POINT('',#38031);
#9302=VERTEX_POINT('',#38032);
#9303=VERTEX_POINT('',#38071);
#9304=VERTEX_POINT('',#38072);
#9305=VERTEX_POINT('',#38097);
#9306=VERTEX_POINT('',#38098);
#9307=VERTEX_POINT('',#38124);
#9308=VERTEX_POINT('',#38125);
#9309=VERTEX_POINT('',#38164);
#9310=VERTEX_POINT('',#38165);
#9311=VERTEX_POINT('',#38218);
#9312=VERTEX_POINT('',#38219);
#9313=VERTEX_POINT('',#38262);
#9314=VERTEX_POINT('',#38263);
#9315=VERTEX_POINT('',#38288);
#9316=VERTEX_POINT('',#38289);
#9317=VERTEX_POINT('',#38314);
#9318=VERTEX_POINT('',#38315);
#9319=VERTEX_POINT('',#38339);
#9320=VERTEX_POINT('',#38340);
#9321=VERTEX_POINT('',#38367);
#9322=VERTEX_POINT('',#38368);
#9323=VERTEX_POINT('',#38393);
#9324=VERTEX_POINT('',#38394);
#9325=VERTEX_POINT('',#38419);
#9326=VERTEX_POINT('',#38420);
#9327=VERTEX_POINT('',#38446);
#9328=VERTEX_POINT('',#38447);
#9329=VERTEX_POINT('',#38472);
#9330=VERTEX_POINT('',#38473);
#9331=VERTEX_POINT('',#38509);
#9332=VERTEX_POINT('',#38510);
#9333=VERTEX_POINT('',#38549);
#9334=VERTEX_POINT('',#38550);
#9335=VERTEX_POINT('',#38593);
#9336=VERTEX_POINT('',#38594);
#9337=VERTEX_POINT('',#38618);
#9338=VERTEX_POINT('',#38619);
#9339=VERTEX_POINT('',#38644);
#9340=VERTEX_POINT('',#38645);
#9341=VERTEX_POINT('',#38672);
#9342=VERTEX_POINT('',#38673);
#9343=VERTEX_POINT('',#38698);
#9344=VERTEX_POINT('',#38699);
#9345=VERTEX_POINT('',#38735);
#9346=VERTEX_POINT('',#38736);
#9347=VERTEX_POINT('',#38760);
#9348=VERTEX_POINT('',#38761);
#9349=VERTEX_POINT('',#38788);
#9350=VERTEX_POINT('',#38789);
#9351=VERTEX_POINT('',#38814);
#9352=VERTEX_POINT('',#38815);
#9353=VERTEX_POINT('',#38840);
#9354=VERTEX_POINT('',#38841);
#9355=VERTEX_POINT('',#38868);
#9356=VERTEX_POINT('',#38869);
#9357=VERTEX_POINT('',#38893);
#9358=VERTEX_POINT('',#38894);
#9359=VERTEX_POINT('',#38930);
#9360=VERTEX_POINT('',#38931);
#9361=VERTEX_POINT('',#38956);
#9362=VERTEX_POINT('',#38957);
#9363=VERTEX_POINT('',#38984);
#9364=VERTEX_POINT('',#38985);
#9365=VERTEX_POINT('',#39010);
#9366=VERTEX_POINT('',#39011);
#9367=VERTEX_POINT('',#39035);
#9368=VERTEX_POINT('',#39036);
#9369=VERTEX_POINT('',#39063);
#9370=VERTEX_POINT('',#39064);
#9371=VERTEX_POINT('',#39088);
#9372=VERTEX_POINT('',#39089);
#9373=VERTEX_POINT('',#39125);
#9374=VERTEX_POINT('',#39126);
#9375=VERTEX_POINT('',#39151);
#9376=VERTEX_POINT('',#39152);
#9377=VERTEX_POINT('',#39179);
#9378=VERTEX_POINT('',#39180);
#9379=VERTEX_POINT('',#39205);
#9380=VERTEX_POINT('',#39206);
#9381=VERTEX_POINT('',#39230);
#9382=VERTEX_POINT('',#39231);
#9383=VERTEX_POINT('',#39258);
#9384=VERTEX_POINT('',#39259);
#9385=VERTEX_POINT('',#39284);
#9386=VERTEX_POINT('',#39285);
#9387=VERTEX_POINT('',#39321);
#9388=VERTEX_POINT('',#39322);
#9389=VERTEX_POINT('',#39347);
#9390=VERTEX_POINT('',#39348);
#9391=VERTEX_POINT('',#39374);
#9392=VERTEX_POINT('',#39375);
#9393=VERTEX_POINT('',#39400);
#9394=VERTEX_POINT('',#39401);
#9395=VERTEX_POINT('',#39426);
#9396=VERTEX_POINT('',#39427);
#9397=VERTEX_POINT('',#39454);
#9398=VERTEX_POINT('',#39455);
#9399=VERTEX_POINT('',#39479);
#9400=VERTEX_POINT('',#39480);
#9401=VERTEX_POINT('',#39505);
#9402=VERTEX_POINT('',#39506);
#9403=VERTEX_POINT('',#39531);
#9404=VERTEX_POINT('',#39532);
#9405=VERTEX_POINT('',#39559);
#9406=VERTEX_POINT('',#39560);
#9407=VERTEX_POINT('',#39585);
#9408=VERTEX_POINT('',#39586);
#9409=VERTEX_POINT('',#39611);
#9410=VERTEX_POINT('',#39612);
#9411=VERTEX_POINT('',#39638);
#9412=VERTEX_POINT('',#39639);
#9413=VERTEX_POINT('',#39664);
#9414=VERTEX_POINT('',#39665);
#9415=VERTEX_POINT('',#39690);
#9416=VERTEX_POINT('',#39691);
#9417=VERTEX_POINT('',#39716);
#9418=VERTEX_POINT('',#39717);
#9419=VERTEX_POINT('',#39743);
#9420=VERTEX_POINT('',#39744);
#9421=VERTEX_POINT('',#39769);
#9422=VERTEX_POINT('',#39770);
#9423=VERTEX_POINT('',#39806);
#9424=VERTEX_POINT('',#39807);
#9425=VERTEX_POINT('',#39834);
#9426=VERTEX_POINT('',#39835);
#9427=VERTEX_POINT('',#39860);
#9428=VERTEX_POINT('',#39861);
#9429=VERTEX_POINT('',#39886);
#9430=VERTEX_POINT('',#39887);
#9431=VERTEX_POINT('',#39911);
#9432=VERTEX_POINT('',#39912);
#9433=VERTEX_POINT('',#39939);
#9434=VERTEX_POINT('',#39940);
#9435=VERTEX_POINT('',#39965);
#9436=VERTEX_POINT('',#39966);
#9437=VERTEX_POINT('',#40002);
#9438=VERTEX_POINT('',#40003);
#9439=VERTEX_POINT('',#40029);
#9440=VERTEX_POINT('',#40030);
#9441=VERTEX_POINT('',#40055);
#9442=VERTEX_POINT('',#40056);
#9443=VERTEX_POINT('',#40092);
#9444=VERTEX_POINT('',#40093);
#9445=VERTEX_POINT('',#40118);
#9446=VERTEX_POINT('',#40119);
#9447=VERTEX_POINT('',#40146);
#9448=VERTEX_POINT('',#40147);
#9449=VERTEX_POINT('',#40171);
#9450=VERTEX_POINT('',#40172);
#9451=VERTEX_POINT('',#40197);
#9452=VERTEX_POINT('',#40198);
#9453=VERTEX_POINT('',#40225);
#9454=VERTEX_POINT('',#40226);
#9455=VERTEX_POINT('',#40251);
#9456=VERTEX_POINT('',#40252);
#9457=VERTEX_POINT('',#40288);
#9458=VERTEX_POINT('',#40289);
#9459=VERTEX_POINT('',#40313);
#9460=VERTEX_POINT('',#40314);
#9461=VERTEX_POINT('',#40341);
#9462=VERTEX_POINT('',#40342);
#9463=VERTEX_POINT('',#40367);
#9464=VERTEX_POINT('',#40368);
#9465=VERTEX_POINT('',#40393);
#9466=VERTEX_POINT('',#40394);
#9467=VERTEX_POINT('',#40420);
#9468=VERTEX_POINT('',#40421);
#9469=VERTEX_POINT('',#40446);
#9470=VERTEX_POINT('',#40448);
#9471=VERTEX_POINT('',#40452);
#9472=VERTEX_POINT('',#40457);
#9473=VERTEX_POINT('',#40459);
#9474=VERTEX_POINT('',#40463);
#9475=VERTEX_POINT('',#40468);
#9476=VERTEX_POINT('',#43480);
#9477=VERTEX_POINT('',#43551);
#9478=VERTEX_POINT('',#43575);
#9479=VERTEX_POINT('',#44095);
#9480=VERTEX_POINT('',#44133);
#11609=EDGE_CURVE('',#9015,#9016,#5422,.T.);
#11610=EDGE_CURVE('',#9015,#9017,#71,.T.);
#11611=EDGE_CURVE('',#9018,#9017,#3860,.T.);
#11612=EDGE_CURVE('',#9018,#9016,#72,.T.);
#11613=EDGE_CURVE('',#9019,#9020,#5423,.T.);
#11614=EDGE_CURVE('',#9019,#9015,#73,.T.);
#11615=EDGE_CURVE('',#9016,#9020,#74,.T.);
#11616=EDGE_CURVE('',#9021,#9022,#5424,.T.);
#11617=EDGE_CURVE('',#9021,#9019,#75,.T.);
#11618=EDGE_CURVE('',#9020,#9022,#76,.T.);
#11619=EDGE_CURVE('',#9023,#9024,#5425,.T.);
#11620=EDGE_CURVE('',#9023,#9021,#77,.T.);
#11621=EDGE_CURVE('',#9022,#9024,#78,.T.);
#11622=EDGE_CURVE('',#9025,#9026,#5426,.T.);
#11623=EDGE_CURVE('',#9025,#9023,#79,.T.);
#11624=EDGE_CURVE('',#9024,#9026,#80,.T.);
#11625=EDGE_CURVE('',#9027,#9028,#5427,.T.);
#11626=EDGE_CURVE('',#9027,#9025,#81,.T.);
#11627=EDGE_CURVE('',#9026,#9028,#82,.T.);
#11628=EDGE_CURVE('',#9029,#9030,#5428,.T.);
#11629=EDGE_CURVE('',#9029,#9027,#83,.T.);
#11630=EDGE_CURVE('',#9028,#9030,#84,.T.);
#11631=EDGE_CURVE('',#9031,#9032,#5429,.T.);
#11632=EDGE_CURVE('',#9031,#9029,#85,.T.);
#11633=EDGE_CURVE('',#9030,#9032,#86,.T.);
#11634=EDGE_CURVE('',#9033,#9034,#5430,.T.);
#11635=EDGE_CURVE('',#9033,#9031,#87,.T.);
#11636=EDGE_CURVE('',#9032,#9034,#88,.T.);
#11637=EDGE_CURVE('',#9035,#9036,#5431,.T.);
#11638=EDGE_CURVE('',#9035,#9033,#89,.T.);
#11639=EDGE_CURVE('',#9034,#9036,#90,.T.);
#11640=EDGE_CURVE('',#9037,#9038,#5432,.T.);
#11641=EDGE_CURVE('',#9037,#9035,#91,.T.);
#11642=EDGE_CURVE('',#9036,#9038,#92,.T.);
#11643=EDGE_CURVE('',#9039,#9040,#5433,.T.);
#11644=EDGE_CURVE('',#9039,#9037,#93,.T.);
#11645=EDGE_CURVE('',#9038,#9040,#94,.T.);
#11646=EDGE_CURVE('',#9041,#9042,#5434,.T.);
#11647=EDGE_CURVE('',#9041,#9039,#95,.T.);
#11648=EDGE_CURVE('',#9040,#9042,#96,.T.);
#11649=EDGE_CURVE('',#9043,#9044,#5435,.T.);
#11650=EDGE_CURVE('',#9043,#9041,#97,.T.);
#11651=EDGE_CURVE('',#9042,#9044,#98,.T.);
#11652=EDGE_CURVE('',#9045,#9046,#5436,.T.);
#11653=EDGE_CURVE('',#9045,#9043,#99,.T.);
#11654=EDGE_CURVE('',#9044,#9046,#100,.T.);
#11655=EDGE_CURVE('',#9047,#9048,#5437,.T.);
#11656=EDGE_CURVE('',#9047,#9045,#101,.T.);
#11657=EDGE_CURVE('',#9046,#9048,#102,.T.);
#11658=EDGE_CURVE('',#9049,#9050,#5438,.T.);
#11659=EDGE_CURVE('',#9049,#9047,#103,.T.);
#11660=EDGE_CURVE('',#9048,#9050,#104,.T.);
#11661=EDGE_CURVE('',#9051,#9052,#5439,.T.);
#11662=EDGE_CURVE('',#9051,#9049,#105,.T.);
#11663=EDGE_CURVE('',#9050,#9052,#106,.T.);
#11664=EDGE_CURVE('',#9053,#9054,#5440,.T.);
#11665=EDGE_CURVE('',#9053,#9051,#107,.T.);
#11666=EDGE_CURVE('',#9052,#9054,#108,.T.);
#11667=EDGE_CURVE('',#9055,#9056,#5441,.T.);
#11668=EDGE_CURVE('',#9055,#9053,#109,.T.);
#11669=EDGE_CURVE('',#9054,#9056,#110,.T.);
#11670=EDGE_CURVE('',#9057,#9058,#5442,.T.);
#11671=EDGE_CURVE('',#9057,#9055,#111,.T.);
#11672=EDGE_CURVE('',#9056,#9058,#112,.T.);
#11673=EDGE_CURVE('',#9059,#9060,#5443,.T.);
#11674=EDGE_CURVE('',#9059,#9057,#113,.T.);
#11675=EDGE_CURVE('',#9058,#9060,#114,.T.);
#11676=EDGE_CURVE('',#9061,#9062,#5444,.T.);
#11677=EDGE_CURVE('',#9061,#9059,#115,.T.);
#11678=EDGE_CURVE('',#9060,#9062,#116,.T.);
#11679=EDGE_CURVE('',#9063,#9064,#5445,.T.);
#11680=EDGE_CURVE('',#9063,#9061,#117,.T.);
#11681=EDGE_CURVE('',#9062,#9064,#118,.T.);
#11682=EDGE_CURVE('',#9065,#9066,#5446,.T.);
#11683=EDGE_CURVE('',#9065,#9063,#119,.T.);
#11684=EDGE_CURVE('',#9064,#9066,#120,.T.);
#11685=EDGE_CURVE('',#9067,#9068,#5447,.T.);
#11686=EDGE_CURVE('',#9067,#9065,#121,.T.);
#11687=EDGE_CURVE('',#9066,#9068,#122,.T.);
#11688=EDGE_CURVE('',#9069,#9070,#5448,.T.);
#11689=EDGE_CURVE('',#9069,#9067,#123,.T.);
#11690=EDGE_CURVE('',#9068,#9070,#124,.T.);
#11691=EDGE_CURVE('',#9071,#9072,#5449,.T.);
#11692=EDGE_CURVE('',#9071,#9069,#125,.T.);
#11693=EDGE_CURVE('',#9070,#9072,#126,.T.);
#11694=EDGE_CURVE('',#9073,#9074,#5450,.T.);
#11695=EDGE_CURVE('',#9073,#9071,#127,.T.);
#11696=EDGE_CURVE('',#9072,#9074,#128,.T.);
#11697=EDGE_CURVE('',#9075,#9076,#5451,.T.);
#11698=EDGE_CURVE('',#9075,#9073,#129,.T.);
#11699=EDGE_CURVE('',#9074,#9076,#130,.T.);
#11700=EDGE_CURVE('',#9077,#9078,#5452,.T.);
#11701=EDGE_CURVE('',#9077,#9075,#131,.T.);
#11702=EDGE_CURVE('',#9076,#9078,#132,.T.);
#11703=EDGE_CURVE('',#9079,#9080,#5453,.T.);
#11704=EDGE_CURVE('',#9079,#9077,#133,.T.);
#11705=EDGE_CURVE('',#9078,#9080,#134,.T.);
#11706=EDGE_CURVE('',#9081,#9082,#5454,.T.);
#11707=EDGE_CURVE('',#9081,#9079,#135,.T.);
#11708=EDGE_CURVE('',#9080,#9082,#136,.T.);
#11709=EDGE_CURVE('',#9083,#9084,#5455,.T.);
#11710=EDGE_CURVE('',#9083,#9081,#137,.T.);
#11711=EDGE_CURVE('',#9082,#9084,#138,.T.);
#11712=EDGE_CURVE('',#9085,#9086,#5456,.T.);
#11713=EDGE_CURVE('',#9085,#9083,#139,.T.);
#11714=EDGE_CURVE('',#9084,#9086,#140,.T.);
#11715=EDGE_CURVE('',#9087,#9088,#5457,.T.);
#11716=EDGE_CURVE('',#9087,#9085,#141,.T.);
#11717=EDGE_CURVE('',#9086,#9088,#142,.T.);
#11718=EDGE_CURVE('',#9089,#9090,#5458,.T.);
#11719=EDGE_CURVE('',#9089,#9087,#143,.T.);
#11720=EDGE_CURVE('',#9088,#9090,#144,.T.);
#11721=EDGE_CURVE('',#9091,#9092,#5459,.T.);
#11722=EDGE_CURVE('',#9091,#9089,#145,.T.);
#11723=EDGE_CURVE('',#9090,#9092,#146,.T.);
#11724=EDGE_CURVE('',#9093,#9094,#5460,.T.);
#11725=EDGE_CURVE('',#9093,#9091,#147,.T.);
#11726=EDGE_CURVE('',#9092,#9094,#148,.T.);
#11727=EDGE_CURVE('',#9095,#9096,#5461,.T.);
#11728=EDGE_CURVE('',#9095,#9093,#149,.T.);
#11729=EDGE_CURVE('',#9094,#9096,#150,.T.);
#11730=EDGE_CURVE('',#9097,#9098,#5462,.T.);
#11731=EDGE_CURVE('',#9097,#9095,#151,.T.);
#11732=EDGE_CURVE('',#9096,#9098,#152,.T.);
#11733=EDGE_CURVE('',#9099,#9100,#5463,.T.);
#11734=EDGE_CURVE('',#9099,#9097,#153,.T.);
#11735=EDGE_CURVE('',#9098,#9100,#154,.T.);
#11736=EDGE_CURVE('',#9101,#9102,#5464,.T.);
#11737=EDGE_CURVE('',#9101,#9099,#155,.T.);
#11738=EDGE_CURVE('',#9100,#9102,#156,.T.);
#11739=EDGE_CURVE('',#9103,#9104,#5465,.T.);
#11740=EDGE_CURVE('',#9103,#9101,#157,.T.);
#11741=EDGE_CURVE('',#9102,#9104,#158,.T.);
#11742=EDGE_CURVE('',#9105,#9106,#5466,.T.);
#11743=EDGE_CURVE('',#9105,#9103,#159,.T.);
#11744=EDGE_CURVE('',#9104,#9106,#160,.T.);
#11745=EDGE_CURVE('',#9107,#9108,#5467,.T.);
#11746=EDGE_CURVE('',#9107,#9105,#161,.T.);
#11747=EDGE_CURVE('',#9106,#9108,#162,.T.);
#11748=EDGE_CURVE('',#9109,#9110,#5468,.T.);
#11749=EDGE_CURVE('',#9109,#9107,#163,.T.);
#11750=EDGE_CURVE('',#9108,#9110,#164,.T.);
#11751=EDGE_CURVE('',#9111,#9112,#5469,.T.);
#11752=EDGE_CURVE('',#9111,#9109,#165,.T.);
#11753=EDGE_CURVE('',#9110,#9112,#166,.T.);
#11754=EDGE_CURVE('',#9113,#9114,#5470,.T.);
#11755=EDGE_CURVE('',#9113,#9111,#167,.T.);
#11756=EDGE_CURVE('',#9112,#9114,#168,.T.);
#11757=EDGE_CURVE('',#9115,#9116,#5471,.T.);
#11758=EDGE_CURVE('',#9115,#9113,#169,.T.);
#11759=EDGE_CURVE('',#9114,#9116,#170,.T.);
#11760=EDGE_CURVE('',#9117,#9118,#5472,.T.);
#11761=EDGE_CURVE('',#9117,#9115,#171,.T.);
#11762=EDGE_CURVE('',#9116,#9118,#172,.T.);
#11763=EDGE_CURVE('',#9119,#9120,#5473,.T.);
#11764=EDGE_CURVE('',#9119,#9117,#173,.T.);
#11765=EDGE_CURVE('',#9118,#9120,#174,.T.);
#11766=EDGE_CURVE('',#9121,#9122,#5474,.T.);
#11767=EDGE_CURVE('',#9121,#9119,#175,.T.);
#11768=EDGE_CURVE('',#9120,#9122,#176,.T.);
#11769=EDGE_CURVE('',#9123,#9124,#5475,.T.);
#11770=EDGE_CURVE('',#9123,#9121,#177,.T.);
#11771=EDGE_CURVE('',#9122,#9124,#178,.T.);
#11772=EDGE_CURVE('',#9125,#9126,#5476,.T.);
#11773=EDGE_CURVE('',#9125,#9123,#179,.T.);
#11774=EDGE_CURVE('',#9124,#9126,#180,.T.);
#11775=EDGE_CURVE('',#9127,#9128,#5477,.T.);
#11776=EDGE_CURVE('',#9127,#9125,#181,.T.);
#11777=EDGE_CURVE('',#9126,#9128,#182,.T.);
#11778=EDGE_CURVE('',#9129,#9130,#5478,.T.);
#11779=EDGE_CURVE('',#9129,#9127,#183,.T.);
#11780=EDGE_CURVE('',#9128,#9130,#184,.T.);
#11781=EDGE_CURVE('',#9131,#9132,#5479,.T.);
#11782=EDGE_CURVE('',#9131,#9129,#185,.T.);
#11783=EDGE_CURVE('',#9130,#9132,#186,.T.);
#11784=EDGE_CURVE('',#9133,#9134,#5480,.T.);
#11785=EDGE_CURVE('',#9133,#9131,#187,.T.);
#11786=EDGE_CURVE('',#9132,#9134,#188,.T.);
#11787=EDGE_CURVE('',#9135,#9136,#5481,.T.);
#11788=EDGE_CURVE('',#9135,#9133,#189,.T.);
#11789=EDGE_CURVE('',#9134,#9136,#190,.T.);
#11790=EDGE_CURVE('',#9137,#9138,#5482,.T.);
#11791=EDGE_CURVE('',#9137,#9135,#191,.T.);
#11792=EDGE_CURVE('',#9136,#9138,#192,.T.);
#11793=EDGE_CURVE('',#9139,#9140,#5483,.T.);
#11794=EDGE_CURVE('',#9139,#9137,#193,.T.);
#11795=EDGE_CURVE('',#9138,#9140,#194,.T.);
#11796=EDGE_CURVE('',#9141,#9142,#5484,.T.);
#11797=EDGE_CURVE('',#9141,#9139,#195,.T.);
#11798=EDGE_CURVE('',#9140,#9142,#196,.T.);
#11799=EDGE_CURVE('',#9143,#9144,#5485,.T.);
#11800=EDGE_CURVE('',#9143,#9141,#197,.T.);
#11801=EDGE_CURVE('',#9142,#9144,#198,.T.);
#11802=EDGE_CURVE('',#9145,#9146,#5486,.T.);
#11803=EDGE_CURVE('',#9145,#9143,#199,.T.);
#11804=EDGE_CURVE('',#9144,#9146,#200,.T.);
#11805=EDGE_CURVE('',#9147,#9148,#5487,.T.);
#11806=EDGE_CURVE('',#9147,#9145,#201,.T.);
#11807=EDGE_CURVE('',#9146,#9148,#202,.T.);
#11808=EDGE_CURVE('',#9149,#9150,#5488,.T.);
#11809=EDGE_CURVE('',#9149,#9147,#203,.T.);
#11810=EDGE_CURVE('',#9148,#9150,#204,.T.);
#11811=EDGE_CURVE('',#9151,#9152,#5489,.T.);
#11812=EDGE_CURVE('',#9151,#9149,#205,.T.);
#11813=EDGE_CURVE('',#9150,#9152,#206,.T.);
#11814=EDGE_CURVE('',#9153,#9154,#5490,.T.);
#11815=EDGE_CURVE('',#9153,#9151,#207,.T.);
#11816=EDGE_CURVE('',#9152,#9154,#208,.T.);
#11817=EDGE_CURVE('',#9155,#9156,#5491,.T.);
#11818=EDGE_CURVE('',#9155,#9153,#209,.T.);
#11819=EDGE_CURVE('',#9154,#9156,#210,.T.);
#11820=EDGE_CURVE('',#9157,#9158,#5492,.T.);
#11821=EDGE_CURVE('',#9157,#9155,#211,.T.);
#11822=EDGE_CURVE('',#9156,#9158,#212,.T.);
#11823=EDGE_CURVE('',#9159,#9160,#5493,.T.);
#11824=EDGE_CURVE('',#9159,#9157,#213,.T.);
#11825=EDGE_CURVE('',#9158,#9160,#214,.T.);
#11826=EDGE_CURVE('',#9161,#9162,#5494,.T.);
#11827=EDGE_CURVE('',#9161,#9159,#215,.T.);
#11828=EDGE_CURVE('',#9160,#9162,#216,.T.);
#11829=EDGE_CURVE('',#9163,#9164,#5495,.T.);
#11830=EDGE_CURVE('',#9163,#9161,#217,.T.);
#11831=EDGE_CURVE('',#9162,#9164,#218,.T.);
#11832=EDGE_CURVE('',#9165,#9166,#5496,.T.);
#11833=EDGE_CURVE('',#9165,#9163,#219,.T.);
#11834=EDGE_CURVE('',#9164,#9166,#220,.T.);
#11835=EDGE_CURVE('',#9167,#9168,#5497,.T.);
#11836=EDGE_CURVE('',#9167,#9165,#221,.T.);
#11837=EDGE_CURVE('',#9166,#9168,#222,.T.);
#11838=EDGE_CURVE('',#9169,#9170,#5498,.T.);
#11839=EDGE_CURVE('',#9169,#9167,#223,.T.);
#11840=EDGE_CURVE('',#9168,#9170,#224,.T.);
#11841=EDGE_CURVE('',#9171,#9172,#5499,.T.);
#11842=EDGE_CURVE('',#9171,#9169,#225,.T.);
#11843=EDGE_CURVE('',#9170,#9172,#226,.T.);
#11844=EDGE_CURVE('',#9173,#9174,#5500,.T.);
#11845=EDGE_CURVE('',#9173,#9171,#227,.T.);
#11846=EDGE_CURVE('',#9172,#9174,#228,.T.);
#11847=EDGE_CURVE('',#9175,#9176,#5501,.T.);
#11848=EDGE_CURVE('',#9175,#9173,#229,.T.);
#11849=EDGE_CURVE('',#9174,#9176,#230,.T.);
#11850=EDGE_CURVE('',#9177,#9178,#5502,.T.);
#11851=EDGE_CURVE('',#9177,#9175,#231,.T.);
#11852=EDGE_CURVE('',#9176,#9178,#232,.T.);
#11853=EDGE_CURVE('',#9179,#9180,#5503,.T.);
#11854=EDGE_CURVE('',#9179,#9177,#233,.T.);
#11855=EDGE_CURVE('',#9178,#9180,#234,.T.);
#11856=EDGE_CURVE('',#9181,#9182,#5504,.T.);
#11857=EDGE_CURVE('',#9181,#9179,#235,.T.);
#11858=EDGE_CURVE('',#9180,#9182,#236,.T.);
#11859=EDGE_CURVE('',#9183,#9184,#5505,.T.);
#11860=EDGE_CURVE('',#9183,#9181,#237,.T.);
#11861=EDGE_CURVE('',#9182,#9184,#238,.T.);
#11862=EDGE_CURVE('',#9185,#9186,#5506,.T.);
#11863=EDGE_CURVE('',#9185,#9183,#239,.T.);
#11864=EDGE_CURVE('',#9184,#9186,#240,.T.);
#11865=EDGE_CURVE('',#9187,#9188,#5507,.T.);
#11866=EDGE_CURVE('',#9187,#9185,#241,.T.);
#11867=EDGE_CURVE('',#9186,#9188,#242,.T.);
#11868=EDGE_CURVE('',#9189,#9190,#5508,.T.);
#11869=EDGE_CURVE('',#9189,#9187,#243,.T.);
#11870=EDGE_CURVE('',#9188,#9190,#244,.T.);
#11871=EDGE_CURVE('',#9191,#9192,#5509,.T.);
#11872=EDGE_CURVE('',#9191,#9189,#245,.T.);
#11873=EDGE_CURVE('',#9190,#9192,#246,.T.);
#11874=EDGE_CURVE('',#9193,#9194,#5510,.T.);
#11875=EDGE_CURVE('',#9193,#9191,#247,.T.);
#11876=EDGE_CURVE('',#9192,#9194,#248,.T.);
#11877=EDGE_CURVE('',#9195,#9196,#5511,.T.);
#11878=EDGE_CURVE('',#9195,#9193,#249,.T.);
#11879=EDGE_CURVE('',#9194,#9196,#250,.T.);
#11880=EDGE_CURVE('',#9197,#9198,#5512,.T.);
#11881=EDGE_CURVE('',#9197,#9195,#251,.T.);
#11882=EDGE_CURVE('',#9196,#9198,#252,.T.);
#11883=EDGE_CURVE('',#9199,#9200,#5513,.T.);
#11884=EDGE_CURVE('',#9199,#9197,#253,.T.);
#11885=EDGE_CURVE('',#9198,#9200,#254,.T.);
#11886=EDGE_CURVE('',#9201,#9202,#5514,.T.);
#11887=EDGE_CURVE('',#9201,#9199,#255,.T.);
#11888=EDGE_CURVE('',#9200,#9202,#256,.T.);
#11889=EDGE_CURVE('',#9203,#9204,#5515,.T.);
#11890=EDGE_CURVE('',#9203,#9201,#257,.T.);
#11891=EDGE_CURVE('',#9202,#9204,#258,.T.);
#11892=EDGE_CURVE('',#9205,#9206,#5516,.T.);
#11893=EDGE_CURVE('',#9205,#9203,#259,.T.);
#11894=EDGE_CURVE('',#9204,#9206,#260,.T.);
#11895=EDGE_CURVE('',#9207,#9208,#5517,.T.);
#11896=EDGE_CURVE('',#9207,#9205,#261,.T.);
#11897=EDGE_CURVE('',#9206,#9208,#262,.T.);
#11898=EDGE_CURVE('',#9209,#9210,#5518,.T.);
#11899=EDGE_CURVE('',#9209,#9207,#263,.T.);
#11900=EDGE_CURVE('',#9208,#9210,#264,.T.);
#11901=EDGE_CURVE('',#9211,#9212,#5519,.T.);
#11902=EDGE_CURVE('',#9211,#9209,#265,.T.);
#11903=EDGE_CURVE('',#9210,#9212,#266,.T.);
#11904=EDGE_CURVE('',#9213,#9214,#5520,.T.);
#11905=EDGE_CURVE('',#9213,#9211,#267,.T.);
#11906=EDGE_CURVE('',#9212,#9214,#268,.T.);
#11907=EDGE_CURVE('',#9215,#9216,#5521,.T.);
#11908=EDGE_CURVE('',#9215,#9213,#269,.T.);
#11909=EDGE_CURVE('',#9214,#9216,#270,.T.);
#11910=EDGE_CURVE('',#9217,#9218,#5522,.T.);
#11911=EDGE_CURVE('',#9217,#9219,#3861,.T.);
#11912=EDGE_CURVE('',#9219,#9215,#271,.T.);
#11913=EDGE_CURVE('',#9216,#9218,#272,.T.);
#11914=EDGE_CURVE('',#9220,#9221,#5523,.T.);
#11915=EDGE_CURVE('',#9220,#9222,#273,.F.);
#11916=EDGE_CURVE('',#9222,#9223,#5524,.T.);
#11917=EDGE_CURVE('',#9223,#9223,#3862,.F.);
#11918=EDGE_CURVE('',#9222,#9224,#274,.F.);
#11919=EDGE_CURVE('',#9224,#9225,#3863,.T.);
#11920=EDGE_CURVE('',#9225,#9221,#275,.F.);
#11921=EDGE_CURVE('',#9226,#9227,#5525,.T.);
#11922=EDGE_CURVE('',#9226,#9220,#276,.F.);
#11923=EDGE_CURVE('',#9221,#9227,#277,.F.);
#11924=EDGE_CURVE('',#9228,#9229,#5526,.T.);
#11925=EDGE_CURVE('',#9228,#9226,#278,.F.);
#11926=EDGE_CURVE('',#9227,#9229,#279,.F.);
#11927=EDGE_CURVE('',#9230,#9231,#5527,.T.);
#11928=EDGE_CURVE('',#9230,#9228,#280,.F.);
#11929=EDGE_CURVE('',#9229,#9231,#281,.F.);
#11930=EDGE_CURVE('',#9232,#9233,#5528,.T.);
#11931=EDGE_CURVE('',#9232,#9230,#282,.F.);
#11932=EDGE_CURVE('',#9231,#9233,#283,.F.);
#11933=EDGE_CURVE('',#9234,#9235,#5529,.T.);
#11934=EDGE_CURVE('',#9234,#9232,#284,.F.);
#11935=EDGE_CURVE('',#9233,#9235,#285,.F.);
#11936=EDGE_CURVE('',#9236,#9237,#5530,.T.);
#11937=EDGE_CURVE('',#9236,#9234,#286,.F.);
#11938=EDGE_CURVE('',#9235,#9237,#287,.F.);
#11939=EDGE_CURVE('',#9238,#9239,#5531,.T.);
#11940=EDGE_CURVE('',#9238,#9236,#288,.F.);
#11941=EDGE_CURVE('',#9237,#9239,#289,.F.);
#11942=EDGE_CURVE('',#9240,#9241,#5532,.T.);
#11943=EDGE_CURVE('',#9240,#9238,#290,.F.);
#11944=EDGE_CURVE('',#9239,#9241,#291,.F.);
#11945=EDGE_CURVE('',#9242,#9243,#5533,.T.);
#11946=EDGE_CURVE('',#9244,#9242,#3864,.F.);
#11947=EDGE_CURVE('',#9244,#9240,#292,.F.);
#11948=EDGE_CURVE('',#9241,#9243,#293,.F.);
#11949=EDGE_CURVE('',#9245,#9246,#5534,.T.);
#11950=EDGE_CURVE('',#9245,#9247,#294,.T.);
#11951=EDGE_CURVE('',#9248,#9247,#3865,.T.);
#11952=EDGE_CURVE('',#9246,#9248,#295,.T.);
#11953=EDGE_CURVE('',#9249,#9250,#5535,.T.);
#11954=EDGE_CURVE('',#9249,#9245,#296,.T.);
#11955=EDGE_CURVE('',#9250,#9246,#297,.T.);
#11956=EDGE_CURVE('',#9251,#9252,#5536,.T.);
#11957=EDGE_CURVE('',#9251,#9249,#298,.T.);
#11958=EDGE_CURVE('',#9252,#9250,#299,.T.);
#11959=EDGE_CURVE('',#9253,#9254,#5537,.T.);
#11960=EDGE_CURVE('',#9253,#9251,#300,.T.);
#11961=EDGE_CURVE('',#9254,#9252,#301,.T.);
#11962=EDGE_CURVE('',#9255,#9256,#5538,.T.);
#11963=EDGE_CURVE('',#9255,#9253,#302,.T.);
#11964=EDGE_CURVE('',#9256,#9254,#303,.T.);
#11965=EDGE_CURVE('',#9257,#9258,#5539,.T.);
#11966=EDGE_CURVE('',#9257,#9255,#304,.T.);
#11967=EDGE_CURVE('',#9258,#9256,#305,.T.);
#11968=EDGE_CURVE('',#9259,#9260,#5540,.T.);
#11969=EDGE_CURVE('',#9259,#9257,#306,.T.);
#11970=EDGE_CURVE('',#9260,#9258,#307,.T.);
#11971=EDGE_CURVE('',#9261,#9262,#5541,.T.);
#11972=EDGE_CURVE('',#9261,#9259,#308,.T.);
#11973=EDGE_CURVE('',#9262,#9260,#309,.T.);
#11974=EDGE_CURVE('',#9263,#9264,#5542,.T.);
#11975=EDGE_CURVE('',#9263,#9261,#310,.T.);
#11976=EDGE_CURVE('',#9264,#9262,#311,.T.);
#11977=EDGE_CURVE('',#9265,#9266,#5543,.T.);
#11978=EDGE_CURVE('',#9265,#9263,#312,.T.);
#11979=EDGE_CURVE('',#9266,#9264,#313,.T.);
#11980=EDGE_CURVE('',#9267,#9268,#5544,.T.);
#11981=EDGE_CURVE('',#9267,#9269,#314,.T.);
#11982=EDGE_CURVE('',#9269,#9270,#3866,.T.);
#11983=EDGE_CURVE('',#9268,#9270,#315,.T.);
#11984=EDGE_CURVE('',#9271,#9272,#5545,.T.);
#11985=EDGE_CURVE('',#9271,#9267,#316,.T.);
#11986=EDGE_CURVE('',#9272,#9268,#317,.T.);
#11987=EDGE_CURVE('',#9273,#9274,#5546,.T.);
#11988=EDGE_CURVE('',#9273,#9271,#318,.T.);
#11989=EDGE_CURVE('',#9274,#9272,#319,.T.);
#11990=EDGE_CURVE('',#9275,#9276,#5547,.T.);
#11991=EDGE_CURVE('',#9275,#9273,#320,.T.);
#11992=EDGE_CURVE('',#9276,#9274,#321,.T.);
#11993=EDGE_CURVE('',#9277,#9278,#5548,.T.);
#11994=EDGE_CURVE('',#9277,#9275,#322,.T.);
#11995=EDGE_CURVE('',#9278,#9276,#323,.T.);
#11996=EDGE_CURVE('',#9279,#9280,#5549,.T.);
#11997=EDGE_CURVE('',#9279,#9277,#324,.T.);
#11998=EDGE_CURVE('',#9280,#9278,#325,.T.);
#11999=EDGE_CURVE('',#9281,#9282,#5550,.T.);
#12000=EDGE_CURVE('',#9281,#9279,#326,.T.);
#12001=EDGE_CURVE('',#9282,#9280,#327,.T.);
#12002=EDGE_CURVE('',#9283,#9284,#5551,.T.);
#12003=EDGE_CURVE('',#9283,#9281,#328,.T.);
#12004=EDGE_CURVE('',#9284,#9282,#329,.T.);
#12005=EDGE_CURVE('',#9285,#9286,#5552,.T.);
#12006=EDGE_CURVE('',#9285,#9283,#330,.T.);
#12007=EDGE_CURVE('',#9286,#9284,#331,.T.);
#12008=EDGE_CURVE('',#9287,#9288,#5553,.T.);
#12009=EDGE_CURVE('',#9287,#9285,#332,.T.);
#12010=EDGE_CURVE('',#9288,#9286,#333,.T.);
#12011=EDGE_CURVE('',#9289,#9290,#5554,.T.);
#12012=EDGE_CURVE('',#9289,#9287,#334,.T.);
#12013=EDGE_CURVE('',#9290,#9288,#335,.T.);
#12014=EDGE_CURVE('',#9291,#9292,#5555,.T.);
#12015=EDGE_CURVE('',#9291,#9289,#336,.T.);
#12016=EDGE_CURVE('',#9292,#9290,#337,.T.);
#12017=EDGE_CURVE('',#9293,#9294,#5556,.T.);
#12018=EDGE_CURVE('',#9293,#9291,#338,.T.);
#12019=EDGE_CURVE('',#9294,#9292,#339,.T.);
#12020=EDGE_CURVE('',#9295,#9296,#5557,.T.);
#12021=EDGE_CURVE('',#9295,#9293,#340,.T.);
#12022=EDGE_CURVE('',#9296,#9294,#341,.T.);
#12023=EDGE_CURVE('',#9297,#9298,#5558,.T.);
#12024=EDGE_CURVE('',#9297,#9295,#342,.T.);
#12025=EDGE_CURVE('',#9298,#9296,#343,.T.);
#12026=EDGE_CURVE('',#9299,#9300,#5559,.T.);
#12027=EDGE_CURVE('',#9299,#9297,#344,.T.);
#12028=EDGE_CURVE('',#9300,#9298,#345,.T.);
#12029=EDGE_CURVE('',#9301,#9302,#5560,.T.);
#12030=EDGE_CURVE('',#9301,#9299,#346,.T.);
#12031=EDGE_CURVE('',#9302,#9300,#347,.T.);
#12032=EDGE_CURVE('',#9303,#9304,#5561,.T.);
#12033=EDGE_CURVE('',#9303,#9301,#348,.T.);
#12034=EDGE_CURVE('',#9304,#9302,#349,.T.);
#12035=EDGE_CURVE('',#9305,#9306,#5562,.T.);
#12036=EDGE_CURVE('',#9305,#9303,#350,.T.);
#12037=EDGE_CURVE('',#9306,#9304,#351,.T.);
#12038=EDGE_CURVE('',#9307,#9308,#5563,.T.);
#12039=EDGE_CURVE('',#9307,#9305,#352,.T.);
#12040=EDGE_CURVE('',#9308,#9306,#353,.T.);
#12041=EDGE_CURVE('',#9309,#9310,#5564,.T.);
#12042=EDGE_CURVE('',#9309,#9307,#354,.T.);
#12043=EDGE_CURVE('',#9310,#9308,#355,.T.);
#12044=EDGE_CURVE('',#9311,#9312,#5565,.T.);
#12045=EDGE_CURVE('',#9311,#9309,#356,.T.);
#12046=EDGE_CURVE('',#9312,#9310,#357,.T.);
#12047=EDGE_CURVE('',#9313,#9314,#5566,.T.);
#12048=EDGE_CURVE('',#9313,#9311,#358,.T.);
#12049=EDGE_CURVE('',#9314,#9312,#359,.T.);
#12050=EDGE_CURVE('',#9315,#9316,#5567,.T.);
#12051=EDGE_CURVE('',#9315,#9313,#360,.T.);
#12052=EDGE_CURVE('',#9316,#9314,#361,.T.);
#12053=EDGE_CURVE('',#9317,#9318,#5568,.T.);
#12054=EDGE_CURVE('',#9317,#9315,#362,.T.);
#12055=EDGE_CURVE('',#9318,#9316,#363,.T.);
#12056=EDGE_CURVE('',#9319,#9320,#5569,.T.);
#12057=EDGE_CURVE('',#9319,#9317,#364,.T.);
#12058=EDGE_CURVE('',#9320,#9318,#365,.T.);
#12059=EDGE_CURVE('',#9321,#9322,#5570,.T.);
#12060=EDGE_CURVE('',#9321,#9319,#366,.T.);
#12061=EDGE_CURVE('',#9322,#9320,#367,.T.);
#12062=EDGE_CURVE('',#9323,#9324,#5571,.T.);
#12063=EDGE_CURVE('',#9323,#9321,#368,.T.);
#12064=EDGE_CURVE('',#9324,#9322,#369,.T.);
#12065=EDGE_CURVE('',#9325,#9326,#5572,.T.);
#12066=EDGE_CURVE('',#9325,#9323,#370,.T.);
#12067=EDGE_CURVE('',#9326,#9324,#371,.T.);
#12068=EDGE_CURVE('',#9327,#9328,#5573,.T.);
#12069=EDGE_CURVE('',#9327,#9325,#372,.T.);
#12070=EDGE_CURVE('',#9328,#9326,#373,.T.);
#12071=EDGE_CURVE('',#9329,#9330,#5574,.T.);
#12072=EDGE_CURVE('',#9329,#9327,#374,.T.);
#12073=EDGE_CURVE('',#9330,#9328,#375,.T.);
#12074=EDGE_CURVE('',#9331,#9332,#5575,.T.);
#12075=EDGE_CURVE('',#9331,#9329,#376,.T.);
#12076=EDGE_CURVE('',#9332,#9330,#377,.T.);
#12077=EDGE_CURVE('',#9333,#9334,#5576,.T.);
#12078=EDGE_CURVE('',#9333,#9331,#378,.T.);
#12079=EDGE_CURVE('',#9334,#9332,#379,.T.);
#12080=EDGE_CURVE('',#9335,#9336,#5577,.T.);
#12081=EDGE_CURVE('',#9335,#9333,#380,.T.);
#12082=EDGE_CURVE('',#9336,#9334,#381,.T.);
#12083=EDGE_CURVE('',#9337,#9338,#5578,.T.);
#12084=EDGE_CURVE('',#9337,#9335,#382,.T.);
#12085=EDGE_CURVE('',#9338,#9336,#383,.T.);
#12086=EDGE_CURVE('',#9339,#9340,#5579,.T.);
#12087=EDGE_CURVE('',#9339,#9337,#384,.T.);
#12088=EDGE_CURVE('',#9340,#9338,#385,.T.);
#12089=EDGE_CURVE('',#9341,#9342,#5580,.T.);
#12090=EDGE_CURVE('',#9341,#9339,#386,.T.);
#12091=EDGE_CURVE('',#9342,#9340,#387,.T.);
#12092=EDGE_CURVE('',#9343,#9344,#5581,.T.);
#12093=EDGE_CURVE('',#9343,#9341,#388,.T.);
#12094=EDGE_CURVE('',#9344,#9342,#389,.T.);
#12095=EDGE_CURVE('',#9345,#9346,#5582,.T.);
#12096=EDGE_CURVE('',#9345,#9343,#390,.T.);
#12097=EDGE_CURVE('',#9346,#9344,#391,.T.);
#12098=EDGE_CURVE('',#9347,#9348,#5583,.T.);
#12099=EDGE_CURVE('',#9347,#9345,#392,.T.);
#12100=EDGE_CURVE('',#9348,#9346,#393,.T.);
#12101=EDGE_CURVE('',#9349,#9350,#5584,.T.);
#12102=EDGE_CURVE('',#9349,#9347,#394,.T.);
#12103=EDGE_CURVE('',#9350,#9348,#395,.T.);
#12104=EDGE_CURVE('',#9351,#9352,#5585,.T.);
#12105=EDGE_CURVE('',#9351,#9349,#396,.T.);
#12106=EDGE_CURVE('',#9352,#9350,#397,.T.);
#12107=EDGE_CURVE('',#9353,#9354,#5586,.T.);
#12108=EDGE_CURVE('',#9353,#9351,#398,.T.);
#12109=EDGE_CURVE('',#9354,#9352,#399,.T.);
#12110=EDGE_CURVE('',#9355,#9356,#5587,.T.);
#12111=EDGE_CURVE('',#9355,#9353,#400,.T.);
#12112=EDGE_CURVE('',#9356,#9354,#401,.T.);
#12113=EDGE_CURVE('',#9357,#9358,#5588,.T.);
#12114=EDGE_CURVE('',#9357,#9355,#402,.T.);
#12115=EDGE_CURVE('',#9358,#9356,#403,.T.);
#12116=EDGE_CURVE('',#9359,#9360,#5589,.T.);
#12117=EDGE_CURVE('',#9359,#9357,#404,.T.);
#12118=EDGE_CURVE('',#9360,#9358,#405,.T.);
#12119=EDGE_CURVE('',#9361,#9362,#5590,.T.);
#12120=EDGE_CURVE('',#9361,#9359,#406,.T.);
#12121=EDGE_CURVE('',#9362,#9360,#407,.T.);
#12122=EDGE_CURVE('',#9363,#9364,#5591,.T.);
#12123=EDGE_CURVE('',#9363,#9361,#408,.T.);
#12124=EDGE_CURVE('',#9364,#9362,#409,.T.);
#12125=EDGE_CURVE('',#9365,#9366,#5592,.T.);
#12126=EDGE_CURVE('',#9365,#9363,#410,.T.);
#12127=EDGE_CURVE('',#9366,#9364,#411,.T.);
#12128=EDGE_CURVE('',#9367,#9368,#5593,.T.);
#12129=EDGE_CURVE('',#9367,#9365,#412,.T.);
#12130=EDGE_CURVE('',#9368,#9366,#413,.T.);
#12131=EDGE_CURVE('',#9369,#9370,#5594,.T.);
#12132=EDGE_CURVE('',#9369,#9367,#414,.T.);
#12133=EDGE_CURVE('',#9370,#9368,#415,.T.);
#12134=EDGE_CURVE('',#9371,#9372,#5595,.T.);
#12135=EDGE_CURVE('',#9371,#9369,#416,.T.);
#12136=EDGE_CURVE('',#9372,#9370,#417,.T.);
#12137=EDGE_CURVE('',#9373,#9374,#5596,.T.);
#12138=EDGE_CURVE('',#9373,#9371,#418,.T.);
#12139=EDGE_CURVE('',#9374,#9372,#419,.T.);
#12140=EDGE_CURVE('',#9375,#9376,#5597,.T.);
#12141=EDGE_CURVE('',#9375,#9373,#420,.T.);
#12142=EDGE_CURVE('',#9376,#9374,#421,.T.);
#12143=EDGE_CURVE('',#9377,#9378,#5598,.T.);
#12144=EDGE_CURVE('',#9377,#9375,#422,.T.);
#12145=EDGE_CURVE('',#9378,#9376,#423,.T.);
#12146=EDGE_CURVE('',#9379,#9380,#5599,.T.);
#12147=EDGE_CURVE('',#9379,#9377,#424,.T.);
#12148=EDGE_CURVE('',#9380,#9378,#425,.T.);
#12149=EDGE_CURVE('',#9381,#9382,#5600,.T.);
#12150=EDGE_CURVE('',#9381,#9379,#426,.T.);
#12151=EDGE_CURVE('',#9382,#9380,#427,.T.);
#12152=EDGE_CURVE('',#9383,#9384,#5601,.T.);
#12153=EDGE_CURVE('',#9383,#9381,#428,.T.);
#12154=EDGE_CURVE('',#9384,#9382,#429,.T.);
#12155=EDGE_CURVE('',#9385,#9386,#5602,.T.);
#12156=EDGE_CURVE('',#9385,#9383,#430,.T.);
#12157=EDGE_CURVE('',#9386,#9384,#431,.T.);
#12158=EDGE_CURVE('',#9387,#9388,#5603,.T.);
#12159=EDGE_CURVE('',#9387,#9385,#432,.T.);
#12160=EDGE_CURVE('',#9388,#9386,#433,.T.);
#12161=EDGE_CURVE('',#9389,#9390,#5604,.T.);
#12162=EDGE_CURVE('',#9389,#9387,#434,.T.);
#12163=EDGE_CURVE('',#9390,#9388,#435,.T.);
#12164=EDGE_CURVE('',#9391,#9392,#5605,.T.);
#12165=EDGE_CURVE('',#9391,#9389,#436,.T.);
#12166=EDGE_CURVE('',#9392,#9390,#437,.T.);
#12167=EDGE_CURVE('',#9393,#9394,#5606,.T.);
#12168=EDGE_CURVE('',#9393,#9391,#438,.T.);
#12169=EDGE_CURVE('',#9394,#9392,#439,.T.);
#12170=EDGE_CURVE('',#9395,#9396,#5607,.T.);
#12171=EDGE_CURVE('',#9395,#9393,#440,.T.);
#12172=EDGE_CURVE('',#9396,#9394,#441,.T.);
#12173=EDGE_CURVE('',#9397,#9398,#5608,.T.);
#12174=EDGE_CURVE('',#9397,#9395,#442,.T.);
#12175=EDGE_CURVE('',#9398,#9396,#443,.T.);
#12176=EDGE_CURVE('',#9399,#9400,#5609,.T.);
#12177=EDGE_CURVE('',#9399,#9397,#444,.T.);
#12178=EDGE_CURVE('',#9400,#9398,#445,.T.);
#12179=EDGE_CURVE('',#9401,#9402,#5610,.T.);
#12180=EDGE_CURVE('',#9401,#9399,#446,.T.);
#12181=EDGE_CURVE('',#9402,#9400,#447,.T.);
#12182=EDGE_CURVE('',#9403,#9404,#5611,.T.);
#12183=EDGE_CURVE('',#9403,#9401,#448,.T.);
#12184=EDGE_CURVE('',#9404,#9402,#449,.T.);
#12185=EDGE_CURVE('',#9405,#9406,#5612,.T.);
#12186=EDGE_CURVE('',#9405,#9403,#450,.T.);
#12187=EDGE_CURVE('',#9406,#9404,#451,.T.);
#12188=EDGE_CURVE('',#9407,#9408,#5613,.T.);
#12189=EDGE_CURVE('',#9407,#9405,#452,.T.);
#12190=EDGE_CURVE('',#9408,#9406,#453,.T.);
#12191=EDGE_CURVE('',#9409,#9410,#5614,.T.);
#12192=EDGE_CURVE('',#9409,#9407,#454,.T.);
#12193=EDGE_CURVE('',#9410,#9408,#455,.T.);
#12194=EDGE_CURVE('',#9411,#9412,#5615,.T.);
#12195=EDGE_CURVE('',#9411,#9409,#456,.T.);
#12196=EDGE_CURVE('',#9412,#9410,#457,.T.);
#12197=EDGE_CURVE('',#9413,#9414,#5616,.T.);
#12198=EDGE_CURVE('',#9413,#9411,#458,.T.);
#12199=EDGE_CURVE('',#9414,#9412,#459,.T.);
#12200=EDGE_CURVE('',#9415,#9416,#5617,.T.);
#12201=EDGE_CURVE('',#9415,#9413,#460,.T.);
#12202=EDGE_CURVE('',#9416,#9414,#461,.T.);
#12203=EDGE_CURVE('',#9417,#9418,#5618,.T.);
#12204=EDGE_CURVE('',#9417,#9415,#462,.T.);
#12205=EDGE_CURVE('',#9418,#9416,#463,.T.);
#12206=EDGE_CURVE('',#9419,#9420,#5619,.T.);
#12207=EDGE_CURVE('',#9419,#9417,#464,.T.);
#12208=EDGE_CURVE('',#9420,#9418,#465,.T.);
#12209=EDGE_CURVE('',#9421,#9422,#5620,.T.);
#12210=EDGE_CURVE('',#9421,#9419,#466,.T.);
#12211=EDGE_CURVE('',#9422,#9420,#467,.T.);
#12212=EDGE_CURVE('',#9423,#9424,#5621,.T.);
#12213=EDGE_CURVE('',#9423,#9421,#468,.T.);
#12214=EDGE_CURVE('',#9424,#9422,#469,.T.);
#12215=EDGE_CURVE('',#9425,#9426,#5622,.T.);
#12216=EDGE_CURVE('',#9425,#9423,#470,.T.);
#12217=EDGE_CURVE('',#9426,#9424,#471,.T.);
#12218=EDGE_CURVE('',#9427,#9428,#5623,.T.);
#12219=EDGE_CURVE('',#9427,#9425,#472,.T.);
#12220=EDGE_CURVE('',#9428,#9426,#473,.T.);
#12221=EDGE_CURVE('',#9429,#9430,#5624,.T.);
#12222=EDGE_CURVE('',#9429,#9427,#474,.T.);
#12223=EDGE_CURVE('',#9430,#9428,#475,.T.);
#12224=EDGE_CURVE('',#9431,#9432,#5625,.T.);
#12225=EDGE_CURVE('',#9431,#9429,#476,.T.);
#12226=EDGE_CURVE('',#9432,#9430,#477,.T.);
#12227=EDGE_CURVE('',#9433,#9434,#5626,.T.);
#12228=EDGE_CURVE('',#9433,#9431,#478,.T.);
#12229=EDGE_CURVE('',#9434,#9432,#479,.T.);
#12230=EDGE_CURVE('',#9435,#9436,#5627,.T.);
#12231=EDGE_CURVE('',#9435,#9433,#480,.T.);
#12232=EDGE_CURVE('',#9436,#9434,#481,.T.);
#12233=EDGE_CURVE('',#9437,#9438,#5628,.T.);
#12234=EDGE_CURVE('',#9437,#9435,#482,.T.);
#12235=EDGE_CURVE('',#9438,#9436,#483,.T.);
#12236=EDGE_CURVE('',#9439,#9440,#5629,.T.);
#12237=EDGE_CURVE('',#9439,#9437,#484,.T.);
#12238=EDGE_CURVE('',#9440,#9438,#485,.T.);
#12239=EDGE_CURVE('',#9441,#9442,#5630,.T.);
#12240=EDGE_CURVE('',#9441,#9439,#486,.T.);
#12241=EDGE_CURVE('',#9442,#9440,#487,.T.);
#12242=EDGE_CURVE('',#9443,#9444,#5631,.T.);
#12243=EDGE_CURVE('',#9443,#9441,#488,.T.);
#12244=EDGE_CURVE('',#9444,#9442,#489,.T.);
#12245=EDGE_CURVE('',#9445,#9446,#5632,.T.);
#12246=EDGE_CURVE('',#9445,#9443,#490,.T.);
#12247=EDGE_CURVE('',#9446,#9444,#491,.T.);
#12248=EDGE_CURVE('',#9447,#9448,#5633,.T.);
#12249=EDGE_CURVE('',#9447,#9445,#492,.T.);
#12250=EDGE_CURVE('',#9448,#9446,#493,.T.);
#12251=EDGE_CURVE('',#9449,#9450,#5634,.T.);
#12252=EDGE_CURVE('',#9449,#9447,#494,.T.);
#12253=EDGE_CURVE('',#9450,#9448,#495,.T.);
#12254=EDGE_CURVE('',#9451,#9452,#5635,.T.);
#12255=EDGE_CURVE('',#9451,#9449,#496,.T.);
#12256=EDGE_CURVE('',#9452,#9450,#497,.T.);
#12257=EDGE_CURVE('',#9453,#9454,#5636,.T.);
#12258=EDGE_CURVE('',#9453,#9451,#498,.T.);
#12259=EDGE_CURVE('',#9454,#9452,#499,.T.);
#12260=EDGE_CURVE('',#9455,#9456,#5637,.T.);
#12261=EDGE_CURVE('',#9455,#9453,#500,.T.);
#12262=EDGE_CURVE('',#9456,#9454,#501,.T.);
#12263=EDGE_CURVE('',#9457,#9458,#5638,.T.);
#12264=EDGE_CURVE('',#9457,#9455,#502,.T.);
#12265=EDGE_CURVE('',#9458,#9456,#503,.T.);
#12266=EDGE_CURVE('',#9459,#9460,#5639,.T.);
#12267=EDGE_CURVE('',#9459,#9457,#504,.T.);
#12268=EDGE_CURVE('',#9460,#9458,#505,.T.);
#12269=EDGE_CURVE('',#9461,#9462,#5640,.T.);
#12270=EDGE_CURVE('',#9461,#9459,#506,.T.);
#12271=EDGE_CURVE('',#9462,#9460,#507,.T.);
#12272=EDGE_CURVE('',#9463,#9464,#5641,.T.);
#12273=EDGE_CURVE('',#9463,#9461,#508,.T.);
#12274=EDGE_CURVE('',#9464,#9462,#509,.T.);
#12275=EDGE_CURVE('',#9465,#9466,#5642,.T.);
#12276=EDGE_CURVE('',#9465,#9463,#510,.T.);
#12277=EDGE_CURVE('',#9466,#9464,#511,.T.);
#12278=EDGE_CURVE('',#9467,#9468,#5643,.T.);
#12279=EDGE_CURVE('',#9467,#9465,#512,.T.);
#12280=EDGE_CURVE('',#9468,#9466,#513,.T.);
#12281=EDGE_CURVE('',#9469,#9469,#3867,.T.);
#12282=EDGE_CURVE('',#9469,#9470,#5644,.T.);
#12283=EDGE_CURVE('',#9470,#9470,#3868,.T.);
#12284=EDGE_CURVE('',#9469,#9471,#5645,.T.);
#12285=EDGE_CURVE('',#9471,#9471,#3869,.T.);
#12286=EDGE_CURVE('',#9472,#9472,#3870,.T.);
#12287=EDGE_CURVE('',#9472,#9473,#5646,.T.);
#12288=EDGE_CURVE('',#9473,#9473,#3871,.T.);
#12289=EDGE_CURVE('',#9473,#9474,#5647,.T.);
#12290=EDGE_CURVE('',#9474,#9474,#3872,.T.);
#12291=EDGE_CURVE('',#9270,#9475,#514,.T.);
#12292=EDGE_CURVE('',#9219,#9269,#515,.T.);
#12293=EDGE_CURVE('',#9475,#9217,#3873,.T.);
#12294=EDGE_CURVE('',#9476,#9467,#516,.T.);
#12295=EDGE_CURVE('',#9017,#9476,#517,.T.);
#12296=EDGE_CURVE('',#9477,#9468,#518,.T.);
#12297=EDGE_CURVE('',#9476,#9477,#3874,.T.);
#12298=EDGE_CURVE('',#9247,#9244,#519,.F.);
#12299=EDGE_CURVE('',#9242,#9478,#3875,.F.);
#12300=EDGE_CURVE('',#9478,#9248,#520,.F.);
#12301=EDGE_CURVE('',#9479,#9266,#521,.T.);
#12302=EDGE_CURVE('',#9243,#9478,#522,.F.);
#12303=EDGE_CURVE('',#9479,#9225,#523,.F.);
#12304=EDGE_CURVE('',#9224,#9480,#524,.F.);
#12305=EDGE_CURVE('',#9480,#9479,#3876,.T.);
#12306=EDGE_CURVE('',#9480,#9265,#525,.T.);
#12307=EDGE_CURVE('',#9477,#9018,#526,.T.);
#12308=EDGE_CURVE('',#9218,#9475,#527,.T.);
#16451=ORIENTED_EDGE('',*,*,#11609,.F.);
#16452=ORIENTED_EDGE('',*,*,#11610,.T.);
#16453=ORIENTED_EDGE('',*,*,#11611,.F.);
#16454=ORIENTED_EDGE('',*,*,#11612,.T.);
#16455=ORIENTED_EDGE('',*,*,#11613,.F.);
#16456=ORIENTED_EDGE('',*,*,#11614,.T.);
#16457=ORIENTED_EDGE('',*,*,#11609,.T.);
#16458=ORIENTED_EDGE('',*,*,#11615,.T.);
#16459=ORIENTED_EDGE('',*,*,#11616,.F.);
#16460=ORIENTED_EDGE('',*,*,#11617,.T.);
#16461=ORIENTED_EDGE('',*,*,#11613,.T.);
#16462=ORIENTED_EDGE('',*,*,#11618,.T.);
#16463=ORIENTED_EDGE('',*,*,#11619,.F.);
#16464=ORIENTED_EDGE('',*,*,#11620,.T.);
#16465=ORIENTED_EDGE('',*,*,#11616,.T.);
#16466=ORIENTED_EDGE('',*,*,#11621,.T.);
#16467=ORIENTED_EDGE('',*,*,#11622,.F.);
#16468=ORIENTED_EDGE('',*,*,#11623,.T.);
#16469=ORIENTED_EDGE('',*,*,#11619,.T.);
#16470=ORIENTED_EDGE('',*,*,#11624,.T.);
#16471=ORIENTED_EDGE('',*,*,#11625,.F.);
#16472=ORIENTED_EDGE('',*,*,#11626,.T.);
#16473=ORIENTED_EDGE('',*,*,#11622,.T.);
#16474=ORIENTED_EDGE('',*,*,#11627,.T.);
#16475=ORIENTED_EDGE('',*,*,#11628,.F.);
#16476=ORIENTED_EDGE('',*,*,#11629,.T.);
#16477=ORIENTED_EDGE('',*,*,#11625,.T.);
#16478=ORIENTED_EDGE('',*,*,#11630,.T.);
#16479=ORIENTED_EDGE('',*,*,#11631,.F.);
#16480=ORIENTED_EDGE('',*,*,#11632,.T.);
#16481=ORIENTED_EDGE('',*,*,#11628,.T.);
#16482=ORIENTED_EDGE('',*,*,#11633,.T.);
#16483=ORIENTED_EDGE('',*,*,#11634,.F.);
#16484=ORIENTED_EDGE('',*,*,#11635,.T.);
#16485=ORIENTED_EDGE('',*,*,#11631,.T.);
#16486=ORIENTED_EDGE('',*,*,#11636,.T.);
#16487=ORIENTED_EDGE('',*,*,#11637,.F.);
#16488=ORIENTED_EDGE('',*,*,#11638,.T.);
#16489=ORIENTED_EDGE('',*,*,#11634,.T.);
#16490=ORIENTED_EDGE('',*,*,#11639,.T.);
#16491=ORIENTED_EDGE('',*,*,#11640,.F.);
#16492=ORIENTED_EDGE('',*,*,#11641,.T.);
#16493=ORIENTED_EDGE('',*,*,#11637,.T.);
#16494=ORIENTED_EDGE('',*,*,#11642,.T.);
#16495=ORIENTED_EDGE('',*,*,#11643,.F.);
#16496=ORIENTED_EDGE('',*,*,#11644,.T.);
#16497=ORIENTED_EDGE('',*,*,#11640,.T.);
#16498=ORIENTED_EDGE('',*,*,#11645,.T.);
#16499=ORIENTED_EDGE('',*,*,#11646,.F.);
#16500=ORIENTED_EDGE('',*,*,#11647,.T.);
#16501=ORIENTED_EDGE('',*,*,#11643,.T.);
#16502=ORIENTED_EDGE('',*,*,#11648,.T.);
#16503=ORIENTED_EDGE('',*,*,#11649,.F.);
#16504=ORIENTED_EDGE('',*,*,#11650,.T.);
#16505=ORIENTED_EDGE('',*,*,#11646,.T.);
#16506=ORIENTED_EDGE('',*,*,#11651,.T.);
#16507=ORIENTED_EDGE('',*,*,#11652,.F.);
#16508=ORIENTED_EDGE('',*,*,#11653,.T.);
#16509=ORIENTED_EDGE('',*,*,#11649,.T.);
#16510=ORIENTED_EDGE('',*,*,#11654,.T.);
#16511=ORIENTED_EDGE('',*,*,#11655,.F.);
#16512=ORIENTED_EDGE('',*,*,#11656,.T.);
#16513=ORIENTED_EDGE('',*,*,#11652,.T.);
#16514=ORIENTED_EDGE('',*,*,#11657,.T.);
#16515=ORIENTED_EDGE('',*,*,#11658,.F.);
#16516=ORIENTED_EDGE('',*,*,#11659,.T.);
#16517=ORIENTED_EDGE('',*,*,#11655,.T.);
#16518=ORIENTED_EDGE('',*,*,#11660,.T.);
#16519=ORIENTED_EDGE('',*,*,#11661,.F.);
#16520=ORIENTED_EDGE('',*,*,#11662,.T.);
#16521=ORIENTED_EDGE('',*,*,#11658,.T.);
#16522=ORIENTED_EDGE('',*,*,#11663,.T.);
#16523=ORIENTED_EDGE('',*,*,#11664,.F.);
#16524=ORIENTED_EDGE('',*,*,#11665,.T.);
#16525=ORIENTED_EDGE('',*,*,#11661,.T.);
#16526=ORIENTED_EDGE('',*,*,#11666,.T.);
#16527=ORIENTED_EDGE('',*,*,#11667,.F.);
#16528=ORIENTED_EDGE('',*,*,#11668,.T.);
#16529=ORIENTED_EDGE('',*,*,#11664,.T.);
#16530=ORIENTED_EDGE('',*,*,#11669,.T.);
#16531=ORIENTED_EDGE('',*,*,#11670,.F.);
#16532=ORIENTED_EDGE('',*,*,#11671,.T.);
#16533=ORIENTED_EDGE('',*,*,#11667,.T.);
#16534=ORIENTED_EDGE('',*,*,#11672,.T.);
#16535=ORIENTED_EDGE('',*,*,#11673,.F.);
#16536=ORIENTED_EDGE('',*,*,#11674,.T.);
#16537=ORIENTED_EDGE('',*,*,#11670,.T.);
#16538=ORIENTED_EDGE('',*,*,#11675,.T.);
#16539=ORIENTED_EDGE('',*,*,#11676,.F.);
#16540=ORIENTED_EDGE('',*,*,#11677,.T.);
#16541=ORIENTED_EDGE('',*,*,#11673,.T.);
#16542=ORIENTED_EDGE('',*,*,#11678,.T.);
#16543=ORIENTED_EDGE('',*,*,#11679,.F.);
#16544=ORIENTED_EDGE('',*,*,#11680,.T.);
#16545=ORIENTED_EDGE('',*,*,#11676,.T.);
#16546=ORIENTED_EDGE('',*,*,#11681,.T.);
#16547=ORIENTED_EDGE('',*,*,#11682,.F.);
#16548=ORIENTED_EDGE('',*,*,#11683,.T.);
#16549=ORIENTED_EDGE('',*,*,#11679,.T.);
#16550=ORIENTED_EDGE('',*,*,#11684,.T.);
#16551=ORIENTED_EDGE('',*,*,#11685,.F.);
#16552=ORIENTED_EDGE('',*,*,#11686,.T.);
#16553=ORIENTED_EDGE('',*,*,#11682,.T.);
#16554=ORIENTED_EDGE('',*,*,#11687,.T.);
#16555=ORIENTED_EDGE('',*,*,#11688,.F.);
#16556=ORIENTED_EDGE('',*,*,#11689,.T.);
#16557=ORIENTED_EDGE('',*,*,#11685,.T.);
#16558=ORIENTED_EDGE('',*,*,#11690,.T.);
#16559=ORIENTED_EDGE('',*,*,#11691,.F.);
#16560=ORIENTED_EDGE('',*,*,#11692,.T.);
#16561=ORIENTED_EDGE('',*,*,#11688,.T.);
#16562=ORIENTED_EDGE('',*,*,#11693,.T.);
#16563=ORIENTED_EDGE('',*,*,#11694,.F.);
#16564=ORIENTED_EDGE('',*,*,#11695,.T.);
#16565=ORIENTED_EDGE('',*,*,#11691,.T.);
#16566=ORIENTED_EDGE('',*,*,#11696,.T.);
#16567=ORIENTED_EDGE('',*,*,#11697,.F.);
#16568=ORIENTED_EDGE('',*,*,#11698,.T.);
#16569=ORIENTED_EDGE('',*,*,#11694,.T.);
#16570=ORIENTED_EDGE('',*,*,#11699,.T.);
#16571=ORIENTED_EDGE('',*,*,#11700,.F.);
#16572=ORIENTED_EDGE('',*,*,#11701,.T.);
#16573=ORIENTED_EDGE('',*,*,#11697,.T.);
#16574=ORIENTED_EDGE('',*,*,#11702,.T.);
#16575=ORIENTED_EDGE('',*,*,#11703,.F.);
#16576=ORIENTED_EDGE('',*,*,#11704,.T.);
#16577=ORIENTED_EDGE('',*,*,#11700,.T.);
#16578=ORIENTED_EDGE('',*,*,#11705,.T.);
#16579=ORIENTED_EDGE('',*,*,#11706,.F.);
#16580=ORIENTED_EDGE('',*,*,#11707,.T.);
#16581=ORIENTED_EDGE('',*,*,#11703,.T.);
#16582=ORIENTED_EDGE('',*,*,#11708,.T.);
#16583=ORIENTED_EDGE('',*,*,#11709,.F.);
#16584=ORIENTED_EDGE('',*,*,#11710,.T.);
#16585=ORIENTED_EDGE('',*,*,#11706,.T.);
#16586=ORIENTED_EDGE('',*,*,#11711,.T.);
#16587=ORIENTED_EDGE('',*,*,#11712,.F.);
#16588=ORIENTED_EDGE('',*,*,#11713,.T.);
#16589=ORIENTED_EDGE('',*,*,#11709,.T.);
#16590=ORIENTED_EDGE('',*,*,#11714,.T.);
#16591=ORIENTED_EDGE('',*,*,#11715,.F.);
#16592=ORIENTED_EDGE('',*,*,#11716,.T.);
#16593=ORIENTED_EDGE('',*,*,#11712,.T.);
#16594=ORIENTED_EDGE('',*,*,#11717,.T.);
#16595=ORIENTED_EDGE('',*,*,#11718,.F.);
#16596=ORIENTED_EDGE('',*,*,#11719,.T.);
#16597=ORIENTED_EDGE('',*,*,#11715,.T.);
#16598=ORIENTED_EDGE('',*,*,#11720,.T.);
#16599=ORIENTED_EDGE('',*,*,#11721,.F.);
#16600=ORIENTED_EDGE('',*,*,#11722,.T.);
#16601=ORIENTED_EDGE('',*,*,#11718,.T.);
#16602=ORIENTED_EDGE('',*,*,#11723,.T.);
#16603=ORIENTED_EDGE('',*,*,#11724,.F.);
#16604=ORIENTED_EDGE('',*,*,#11725,.T.);
#16605=ORIENTED_EDGE('',*,*,#11721,.T.);
#16606=ORIENTED_EDGE('',*,*,#11726,.T.);
#16607=ORIENTED_EDGE('',*,*,#11727,.F.);
#16608=ORIENTED_EDGE('',*,*,#11728,.T.);
#16609=ORIENTED_EDGE('',*,*,#11724,.T.);
#16610=ORIENTED_EDGE('',*,*,#11729,.T.);
#16611=ORIENTED_EDGE('',*,*,#11730,.F.);
#16612=ORIENTED_EDGE('',*,*,#11731,.T.);
#16613=ORIENTED_EDGE('',*,*,#11727,.T.);
#16614=ORIENTED_EDGE('',*,*,#11732,.T.);
#16615=ORIENTED_EDGE('',*,*,#11733,.F.);
#16616=ORIENTED_EDGE('',*,*,#11734,.T.);
#16617=ORIENTED_EDGE('',*,*,#11730,.T.);
#16618=ORIENTED_EDGE('',*,*,#11735,.T.);
#16619=ORIENTED_EDGE('',*,*,#11736,.F.);
#16620=ORIENTED_EDGE('',*,*,#11737,.T.);
#16621=ORIENTED_EDGE('',*,*,#11733,.T.);
#16622=ORIENTED_EDGE('',*,*,#11738,.T.);
#16623=ORIENTED_EDGE('',*,*,#11739,.F.);
#16624=ORIENTED_EDGE('',*,*,#11740,.T.);
#16625=ORIENTED_EDGE('',*,*,#11736,.T.);
#16626=ORIENTED_EDGE('',*,*,#11741,.T.);
#16627=ORIENTED_EDGE('',*,*,#11742,.F.);
#16628=ORIENTED_EDGE('',*,*,#11743,.T.);
#16629=ORIENTED_EDGE('',*,*,#11739,.T.);
#16630=ORIENTED_EDGE('',*,*,#11744,.T.);
#16631=ORIENTED_EDGE('',*,*,#11745,.F.);
#16632=ORIENTED_EDGE('',*,*,#11746,.T.);
#16633=ORIENTED_EDGE('',*,*,#11742,.T.);
#16634=ORIENTED_EDGE('',*,*,#11747,.T.);
#16635=ORIENTED_EDGE('',*,*,#11748,.F.);
#16636=ORIENTED_EDGE('',*,*,#11749,.T.);
#16637=ORIENTED_EDGE('',*,*,#11745,.T.);
#16638=ORIENTED_EDGE('',*,*,#11750,.T.);
#16639=ORIENTED_EDGE('',*,*,#11751,.F.);
#16640=ORIENTED_EDGE('',*,*,#11752,.T.);
#16641=ORIENTED_EDGE('',*,*,#11748,.T.);
#16642=ORIENTED_EDGE('',*,*,#11753,.T.);
#16643=ORIENTED_EDGE('',*,*,#11754,.F.);
#16644=ORIENTED_EDGE('',*,*,#11755,.T.);
#16645=ORIENTED_EDGE('',*,*,#11751,.T.);
#16646=ORIENTED_EDGE('',*,*,#11756,.T.);
#16647=ORIENTED_EDGE('',*,*,#11757,.F.);
#16648=ORIENTED_EDGE('',*,*,#11758,.T.);
#16649=ORIENTED_EDGE('',*,*,#11754,.T.);
#16650=ORIENTED_EDGE('',*,*,#11759,.T.);
#16651=ORIENTED_EDGE('',*,*,#11760,.F.);
#16652=ORIENTED_EDGE('',*,*,#11761,.T.);
#16653=ORIENTED_EDGE('',*,*,#11757,.T.);
#16654=ORIENTED_EDGE('',*,*,#11762,.T.);
#16655=ORIENTED_EDGE('',*,*,#11763,.F.);
#16656=ORIENTED_EDGE('',*,*,#11764,.T.);
#16657=ORIENTED_EDGE('',*,*,#11760,.T.);
#16658=ORIENTED_EDGE('',*,*,#11765,.T.);
#16659=ORIENTED_EDGE('',*,*,#11766,.F.);
#16660=ORIENTED_EDGE('',*,*,#11767,.T.);
#16661=ORIENTED_EDGE('',*,*,#11763,.T.);
#16662=ORIENTED_EDGE('',*,*,#11768,.T.);
#16663=ORIENTED_EDGE('',*,*,#11769,.F.);
#16664=ORIENTED_EDGE('',*,*,#11770,.T.);
#16665=ORIENTED_EDGE('',*,*,#11766,.T.);
#16666=ORIENTED_EDGE('',*,*,#11771,.T.);
#16667=ORIENTED_EDGE('',*,*,#11772,.F.);
#16668=ORIENTED_EDGE('',*,*,#11773,.T.);
#16669=ORIENTED_EDGE('',*,*,#11769,.T.);
#16670=ORIENTED_EDGE('',*,*,#11774,.T.);
#16671=ORIENTED_EDGE('',*,*,#11775,.F.);
#16672=ORIENTED_EDGE('',*,*,#11776,.T.);
#16673=ORIENTED_EDGE('',*,*,#11772,.T.);
#16674=ORIENTED_EDGE('',*,*,#11777,.T.);
#16675=ORIENTED_EDGE('',*,*,#11778,.F.);
#16676=ORIENTED_EDGE('',*,*,#11779,.T.);
#16677=ORIENTED_EDGE('',*,*,#11775,.T.);
#16678=ORIENTED_EDGE('',*,*,#11780,.T.);
#16679=ORIENTED_EDGE('',*,*,#11781,.F.);
#16680=ORIENTED_EDGE('',*,*,#11782,.T.);
#16681=ORIENTED_EDGE('',*,*,#11778,.T.);
#16682=ORIENTED_EDGE('',*,*,#11783,.T.);
#16683=ORIENTED_EDGE('',*,*,#11784,.F.);
#16684=ORIENTED_EDGE('',*,*,#11785,.T.);
#16685=ORIENTED_EDGE('',*,*,#11781,.T.);
#16686=ORIENTED_EDGE('',*,*,#11786,.T.);
#16687=ORIENTED_EDGE('',*,*,#11787,.F.);
#16688=ORIENTED_EDGE('',*,*,#11788,.T.);
#16689=ORIENTED_EDGE('',*,*,#11784,.T.);
#16690=ORIENTED_EDGE('',*,*,#11789,.T.);
#16691=ORIENTED_EDGE('',*,*,#11790,.F.);
#16692=ORIENTED_EDGE('',*,*,#11791,.T.);
#16693=ORIENTED_EDGE('',*,*,#11787,.T.);
#16694=ORIENTED_EDGE('',*,*,#11792,.T.);
#16695=ORIENTED_EDGE('',*,*,#11793,.F.);
#16696=ORIENTED_EDGE('',*,*,#11794,.T.);
#16697=ORIENTED_EDGE('',*,*,#11790,.T.);
#16698=ORIENTED_EDGE('',*,*,#11795,.T.);
#16699=ORIENTED_EDGE('',*,*,#11796,.F.);
#16700=ORIENTED_EDGE('',*,*,#11797,.T.);
#16701=ORIENTED_EDGE('',*,*,#11793,.T.);
#16702=ORIENTED_EDGE('',*,*,#11798,.T.);
#16703=ORIENTED_EDGE('',*,*,#11799,.F.);
#16704=ORIENTED_EDGE('',*,*,#11800,.T.);
#16705=ORIENTED_EDGE('',*,*,#11796,.T.);
#16706=ORIENTED_EDGE('',*,*,#11801,.T.);
#16707=ORIENTED_EDGE('',*,*,#11802,.F.);
#16708=ORIENTED_EDGE('',*,*,#11803,.T.);
#16709=ORIENTED_EDGE('',*,*,#11799,.T.);
#16710=ORIENTED_EDGE('',*,*,#11804,.T.);
#16711=ORIENTED_EDGE('',*,*,#11805,.F.);
#16712=ORIENTED_EDGE('',*,*,#11806,.T.);
#16713=ORIENTED_EDGE('',*,*,#11802,.T.);
#16714=ORIENTED_EDGE('',*,*,#11807,.T.);
#16715=ORIENTED_EDGE('',*,*,#11808,.F.);
#16716=ORIENTED_EDGE('',*,*,#11809,.T.);
#16717=ORIENTED_EDGE('',*,*,#11805,.T.);
#16718=ORIENTED_EDGE('',*,*,#11810,.T.);
#16719=ORIENTED_EDGE('',*,*,#11811,.F.);
#16720=ORIENTED_EDGE('',*,*,#11812,.T.);
#16721=ORIENTED_EDGE('',*,*,#11808,.T.);
#16722=ORIENTED_EDGE('',*,*,#11813,.T.);
#16723=ORIENTED_EDGE('',*,*,#11814,.F.);
#16724=ORIENTED_EDGE('',*,*,#11815,.T.);
#16725=ORIENTED_EDGE('',*,*,#11811,.T.);
#16726=ORIENTED_EDGE('',*,*,#11816,.T.);
#16727=ORIENTED_EDGE('',*,*,#11817,.F.);
#16728=ORIENTED_EDGE('',*,*,#11818,.T.);
#16729=ORIENTED_EDGE('',*,*,#11814,.T.);
#16730=ORIENTED_EDGE('',*,*,#11819,.T.);
#16731=ORIENTED_EDGE('',*,*,#11820,.F.);
#16732=ORIENTED_EDGE('',*,*,#11821,.T.);
#16733=ORIENTED_EDGE('',*,*,#11817,.T.);
#16734=ORIENTED_EDGE('',*,*,#11822,.T.);
#16735=ORIENTED_EDGE('',*,*,#11823,.F.);
#16736=ORIENTED_EDGE('',*,*,#11824,.T.);
#16737=ORIENTED_EDGE('',*,*,#11820,.T.);
#16738=ORIENTED_EDGE('',*,*,#11825,.T.);
#16739=ORIENTED_EDGE('',*,*,#11826,.F.);
#16740=ORIENTED_EDGE('',*,*,#11827,.T.);
#16741=ORIENTED_EDGE('',*,*,#11823,.T.);
#16742=ORIENTED_EDGE('',*,*,#11828,.T.);
#16743=ORIENTED_EDGE('',*,*,#11829,.F.);
#16744=ORIENTED_EDGE('',*,*,#11830,.T.);
#16745=ORIENTED_EDGE('',*,*,#11826,.T.);
#16746=ORIENTED_EDGE('',*,*,#11831,.T.);
#16747=ORIENTED_EDGE('',*,*,#11832,.F.);
#16748=ORIENTED_EDGE('',*,*,#11833,.T.);
#16749=ORIENTED_EDGE('',*,*,#11829,.T.);
#16750=ORIENTED_EDGE('',*,*,#11834,.T.);
#16751=ORIENTED_EDGE('',*,*,#11835,.F.);
#16752=ORIENTED_EDGE('',*,*,#11836,.T.);
#16753=ORIENTED_EDGE('',*,*,#11832,.T.);
#16754=ORIENTED_EDGE('',*,*,#11837,.T.);
#16755=ORIENTED_EDGE('',*,*,#11838,.F.);
#16756=ORIENTED_EDGE('',*,*,#11839,.T.);
#16757=ORIENTED_EDGE('',*,*,#11835,.T.);
#16758=ORIENTED_EDGE('',*,*,#11840,.T.);
#16759=ORIENTED_EDGE('',*,*,#11841,.F.);
#16760=ORIENTED_EDGE('',*,*,#11842,.T.);
#16761=ORIENTED_EDGE('',*,*,#11838,.T.);
#16762=ORIENTED_EDGE('',*,*,#11843,.T.);
#16763=ORIENTED_EDGE('',*,*,#11844,.F.);
#16764=ORIENTED_EDGE('',*,*,#11845,.T.);
#16765=ORIENTED_EDGE('',*,*,#11841,.T.);
#16766=ORIENTED_EDGE('',*,*,#11846,.T.);
#16767=ORIENTED_EDGE('',*,*,#11847,.F.);
#16768=ORIENTED_EDGE('',*,*,#11848,.T.);
#16769=ORIENTED_EDGE('',*,*,#11844,.T.);
#16770=ORIENTED_EDGE('',*,*,#11849,.T.);
#16771=ORIENTED_EDGE('',*,*,#11850,.F.);
#16772=ORIENTED_EDGE('',*,*,#11851,.T.);
#16773=ORIENTED_EDGE('',*,*,#11847,.T.);
#16774=ORIENTED_EDGE('',*,*,#11852,.T.);
#16775=ORIENTED_EDGE('',*,*,#11853,.F.);
#16776=ORIENTED_EDGE('',*,*,#11854,.T.);
#16777=ORIENTED_EDGE('',*,*,#11850,.T.);
#16778=ORIENTED_EDGE('',*,*,#11855,.T.);
#16779=ORIENTED_EDGE('',*,*,#11856,.F.);
#16780=ORIENTED_EDGE('',*,*,#11857,.T.);
#16781=ORIENTED_EDGE('',*,*,#11853,.T.);
#16782=ORIENTED_EDGE('',*,*,#11858,.T.);
#16783=ORIENTED_EDGE('',*,*,#11859,.F.);
#16784=ORIENTED_EDGE('',*,*,#11860,.T.);
#16785=ORIENTED_EDGE('',*,*,#11856,.T.);
#16786=ORIENTED_EDGE('',*,*,#11861,.T.);
#16787=ORIENTED_EDGE('',*,*,#11862,.F.);
#16788=ORIENTED_EDGE('',*,*,#11863,.T.);
#16789=ORIENTED_EDGE('',*,*,#11859,.T.);
#16790=ORIENTED_EDGE('',*,*,#11864,.T.);
#16791=ORIENTED_EDGE('',*,*,#11865,.F.);
#16792=ORIENTED_EDGE('',*,*,#11866,.T.);
#16793=ORIENTED_EDGE('',*,*,#11862,.T.);
#16794=ORIENTED_EDGE('',*,*,#11867,.T.);
#16795=ORIENTED_EDGE('',*,*,#11868,.F.);
#16796=ORIENTED_EDGE('',*,*,#11869,.T.);
#16797=ORIENTED_EDGE('',*,*,#11865,.T.);
#16798=ORIENTED_EDGE('',*,*,#11870,.T.);
#16799=ORIENTED_EDGE('',*,*,#11871,.F.);
#16800=ORIENTED_EDGE('',*,*,#11872,.T.);
#16801=ORIENTED_EDGE('',*,*,#11868,.T.);
#16802=ORIENTED_EDGE('',*,*,#11873,.T.);
#16803=ORIENTED_EDGE('',*,*,#11874,.F.);
#16804=ORIENTED_EDGE('',*,*,#11875,.T.);
#16805=ORIENTED_EDGE('',*,*,#11871,.T.);
#16806=ORIENTED_EDGE('',*,*,#11876,.T.);
#16807=ORIENTED_EDGE('',*,*,#11877,.F.);
#16808=ORIENTED_EDGE('',*,*,#11878,.T.);
#16809=ORIENTED_EDGE('',*,*,#11874,.T.);
#16810=ORIENTED_EDGE('',*,*,#11879,.T.);
#16811=ORIENTED_EDGE('',*,*,#11880,.F.);
#16812=ORIENTED_EDGE('',*,*,#11881,.T.);
#16813=ORIENTED_EDGE('',*,*,#11877,.T.);
#16814=ORIENTED_EDGE('',*,*,#11882,.T.);
#16815=ORIENTED_EDGE('',*,*,#11883,.F.);
#16816=ORIENTED_EDGE('',*,*,#11884,.T.);
#16817=ORIENTED_EDGE('',*,*,#11880,.T.);
#16818=ORIENTED_EDGE('',*,*,#11885,.T.);
#16819=ORIENTED_EDGE('',*,*,#11886,.F.);
#16820=ORIENTED_EDGE('',*,*,#11887,.T.);
#16821=ORIENTED_EDGE('',*,*,#11883,.T.);
#16822=ORIENTED_EDGE('',*,*,#11888,.T.);
#16823=ORIENTED_EDGE('',*,*,#11889,.F.);
#16824=ORIENTED_EDGE('',*,*,#11890,.T.);
#16825=ORIENTED_EDGE('',*,*,#11886,.T.);
#16826=ORIENTED_EDGE('',*,*,#11891,.T.);
#16827=ORIENTED_EDGE('',*,*,#11892,.F.);
#16828=ORIENTED_EDGE('',*,*,#11893,.T.);
#16829=ORIENTED_EDGE('',*,*,#11889,.T.);
#16830=ORIENTED_EDGE('',*,*,#11894,.T.);
#16831=ORIENTED_EDGE('',*,*,#11895,.F.);
#16832=ORIENTED_EDGE('',*,*,#11896,.T.);
#16833=ORIENTED_EDGE('',*,*,#11892,.T.);
#16834=ORIENTED_EDGE('',*,*,#11897,.T.);
#16835=ORIENTED_EDGE('',*,*,#11898,.F.);
#16836=ORIENTED_EDGE('',*,*,#11899,.T.);
#16837=ORIENTED_EDGE('',*,*,#11895,.T.);
#16838=ORIENTED_EDGE('',*,*,#11900,.T.);
#16839=ORIENTED_EDGE('',*,*,#11901,.F.);
#16840=ORIENTED_EDGE('',*,*,#11902,.T.);
#16841=ORIENTED_EDGE('',*,*,#11898,.T.);
#16842=ORIENTED_EDGE('',*,*,#11903,.T.);
#16843=ORIENTED_EDGE('',*,*,#11904,.F.);
#16844=ORIENTED_EDGE('',*,*,#11905,.T.);
#16845=ORIENTED_EDGE('',*,*,#11901,.T.);
#16846=ORIENTED_EDGE('',*,*,#11906,.T.);
#16847=ORIENTED_EDGE('',*,*,#11907,.F.);
#16848=ORIENTED_EDGE('',*,*,#11908,.T.);
#16849=ORIENTED_EDGE('',*,*,#11904,.T.);
#16850=ORIENTED_EDGE('',*,*,#11909,.T.);
#16851=ORIENTED_EDGE('',*,*,#11910,.F.);
#16852=ORIENTED_EDGE('',*,*,#11911,.T.);
#16853=ORIENTED_EDGE('',*,*,#11912,.T.);
#16854=ORIENTED_EDGE('',*,*,#11907,.T.);
#16855=ORIENTED_EDGE('',*,*,#11913,.T.);
#16856=ORIENTED_EDGE('',*,*,#11914,.F.);
#16857=ORIENTED_EDGE('',*,*,#11915,.T.);
#16858=ORIENTED_EDGE('',*,*,#11916,.T.);
#16859=ORIENTED_EDGE('',*,*,#11917,.F.);
#16860=ORIENTED_EDGE('',*,*,#11916,.F.);
#16861=ORIENTED_EDGE('',*,*,#11918,.T.);
#16862=ORIENTED_EDGE('',*,*,#11919,.T.);
#16863=ORIENTED_EDGE('',*,*,#11920,.T.);
#16864=ORIENTED_EDGE('',*,*,#11921,.F.);
#16865=ORIENTED_EDGE('',*,*,#11922,.T.);
#16866=ORIENTED_EDGE('',*,*,#11914,.T.);
#16867=ORIENTED_EDGE('',*,*,#11923,.T.);
#16868=ORIENTED_EDGE('',*,*,#11924,.F.);
#16869=ORIENTED_EDGE('',*,*,#11925,.T.);
#16870=ORIENTED_EDGE('',*,*,#11921,.T.);
#16871=ORIENTED_EDGE('',*,*,#11926,.T.);
#16872=ORIENTED_EDGE('',*,*,#11927,.F.);
#16873=ORIENTED_EDGE('',*,*,#11928,.T.);
#16874=ORIENTED_EDGE('',*,*,#11924,.T.);
#16875=ORIENTED_EDGE('',*,*,#11929,.T.);
#16876=ORIENTED_EDGE('',*,*,#11930,.F.);
#16877=ORIENTED_EDGE('',*,*,#11931,.T.);
#16878=ORIENTED_EDGE('',*,*,#11927,.T.);
#16879=ORIENTED_EDGE('',*,*,#11932,.T.);
#16880=ORIENTED_EDGE('',*,*,#11933,.F.);
#16881=ORIENTED_EDGE('',*,*,#11934,.T.);
#16882=ORIENTED_EDGE('',*,*,#11930,.T.);
#16883=ORIENTED_EDGE('',*,*,#11935,.T.);
#16884=ORIENTED_EDGE('',*,*,#11936,.F.);
#16885=ORIENTED_EDGE('',*,*,#11937,.T.);
#16886=ORIENTED_EDGE('',*,*,#11933,.T.);
#16887=ORIENTED_EDGE('',*,*,#11938,.T.);
#16888=ORIENTED_EDGE('',*,*,#11939,.F.);
#16889=ORIENTED_EDGE('',*,*,#11940,.T.);
#16890=ORIENTED_EDGE('',*,*,#11936,.T.);
#16891=ORIENTED_EDGE('',*,*,#11941,.T.);
#16892=ORIENTED_EDGE('',*,*,#11942,.F.);
#16893=ORIENTED_EDGE('',*,*,#11943,.T.);
#16894=ORIENTED_EDGE('',*,*,#11939,.T.);
#16895=ORIENTED_EDGE('',*,*,#11944,.T.);
#16896=ORIENTED_EDGE('',*,*,#11945,.F.);
#16897=ORIENTED_EDGE('',*,*,#11946,.F.);
#16898=ORIENTED_EDGE('',*,*,#11947,.T.);
#16899=ORIENTED_EDGE('',*,*,#11942,.T.);
#16900=ORIENTED_EDGE('',*,*,#11948,.T.);
#16901=ORIENTED_EDGE('',*,*,#11949,.F.);
#16902=ORIENTED_EDGE('',*,*,#11950,.T.);
#16903=ORIENTED_EDGE('',*,*,#11951,.F.);
#16904=ORIENTED_EDGE('',*,*,#11952,.F.);
#16905=ORIENTED_EDGE('',*,*,#11953,.F.);
#16906=ORIENTED_EDGE('',*,*,#11954,.T.);
#16907=ORIENTED_EDGE('',*,*,#11949,.T.);
#16908=ORIENTED_EDGE('',*,*,#11955,.F.);
#16909=ORIENTED_EDGE('',*,*,#11956,.F.);
#16910=ORIENTED_EDGE('',*,*,#11957,.T.);
#16911=ORIENTED_EDGE('',*,*,#11953,.T.);
#16912=ORIENTED_EDGE('',*,*,#11958,.F.);
#16913=ORIENTED_EDGE('',*,*,#11959,.F.);
#16914=ORIENTED_EDGE('',*,*,#11960,.T.);
#16915=ORIENTED_EDGE('',*,*,#11956,.T.);
#16916=ORIENTED_EDGE('',*,*,#11961,.F.);
#16917=ORIENTED_EDGE('',*,*,#11962,.F.);
#16918=ORIENTED_EDGE('',*,*,#11963,.T.);
#16919=ORIENTED_EDGE('',*,*,#11959,.T.);
#16920=ORIENTED_EDGE('',*,*,#11964,.F.);
#16921=ORIENTED_EDGE('',*,*,#11965,.F.);
#16922=ORIENTED_EDGE('',*,*,#11966,.T.);
#16923=ORIENTED_EDGE('',*,*,#11962,.T.);
#16924=ORIENTED_EDGE('',*,*,#11967,.F.);
#16925=ORIENTED_EDGE('',*,*,#11968,.F.);
#16926=ORIENTED_EDGE('',*,*,#11969,.T.);
#16927=ORIENTED_EDGE('',*,*,#11965,.T.);
#16928=ORIENTED_EDGE('',*,*,#11970,.F.);
#16929=ORIENTED_EDGE('',*,*,#11971,.F.);
#16930=ORIENTED_EDGE('',*,*,#11972,.T.);
#16931=ORIENTED_EDGE('',*,*,#11968,.T.);
#16932=ORIENTED_EDGE('',*,*,#11973,.F.);
#16933=ORIENTED_EDGE('',*,*,#11974,.F.);
#16934=ORIENTED_EDGE('',*,*,#11975,.T.);
#16935=ORIENTED_EDGE('',*,*,#11971,.T.);
#16936=ORIENTED_EDGE('',*,*,#11976,.F.);
#16937=ORIENTED_EDGE('',*,*,#11977,.F.);
#16938=ORIENTED_EDGE('',*,*,#11978,.T.);
#16939=ORIENTED_EDGE('',*,*,#11974,.T.);
#16940=ORIENTED_EDGE('',*,*,#11979,.F.);
#16941=ORIENTED_EDGE('',*,*,#11980,.F.);
#16942=ORIENTED_EDGE('',*,*,#11981,.T.);
#16943=ORIENTED_EDGE('',*,*,#11982,.T.);
#16944=ORIENTED_EDGE('',*,*,#11983,.F.);
#16945=ORIENTED_EDGE('',*,*,#11984,.F.);
#16946=ORIENTED_EDGE('',*,*,#11985,.T.);
#16947=ORIENTED_EDGE('',*,*,#11980,.T.);
#16948=ORIENTED_EDGE('',*,*,#11986,.F.);
#16949=ORIENTED_EDGE('',*,*,#11987,.F.);
#16950=ORIENTED_EDGE('',*,*,#11988,.T.);
#16951=ORIENTED_EDGE('',*,*,#11984,.T.);
#16952=ORIENTED_EDGE('',*,*,#11989,.F.);
#16953=ORIENTED_EDGE('',*,*,#11990,.F.);
#16954=ORIENTED_EDGE('',*,*,#11991,.T.);
#16955=ORIENTED_EDGE('',*,*,#11987,.T.);
#16956=ORIENTED_EDGE('',*,*,#11992,.F.);
#16957=ORIENTED_EDGE('',*,*,#11993,.F.);
#16958=ORIENTED_EDGE('',*,*,#11994,.T.);
#16959=ORIENTED_EDGE('',*,*,#11990,.T.);
#16960=ORIENTED_EDGE('',*,*,#11995,.F.);
#16961=ORIENTED_EDGE('',*,*,#11996,.F.);
#16962=ORIENTED_EDGE('',*,*,#11997,.T.);
#16963=ORIENTED_EDGE('',*,*,#11993,.T.);
#16964=ORIENTED_EDGE('',*,*,#11998,.F.);
#16965=ORIENTED_EDGE('',*,*,#11999,.F.);
#16966=ORIENTED_EDGE('',*,*,#12000,.T.);
#16967=ORIENTED_EDGE('',*,*,#11996,.T.);
#16968=ORIENTED_EDGE('',*,*,#12001,.F.);
#16969=ORIENTED_EDGE('',*,*,#12002,.F.);
#16970=ORIENTED_EDGE('',*,*,#12003,.T.);
#16971=ORIENTED_EDGE('',*,*,#11999,.T.);
#16972=ORIENTED_EDGE('',*,*,#12004,.F.);
#16973=ORIENTED_EDGE('',*,*,#12005,.F.);
#16974=ORIENTED_EDGE('',*,*,#12006,.T.);
#16975=ORIENTED_EDGE('',*,*,#12002,.T.);
#16976=ORIENTED_EDGE('',*,*,#12007,.F.);
#16977=ORIENTED_EDGE('',*,*,#12008,.F.);
#16978=ORIENTED_EDGE('',*,*,#12009,.T.);
#16979=ORIENTED_EDGE('',*,*,#12005,.T.);
#16980=ORIENTED_EDGE('',*,*,#12010,.F.);
#16981=ORIENTED_EDGE('',*,*,#12011,.F.);
#16982=ORIENTED_EDGE('',*,*,#12012,.T.);
#16983=ORIENTED_EDGE('',*,*,#12008,.T.);
#16984=ORIENTED_EDGE('',*,*,#12013,.F.);
#16985=ORIENTED_EDGE('',*,*,#12014,.F.);
#16986=ORIENTED_EDGE('',*,*,#12015,.T.);
#16987=ORIENTED_EDGE('',*,*,#12011,.T.);
#16988=ORIENTED_EDGE('',*,*,#12016,.F.);
#16989=ORIENTED_EDGE('',*,*,#12017,.F.);
#16990=ORIENTED_EDGE('',*,*,#12018,.T.);
#16991=ORIENTED_EDGE('',*,*,#12014,.T.);
#16992=ORIENTED_EDGE('',*,*,#12019,.F.);
#16993=ORIENTED_EDGE('',*,*,#12020,.F.);
#16994=ORIENTED_EDGE('',*,*,#12021,.T.);
#16995=ORIENTED_EDGE('',*,*,#12017,.T.);
#16996=ORIENTED_EDGE('',*,*,#12022,.F.);
#16997=ORIENTED_EDGE('',*,*,#12023,.F.);
#16998=ORIENTED_EDGE('',*,*,#12024,.T.);
#16999=ORIENTED_EDGE('',*,*,#12020,.T.);
#17000=ORIENTED_EDGE('',*,*,#12025,.F.);
#17001=ORIENTED_EDGE('',*,*,#12026,.F.);
#17002=ORIENTED_EDGE('',*,*,#12027,.T.);
#17003=ORIENTED_EDGE('',*,*,#12023,.T.);
#17004=ORIENTED_EDGE('',*,*,#12028,.F.);
#17005=ORIENTED_EDGE('',*,*,#12029,.F.);
#17006=ORIENTED_EDGE('',*,*,#12030,.T.);
#17007=ORIENTED_EDGE('',*,*,#12026,.T.);
#17008=ORIENTED_EDGE('',*,*,#12031,.F.);
#17009=ORIENTED_EDGE('',*,*,#12032,.F.);
#17010=ORIENTED_EDGE('',*,*,#12033,.T.);
#17011=ORIENTED_EDGE('',*,*,#12029,.T.);
#17012=ORIENTED_EDGE('',*,*,#12034,.F.);
#17013=ORIENTED_EDGE('',*,*,#12035,.F.);
#17014=ORIENTED_EDGE('',*,*,#12036,.T.);
#17015=ORIENTED_EDGE('',*,*,#12032,.T.);
#17016=ORIENTED_EDGE('',*,*,#12037,.F.);
#17017=ORIENTED_EDGE('',*,*,#12038,.F.);
#17018=ORIENTED_EDGE('',*,*,#12039,.T.);
#17019=ORIENTED_EDGE('',*,*,#12035,.T.);
#17020=ORIENTED_EDGE('',*,*,#12040,.F.);
#17021=ORIENTED_EDGE('',*,*,#12041,.F.);
#17022=ORIENTED_EDGE('',*,*,#12042,.T.);
#17023=ORIENTED_EDGE('',*,*,#12038,.T.);
#17024=ORIENTED_EDGE('',*,*,#12043,.F.);
#17025=ORIENTED_EDGE('',*,*,#12044,.F.);
#17026=ORIENTED_EDGE('',*,*,#12045,.T.);
#17027=ORIENTED_EDGE('',*,*,#12041,.T.);
#17028=ORIENTED_EDGE('',*,*,#12046,.F.);
#17029=ORIENTED_EDGE('',*,*,#12047,.F.);
#17030=ORIENTED_EDGE('',*,*,#12048,.T.);
#17031=ORIENTED_EDGE('',*,*,#12044,.T.);
#17032=ORIENTED_EDGE('',*,*,#12049,.F.);
#17033=ORIENTED_EDGE('',*,*,#12050,.F.);
#17034=ORIENTED_EDGE('',*,*,#12051,.T.);
#17035=ORIENTED_EDGE('',*,*,#12047,.T.);
#17036=ORIENTED_EDGE('',*,*,#12052,.F.);
#17037=ORIENTED_EDGE('',*,*,#12053,.F.);
#17038=ORIENTED_EDGE('',*,*,#12054,.T.);
#17039=ORIENTED_EDGE('',*,*,#12050,.T.);
#17040=ORIENTED_EDGE('',*,*,#12055,.F.);
#17041=ORIENTED_EDGE('',*,*,#12056,.F.);
#17042=ORIENTED_EDGE('',*,*,#12057,.T.);
#17043=ORIENTED_EDGE('',*,*,#12053,.T.);
#17044=ORIENTED_EDGE('',*,*,#12058,.F.);
#17045=ORIENTED_EDGE('',*,*,#12059,.F.);
#17046=ORIENTED_EDGE('',*,*,#12060,.T.);
#17047=ORIENTED_EDGE('',*,*,#12056,.T.);
#17048=ORIENTED_EDGE('',*,*,#12061,.F.);
#17049=ORIENTED_EDGE('',*,*,#12062,.F.);
#17050=ORIENTED_EDGE('',*,*,#12063,.T.);
#17051=ORIENTED_EDGE('',*,*,#12059,.T.);
#17052=ORIENTED_EDGE('',*,*,#12064,.F.);
#17053=ORIENTED_EDGE('',*,*,#12065,.F.);
#17054=ORIENTED_EDGE('',*,*,#12066,.T.);
#17055=ORIENTED_EDGE('',*,*,#12062,.T.);
#17056=ORIENTED_EDGE('',*,*,#12067,.F.);
#17057=ORIENTED_EDGE('',*,*,#12068,.F.);
#17058=ORIENTED_EDGE('',*,*,#12069,.T.);
#17059=ORIENTED_EDGE('',*,*,#12065,.T.);
#17060=ORIENTED_EDGE('',*,*,#12070,.F.);
#17061=ORIENTED_EDGE('',*,*,#12071,.F.);
#17062=ORIENTED_EDGE('',*,*,#12072,.T.);
#17063=ORIENTED_EDGE('',*,*,#12068,.T.);
#17064=ORIENTED_EDGE('',*,*,#12073,.F.);
#17065=ORIENTED_EDGE('',*,*,#12074,.F.);
#17066=ORIENTED_EDGE('',*,*,#12075,.T.);
#17067=ORIENTED_EDGE('',*,*,#12071,.T.);
#17068=ORIENTED_EDGE('',*,*,#12076,.F.);
#17069=ORIENTED_EDGE('',*,*,#12077,.F.);
#17070=ORIENTED_EDGE('',*,*,#12078,.T.);
#17071=ORIENTED_EDGE('',*,*,#12074,.T.);
#17072=ORIENTED_EDGE('',*,*,#12079,.F.);
#17073=ORIENTED_EDGE('',*,*,#12080,.F.);
#17074=ORIENTED_EDGE('',*,*,#12081,.T.);
#17075=ORIENTED_EDGE('',*,*,#12077,.T.);
#17076=ORIENTED_EDGE('',*,*,#12082,.F.);
#17077=ORIENTED_EDGE('',*,*,#12083,.F.);
#17078=ORIENTED_EDGE('',*,*,#12084,.T.);
#17079=ORIENTED_EDGE('',*,*,#12080,.T.);
#17080=ORIENTED_EDGE('',*,*,#12085,.F.);
#17081=ORIENTED_EDGE('',*,*,#12086,.F.);
#17082=ORIENTED_EDGE('',*,*,#12087,.T.);
#17083=ORIENTED_EDGE('',*,*,#12083,.T.);
#17084=ORIENTED_EDGE('',*,*,#12088,.F.);
#17085=ORIENTED_EDGE('',*,*,#12089,.F.);
#17086=ORIENTED_EDGE('',*,*,#12090,.T.);
#17087=ORIENTED_EDGE('',*,*,#12086,.T.);
#17088=ORIENTED_EDGE('',*,*,#12091,.F.);
#17089=ORIENTED_EDGE('',*,*,#12092,.F.);
#17090=ORIENTED_EDGE('',*,*,#12093,.T.);
#17091=ORIENTED_EDGE('',*,*,#12089,.T.);
#17092=ORIENTED_EDGE('',*,*,#12094,.F.);
#17093=ORIENTED_EDGE('',*,*,#12095,.F.);
#17094=ORIENTED_EDGE('',*,*,#12096,.T.);
#17095=ORIENTED_EDGE('',*,*,#12092,.T.);
#17096=ORIENTED_EDGE('',*,*,#12097,.F.);
#17097=ORIENTED_EDGE('',*,*,#12098,.F.);
#17098=ORIENTED_EDGE('',*,*,#12099,.T.);
#17099=ORIENTED_EDGE('',*,*,#12095,.T.);
#17100=ORIENTED_EDGE('',*,*,#12100,.F.);
#17101=ORIENTED_EDGE('',*,*,#12101,.F.);
#17102=ORIENTED_EDGE('',*,*,#12102,.T.);
#17103=ORIENTED_EDGE('',*,*,#12098,.T.);
#17104=ORIENTED_EDGE('',*,*,#12103,.F.);
#17105=ORIENTED_EDGE('',*,*,#12104,.F.);
#17106=ORIENTED_EDGE('',*,*,#12105,.T.);
#17107=ORIENTED_EDGE('',*,*,#12101,.T.);
#17108=ORIENTED_EDGE('',*,*,#12106,.F.);
#17109=ORIENTED_EDGE('',*,*,#12107,.F.);
#17110=ORIENTED_EDGE('',*,*,#12108,.T.);
#17111=ORIENTED_EDGE('',*,*,#12104,.T.);
#17112=ORIENTED_EDGE('',*,*,#12109,.F.);
#17113=ORIENTED_EDGE('',*,*,#12110,.F.);
#17114=ORIENTED_EDGE('',*,*,#12111,.T.);
#17115=ORIENTED_EDGE('',*,*,#12107,.T.);
#17116=ORIENTED_EDGE('',*,*,#12112,.F.);
#17117=ORIENTED_EDGE('',*,*,#12113,.F.);
#17118=ORIENTED_EDGE('',*,*,#12114,.T.);
#17119=ORIENTED_EDGE('',*,*,#12110,.T.);
#17120=ORIENTED_EDGE('',*,*,#12115,.F.);
#17121=ORIENTED_EDGE('',*,*,#12116,.F.);
#17122=ORIENTED_EDGE('',*,*,#12117,.T.);
#17123=ORIENTED_EDGE('',*,*,#12113,.T.);
#17124=ORIENTED_EDGE('',*,*,#12118,.F.);
#17125=ORIENTED_EDGE('',*,*,#12119,.F.);
#17126=ORIENTED_EDGE('',*,*,#12120,.T.);
#17127=ORIENTED_EDGE('',*,*,#12116,.T.);
#17128=ORIENTED_EDGE('',*,*,#12121,.F.);
#17129=ORIENTED_EDGE('',*,*,#12122,.F.);
#17130=ORIENTED_EDGE('',*,*,#12123,.T.);
#17131=ORIENTED_EDGE('',*,*,#12119,.T.);
#17132=ORIENTED_EDGE('',*,*,#12124,.F.);
#17133=ORIENTED_EDGE('',*,*,#12125,.F.);
#17134=ORIENTED_EDGE('',*,*,#12126,.T.);
#17135=ORIENTED_EDGE('',*,*,#12122,.T.);
#17136=ORIENTED_EDGE('',*,*,#12127,.F.);
#17137=ORIENTED_EDGE('',*,*,#12128,.F.);
#17138=ORIENTED_EDGE('',*,*,#12129,.T.);
#17139=ORIENTED_EDGE('',*,*,#12125,.T.);
#17140=ORIENTED_EDGE('',*,*,#12130,.F.);
#17141=ORIENTED_EDGE('',*,*,#12131,.F.);
#17142=ORIENTED_EDGE('',*,*,#12132,.T.);
#17143=ORIENTED_EDGE('',*,*,#12128,.T.);
#17144=ORIENTED_EDGE('',*,*,#12133,.F.);
#17145=ORIENTED_EDGE('',*,*,#12134,.F.);
#17146=ORIENTED_EDGE('',*,*,#12135,.T.);
#17147=ORIENTED_EDGE('',*,*,#12131,.T.);
#17148=ORIENTED_EDGE('',*,*,#12136,.F.);
#17149=ORIENTED_EDGE('',*,*,#12137,.F.);
#17150=ORIENTED_EDGE('',*,*,#12138,.T.);
#17151=ORIENTED_EDGE('',*,*,#12134,.T.);
#17152=ORIENTED_EDGE('',*,*,#12139,.F.);
#17153=ORIENTED_EDGE('',*,*,#12140,.F.);
#17154=ORIENTED_EDGE('',*,*,#12141,.T.);
#17155=ORIENTED_EDGE('',*,*,#12137,.T.);
#17156=ORIENTED_EDGE('',*,*,#12142,.F.);
#17157=ORIENTED_EDGE('',*,*,#12143,.F.);
#17158=ORIENTED_EDGE('',*,*,#12144,.T.);
#17159=ORIENTED_EDGE('',*,*,#12140,.T.);
#17160=ORIENTED_EDGE('',*,*,#12145,.F.);
#17161=ORIENTED_EDGE('',*,*,#12146,.F.);
#17162=ORIENTED_EDGE('',*,*,#12147,.T.);
#17163=ORIENTED_EDGE('',*,*,#12143,.T.);
#17164=ORIENTED_EDGE('',*,*,#12148,.F.);
#17165=ORIENTED_EDGE('',*,*,#12149,.F.);
#17166=ORIENTED_EDGE('',*,*,#12150,.T.);
#17167=ORIENTED_EDGE('',*,*,#12146,.T.);
#17168=ORIENTED_EDGE('',*,*,#12151,.F.);
#17169=ORIENTED_EDGE('',*,*,#12152,.F.);
#17170=ORIENTED_EDGE('',*,*,#12153,.T.);
#17171=ORIENTED_EDGE('',*,*,#12149,.T.);
#17172=ORIENTED_EDGE('',*,*,#12154,.F.);
#17173=ORIENTED_EDGE('',*,*,#12155,.F.);
#17174=ORIENTED_EDGE('',*,*,#12156,.T.);
#17175=ORIENTED_EDGE('',*,*,#12152,.T.);
#17176=ORIENTED_EDGE('',*,*,#12157,.F.);
#17177=ORIENTED_EDGE('',*,*,#12158,.F.);
#17178=ORIENTED_EDGE('',*,*,#12159,.T.);
#17179=ORIENTED_EDGE('',*,*,#12155,.T.);
#17180=ORIENTED_EDGE('',*,*,#12160,.F.);
#17181=ORIENTED_EDGE('',*,*,#12161,.F.);
#17182=ORIENTED_EDGE('',*,*,#12162,.T.);
#17183=ORIENTED_EDGE('',*,*,#12158,.T.);
#17184=ORIENTED_EDGE('',*,*,#12163,.F.);
#17185=ORIENTED_EDGE('',*,*,#12164,.F.);
#17186=ORIENTED_EDGE('',*,*,#12165,.T.);
#17187=ORIENTED_EDGE('',*,*,#12161,.T.);
#17188=ORIENTED_EDGE('',*,*,#12166,.F.);
#17189=ORIENTED_EDGE('',*,*,#12167,.F.);
#17190=ORIENTED_EDGE('',*,*,#12168,.T.);
#17191=ORIENTED_EDGE('',*,*,#12164,.T.);
#17192=ORIENTED_EDGE('',*,*,#12169,.F.);
#17193=ORIENTED_EDGE('',*,*,#12170,.F.);
#17194=ORIENTED_EDGE('',*,*,#12171,.T.);
#17195=ORIENTED_EDGE('',*,*,#12167,.T.);
#17196=ORIENTED_EDGE('',*,*,#12172,.F.);
#17197=ORIENTED_EDGE('',*,*,#12173,.F.);
#17198=ORIENTED_EDGE('',*,*,#12174,.T.);
#17199=ORIENTED_EDGE('',*,*,#12170,.T.);
#17200=ORIENTED_EDGE('',*,*,#12175,.F.);
#17201=ORIENTED_EDGE('',*,*,#12176,.F.);
#17202=ORIENTED_EDGE('',*,*,#12177,.T.);
#17203=ORIENTED_EDGE('',*,*,#12173,.T.);
#17204=ORIENTED_EDGE('',*,*,#12178,.F.);
#17205=ORIENTED_EDGE('',*,*,#12179,.F.);
#17206=ORIENTED_EDGE('',*,*,#12180,.T.);
#17207=ORIENTED_EDGE('',*,*,#12176,.T.);
#17208=ORIENTED_EDGE('',*,*,#12181,.F.);
#17209=ORIENTED_EDGE('',*,*,#12182,.F.);
#17210=ORIENTED_EDGE('',*,*,#12183,.T.);
#17211=ORIENTED_EDGE('',*,*,#12179,.T.);
#17212=ORIENTED_EDGE('',*,*,#12184,.F.);
#17213=ORIENTED_EDGE('',*,*,#12185,.F.);
#17214=ORIENTED_EDGE('',*,*,#12186,.T.);
#17215=ORIENTED_EDGE('',*,*,#12182,.T.);
#17216=ORIENTED_EDGE('',*,*,#12187,.F.);
#17217=ORIENTED_EDGE('',*,*,#12188,.F.);
#17218=ORIENTED_EDGE('',*,*,#12189,.T.);
#17219=ORIENTED_EDGE('',*,*,#12185,.T.);
#17220=ORIENTED_EDGE('',*,*,#12190,.F.);
#17221=ORIENTED_EDGE('',*,*,#12191,.F.);
#17222=ORIENTED_EDGE('',*,*,#12192,.T.);
#17223=ORIENTED_EDGE('',*,*,#12188,.T.);
#17224=ORIENTED_EDGE('',*,*,#12193,.F.);
#17225=ORIENTED_EDGE('',*,*,#12194,.F.);
#17226=ORIENTED_EDGE('',*,*,#12195,.T.);
#17227=ORIENTED_EDGE('',*,*,#12191,.T.);
#17228=ORIENTED_EDGE('',*,*,#12196,.F.);
#17229=ORIENTED_EDGE('',*,*,#12197,.F.);
#17230=ORIENTED_EDGE('',*,*,#12198,.T.);
#17231=ORIENTED_EDGE('',*,*,#12194,.T.);
#17232=ORIENTED_EDGE('',*,*,#12199,.F.);
#17233=ORIENTED_EDGE('',*,*,#12200,.F.);
#17234=ORIENTED_EDGE('',*,*,#12201,.T.);
#17235=ORIENTED_EDGE('',*,*,#12197,.T.);
#17236=ORIENTED_EDGE('',*,*,#12202,.F.);
#17237=ORIENTED_EDGE('',*,*,#12203,.F.);
#17238=ORIENTED_EDGE('',*,*,#12204,.T.);
#17239=ORIENTED_EDGE('',*,*,#12200,.T.);
#17240=ORIENTED_EDGE('',*,*,#12205,.F.);
#17241=ORIENTED_EDGE('',*,*,#12206,.F.);
#17242=ORIENTED_EDGE('',*,*,#12207,.T.);
#17243=ORIENTED_EDGE('',*,*,#12203,.T.);
#17244=ORIENTED_EDGE('',*,*,#12208,.F.);
#17245=ORIENTED_EDGE('',*,*,#12209,.F.);
#17246=ORIENTED_EDGE('',*,*,#12210,.T.);
#17247=ORIENTED_EDGE('',*,*,#12206,.T.);
#17248=ORIENTED_EDGE('',*,*,#12211,.F.);
#17249=ORIENTED_EDGE('',*,*,#12212,.F.);
#17250=ORIENTED_EDGE('',*,*,#12213,.T.);
#17251=ORIENTED_EDGE('',*,*,#12209,.T.);
#17252=ORIENTED_EDGE('',*,*,#12214,.F.);
#17253=ORIENTED_EDGE('',*,*,#12215,.F.);
#17254=ORIENTED_EDGE('',*,*,#12216,.T.);
#17255=ORIENTED_EDGE('',*,*,#12212,.T.);
#17256=ORIENTED_EDGE('',*,*,#12217,.F.);
#17257=ORIENTED_EDGE('',*,*,#12218,.F.);
#17258=ORIENTED_EDGE('',*,*,#12219,.T.);
#17259=ORIENTED_EDGE('',*,*,#12215,.T.);
#17260=ORIENTED_EDGE('',*,*,#12220,.F.);
#17261=ORIENTED_EDGE('',*,*,#12221,.F.);
#17262=ORIENTED_EDGE('',*,*,#12222,.T.);
#17263=ORIENTED_EDGE('',*,*,#12218,.T.);
#17264=ORIENTED_EDGE('',*,*,#12223,.F.);
#17265=ORIENTED_EDGE('',*,*,#12224,.F.);
#17266=ORIENTED_EDGE('',*,*,#12225,.T.);
#17267=ORIENTED_EDGE('',*,*,#12221,.T.);
#17268=ORIENTED_EDGE('',*,*,#12226,.F.);
#17269=ORIENTED_EDGE('',*,*,#12227,.F.);
#17270=ORIENTED_EDGE('',*,*,#12228,.T.);
#17271=ORIENTED_EDGE('',*,*,#12224,.T.);
#17272=ORIENTED_EDGE('',*,*,#12229,.F.);
#17273=ORIENTED_EDGE('',*,*,#12230,.F.);
#17274=ORIENTED_EDGE('',*,*,#12231,.T.);
#17275=ORIENTED_EDGE('',*,*,#12227,.T.);
#17276=ORIENTED_EDGE('',*,*,#12232,.F.);
#17277=ORIENTED_EDGE('',*,*,#12233,.F.);
#17278=ORIENTED_EDGE('',*,*,#12234,.T.);
#17279=ORIENTED_EDGE('',*,*,#12230,.T.);
#17280=ORIENTED_EDGE('',*,*,#12235,.F.);
#17281=ORIENTED_EDGE('',*,*,#12236,.F.);
#17282=ORIENTED_EDGE('',*,*,#12237,.T.);
#17283=ORIENTED_EDGE('',*,*,#12233,.T.);
#17284=ORIENTED_EDGE('',*,*,#12238,.F.);
#17285=ORIENTED_EDGE('',*,*,#12239,.F.);
#17286=ORIENTED_EDGE('',*,*,#12240,.T.);
#17287=ORIENTED_EDGE('',*,*,#12236,.T.);
#17288=ORIENTED_EDGE('',*,*,#12241,.F.);
#17289=ORIENTED_EDGE('',*,*,#12242,.F.);
#17290=ORIENTED_EDGE('',*,*,#12243,.T.);
#17291=ORIENTED_EDGE('',*,*,#12239,.T.);
#17292=ORIENTED_EDGE('',*,*,#12244,.F.);
#17293=ORIENTED_EDGE('',*,*,#12245,.F.);
#17294=ORIENTED_EDGE('',*,*,#12246,.T.);
#17295=ORIENTED_EDGE('',*,*,#12242,.T.);
#17296=ORIENTED_EDGE('',*,*,#12247,.F.);
#17297=ORIENTED_EDGE('',*,*,#12248,.F.);
#17298=ORIENTED_EDGE('',*,*,#12249,.T.);
#17299=ORIENTED_EDGE('',*,*,#12245,.T.);
#17300=ORIENTED_EDGE('',*,*,#12250,.F.);
#17301=ORIENTED_EDGE('',*,*,#12251,.F.);
#17302=ORIENTED_EDGE('',*,*,#12252,.T.);
#17303=ORIENTED_EDGE('',*,*,#12248,.T.);
#17304=ORIENTED_EDGE('',*,*,#12253,.F.);
#17305=ORIENTED_EDGE('',*,*,#12254,.F.);
#17306=ORIENTED_EDGE('',*,*,#12255,.T.);
#17307=ORIENTED_EDGE('',*,*,#12251,.T.);
#17308=ORIENTED_EDGE('',*,*,#12256,.F.);
#17309=ORIENTED_EDGE('',*,*,#12257,.F.);
#17310=ORIENTED_EDGE('',*,*,#12258,.T.);
#17311=ORIENTED_EDGE('',*,*,#12254,.T.);
#17312=ORIENTED_EDGE('',*,*,#12259,.F.);
#17313=ORIENTED_EDGE('',*,*,#12260,.F.);
#17314=ORIENTED_EDGE('',*,*,#12261,.T.);
#17315=ORIENTED_EDGE('',*,*,#12257,.T.);
#17316=ORIENTED_EDGE('',*,*,#12262,.F.);
#17317=ORIENTED_EDGE('',*,*,#12263,.F.);
#17318=ORIENTED_EDGE('',*,*,#12264,.T.);
#17319=ORIENTED_EDGE('',*,*,#12260,.T.);
#17320=ORIENTED_EDGE('',*,*,#12265,.F.);
#17321=ORIENTED_EDGE('',*,*,#12266,.F.);
#17322=ORIENTED_EDGE('',*,*,#12267,.T.);
#17323=ORIENTED_EDGE('',*,*,#12263,.T.);
#17324=ORIENTED_EDGE('',*,*,#12268,.F.);
#17325=ORIENTED_EDGE('',*,*,#12269,.F.);
#17326=ORIENTED_EDGE('',*,*,#12270,.T.);
#17327=ORIENTED_EDGE('',*,*,#12266,.T.);
#17328=ORIENTED_EDGE('',*,*,#12271,.F.);
#17329=ORIENTED_EDGE('',*,*,#12272,.F.);
#17330=ORIENTED_EDGE('',*,*,#12273,.T.);
#17331=ORIENTED_EDGE('',*,*,#12269,.T.);
#17332=ORIENTED_EDGE('',*,*,#12274,.F.);
#17333=ORIENTED_EDGE('',*,*,#12275,.F.);
#17334=ORIENTED_EDGE('',*,*,#12276,.T.);
#17335=ORIENTED_EDGE('',*,*,#12272,.T.);
#17336=ORIENTED_EDGE('',*,*,#12277,.F.);
#17337=ORIENTED_EDGE('',*,*,#12278,.F.);
#17338=ORIENTED_EDGE('',*,*,#12279,.T.);
#17339=ORIENTED_EDGE('',*,*,#12275,.T.);
#17340=ORIENTED_EDGE('',*,*,#12280,.F.);
#17341=ORIENTED_EDGE('',*,*,#12281,.T.);
#17342=ORIENTED_EDGE('',*,*,#12282,.T.);
#17343=ORIENTED_EDGE('',*,*,#12283,.T.);
#17344=ORIENTED_EDGE('',*,*,#12282,.F.);
#17345=ORIENTED_EDGE('',*,*,#12281,.F.);
#17346=ORIENTED_EDGE('',*,*,#12284,.T.);
#17347=ORIENTED_EDGE('',*,*,#12285,.T.);
#17348=ORIENTED_EDGE('',*,*,#12284,.F.);
#17349=ORIENTED_EDGE('',*,*,#12283,.F.);
#17350=ORIENTED_EDGE('',*,*,#12286,.T.);
#17351=ORIENTED_EDGE('',*,*,#12287,.T.);
#17352=ORIENTED_EDGE('',*,*,#12288,.T.);
#17353=ORIENTED_EDGE('',*,*,#12287,.F.);
#17354=ORIENTED_EDGE('',*,*,#12288,.F.);
#17355=ORIENTED_EDGE('',*,*,#12289,.T.);
#17356=ORIENTED_EDGE('',*,*,#12290,.T.);
#17357=ORIENTED_EDGE('',*,*,#12289,.F.);
#17358=ORIENTED_EDGE('',*,*,#12286,.F.);
#17359=ORIENTED_EDGE('',*,*,#12291,.F.);
#17360=ORIENTED_EDGE('',*,*,#11982,.F.);
#17361=ORIENTED_EDGE('',*,*,#12292,.F.);
#17362=ORIENTED_EDGE('',*,*,#11911,.F.);
#17363=ORIENTED_EDGE('',*,*,#12293,.F.);
#17364=ORIENTED_EDGE('',*,*,#12290,.F.);
#17365=ORIENTED_EDGE('',*,*,#12294,.F.);
#17366=ORIENTED_EDGE('',*,*,#12295,.F.);
#17367=ORIENTED_EDGE('',*,*,#11610,.F.);
#17368=ORIENTED_EDGE('',*,*,#11614,.F.);
#17369=ORIENTED_EDGE('',*,*,#11617,.F.);
#17370=ORIENTED_EDGE('',*,*,#11620,.F.);
#17371=ORIENTED_EDGE('',*,*,#11623,.F.);
#17372=ORIENTED_EDGE('',*,*,#11626,.F.);
#17373=ORIENTED_EDGE('',*,*,#11629,.F.);
#17374=ORIENTED_EDGE('',*,*,#11632,.F.);
#17375=ORIENTED_EDGE('',*,*,#11635,.F.);
#17376=ORIENTED_EDGE('',*,*,#11638,.F.);
#17377=ORIENTED_EDGE('',*,*,#11641,.F.);
#17378=ORIENTED_EDGE('',*,*,#11644,.F.);
#17379=ORIENTED_EDGE('',*,*,#11647,.F.);
#17380=ORIENTED_EDGE('',*,*,#11650,.F.);
#17381=ORIENTED_EDGE('',*,*,#11653,.F.);
#17382=ORIENTED_EDGE('',*,*,#11656,.F.);
#17383=ORIENTED_EDGE('',*,*,#11659,.F.);
#17384=ORIENTED_EDGE('',*,*,#11662,.F.);
#17385=ORIENTED_EDGE('',*,*,#11665,.F.);
#17386=ORIENTED_EDGE('',*,*,#11668,.F.);
#17387=ORIENTED_EDGE('',*,*,#11671,.F.);
#17388=ORIENTED_EDGE('',*,*,#11674,.F.);
#17389=ORIENTED_EDGE('',*,*,#11677,.F.);
#17390=ORIENTED_EDGE('',*,*,#11680,.F.);
#17391=ORIENTED_EDGE('',*,*,#11683,.F.);
#17392=ORIENTED_EDGE('',*,*,#11686,.F.);
#17393=ORIENTED_EDGE('',*,*,#11689,.F.);
#17394=ORIENTED_EDGE('',*,*,#11692,.F.);
#17395=ORIENTED_EDGE('',*,*,#11695,.F.);
#17396=ORIENTED_EDGE('',*,*,#11698,.F.);
#17397=ORIENTED_EDGE('',*,*,#11701,.F.);
#17398=ORIENTED_EDGE('',*,*,#11704,.F.);
#17399=ORIENTED_EDGE('',*,*,#11707,.F.);
#17400=ORIENTED_EDGE('',*,*,#11710,.F.);
#17401=ORIENTED_EDGE('',*,*,#11713,.F.);
#17402=ORIENTED_EDGE('',*,*,#11716,.F.);
#17403=ORIENTED_EDGE('',*,*,#11719,.F.);
#17404=ORIENTED_EDGE('',*,*,#11722,.F.);
#17405=ORIENTED_EDGE('',*,*,#11725,.F.);
#17406=ORIENTED_EDGE('',*,*,#11728,.F.);
#17407=ORIENTED_EDGE('',*,*,#11731,.F.);
#17408=ORIENTED_EDGE('',*,*,#11734,.F.);
#17409=ORIENTED_EDGE('',*,*,#11737,.F.);
#17410=ORIENTED_EDGE('',*,*,#11740,.F.);
#17411=ORIENTED_EDGE('',*,*,#11743,.F.);
#17412=ORIENTED_EDGE('',*,*,#11746,.F.);
#17413=ORIENTED_EDGE('',*,*,#11749,.F.);
#17414=ORIENTED_EDGE('',*,*,#11752,.F.);
#17415=ORIENTED_EDGE('',*,*,#11755,.F.);
#17416=ORIENTED_EDGE('',*,*,#11758,.F.);
#17417=ORIENTED_EDGE('',*,*,#11761,.F.);
#17418=ORIENTED_EDGE('',*,*,#11764,.F.);
#17419=ORIENTED_EDGE('',*,*,#11767,.F.);
#17420=ORIENTED_EDGE('',*,*,#11770,.F.);
#17421=ORIENTED_EDGE('',*,*,#11773,.F.);
#17422=ORIENTED_EDGE('',*,*,#11776,.F.);
#17423=ORIENTED_EDGE('',*,*,#11779,.F.);
#17424=ORIENTED_EDGE('',*,*,#11782,.F.);
#17425=ORIENTED_EDGE('',*,*,#11785,.F.);
#17426=ORIENTED_EDGE('',*,*,#11788,.F.);
#17427=ORIENTED_EDGE('',*,*,#11791,.F.);
#17428=ORIENTED_EDGE('',*,*,#11794,.F.);
#17429=ORIENTED_EDGE('',*,*,#11797,.F.);
#17430=ORIENTED_EDGE('',*,*,#11800,.F.);
#17431=ORIENTED_EDGE('',*,*,#11803,.F.);
#17432=ORIENTED_EDGE('',*,*,#11806,.F.);
#17433=ORIENTED_EDGE('',*,*,#11809,.F.);
#17434=ORIENTED_EDGE('',*,*,#11812,.F.);
#17435=ORIENTED_EDGE('',*,*,#11815,.F.);
#17436=ORIENTED_EDGE('',*,*,#11818,.F.);
#17437=ORIENTED_EDGE('',*,*,#11821,.F.);
#17438=ORIENTED_EDGE('',*,*,#11824,.F.);
#17439=ORIENTED_EDGE('',*,*,#11827,.F.);
#17440=ORIENTED_EDGE('',*,*,#11830,.F.);
#17441=ORIENTED_EDGE('',*,*,#11833,.F.);
#17442=ORIENTED_EDGE('',*,*,#11836,.F.);
#17443=ORIENTED_EDGE('',*,*,#11839,.F.);
#17444=ORIENTED_EDGE('',*,*,#11842,.F.);
#17445=ORIENTED_EDGE('',*,*,#11845,.F.);
#17446=ORIENTED_EDGE('',*,*,#11848,.F.);
#17447=ORIENTED_EDGE('',*,*,#11851,.F.);
#17448=ORIENTED_EDGE('',*,*,#11854,.F.);
#17449=ORIENTED_EDGE('',*,*,#11857,.F.);
#17450=ORIENTED_EDGE('',*,*,#11860,.F.);
#17451=ORIENTED_EDGE('',*,*,#11863,.F.);
#17452=ORIENTED_EDGE('',*,*,#11866,.F.);
#17453=ORIENTED_EDGE('',*,*,#11869,.F.);
#17454=ORIENTED_EDGE('',*,*,#11872,.F.);
#17455=ORIENTED_EDGE('',*,*,#11875,.F.);
#17456=ORIENTED_EDGE('',*,*,#11878,.F.);
#17457=ORIENTED_EDGE('',*,*,#11881,.F.);
#17458=ORIENTED_EDGE('',*,*,#11884,.F.);
#17459=ORIENTED_EDGE('',*,*,#11887,.F.);
#17460=ORIENTED_EDGE('',*,*,#11890,.F.);
#17461=ORIENTED_EDGE('',*,*,#11893,.F.);
#17462=ORIENTED_EDGE('',*,*,#11896,.F.);
#17463=ORIENTED_EDGE('',*,*,#11899,.F.);
#17464=ORIENTED_EDGE('',*,*,#11902,.F.);
#17465=ORIENTED_EDGE('',*,*,#11905,.F.);
#17466=ORIENTED_EDGE('',*,*,#11908,.F.);
#17467=ORIENTED_EDGE('',*,*,#11912,.F.);
#17468=ORIENTED_EDGE('',*,*,#12292,.T.);
#17469=ORIENTED_EDGE('',*,*,#11981,.F.);
#17470=ORIENTED_EDGE('',*,*,#11985,.F.);
#17471=ORIENTED_EDGE('',*,*,#11988,.F.);
#17472=ORIENTED_EDGE('',*,*,#11991,.F.);
#17473=ORIENTED_EDGE('',*,*,#11994,.F.);
#17474=ORIENTED_EDGE('',*,*,#11997,.F.);
#17475=ORIENTED_EDGE('',*,*,#12000,.F.);
#17476=ORIENTED_EDGE('',*,*,#12003,.F.);
#17477=ORIENTED_EDGE('',*,*,#12006,.F.);
#17478=ORIENTED_EDGE('',*,*,#12009,.F.);
#17479=ORIENTED_EDGE('',*,*,#12012,.F.);
#17480=ORIENTED_EDGE('',*,*,#12015,.F.);
#17481=ORIENTED_EDGE('',*,*,#12018,.F.);
#17482=ORIENTED_EDGE('',*,*,#12021,.F.);
#17483=ORIENTED_EDGE('',*,*,#12024,.F.);
#17484=ORIENTED_EDGE('',*,*,#12027,.F.);
#17485=ORIENTED_EDGE('',*,*,#12030,.F.);
#17486=ORIENTED_EDGE('',*,*,#12033,.F.);
#17487=ORIENTED_EDGE('',*,*,#12036,.F.);
#17488=ORIENTED_EDGE('',*,*,#12039,.F.);
#17489=ORIENTED_EDGE('',*,*,#12042,.F.);
#17490=ORIENTED_EDGE('',*,*,#12045,.F.);
#17491=ORIENTED_EDGE('',*,*,#12048,.F.);
#17492=ORIENTED_EDGE('',*,*,#12051,.F.);
#17493=ORIENTED_EDGE('',*,*,#12054,.F.);
#17494=ORIENTED_EDGE('',*,*,#12057,.F.);
#17495=ORIENTED_EDGE('',*,*,#12060,.F.);
#17496=ORIENTED_EDGE('',*,*,#12063,.F.);
#17497=ORIENTED_EDGE('',*,*,#12066,.F.);
#17498=ORIENTED_EDGE('',*,*,#12069,.F.);
#17499=ORIENTED_EDGE('',*,*,#12072,.F.);
#17500=ORIENTED_EDGE('',*,*,#12075,.F.);
#17501=ORIENTED_EDGE('',*,*,#12078,.F.);
#17502=ORIENTED_EDGE('',*,*,#12081,.F.);
#17503=ORIENTED_EDGE('',*,*,#12084,.F.);
#17504=ORIENTED_EDGE('',*,*,#12087,.F.);
#17505=ORIENTED_EDGE('',*,*,#12090,.F.);
#17506=ORIENTED_EDGE('',*,*,#12093,.F.);
#17507=ORIENTED_EDGE('',*,*,#12096,.F.);
#17508=ORIENTED_EDGE('',*,*,#12099,.F.);
#17509=ORIENTED_EDGE('',*,*,#12102,.F.);
#17510=ORIENTED_EDGE('',*,*,#12105,.F.);
#17511=ORIENTED_EDGE('',*,*,#12108,.F.);
#17512=ORIENTED_EDGE('',*,*,#12111,.F.);
#17513=ORIENTED_EDGE('',*,*,#12114,.F.);
#17514=ORIENTED_EDGE('',*,*,#12117,.F.);
#17515=ORIENTED_EDGE('',*,*,#12120,.F.);
#17516=ORIENTED_EDGE('',*,*,#12123,.F.);
#17517=ORIENTED_EDGE('',*,*,#12126,.F.);
#17518=ORIENTED_EDGE('',*,*,#12129,.F.);
#17519=ORIENTED_EDGE('',*,*,#12132,.F.);
#17520=ORIENTED_EDGE('',*,*,#12135,.F.);
#17521=ORIENTED_EDGE('',*,*,#12138,.F.);
#17522=ORIENTED_EDGE('',*,*,#12141,.F.);
#17523=ORIENTED_EDGE('',*,*,#12144,.F.);
#17524=ORIENTED_EDGE('',*,*,#12147,.F.);
#17525=ORIENTED_EDGE('',*,*,#12150,.F.);
#17526=ORIENTED_EDGE('',*,*,#12153,.F.);
#17527=ORIENTED_EDGE('',*,*,#12156,.F.);
#17528=ORIENTED_EDGE('',*,*,#12159,.F.);
#17529=ORIENTED_EDGE('',*,*,#12162,.F.);
#17530=ORIENTED_EDGE('',*,*,#12165,.F.);
#17531=ORIENTED_EDGE('',*,*,#12168,.F.);
#17532=ORIENTED_EDGE('',*,*,#12171,.F.);
#17533=ORIENTED_EDGE('',*,*,#12174,.F.);
#17534=ORIENTED_EDGE('',*,*,#12177,.F.);
#17535=ORIENTED_EDGE('',*,*,#12180,.F.);
#17536=ORIENTED_EDGE('',*,*,#12183,.F.);
#17537=ORIENTED_EDGE('',*,*,#12186,.F.);
#17538=ORIENTED_EDGE('',*,*,#12189,.F.);
#17539=ORIENTED_EDGE('',*,*,#12192,.F.);
#17540=ORIENTED_EDGE('',*,*,#12195,.F.);
#17541=ORIENTED_EDGE('',*,*,#12198,.F.);
#17542=ORIENTED_EDGE('',*,*,#12201,.F.);
#17543=ORIENTED_EDGE('',*,*,#12204,.F.);
#17544=ORIENTED_EDGE('',*,*,#12207,.F.);
#17545=ORIENTED_EDGE('',*,*,#12210,.F.);
#17546=ORIENTED_EDGE('',*,*,#12213,.F.);
#17547=ORIENTED_EDGE('',*,*,#12216,.F.);
#17548=ORIENTED_EDGE('',*,*,#12219,.F.);
#17549=ORIENTED_EDGE('',*,*,#12222,.F.);
#17550=ORIENTED_EDGE('',*,*,#12225,.F.);
#17551=ORIENTED_EDGE('',*,*,#12228,.F.);
#17552=ORIENTED_EDGE('',*,*,#12231,.F.);
#17553=ORIENTED_EDGE('',*,*,#12234,.F.);
#17554=ORIENTED_EDGE('',*,*,#12237,.F.);
#17555=ORIENTED_EDGE('',*,*,#12240,.F.);
#17556=ORIENTED_EDGE('',*,*,#12243,.F.);
#17557=ORIENTED_EDGE('',*,*,#12246,.F.);
#17558=ORIENTED_EDGE('',*,*,#12249,.F.);
#17559=ORIENTED_EDGE('',*,*,#12252,.F.);
#17560=ORIENTED_EDGE('',*,*,#12255,.F.);
#17561=ORIENTED_EDGE('',*,*,#12258,.F.);
#17562=ORIENTED_EDGE('',*,*,#12261,.F.);
#17563=ORIENTED_EDGE('',*,*,#12264,.F.);
#17564=ORIENTED_EDGE('',*,*,#12267,.F.);
#17565=ORIENTED_EDGE('',*,*,#12270,.F.);
#17566=ORIENTED_EDGE('',*,*,#12273,.F.);
#17567=ORIENTED_EDGE('',*,*,#12276,.F.);
#17568=ORIENTED_EDGE('',*,*,#12279,.F.);
#17569=ORIENTED_EDGE('',*,*,#12278,.T.);
#17570=ORIENTED_EDGE('',*,*,#12296,.F.);
#17571=ORIENTED_EDGE('',*,*,#12297,.F.);
#17572=ORIENTED_EDGE('',*,*,#12294,.T.);
#17573=ORIENTED_EDGE('',*,*,#12285,.F.);
#17574=ORIENTED_EDGE('',*,*,#11951,.T.);
#17575=ORIENTED_EDGE('',*,*,#12298,.T.);
#17576=ORIENTED_EDGE('',*,*,#11946,.T.);
#17577=ORIENTED_EDGE('',*,*,#12299,.T.);
#17578=ORIENTED_EDGE('',*,*,#12300,.T.);
#17579=ORIENTED_EDGE('',*,*,#12301,.T.);
#17580=ORIENTED_EDGE('',*,*,#11979,.T.);
#17581=ORIENTED_EDGE('',*,*,#11976,.T.);
#17582=ORIENTED_EDGE('',*,*,#11973,.T.);
#17583=ORIENTED_EDGE('',*,*,#11970,.T.);
#17584=ORIENTED_EDGE('',*,*,#11967,.T.);
#17585=ORIENTED_EDGE('',*,*,#11964,.T.);
#17586=ORIENTED_EDGE('',*,*,#11961,.T.);
#17587=ORIENTED_EDGE('',*,*,#11958,.T.);
#17588=ORIENTED_EDGE('',*,*,#11955,.T.);
#17589=ORIENTED_EDGE('',*,*,#11952,.T.);
#17590=ORIENTED_EDGE('',*,*,#12300,.F.);
#17591=ORIENTED_EDGE('',*,*,#12302,.F.);
#17592=ORIENTED_EDGE('',*,*,#11948,.F.);
#17593=ORIENTED_EDGE('',*,*,#11944,.F.);
#17594=ORIENTED_EDGE('',*,*,#11941,.F.);
#17595=ORIENTED_EDGE('',*,*,#11938,.F.);
#17596=ORIENTED_EDGE('',*,*,#11935,.F.);
#17597=ORIENTED_EDGE('',*,*,#11932,.F.);
#17598=ORIENTED_EDGE('',*,*,#11929,.F.);
#17599=ORIENTED_EDGE('',*,*,#11926,.F.);
#17600=ORIENTED_EDGE('',*,*,#11923,.F.);
#17601=ORIENTED_EDGE('',*,*,#11920,.F.);
#17602=ORIENTED_EDGE('',*,*,#12303,.F.);
#17603=ORIENTED_EDGE('',*,*,#11919,.F.);
#17604=ORIENTED_EDGE('',*,*,#12304,.T.);
#17605=ORIENTED_EDGE('',*,*,#12305,.T.);
#17606=ORIENTED_EDGE('',*,*,#12303,.T.);
#17607=ORIENTED_EDGE('',*,*,#11977,.T.);
#17608=ORIENTED_EDGE('',*,*,#12301,.F.);
#17609=ORIENTED_EDGE('',*,*,#12305,.F.);
#17610=ORIENTED_EDGE('',*,*,#12306,.T.);
#17611=ORIENTED_EDGE('',*,*,#12298,.F.);
#17612=ORIENTED_EDGE('',*,*,#11950,.F.);
#17613=ORIENTED_EDGE('',*,*,#11954,.F.);
#17614=ORIENTED_EDGE('',*,*,#11957,.F.);
#17615=ORIENTED_EDGE('',*,*,#11960,.F.);
#17616=ORIENTED_EDGE('',*,*,#11963,.F.);
#17617=ORIENTED_EDGE('',*,*,#11966,.F.);
#17618=ORIENTED_EDGE('',*,*,#11969,.F.);
#17619=ORIENTED_EDGE('',*,*,#11972,.F.);
#17620=ORIENTED_EDGE('',*,*,#11975,.F.);
#17621=ORIENTED_EDGE('',*,*,#11978,.F.);
#17622=ORIENTED_EDGE('',*,*,#12306,.F.);
#17623=ORIENTED_EDGE('',*,*,#12304,.F.);
#17624=ORIENTED_EDGE('',*,*,#11918,.F.);
#17625=ORIENTED_EDGE('',*,*,#11915,.F.);
#17626=ORIENTED_EDGE('',*,*,#11922,.F.);
#17627=ORIENTED_EDGE('',*,*,#11925,.F.);
#17628=ORIENTED_EDGE('',*,*,#11928,.F.);
#17629=ORIENTED_EDGE('',*,*,#11931,.F.);
#17630=ORIENTED_EDGE('',*,*,#11934,.F.);
#17631=ORIENTED_EDGE('',*,*,#11937,.F.);
#17632=ORIENTED_EDGE('',*,*,#11940,.F.);
#17633=ORIENTED_EDGE('',*,*,#11943,.F.);
#17634=ORIENTED_EDGE('',*,*,#11947,.F.);
#17635=ORIENTED_EDGE('',*,*,#11945,.T.);
#17636=ORIENTED_EDGE('',*,*,#12302,.T.);
#17637=ORIENTED_EDGE('',*,*,#12299,.F.);
#17638=ORIENTED_EDGE('',*,*,#12297,.T.);
#17639=ORIENTED_EDGE('',*,*,#12307,.T.);
#17640=ORIENTED_EDGE('',*,*,#11611,.T.);
#17641=ORIENTED_EDGE('',*,*,#12295,.T.);
#17642=ORIENTED_EDGE('',*,*,#11917,.T.);
#17643=ORIENTED_EDGE('',*,*,#12307,.F.);
#17644=ORIENTED_EDGE('',*,*,#12296,.T.);
#17645=ORIENTED_EDGE('',*,*,#12280,.T.);
#17646=ORIENTED_EDGE('',*,*,#12277,.T.);
#17647=ORIENTED_EDGE('',*,*,#12274,.T.);
#17648=ORIENTED_EDGE('',*,*,#12271,.T.);
#17649=ORIENTED_EDGE('',*,*,#12268,.T.);
#17650=ORIENTED_EDGE('',*,*,#12265,.T.);
#17651=ORIENTED_EDGE('',*,*,#12262,.T.);
#17652=ORIENTED_EDGE('',*,*,#12259,.T.);
#17653=ORIENTED_EDGE('',*,*,#12256,.T.);
#17654=ORIENTED_EDGE('',*,*,#12253,.T.);
#17655=ORIENTED_EDGE('',*,*,#12250,.T.);
#17656=ORIENTED_EDGE('',*,*,#12247,.T.);
#17657=ORIENTED_EDGE('',*,*,#12244,.T.);
#17658=ORIENTED_EDGE('',*,*,#12241,.T.);
#17659=ORIENTED_EDGE('',*,*,#12238,.T.);
#17660=ORIENTED_EDGE('',*,*,#12235,.T.);
#17661=ORIENTED_EDGE('',*,*,#12232,.T.);
#17662=ORIENTED_EDGE('',*,*,#12229,.T.);
#17663=ORIENTED_EDGE('',*,*,#12226,.T.);
#17664=ORIENTED_EDGE('',*,*,#12223,.T.);
#17665=ORIENTED_EDGE('',*,*,#12220,.T.);
#17666=ORIENTED_EDGE('',*,*,#12217,.T.);
#17667=ORIENTED_EDGE('',*,*,#12214,.T.);
#17668=ORIENTED_EDGE('',*,*,#12211,.T.);
#17669=ORIENTED_EDGE('',*,*,#12208,.T.);
#17670=ORIENTED_EDGE('',*,*,#12205,.T.);
#17671=ORIENTED_EDGE('',*,*,#12202,.T.);
#17672=ORIENTED_EDGE('',*,*,#12199,.T.);
#17673=ORIENTED_EDGE('',*,*,#12196,.T.);
#17674=ORIENTED_EDGE('',*,*,#12193,.T.);
#17675=ORIENTED_EDGE('',*,*,#12190,.T.);
#17676=ORIENTED_EDGE('',*,*,#12187,.T.);
#17677=ORIENTED_EDGE('',*,*,#12184,.T.);
#17678=ORIENTED_EDGE('',*,*,#12181,.T.);
#17679=ORIENTED_EDGE('',*,*,#12178,.T.);
#17680=ORIENTED_EDGE('',*,*,#12175,.T.);
#17681=ORIENTED_EDGE('',*,*,#12172,.T.);
#17682=ORIENTED_EDGE('',*,*,#12169,.T.);
#17683=ORIENTED_EDGE('',*,*,#12166,.T.);
#17684=ORIENTED_EDGE('',*,*,#12163,.T.);
#17685=ORIENTED_EDGE('',*,*,#12160,.T.);
#17686=ORIENTED_EDGE('',*,*,#12157,.T.);
#17687=ORIENTED_EDGE('',*,*,#12154,.T.);
#17688=ORIENTED_EDGE('',*,*,#12151,.T.);
#17689=ORIENTED_EDGE('',*,*,#12148,.T.);
#17690=ORIENTED_EDGE('',*,*,#12145,.T.);
#17691=ORIENTED_EDGE('',*,*,#12142,.T.);
#17692=ORIENTED_EDGE('',*,*,#12139,.T.);
#17693=ORIENTED_EDGE('',*,*,#12136,.T.);
#17694=ORIENTED_EDGE('',*,*,#12133,.T.);
#17695=ORIENTED_EDGE('',*,*,#12130,.T.);
#17696=ORIENTED_EDGE('',*,*,#12127,.T.);
#17697=ORIENTED_EDGE('',*,*,#12124,.T.);
#17698=ORIENTED_EDGE('',*,*,#12121,.T.);
#17699=ORIENTED_EDGE('',*,*,#12118,.T.);
#17700=ORIENTED_EDGE('',*,*,#12115,.T.);
#17701=ORIENTED_EDGE('',*,*,#12112,.T.);
#17702=ORIENTED_EDGE('',*,*,#12109,.T.);
#17703=ORIENTED_EDGE('',*,*,#12106,.T.);
#17704=ORIENTED_EDGE('',*,*,#12103,.T.);
#17705=ORIENTED_EDGE('',*,*,#12100,.T.);
#17706=ORIENTED_EDGE('',*,*,#12097,.T.);
#17707=ORIENTED_EDGE('',*,*,#12094,.T.);
#17708=ORIENTED_EDGE('',*,*,#12091,.T.);
#17709=ORIENTED_EDGE('',*,*,#12088,.T.);
#17710=ORIENTED_EDGE('',*,*,#12085,.T.);
#17711=ORIENTED_EDGE('',*,*,#12082,.T.);
#17712=ORIENTED_EDGE('',*,*,#12079,.T.);
#17713=ORIENTED_EDGE('',*,*,#12076,.T.);
#17714=ORIENTED_EDGE('',*,*,#12073,.T.);
#17715=ORIENTED_EDGE('',*,*,#12070,.T.);
#17716=ORIENTED_EDGE('',*,*,#12067,.T.);
#17717=ORIENTED_EDGE('',*,*,#12064,.T.);
#17718=ORIENTED_EDGE('',*,*,#12061,.T.);
#17719=ORIENTED_EDGE('',*,*,#12058,.T.);
#17720=ORIENTED_EDGE('',*,*,#12055,.T.);
#17721=ORIENTED_EDGE('',*,*,#12052,.T.);
#17722=ORIENTED_EDGE('',*,*,#12049,.T.);
#17723=ORIENTED_EDGE('',*,*,#12046,.T.);
#17724=ORIENTED_EDGE('',*,*,#12043,.T.);
#17725=ORIENTED_EDGE('',*,*,#12040,.T.);
#17726=ORIENTED_EDGE('',*,*,#12037,.T.);
#17727=ORIENTED_EDGE('',*,*,#12034,.T.);
#17728=ORIENTED_EDGE('',*,*,#12031,.T.);
#17729=ORIENTED_EDGE('',*,*,#12028,.T.);
#17730=ORIENTED_EDGE('',*,*,#12025,.T.);
#17731=ORIENTED_EDGE('',*,*,#12022,.T.);
#17732=ORIENTED_EDGE('',*,*,#12019,.T.);
#17733=ORIENTED_EDGE('',*,*,#12016,.T.);
#17734=ORIENTED_EDGE('',*,*,#12013,.T.);
#17735=ORIENTED_EDGE('',*,*,#12010,.T.);
#17736=ORIENTED_EDGE('',*,*,#12007,.T.);
#17737=ORIENTED_EDGE('',*,*,#12004,.T.);
#17738=ORIENTED_EDGE('',*,*,#12001,.T.);
#17739=ORIENTED_EDGE('',*,*,#11998,.T.);
#17740=ORIENTED_EDGE('',*,*,#11995,.T.);
#17741=ORIENTED_EDGE('',*,*,#11992,.T.);
#17742=ORIENTED_EDGE('',*,*,#11989,.T.);
#17743=ORIENTED_EDGE('',*,*,#11986,.T.);
#17744=ORIENTED_EDGE('',*,*,#11983,.T.);
#17745=ORIENTED_EDGE('',*,*,#12291,.T.);
#17746=ORIENTED_EDGE('',*,*,#12308,.F.);
#17747=ORIENTED_EDGE('',*,*,#11913,.F.);
#17748=ORIENTED_EDGE('',*,*,#11909,.F.);
#17749=ORIENTED_EDGE('',*,*,#11906,.F.);
#17750=ORIENTED_EDGE('',*,*,#11903,.F.);
#17751=ORIENTED_EDGE('',*,*,#11900,.F.);
#17752=ORIENTED_EDGE('',*,*,#11897,.F.);
#17753=ORIENTED_EDGE('',*,*,#11894,.F.);
#17754=ORIENTED_EDGE('',*,*,#11891,.F.);
#17755=ORIENTED_EDGE('',*,*,#11888,.F.);
#17756=ORIENTED_EDGE('',*,*,#11885,.F.);
#17757=ORIENTED_EDGE('',*,*,#11882,.F.);
#17758=ORIENTED_EDGE('',*,*,#11879,.F.);
#17759=ORIENTED_EDGE('',*,*,#11876,.F.);
#17760=ORIENTED_EDGE('',*,*,#11873,.F.);
#17761=ORIENTED_EDGE('',*,*,#11870,.F.);
#17762=ORIENTED_EDGE('',*,*,#11867,.F.);
#17763=ORIENTED_EDGE('',*,*,#11864,.F.);
#17764=ORIENTED_EDGE('',*,*,#11861,.F.);
#17765=ORIENTED_EDGE('',*,*,#11858,.F.);
#17766=ORIENTED_EDGE('',*,*,#11855,.F.);
#17767=ORIENTED_EDGE('',*,*,#11852,.F.);
#17768=ORIENTED_EDGE('',*,*,#11849,.F.);
#17769=ORIENTED_EDGE('',*,*,#11846,.F.);
#17770=ORIENTED_EDGE('',*,*,#11843,.F.);
#17771=ORIENTED_EDGE('',*,*,#11840,.F.);
#17772=ORIENTED_EDGE('',*,*,#11837,.F.);
#17773=ORIENTED_EDGE('',*,*,#11834,.F.);
#17774=ORIENTED_EDGE('',*,*,#11831,.F.);
#17775=ORIENTED_EDGE('',*,*,#11828,.F.);
#17776=ORIENTED_EDGE('',*,*,#11825,.F.);
#17777=ORIENTED_EDGE('',*,*,#11822,.F.);
#17778=ORIENTED_EDGE('',*,*,#11819,.F.);
#17779=ORIENTED_EDGE('',*,*,#11816,.F.);
#17780=ORIENTED_EDGE('',*,*,#11813,.F.);
#17781=ORIENTED_EDGE('',*,*,#11810,.F.);
#17782=ORIENTED_EDGE('',*,*,#11807,.F.);
#17783=ORIENTED_EDGE('',*,*,#11804,.F.);
#17784=ORIENTED_EDGE('',*,*,#11801,.F.);
#17785=ORIENTED_EDGE('',*,*,#11798,.F.);
#17786=ORIENTED_EDGE('',*,*,#11795,.F.);
#17787=ORIENTED_EDGE('',*,*,#11792,.F.);
#17788=ORIENTED_EDGE('',*,*,#11789,.F.);
#17789=ORIENTED_EDGE('',*,*,#11786,.F.);
#17790=ORIENTED_EDGE('',*,*,#11783,.F.);
#17791=ORIENTED_EDGE('',*,*,#11780,.F.);
#17792=ORIENTED_EDGE('',*,*,#11777,.F.);
#17793=ORIENTED_EDGE('',*,*,#11774,.F.);
#17794=ORIENTED_EDGE('',*,*,#11771,.F.);
#17795=ORIENTED_EDGE('',*,*,#11768,.F.);
#17796=ORIENTED_EDGE('',*,*,#11765,.F.);
#17797=ORIENTED_EDGE('',*,*,#11762,.F.);
#17798=ORIENTED_EDGE('',*,*,#11759,.F.);
#17799=ORIENTED_EDGE('',*,*,#11756,.F.);
#17800=ORIENTED_EDGE('',*,*,#11753,.F.);
#17801=ORIENTED_EDGE('',*,*,#11750,.F.);
#17802=ORIENTED_EDGE('',*,*,#11747,.F.);
#17803=ORIENTED_EDGE('',*,*,#11744,.F.);
#17804=ORIENTED_EDGE('',*,*,#11741,.F.);
#17805=ORIENTED_EDGE('',*,*,#11738,.F.);
#17806=ORIENTED_EDGE('',*,*,#11735,.F.);
#17807=ORIENTED_EDGE('',*,*,#11732,.F.);
#17808=ORIENTED_EDGE('',*,*,#11729,.F.);
#17809=ORIENTED_EDGE('',*,*,#11726,.F.);
#17810=ORIENTED_EDGE('',*,*,#11723,.F.);
#17811=ORIENTED_EDGE('',*,*,#11720,.F.);
#17812=ORIENTED_EDGE('',*,*,#11717,.F.);
#17813=ORIENTED_EDGE('',*,*,#11714,.F.);
#17814=ORIENTED_EDGE('',*,*,#11711,.F.);
#17815=ORIENTED_EDGE('',*,*,#11708,.F.);
#17816=ORIENTED_EDGE('',*,*,#11705,.F.);
#17817=ORIENTED_EDGE('',*,*,#11702,.F.);
#17818=ORIENTED_EDGE('',*,*,#11699,.F.);
#17819=ORIENTED_EDGE('',*,*,#11696,.F.);
#17820=ORIENTED_EDGE('',*,*,#11693,.F.);
#17821=ORIENTED_EDGE('',*,*,#11690,.F.);
#17822=ORIENTED_EDGE('',*,*,#11687,.F.);
#17823=ORIENTED_EDGE('',*,*,#11684,.F.);
#17824=ORIENTED_EDGE('',*,*,#11681,.F.);
#17825=ORIENTED_EDGE('',*,*,#11678,.F.);
#17826=ORIENTED_EDGE('',*,*,#11675,.F.);
#17827=ORIENTED_EDGE('',*,*,#11672,.F.);
#17828=ORIENTED_EDGE('',*,*,#11669,.F.);
#17829=ORIENTED_EDGE('',*,*,#11666,.F.);
#17830=ORIENTED_EDGE('',*,*,#11663,.F.);
#17831=ORIENTED_EDGE('',*,*,#11660,.F.);
#17832=ORIENTED_EDGE('',*,*,#11657,.F.);
#17833=ORIENTED_EDGE('',*,*,#11654,.F.);
#17834=ORIENTED_EDGE('',*,*,#11651,.F.);
#17835=ORIENTED_EDGE('',*,*,#11648,.F.);
#17836=ORIENTED_EDGE('',*,*,#11645,.F.);
#17837=ORIENTED_EDGE('',*,*,#11642,.F.);
#17838=ORIENTED_EDGE('',*,*,#11639,.F.);
#17839=ORIENTED_EDGE('',*,*,#11636,.F.);
#17840=ORIENTED_EDGE('',*,*,#11633,.F.);
#17841=ORIENTED_EDGE('',*,*,#11630,.F.);
#17842=ORIENTED_EDGE('',*,*,#11627,.F.);
#17843=ORIENTED_EDGE('',*,*,#11624,.F.);
#17844=ORIENTED_EDGE('',*,*,#11621,.F.);
#17845=ORIENTED_EDGE('',*,*,#11618,.F.);
#17846=ORIENTED_EDGE('',*,*,#11615,.F.);
#17847=ORIENTED_EDGE('',*,*,#11612,.F.);
#17848=ORIENTED_EDGE('',*,*,#11910,.T.);
#17849=ORIENTED_EDGE('',*,*,#12308,.T.);
#17850=ORIENTED_EDGE('',*,*,#12293,.T.);
#18989=PLANE('',#21644);
#18990=PLANE('',#21650);
#18991=PLANE('',#21651);
#18992=PLANE('',#21655);
#18993=PLANE('',#21657);
#18994=PLANE('',#21661);
#19742=ADVANCED_FACE('',(#1885),#922,.T.);
#19743=ADVANCED_FACE('',(#1886),#923,.T.);
#19744=ADVANCED_FACE('',(#1887),#924,.T.);
#19745=ADVANCED_FACE('',(#1888),#925,.T.);
#19746=ADVANCED_FACE('',(#1889),#926,.T.);
#19747=ADVANCED_FACE('',(#1890),#927,.T.);
#19748=ADVANCED_FACE('',(#1891),#928,.T.);
#19749=ADVANCED_FACE('',(#1892),#929,.T.);
#19750=ADVANCED_FACE('',(#1893),#930,.T.);
#19751=ADVANCED_FACE('',(#1894),#931,.T.);
#19752=ADVANCED_FACE('',(#1895),#932,.T.);
#19753=ADVANCED_FACE('',(#1896),#933,.T.);
#19754=ADVANCED_FACE('',(#1897),#934,.T.);
#19755=ADVANCED_FACE('',(#1898),#935,.T.);
#19756=ADVANCED_FACE('',(#1899),#936,.T.);
#19757=ADVANCED_FACE('',(#1900),#937,.T.);
#19758=ADVANCED_FACE('',(#1901),#938,.T.);
#19759=ADVANCED_FACE('',(#1902),#939,.T.);
#19760=ADVANCED_FACE('',(#1903),#940,.T.);
#19761=ADVANCED_FACE('',(#1904),#941,.T.);
#19762=ADVANCED_FACE('',(#1905),#942,.T.);
#19763=ADVANCED_FACE('',(#1906),#943,.T.);
#19764=ADVANCED_FACE('',(#1907),#944,.T.);
#19765=ADVANCED_FACE('',(#1908),#945,.T.);
#19766=ADVANCED_FACE('',(#1909),#946,.T.);
#19767=ADVANCED_FACE('',(#1910),#947,.T.);
#19768=ADVANCED_FACE('',(#1911),#948,.T.);
#19769=ADVANCED_FACE('',(#1912),#949,.T.);
#19770=ADVANCED_FACE('',(#1913),#950,.T.);
#19771=ADVANCED_FACE('',(#1914),#951,.T.);
#19772=ADVANCED_FACE('',(#1915),#952,.T.);
#19773=ADVANCED_FACE('',(#1916),#953,.T.);
#19774=ADVANCED_FACE('',(#1917),#954,.T.);
#19775=ADVANCED_FACE('',(#1918),#955,.T.);
#19776=ADVANCED_FACE('',(#1919),#956,.T.);
#19777=ADVANCED_FACE('',(#1920),#957,.T.);
#19778=ADVANCED_FACE('',(#1921),#958,.T.);
#19779=ADVANCED_FACE('',(#1922),#959,.T.);
#19780=ADVANCED_FACE('',(#1923),#960,.T.);
#19781=ADVANCED_FACE('',(#1924),#961,.T.);
#19782=ADVANCED_FACE('',(#1925),#962,.T.);
#19783=ADVANCED_FACE('',(#1926),#963,.T.);
#19784=ADVANCED_FACE('',(#1927),#964,.T.);
#19785=ADVANCED_FACE('',(#1928),#965,.T.);
#19786=ADVANCED_FACE('',(#1929),#966,.T.);
#19787=ADVANCED_FACE('',(#1930),#967,.T.);
#19788=ADVANCED_FACE('',(#1931),#968,.T.);
#19789=ADVANCED_FACE('',(#1932),#969,.T.);
#19790=ADVANCED_FACE('',(#1933),#970,.T.);
#19791=ADVANCED_FACE('',(#1934),#971,.T.);
#19792=ADVANCED_FACE('',(#1935),#972,.T.);
#19793=ADVANCED_FACE('',(#1936),#973,.T.);
#19794=ADVANCED_FACE('',(#1937),#974,.T.);
#19795=ADVANCED_FACE('',(#1938),#975,.T.);
#19796=ADVANCED_FACE('',(#1939),#976,.T.);
#19797=ADVANCED_FACE('',(#1940),#977,.T.);
#19798=ADVANCED_FACE('',(#1941),#978,.T.);
#19799=ADVANCED_FACE('',(#1942),#979,.T.);
#19800=ADVANCED_FACE('',(#1943),#980,.T.);
#19801=ADVANCED_FACE('',(#1944),#981,.T.);
#19802=ADVANCED_FACE('',(#1945),#982,.T.);
#19803=ADVANCED_FACE('',(#1946),#983,.T.);
#19804=ADVANCED_FACE('',(#1947),#984,.T.);
#19805=ADVANCED_FACE('',(#1948),#985,.T.);
#19806=ADVANCED_FACE('',(#1949),#986,.T.);
#19807=ADVANCED_FACE('',(#1950),#987,.T.);
#19808=ADVANCED_FACE('',(#1951),#988,.T.);
#19809=ADVANCED_FACE('',(#1952),#989,.T.);
#19810=ADVANCED_FACE('',(#1953),#990,.T.);
#19811=ADVANCED_FACE('',(#1954),#991,.T.);
#19812=ADVANCED_FACE('',(#1955),#992,.T.);
#19813=ADVANCED_FACE('',(#1956),#993,.T.);
#19814=ADVANCED_FACE('',(#1957),#994,.T.);
#19815=ADVANCED_FACE('',(#1958),#995,.T.);
#19816=ADVANCED_FACE('',(#1959),#996,.T.);
#19817=ADVANCED_FACE('',(#1960),#997,.T.);
#19818=ADVANCED_FACE('',(#1961),#998,.T.);
#19819=ADVANCED_FACE('',(#1962),#999,.T.);
#19820=ADVANCED_FACE('',(#1963),#1000,.T.);
#19821=ADVANCED_FACE('',(#1964),#1001,.T.);
#19822=ADVANCED_FACE('',(#1965),#1002,.T.);
#19823=ADVANCED_FACE('',(#1966),#1003,.T.);
#19824=ADVANCED_FACE('',(#1967),#1004,.T.);
#19825=ADVANCED_FACE('',(#1968),#1005,.T.);
#19826=ADVANCED_FACE('',(#1969),#1006,.T.);
#19827=ADVANCED_FACE('',(#1970),#1007,.T.);
#19828=ADVANCED_FACE('',(#1971),#1008,.T.);
#19829=ADVANCED_FACE('',(#1972),#1009,.T.);
#19830=ADVANCED_FACE('',(#1973),#1010,.T.);
#19831=ADVANCED_FACE('',(#1974),#1011,.T.);
#19832=ADVANCED_FACE('',(#1975),#1012,.T.);
#19833=ADVANCED_FACE('',(#1976),#1013,.T.);
#19834=ADVANCED_FACE('',(#1977),#1014,.T.);
#19835=ADVANCED_FACE('',(#1978),#1015,.T.);
#19836=ADVANCED_FACE('',(#1979),#1016,.T.);
#19837=ADVANCED_FACE('',(#1980),#1017,.T.);
#19838=ADVANCED_FACE('',(#1981),#1018,.T.);
#19839=ADVANCED_FACE('',(#1982),#1019,.T.);
#19840=ADVANCED_FACE('',(#1983),#1020,.T.);
#19841=ADVANCED_FACE('',(#1984),#1021,.T.);
#19842=ADVANCED_FACE('',(#1985),#1022,.T.);
#19843=ADVANCED_FACE('',(#1986),#1023,.T.);
#19844=ADVANCED_FACE('',(#1987),#1024,.T.);
#19845=ADVANCED_FACE('',(#1988),#1025,.T.);
#19846=ADVANCED_FACE('',(#1989),#1026,.T.);
#19847=ADVANCED_FACE('',(#1990),#1027,.T.);
#19848=ADVANCED_FACE('',(#1991),#1028,.T.);
#19849=ADVANCED_FACE('',(#1992),#1029,.T.);
#19850=ADVANCED_FACE('',(#1993),#1030,.T.);
#19851=ADVANCED_FACE('',(#1994),#1031,.T.);
#19852=ADVANCED_FACE('',(#1995),#1032,.T.);
#19853=ADVANCED_FACE('',(#1996),#1033,.T.);
#19854=ADVANCED_FACE('',(#1997),#1034,.T.);
#19855=ADVANCED_FACE('',(#1998),#1035,.T.);
#19856=ADVANCED_FACE('',(#1999),#1036,.T.);
#19857=ADVANCED_FACE('',(#2000),#1037,.T.);
#19858=ADVANCED_FACE('',(#2001),#1038,.T.);
#19859=ADVANCED_FACE('',(#2002),#1039,.T.);
#19860=ADVANCED_FACE('',(#2003),#1040,.T.);
#19861=ADVANCED_FACE('',(#2004),#1041,.T.);
#19862=ADVANCED_FACE('',(#2005),#1042,.T.);
#19863=ADVANCED_FACE('',(#2006),#1043,.T.);
#19864=ADVANCED_FACE('',(#2007),#1044,.T.);
#19865=ADVANCED_FACE('',(#2008),#1045,.T.);
#19866=ADVANCED_FACE('',(#2009),#1046,.T.);
#19867=ADVANCED_FACE('',(#2010),#1047,.T.);
#19868=ADVANCED_FACE('',(#2011),#1048,.T.);
#19869=ADVANCED_FACE('',(#2012),#1049,.T.);
#19870=ADVANCED_FACE('',(#2013),#1050,.T.);
#19871=ADVANCED_FACE('',(#2014),#1051,.T.);
#19872=ADVANCED_FACE('',(#2015),#1052,.T.);
#19873=ADVANCED_FACE('',(#2016),#1053,.T.);
#19874=ADVANCED_FACE('',(#2017),#1054,.T.);
#19875=ADVANCED_FACE('',(#2018),#1055,.T.);
#19876=ADVANCED_FACE('',(#2019),#1056,.T.);
#19877=ADVANCED_FACE('',(#2020),#1057,.T.);
#19878=ADVANCED_FACE('',(#2021),#1058,.T.);
#19879=ADVANCED_FACE('',(#2022),#1059,.T.);
#19880=ADVANCED_FACE('',(#2023),#1060,.T.);
#19881=ADVANCED_FACE('',(#2024),#1061,.T.);
#19882=ADVANCED_FACE('',(#2025),#1062,.T.);
#19883=ADVANCED_FACE('',(#2026),#1063,.T.);
#19884=ADVANCED_FACE('',(#2027),#1064,.T.);
#19885=ADVANCED_FACE('',(#2028),#1065,.T.);
#19886=ADVANCED_FACE('',(#2029),#1066,.T.);
#19887=ADVANCED_FACE('',(#2030),#1067,.T.);
#19888=ADVANCED_FACE('',(#2031),#1068,.T.);
#19889=ADVANCED_FACE('',(#2032),#1069,.T.);
#19890=ADVANCED_FACE('',(#2033),#1070,.T.);
#19891=ADVANCED_FACE('',(#2034),#1071,.T.);
#19892=ADVANCED_FACE('',(#2035),#1072,.T.);
#19893=ADVANCED_FACE('',(#2036),#1073,.T.);
#19894=ADVANCED_FACE('',(#2037),#1074,.T.);
#19895=ADVANCED_FACE('',(#2038),#1075,.T.);
#19896=ADVANCED_FACE('',(#2039),#1076,.T.);
#19897=ADVANCED_FACE('',(#2040),#1077,.T.);
#19898=ADVANCED_FACE('',(#2041),#1078,.T.);
#19899=ADVANCED_FACE('',(#2042),#1079,.T.);
#19900=ADVANCED_FACE('',(#2043),#1080,.T.);
#19901=ADVANCED_FACE('',(#2044),#1081,.T.);
#19902=ADVANCED_FACE('',(#2045),#1082,.T.);
#19903=ADVANCED_FACE('',(#2046),#1083,.T.);
#19904=ADVANCED_FACE('',(#2047),#1084,.T.);
#19905=ADVANCED_FACE('',(#2048),#1085,.T.);
#19906=ADVANCED_FACE('',(#2049),#1086,.T.);
#19907=ADVANCED_FACE('',(#2050),#1087,.T.);
#19908=ADVANCED_FACE('',(#2051),#1088,.T.);
#19909=ADVANCED_FACE('',(#2052),#1089,.T.);
#19910=ADVANCED_FACE('',(#2053),#1090,.T.);
#19911=ADVANCED_FACE('',(#2054),#1091,.T.);
#19912=ADVANCED_FACE('',(#2055),#1092,.T.);
#19913=ADVANCED_FACE('',(#2056),#1093,.T.);
#19914=ADVANCED_FACE('',(#2057),#1094,.T.);
#19915=ADVANCED_FACE('',(#2058),#1095,.T.);
#19916=ADVANCED_FACE('',(#2059),#1096,.T.);
#19917=ADVANCED_FACE('',(#2060),#1097,.T.);
#19918=ADVANCED_FACE('',(#2061),#1098,.T.);
#19919=ADVANCED_FACE('',(#2062),#1099,.T.);
#19920=ADVANCED_FACE('',(#2063),#1100,.T.);
#19921=ADVANCED_FACE('',(#2064),#1101,.T.);
#19922=ADVANCED_FACE('',(#2065),#1102,.T.);
#19923=ADVANCED_FACE('',(#2066),#1103,.T.);
#19924=ADVANCED_FACE('',(#2067),#1104,.T.);
#19925=ADVANCED_FACE('',(#2068),#1105,.T.);
#19926=ADVANCED_FACE('',(#2069),#1106,.T.);
#19927=ADVANCED_FACE('',(#2070),#1107,.T.);
#19928=ADVANCED_FACE('',(#2071),#1108,.T.);
#19929=ADVANCED_FACE('',(#2072),#1109,.T.);
#19930=ADVANCED_FACE('',(#2073),#1110,.T.);
#19931=ADVANCED_FACE('',(#2074),#1111,.T.);
#19932=ADVANCED_FACE('',(#2075),#1112,.T.);
#19933=ADVANCED_FACE('',(#2076),#1113,.T.);
#19934=ADVANCED_FACE('',(#2077),#1114,.T.);
#19935=ADVANCED_FACE('',(#2078),#1115,.T.);
#19936=ADVANCED_FACE('',(#2079),#1116,.T.);
#19937=ADVANCED_FACE('',(#2080),#1117,.T.);
#19938=ADVANCED_FACE('',(#2081),#1118,.T.);
#19939=ADVANCED_FACE('',(#2082),#1119,.T.);
#19940=ADVANCED_FACE('',(#2083),#1120,.T.);
#19941=ADVANCED_FACE('',(#2084),#1121,.T.);
#19942=ADVANCED_FACE('',(#2085),#1122,.T.);
#19943=ADVANCED_FACE('',(#2086),#1123,.T.);
#19944=ADVANCED_FACE('',(#2087),#1124,.T.);
#19945=ADVANCED_FACE('',(#2088),#1125,.T.);
#19946=ADVANCED_FACE('',(#2089),#1126,.T.);
#19947=ADVANCED_FACE('',(#2090),#1127,.T.);
#19948=ADVANCED_FACE('',(#2091),#1128,.T.);
#19949=ADVANCED_FACE('',(#2092),#1129,.T.);
#19950=ADVANCED_FACE('',(#2093),#1130,.T.);
#19951=ADVANCED_FACE('',(#2094),#1131,.T.);
#19952=ADVANCED_FACE('',(#2095),#1132,.T.);
#19953=ADVANCED_FACE('',(#2096),#1133,.T.);
#19954=ADVANCED_FACE('',(#2097),#1134,.T.);
#19955=ADVANCED_FACE('',(#2098),#1135,.T.);
#19956=ADVANCED_FACE('',(#2099),#1136,.T.);
#19957=ADVANCED_FACE('',(#2100),#1137,.T.);
#19958=ADVANCED_FACE('',(#2101),#1138,.T.);
#19959=ADVANCED_FACE('',(#2102),#1139,.T.);
#19960=ADVANCED_FACE('',(#2103),#1140,.T.);
#19961=ADVANCED_FACE('',(#2104),#1141,.T.);
#19962=ADVANCED_FACE('',(#2105),#1142,.T.);
#19963=ADVANCED_FACE('',(#2106),#592,.T.);
#19964=ADVANCED_FACE('',(#2107),#1143,.T.);
#19965=ADVANCED_FACE('',(#2108),#18989,.T.);
#19966=ADVANCED_FACE('',(#2109),#593,.T.);
#19967=ADVANCED_FACE('',(#2110),#1144,.T.);
#19968=ADVANCED_FACE('',(#2111),#18990,.T.);
#19969=ADVANCED_FACE('',(#2112,#685),#18991,.T.);
#19970=ADVANCED_FACE('',(#2113),#67,.F.);
#19971=ADVANCED_FACE('',(#2114),#1145,.T.);
#19972=ADVANCED_FACE('',(#2115,#686),#18992,.F.);
#19973=ADVANCED_FACE('',(#2116),#68,.T.);
#19974=ADVANCED_FACE('',(#2117),#18993,.F.);
#19975=ADVANCED_FACE('',(#2118),#1146,.T.);
#19976=ADVANCED_FACE('',(#2119),#69,.T.);
#19977=ADVANCED_FACE('',(#2120),#1147,.T.);
#19978=ADVANCED_FACE('',(#2121,#687),#18994,.T.);
#19979=ADVANCED_FACE('',(#2122),#70,.F.);
#19980=ADVANCED_FACE('',(#2123),#1148,.T.);
#20127=CLOSED_SHELL('',(#19742,#19743,#19744,#19745,#19746,#19747,#19748,
#19749,#19750,#19751,#19752,#19753,#19754,#19755,#19756,#19757,#19758,#19759,
#19760,#19761,#19762,#19763,#19764,#19765,#19766,#19767,#19768,#19769,#19770,
#19771,#19772,#19773,#19774,#19775,#19776,#19777,#19778,#19779,#19780,#19781,
#19782,#19783,#19784,#19785,#19786,#19787,#19788,#19789,#19790,#19791,#19792,
#19793,#19794,#19795,#19796,#19797,#19798,#19799,#19800,#19801,#19802,#19803,
#19804,#19805,#19806,#19807,#19808,#19809,#19810,#19811,#19812,#19813,#19814,
#19815,#19816,#19817,#19818,#19819,#19820,#19821,#19822,#19823,#19824,#19825,
#19826,#19827,#19828,#19829,#19830,#19831,#19832,#19833,#19834,#19835,#19836,
#19837,#19838,#19839,#19840,#19841,#19842,#19843,#19844,#19845,#19846,#19847,
#19848,#19849,#19850,#19851,#19852,#19853,#19854,#19855,#19856,#19857,#19858,
#19859,#19860,#19861,#19862,#19863,#19864,#19865,#19866,#19867,#19868,#19869,
#19870,#19871,#19872,#19873,#19874,#19875,#19876,#19877,#19878,#19879,#19880,
#19881,#19882,#19883,#19884,#19885,#19886,#19887,#19888,#19889,#19890,#19891,
#19892,#19893,#19894,#19895,#19896,#19897,#19898,#19899,#19900,#19901,#19902,
#19903,#19904,#19905,#19906,#19907,#19908,#19909,#19910,#19911,#19912,#19913,
#19914,#19915,#19916,#19917,#19918,#19919,#19920,#19921,#19922,#19923,#19924,
#19925,#19926,#19927,#19928,#19929,#19930,#19931,#19932,#19933,#19934,#19935,
#19936,#19937,#19938,#19939,#19940,#19941,#19942,#19943,#19944,#19945,#19946,
#19947,#19948,#19949,#19950,#19951,#19952,#19953,#19954,#19955,#19956,#19957,
#19958,#19959,#19960,#19961,#19962,#19963,#19964,#19965,#19966,#19967,#19968,
#19969,#19970,#19971,#19972,#19973,#19974,#19975,#19976,#19977,#19978,#19979,
#19980));
#21410=AXIS2_PLACEMENT_3D('',#30990,#25663,#25664);
#21411=AXIS2_PLACEMENT_3D('',#30991,#25665,#25666);
#21412=AXIS2_PLACEMENT_3D('',#31010,#25668,#25669);
#21413=AXIS2_PLACEMENT_3D('',#31015,#25670,#25671);
#21414=AXIS2_PLACEMENT_3D('',#31069,#25673,#25674);
#21415=AXIS2_PLACEMENT_3D('',#31126,#25676,#25677);
#21416=AXIS2_PLACEMENT_3D('',#31180,#25679,#25680);
#21417=AXIS2_PLACEMENT_3D('',#31234,#25682,#25683);
#21418=AXIS2_PLACEMENT_3D('',#31288,#25685,#25686);
#21419=AXIS2_PLACEMENT_3D('',#31339,#25688,#25689);
#21420=AXIS2_PLACEMENT_3D('',#31393,#25691,#25692);
#21421=AXIS2_PLACEMENT_3D('',#31447,#25694,#25695);
#21422=AXIS2_PLACEMENT_3D('',#31501,#25697,#25698);
#21423=AXIS2_PLACEMENT_3D('',#31555,#25700,#25701);
#21424=AXIS2_PLACEMENT_3D('',#31609,#25703,#25704);
#21425=AXIS2_PLACEMENT_3D('',#31663,#25706,#25707);
#21426=AXIS2_PLACEMENT_3D('',#31717,#25709,#25710);
#21427=AXIS2_PLACEMENT_3D('',#31771,#25712,#25713);
#21428=AXIS2_PLACEMENT_3D('',#31825,#25715,#25716);
#21429=AXIS2_PLACEMENT_3D('',#31879,#25718,#25719);
#21430=AXIS2_PLACEMENT_3D('',#31936,#25721,#25722);
#21431=AXIS2_PLACEMENT_3D('',#31990,#25724,#25725);
#21432=AXIS2_PLACEMENT_3D('',#32044,#25727,#25728);
#21433=AXIS2_PLACEMENT_3D('',#32098,#25730,#25731);
#21434=AXIS2_PLACEMENT_3D('',#32149,#25733,#25734);
#21435=AXIS2_PLACEMENT_3D('',#32203,#25736,#25737);
#21436=AXIS2_PLACEMENT_3D('',#32257,#25739,#25740);
#21437=AXIS2_PLACEMENT_3D('',#32311,#25742,#25743);
#21438=AXIS2_PLACEMENT_3D('',#32365,#25745,#25746);
#21439=AXIS2_PLACEMENT_3D('',#32419,#25748,#25749);
#21440=AXIS2_PLACEMENT_3D('',#32476,#25751,#25752);
#21441=AXIS2_PLACEMENT_3D('',#32530,#25754,#25755);
#21442=AXIS2_PLACEMENT_3D('',#32584,#25757,#25758);
#21443=AXIS2_PLACEMENT_3D('',#32641,#25760,#25761);
#21444=AXIS2_PLACEMENT_3D('',#32695,#25763,#25764);
#21445=AXIS2_PLACEMENT_3D('',#32749,#25766,#25767);
#21446=AXIS2_PLACEMENT_3D('',#32803,#25769,#25770);
#21447=AXIS2_PLACEMENT_3D('',#32857,#25772,#25773);
#21448=AXIS2_PLACEMENT_3D('',#32911,#25775,#25776);
#21449=AXIS2_PLACEMENT_3D('',#32962,#25778,#25779);
#21450=AXIS2_PLACEMENT_3D('',#33016,#25781,#25782);
#21451=AXIS2_PLACEMENT_3D('',#33070,#25784,#25785);
#21452=AXIS2_PLACEMENT_3D('',#33124,#25787,#25788);
#21453=AXIS2_PLACEMENT_3D('',#33181,#25790,#25791);
#21454=AXIS2_PLACEMENT_3D('',#33235,#25793,#25794);
#21455=AXIS2_PLACEMENT_3D('',#33289,#25796,#25797);
#21456=AXIS2_PLACEMENT_3D('',#33343,#25799,#25800);
#21457=AXIS2_PLACEMENT_3D('',#33397,#25802,#25803);
#21458=AXIS2_PLACEMENT_3D('',#33451,#25805,#25806);
#21459=AXIS2_PLACEMENT_3D('',#33505,#25808,#25809);
#21460=AXIS2_PLACEMENT_3D('',#33559,#25811,#25812);
#21461=AXIS2_PLACEMENT_3D('',#33613,#25814,#25815);
#21462=AXIS2_PLACEMENT_3D('',#33667,#25817,#25818);
#21463=AXIS2_PLACEMENT_3D('',#33721,#25820,#25821);
#21464=AXIS2_PLACEMENT_3D('',#33772,#25823,#25824);
#21465=AXIS2_PLACEMENT_3D('',#33826,#25826,#25827);
#21466=AXIS2_PLACEMENT_3D('',#33880,#25829,#25830);
#21467=AXIS2_PLACEMENT_3D('',#33934,#25832,#25833);
#21468=AXIS2_PLACEMENT_3D('',#33988,#25835,#25836);
#21469=AXIS2_PLACEMENT_3D('',#34042,#25838,#25839);
#21470=AXIS2_PLACEMENT_3D('',#34096,#25841,#25842);
#21471=AXIS2_PLACEMENT_3D('',#34147,#25844,#25845);
#21472=AXIS2_PLACEMENT_3D('',#34201,#25847,#25848);
#21473=AXIS2_PLACEMENT_3D('',#34255,#25850,#25851);
#21474=AXIS2_PLACEMENT_3D('',#34309,#25853,#25854);
#21475=AXIS2_PLACEMENT_3D('',#34360,#25856,#25857);
#21476=AXIS2_PLACEMENT_3D('',#34414,#25859,#25860);
#21477=AXIS2_PLACEMENT_3D('',#34468,#25862,#25863);
#21478=AXIS2_PLACEMENT_3D('',#34522,#25865,#25866);
#21479=AXIS2_PLACEMENT_3D('',#34576,#25868,#25869);
#21480=AXIS2_PLACEMENT_3D('',#34630,#25871,#25872);
#21481=AXIS2_PLACEMENT_3D('',#34687,#25874,#25875);
#21482=AXIS2_PLACEMENT_3D('',#34741,#25877,#25878);
#21483=AXIS2_PLACEMENT_3D('',#34795,#25880,#25881);
#21484=AXIS2_PLACEMENT_3D('',#34849,#25883,#25884);
#21485=AXIS2_PLACEMENT_3D('',#34903,#25886,#25887);
#21486=AXIS2_PLACEMENT_3D('',#34960,#25889,#25890);
#21487=AXIS2_PLACEMENT_3D('',#35014,#25892,#25893);
#21488=AXIS2_PLACEMENT_3D('',#35071,#25895,#25896);
#21489=AXIS2_PLACEMENT_3D('',#35125,#25898,#25899);
#21490=AXIS2_PLACEMENT_3D('',#35176,#25901,#25902);
#21491=AXIS2_PLACEMENT_3D('',#35230,#25904,#25905);
#21492=AXIS2_PLACEMENT_3D('',#35284,#25907,#25908);
#21493=AXIS2_PLACEMENT_3D('',#35338,#25910,#25911);
#21494=AXIS2_PLACEMENT_3D('',#35392,#25913,#25914);
#21495=AXIS2_PLACEMENT_3D('',#35446,#25916,#25917);
#21496=AXIS2_PLACEMENT_3D('',#35503,#25919,#25920);
#21497=AXIS2_PLACEMENT_3D('',#35557,#25922,#25923);
#21498=AXIS2_PLACEMENT_3D('',#35611,#25925,#25926);
#21499=AXIS2_PLACEMENT_3D('',#35665,#25928,#25929);
#21500=AXIS2_PLACEMENT_3D('',#35719,#25931,#25932);
#21501=AXIS2_PLACEMENT_3D('',#35773,#25934,#25935);
#21502=AXIS2_PLACEMENT_3D('',#35827,#25937,#25938);
#21503=AXIS2_PLACEMENT_3D('',#35881,#25940,#25941);
#21504=AXIS2_PLACEMENT_3D('',#35935,#25943,#25944);
#21505=AXIS2_PLACEMENT_3D('',#35986,#25946,#25947);
#21506=AXIS2_PLACEMENT_3D('',#36040,#25949,#25950);
#21507=AXIS2_PLACEMENT_3D('',#36094,#25952,#25953);
#21508=AXIS2_PLACEMENT_3D('',#36148,#25955,#25956);
#21509=AXIS2_PLACEMENT_3D('',#36202,#25958,#25959);
#21510=AXIS2_PLACEMENT_3D('',#36259,#25961,#25962);
#21511=AXIS2_PLACEMENT_3D('',#36313,#25964,#25965);
#21512=AXIS2_PLACEMENT_3D('',#36367,#25967,#25968);
#21513=AXIS2_PLACEMENT_3D('',#36372,#25970,#25971);
#21514=AXIS2_PLACEMENT_3D('',#36420,#25972,#25973);
#21515=AXIS2_PLACEMENT_3D('',#36444,#25976,#25977);
#21516=AXIS2_PLACEMENT_3D('',#36452,#25978,#25979);
#21517=AXIS2_PLACEMENT_3D('',#36466,#25980,#25981);
#21518=AXIS2_PLACEMENT_3D('',#36529,#25983,#25984);
#21519=AXIS2_PLACEMENT_3D('',#36590,#25986,#25987);
#21520=AXIS2_PLACEMENT_3D('',#36654,#25989,#25990);
#21521=AXIS2_PLACEMENT_3D('',#36718,#25992,#25993);
#21522=AXIS2_PLACEMENT_3D('',#36781,#25995,#25996);
#21523=AXIS2_PLACEMENT_3D('',#36842,#25998,#25999);
#21524=AXIS2_PLACEMENT_3D('',#36906,#26001,#26002);
#21525=AXIS2_PLACEMENT_3D('',#36969,#26004,#26005);
#21526=AXIS2_PLACEMENT_3D('',#36974,#26007,#26008);
#21527=AXIS2_PLACEMENT_3D('',#37030,#26009,#26010);
#21528=AXIS2_PLACEMENT_3D('',#37048,#26012,#26013);
#21529=AXIS2_PLACEMENT_3D('',#37058,#26014,#26015);
#21530=AXIS2_PLACEMENT_3D('',#37095,#26017,#26018);
#21531=AXIS2_PLACEMENT_3D('',#37133,#26020,#26021);
#21532=AXIS2_PLACEMENT_3D('',#37171,#26023,#26024);
#21533=AXIS2_PLACEMENT_3D('',#37207,#26026,#26027);
#21534=AXIS2_PLACEMENT_3D('',#37245,#26029,#26030);
#21535=AXIS2_PLACEMENT_3D('',#37283,#26032,#26033);
#21536=AXIS2_PLACEMENT_3D('',#37321,#26035,#26036);
#21537=AXIS2_PLACEMENT_3D('',#37357,#26038,#26039);
#21538=AXIS2_PLACEMENT_3D('',#37395,#26041,#26042);
#21539=AXIS2_PLACEMENT_3D('',#37410,#26044,#26045);
#21540=AXIS2_PLACEMENT_3D('',#37418,#26046,#26047);
#21541=AXIS2_PLACEMENT_3D('',#37444,#26049,#26050);
#21542=AXIS2_PLACEMENT_3D('',#37481,#26052,#26053);
#21543=AXIS2_PLACEMENT_3D('',#37524,#26055,#26056);
#21544=AXIS2_PLACEMENT_3D('',#37578,#26058,#26059);
#21545=AXIS2_PLACEMENT_3D('',#37629,#26061,#26062);
#21546=AXIS2_PLACEMENT_3D('',#37655,#26064,#26065);
#21547=AXIS2_PLACEMENT_3D('',#37683,#26067,#26068);
#21548=AXIS2_PLACEMENT_3D('',#37720,#26070,#26071);
#21549=AXIS2_PLACEMENT_3D('',#37774,#26073,#26074);
#21550=AXIS2_PLACEMENT_3D('',#37814,#26076,#26077);
#21551=AXIS2_PLACEMENT_3D('',#37842,#26079,#26080);
#21552=AXIS2_PLACEMENT_3D('',#37879,#26082,#26083);
#21553=AXIS2_PLACEMENT_3D('',#37919,#26085,#26086);
#21554=AXIS2_PLACEMENT_3D('',#37976,#26088,#26089);
#21555=AXIS2_PLACEMENT_3D('',#38030,#26091,#26092);
#21556=AXIS2_PLACEMENT_3D('',#38070,#26094,#26095);
#21557=AXIS2_PLACEMENT_3D('',#38096,#26097,#26098);
#21558=AXIS2_PLACEMENT_3D('',#38123,#26100,#26101);
#21559=AXIS2_PLACEMENT_3D('',#38163,#26103,#26104);
#21560=AXIS2_PLACEMENT_3D('',#38217,#26106,#26107);
#21561=AXIS2_PLACEMENT_3D('',#38261,#26109,#26110);
#21562=AXIS2_PLACEMENT_3D('',#38287,#26112,#26113);
#21563=AXIS2_PLACEMENT_3D('',#38313,#26115,#26116);
#21564=AXIS2_PLACEMENT_3D('',#38338,#26118,#26119);
#21565=AXIS2_PLACEMENT_3D('',#38366,#26121,#26122);
#21566=AXIS2_PLACEMENT_3D('',#38392,#26124,#26125);
#21567=AXIS2_PLACEMENT_3D('',#38418,#26127,#26128);
#21568=AXIS2_PLACEMENT_3D('',#38445,#26130,#26131);
#21569=AXIS2_PLACEMENT_3D('',#38471,#26133,#26134);
#21570=AXIS2_PLACEMENT_3D('',#38508,#26136,#26137);
#21571=AXIS2_PLACEMENT_3D('',#38548,#26139,#26140);
#21572=AXIS2_PLACEMENT_3D('',#38592,#26142,#26143);
#21573=AXIS2_PLACEMENT_3D('',#38617,#26145,#26146);
#21574=AXIS2_PLACEMENT_3D('',#38643,#26148,#26149);
#21575=AXIS2_PLACEMENT_3D('',#38671,#26151,#26152);
#21576=AXIS2_PLACEMENT_3D('',#38697,#26154,#26155);
#21577=AXIS2_PLACEMENT_3D('',#38734,#26157,#26158);
#21578=AXIS2_PLACEMENT_3D('',#38759,#26160,#26161);
#21579=AXIS2_PLACEMENT_3D('',#38787,#26163,#26164);
#21580=AXIS2_PLACEMENT_3D('',#38813,#26166,#26167);
#21581=AXIS2_PLACEMENT_3D('',#38839,#26169,#26170);
#21582=AXIS2_PLACEMENT_3D('',#38867,#26172,#26173);
#21583=AXIS2_PLACEMENT_3D('',#38892,#26175,#26176);
#21584=AXIS2_PLACEMENT_3D('',#38929,#26178,#26179);
#21585=AXIS2_PLACEMENT_3D('',#38955,#26181,#26182);
#21586=AXIS2_PLACEMENT_3D('',#38983,#26184,#26185);
#21587=AXIS2_PLACEMENT_3D('',#39009,#26187,#26188);
#21588=AXIS2_PLACEMENT_3D('',#39034,#26190,#26191);
#21589=AXIS2_PLACEMENT_3D('',#39062,#26193,#26194);
#21590=AXIS2_PLACEMENT_3D('',#39087,#26196,#26197);
#21591=AXIS2_PLACEMENT_3D('',#39124,#26199,#26200);
#21592=AXIS2_PLACEMENT_3D('',#39150,#26202,#26203);
#21593=AXIS2_PLACEMENT_3D('',#39178,#26205,#26206);
#21594=AXIS2_PLACEMENT_3D('',#39204,#26208,#26209);
#21595=AXIS2_PLACEMENT_3D('',#39229,#26211,#26212);
#21596=AXIS2_PLACEMENT_3D('',#39257,#26214,#26215);
#21597=AXIS2_PLACEMENT_3D('',#39283,#26217,#26218);
#21598=AXIS2_PLACEMENT_3D('',#39320,#26220,#26221);
#21599=AXIS2_PLACEMENT_3D('',#39346,#26223,#26224);
#21600=AXIS2_PLACEMENT_3D('',#39373,#26226,#26227);
#21601=AXIS2_PLACEMENT_3D('',#39399,#26229,#26230);
#21602=AXIS2_PLACEMENT_3D('',#39425,#26232,#26233);
#21603=AXIS2_PLACEMENT_3D('',#39453,#26235,#26236);
#21604=AXIS2_PLACEMENT_3D('',#39478,#26238,#26239);
#21605=AXIS2_PLACEMENT_3D('',#39504,#26241,#26242);
#21606=AXIS2_PLACEMENT_3D('',#39530,#26244,#26245);
#21607=AXIS2_PLACEMENT_3D('',#39558,#26247,#26248);
#21608=AXIS2_PLACEMENT_3D('',#39584,#26250,#26251);
#21609=AXIS2_PLACEMENT_3D('',#39610,#26253,#26254);
#21610=AXIS2_PLACEMENT_3D('',#39637,#26256,#26257);
#21611=AXIS2_PLACEMENT_3D('',#39663,#26259,#26260);
#21612=AXIS2_PLACEMENT_3D('',#39689,#26262,#26263);
#21613=AXIS2_PLACEMENT_3D('',#39715,#26265,#26266);
#21614=AXIS2_PLACEMENT_3D('',#39742,#26268,#26269);
#21615=AXIS2_PLACEMENT_3D('',#39768,#26271,#26272);
#21616=AXIS2_PLACEMENT_3D('',#39805,#26274,#26275);
#21617=AXIS2_PLACEMENT_3D('',#39833,#26277,#26278);
#21618=AXIS2_PLACEMENT_3D('',#39859,#26280,#26281);
#21619=AXIS2_PLACEMENT_3D('',#39885,#26283,#26284);
#21620=AXIS2_PLACEMENT_3D('',#39910,#26286,#26287);
#21621=AXIS2_PLACEMENT_3D('',#39938,#26289,#26290);
#21622=AXIS2_PLACEMENT_3D('',#39964,#26292,#26293);
#21623=AXIS2_PLACEMENT_3D('',#40001,#26295,#26296);
#21624=AXIS2_PLACEMENT_3D('',#40028,#26298,#26299);
#21625=AXIS2_PLACEMENT_3D('',#40054,#26301,#26302);
#21626=AXIS2_PLACEMENT_3D('',#40091,#26304,#26305);
#21627=AXIS2_PLACEMENT_3D('',#40117,#26307,#26308);
#21628=AXIS2_PLACEMENT_3D('',#40145,#26310,#26311);
#21629=AXIS2_PLACEMENT_3D('',#40170,#26313,#26314);
#21630=AXIS2_PLACEMENT_3D('',#40196,#26316,#26317);
#21631=AXIS2_PLACEMENT_3D('',#40224,#26319,#26320);
#21632=AXIS2_PLACEMENT_3D('',#40250,#26322,#26323);
#21633=AXIS2_PLACEMENT_3D('',#40287,#26325,#26326);
#21634=AXIS2_PLACEMENT_3D('',#40312,#26328,#26329);
#21635=AXIS2_PLACEMENT_3D('',#40340,#26331,#26332);
#21636=AXIS2_PLACEMENT_3D('',#40366,#26334,#26335);
#21637=AXIS2_PLACEMENT_3D('',#40392,#26337,#26338);
#21638=AXIS2_PLACEMENT_3D('',#40419,#26340,#26341);
#21639=AXIS2_PLACEMENT_3D('',#40445,#26343,#26344);
#21640=AXIS2_PLACEMENT_3D('',#40447,#26345,#26346);
#21641=AXIS2_PLACEMENT_3D('',#40450,#26348,#26349);
#21642=AXIS2_PLACEMENT_3D('',#40451,#26350,#26351);
#21643=AXIS2_PLACEMENT_3D('',#40454,#26353,#26354);
#21644=AXIS2_PLACEMENT_3D('',#40455,#26355,#26356);
#21645=AXIS2_PLACEMENT_3D('',#40456,#26357,#26358);
#21646=AXIS2_PLACEMENT_3D('',#40458,#26359,#26360);
#21647=AXIS2_PLACEMENT_3D('',#40461,#26362,#26363);
#21648=AXIS2_PLACEMENT_3D('',#40462,#26364,#26365);
#21649=AXIS2_PLACEMENT_3D('',#40465,#26367,#26368);
#21650=AXIS2_PLACEMENT_3D('',#40466,#26369,#26370);
#21651=AXIS2_PLACEMENT_3D('',#40467,#26371,#26372);
#21652=AXIS2_PLACEMENT_3D('',#40579,#26373,#26374);
#21653=AXIS2_PLACEMENT_3D('',#43550,#26375,#26376);
#21654=AXIS2_PLACEMENT_3D('',#43563,#26377,#26378);
#21655=AXIS2_PLACEMENT_3D('',#43564,#26379,#26380);
#21656=AXIS2_PLACEMENT_3D('',#43576,#26381,#26382);
#21657=AXIS2_PLACEMENT_3D('',#44132,#26383,#26384);
#21658=AXIS2_PLACEMENT_3D('',#44144,#26385,#26386);
#21659=AXIS2_PLACEMENT_3D('',#44145,#26387,#26388);
#21660=AXIS2_PLACEMENT_3D('',#44659,#26389,#26390);
#21661=AXIS2_PLACEMENT_3D('',#44660,#26391,#26392);
#21662=AXIS2_PLACEMENT_3D('',#47626,#26393,#26394);
#25663=DIRECTION('axis',(0.,0.,1.));
#25664=DIRECTION('refdir',(1.,0.,0.));
#25665=DIRECTION('center_axis',(0.,-1.,0.));
#25666=DIRECTION('ref_axis',(-1.,0.,0.));
#25667=DIRECTION('',(0.,1.,0.));
#25668=DIRECTION('center_axis',(0.,1.,0.));
#25669=DIRECTION('ref_axis',(-1.,0.,0.));
#25670=DIRECTION('center_axis',(0.,-1.,0.));
#25671=DIRECTION('ref_axis',(-1.,0.,0.));
#25672=DIRECTION('',(0.,1.,0.));
#25673=DIRECTION('center_axis',(0.,-1.,0.));
#25674=DIRECTION('ref_axis',(-1.,0.,0.));
#25675=DIRECTION('',(0.,1.,0.));
#25676=DIRECTION('center_axis',(0.,-1.,0.));
#25677=DIRECTION('ref_axis',(-1.,0.,0.));
#25678=DIRECTION('',(0.,1.,0.));
#25679=DIRECTION('center_axis',(0.,-1.,0.));
#25680=DIRECTION('ref_axis',(-1.,0.,0.));
#25681=DIRECTION('',(0.,1.,0.));
#25682=DIRECTION('center_axis',(0.,-1.,0.));
#25683=DIRECTION('ref_axis',(-1.,0.,0.));
#25684=DIRECTION('',(0.,1.,0.));
#25685=DIRECTION('center_axis',(0.,-1.,0.));
#25686=DIRECTION('ref_axis',(-1.,0.,0.));
#25687=DIRECTION('',(0.,1.,0.));
#25688=DIRECTION('center_axis',(0.,-1.,0.));
#25689=DIRECTION('ref_axis',(-1.,0.,0.));
#25690=DIRECTION('',(0.,1.,0.));
#25691=DIRECTION('center_axis',(0.,-1.,0.));
#25692=DIRECTION('ref_axis',(-1.,0.,0.));
#25693=DIRECTION('',(0.,1.,0.));
#25694=DIRECTION('center_axis',(0.,-1.,0.));
#25695=DIRECTION('ref_axis',(-1.,0.,0.));
#25696=DIRECTION('',(0.,1.,0.));
#25697=DIRECTION('center_axis',(0.,-1.,0.));
#25698=DIRECTION('ref_axis',(-1.,0.,0.));
#25699=DIRECTION('',(0.,1.,0.));
#25700=DIRECTION('center_axis',(0.,-1.,0.));
#25701=DIRECTION('ref_axis',(-1.,0.,0.));
#25702=DIRECTION('',(0.,1.,0.));
#25703=DIRECTION('center_axis',(0.,-1.,0.));
#25704=DIRECTION('ref_axis',(-1.,0.,0.));
#25705=DIRECTION('',(0.,1.,0.));
#25706=DIRECTION('center_axis',(0.,-1.,0.));
#25707=DIRECTION('ref_axis',(-1.,0.,0.));
#25708=DIRECTION('',(0.,1.,0.));
#25709=DIRECTION('center_axis',(0.,-1.,0.));
#25710=DIRECTION('ref_axis',(-1.,0.,0.));
#25711=DIRECTION('',(0.,1.,0.));
#25712=DIRECTION('center_axis',(0.,-1.,0.));
#25713=DIRECTION('ref_axis',(-1.,0.,0.));
#25714=DIRECTION('',(0.,1.,0.));
#25715=DIRECTION('center_axis',(0.,-1.,0.));
#25716=DIRECTION('ref_axis',(-1.,0.,0.));
#25717=DIRECTION('',(0.,1.,0.));
#25718=DIRECTION('center_axis',(0.,-1.,0.));
#25719=DIRECTION('ref_axis',(-1.,0.,0.));
#25720=DIRECTION('',(0.,1.,0.));
#25721=DIRECTION('center_axis',(0.,-1.,0.));
#25722=DIRECTION('ref_axis',(-1.,0.,0.));
#25723=DIRECTION('',(0.,1.,0.));
#25724=DIRECTION('center_axis',(0.,-1.,0.));
#25725=DIRECTION('ref_axis',(-1.,0.,0.));
#25726=DIRECTION('',(0.,1.,0.));
#25727=DIRECTION('center_axis',(0.,-1.,0.));
#25728=DIRECTION('ref_axis',(-1.,0.,0.));
#25729=DIRECTION('',(0.,1.,0.));
#25730=DIRECTION('center_axis',(0.,-1.,0.));
#25731=DIRECTION('ref_axis',(-1.,0.,0.));
#25732=DIRECTION('',(0.,1.,0.));
#25733=DIRECTION('center_axis',(0.,-1.,0.));
#25734=DIRECTION('ref_axis',(-1.,0.,0.));
#25735=DIRECTION('',(0.,1.,0.));
#25736=DIRECTION('center_axis',(0.,-1.,0.));
#25737=DIRECTION('ref_axis',(-1.,0.,0.));
#25738=DIRECTION('',(0.,1.,0.));
#25739=DIRECTION('center_axis',(0.,-1.,0.));
#25740=DIRECTION('ref_axis',(-1.,0.,0.));
#25741=DIRECTION('',(0.,1.,0.));
#25742=DIRECTION('center_axis',(0.,-1.,0.));
#25743=DIRECTION('ref_axis',(-1.,0.,0.));
#25744=DIRECTION('',(0.,1.,0.));
#25745=DIRECTION('center_axis',(0.,-1.,0.));
#25746=DIRECTION('ref_axis',(-1.,0.,0.));
#25747=DIRECTION('',(0.,1.,0.));
#25748=DIRECTION('center_axis',(0.,-1.,0.));
#25749=DIRECTION('ref_axis',(-1.,0.,0.));
#25750=DIRECTION('',(0.,1.,0.));
#25751=DIRECTION('center_axis',(0.,-1.,0.));
#25752=DIRECTION('ref_axis',(-1.,0.,0.));
#25753=DIRECTION('',(0.,1.,0.));
#25754=DIRECTION('center_axis',(0.,-1.,0.));
#25755=DIRECTION('ref_axis',(-1.,0.,0.));
#25756=DIRECTION('',(0.,1.,0.));
#25757=DIRECTION('center_axis',(0.,-1.,0.));
#25758=DIRECTION('ref_axis',(-1.,0.,0.));
#25759=DIRECTION('',(0.,1.,0.));
#25760=DIRECTION('center_axis',(0.,-1.,0.));
#25761=DIRECTION('ref_axis',(-1.,0.,0.));
#25762=DIRECTION('',(0.,1.,0.));
#25763=DIRECTION('center_axis',(0.,-1.,0.));
#25764=DIRECTION('ref_axis',(-1.,0.,0.));
#25765=DIRECTION('',(0.,1.,0.));
#25766=DIRECTION('center_axis',(0.,-1.,0.));
#25767=DIRECTION('ref_axis',(-1.,0.,0.));
#25768=DIRECTION('',(0.,1.,0.));
#25769=DIRECTION('center_axis',(0.,-1.,0.));
#25770=DIRECTION('ref_axis',(-1.,0.,0.));
#25771=DIRECTION('',(0.,1.,0.));
#25772=DIRECTION('center_axis',(0.,-1.,0.));
#25773=DIRECTION('ref_axis',(-1.,0.,0.));
#25774=DIRECTION('',(0.,1.,0.));
#25775=DIRECTION('center_axis',(0.,-1.,0.));
#25776=DIRECTION('ref_axis',(-1.,0.,0.));
#25777=DIRECTION('',(0.,1.,0.));
#25778=DIRECTION('center_axis',(0.,-1.,0.));
#25779=DIRECTION('ref_axis',(-1.,0.,0.));
#25780=DIRECTION('',(0.,1.,0.));
#25781=DIRECTION('center_axis',(0.,-1.,0.));
#25782=DIRECTION('ref_axis',(-1.,0.,0.));
#25783=DIRECTION('',(0.,1.,0.));
#25784=DIRECTION('center_axis',(0.,-1.,0.));
#25785=DIRECTION('ref_axis',(-1.,0.,0.));
#25786=DIRECTION('',(0.,1.,0.));
#25787=DIRECTION('center_axis',(0.,-1.,0.));
#25788=DIRECTION('ref_axis',(-1.,0.,0.));
#25789=DIRECTION('',(0.,1.,0.));
#25790=DIRECTION('center_axis',(0.,-1.,0.));
#25791=DIRECTION('ref_axis',(-1.,0.,0.));
#25792=DIRECTION('',(0.,1.,0.));
#25793=DIRECTION('center_axis',(0.,-1.,0.));
#25794=DIRECTION('ref_axis',(-1.,0.,0.));
#25795=DIRECTION('',(0.,1.,0.));
#25796=DIRECTION('center_axis',(0.,-1.,0.));
#25797=DIRECTION('ref_axis',(-1.,0.,0.));
#25798=DIRECTION('',(0.,1.,0.));
#25799=DIRECTION('center_axis',(0.,-1.,0.));
#25800=DIRECTION('ref_axis',(-1.,0.,0.));
#25801=DIRECTION('',(0.,1.,0.));
#25802=DIRECTION('center_axis',(0.,-1.,0.));
#25803=DIRECTION('ref_axis',(-1.,0.,0.));
#25804=DIRECTION('',(0.,1.,0.));
#25805=DIRECTION('center_axis',(0.,-1.,0.));
#25806=DIRECTION('ref_axis',(-1.,0.,0.));
#25807=DIRECTION('',(0.,1.,0.));
#25808=DIRECTION('center_axis',(0.,-1.,0.));
#25809=DIRECTION('ref_axis',(-1.,0.,0.));
#25810=DIRECTION('',(0.,1.,0.));
#25811=DIRECTION('center_axis',(0.,-1.,0.));
#25812=DIRECTION('ref_axis',(-1.,0.,0.));
#25813=DIRECTION('',(0.,1.,0.));
#25814=DIRECTION('center_axis',(0.,-1.,0.));
#25815=DIRECTION('ref_axis',(-1.,0.,0.));
#25816=DIRECTION('',(0.,1.,0.));
#25817=DIRECTION('center_axis',(0.,-1.,0.));
#25818=DIRECTION('ref_axis',(-1.,0.,0.));
#25819=DIRECTION('',(0.,1.,0.));
#25820=DIRECTION('center_axis',(0.,-1.,0.));
#25821=DIRECTION('ref_axis',(-1.,0.,0.));
#25822=DIRECTION('',(0.,1.,0.));
#25823=DIRECTION('center_axis',(0.,-1.,0.));
#25824=DIRECTION('ref_axis',(-1.,0.,0.));
#25825=DIRECTION('',(0.,1.,0.));
#25826=DIRECTION('center_axis',(0.,-1.,0.));
#25827=DIRECTION('ref_axis',(-1.,0.,0.));
#25828=DIRECTION('',(0.,1.,0.));
#25829=DIRECTION('center_axis',(0.,-1.,0.));
#25830=DIRECTION('ref_axis',(-1.,0.,0.));
#25831=DIRECTION('',(0.,1.,0.));
#25832=DIRECTION('center_axis',(0.,-1.,0.));
#25833=DIRECTION('ref_axis',(-1.,0.,0.));
#25834=DIRECTION('',(0.,1.,0.));
#25835=DIRECTION('center_axis',(0.,-1.,0.));
#25836=DIRECTION('ref_axis',(-1.,0.,0.));
#25837=DIRECTION('',(0.,1.,0.));
#25838=DIRECTION('center_axis',(0.,-1.,0.));
#25839=DIRECTION('ref_axis',(-1.,0.,0.));
#25840=DIRECTION('',(0.,1.,0.));
#25841=DIRECTION('center_axis',(0.,-1.,0.));
#25842=DIRECTION('ref_axis',(-1.,0.,0.));
#25843=DIRECTION('',(0.,1.,0.));
#25844=DIRECTION('center_axis',(0.,-1.,0.));
#25845=DIRECTION('ref_axis',(-1.,0.,0.));
#25846=DIRECTION('',(0.,1.,0.));
#25847=DIRECTION('center_axis',(0.,-1.,0.));
#25848=DIRECTION('ref_axis',(-1.,0.,0.));
#25849=DIRECTION('',(0.,1.,0.));
#25850=DIRECTION('center_axis',(0.,-1.,0.));
#25851=DIRECTION('ref_axis',(-1.,0.,0.));
#25852=DIRECTION('',(0.,1.,0.));
#25853=DIRECTION('center_axis',(0.,-1.,0.));
#25854=DIRECTION('ref_axis',(-1.,0.,0.));
#25855=DIRECTION('',(0.,1.,0.));
#25856=DIRECTION('center_axis',(0.,-1.,0.));
#25857=DIRECTION('ref_axis',(-1.,0.,0.));
#25858=DIRECTION('',(0.,1.,0.));
#25859=DIRECTION('center_axis',(0.,-1.,0.));
#25860=DIRECTION('ref_axis',(-1.,0.,0.));
#25861=DIRECTION('',(0.,1.,0.));
#25862=DIRECTION('center_axis',(0.,-1.,0.));
#25863=DIRECTION('ref_axis',(-1.,0.,0.));
#25864=DIRECTION('',(0.,1.,0.));
#25865=DIRECTION('center_axis',(0.,-1.,0.));
#25866=DIRECTION('ref_axis',(-1.,0.,0.));
#25867=DIRECTION('',(0.,1.,0.));
#25868=DIRECTION('center_axis',(0.,-1.,0.));
#25869=DIRECTION('ref_axis',(-1.,0.,0.));
#25870=DIRECTION('',(0.,1.,0.));
#25871=DIRECTION('center_axis',(0.,-1.,0.));
#25872=DIRECTION('ref_axis',(-1.,0.,0.));
#25873=DIRECTION('',(0.,1.,0.));
#25874=DIRECTION('center_axis',(0.,-1.,0.));
#25875=DIRECTION('ref_axis',(-1.,0.,0.));
#25876=DIRECTION('',(0.,1.,0.));
#25877=DIRECTION('center_axis',(0.,-1.,0.));
#25878=DIRECTION('ref_axis',(-1.,0.,0.));
#25879=DIRECTION('',(0.,1.,0.));
#25880=DIRECTION('center_axis',(0.,-1.,0.));
#25881=DIRECTION('ref_axis',(-1.,0.,0.));
#25882=DIRECTION('',(0.,1.,0.));
#25883=DIRECTION('center_axis',(0.,-1.,0.));
#25884=DIRECTION('ref_axis',(-1.,0.,0.));
#25885=DIRECTION('',(0.,1.,0.));
#25886=DIRECTION('center_axis',(0.,-1.,0.));
#25887=DIRECTION('ref_axis',(-1.,0.,0.));
#25888=DIRECTION('',(0.,1.,0.));
#25889=DIRECTION('center_axis',(0.,-1.,0.));
#25890=DIRECTION('ref_axis',(-1.,0.,0.));
#25891=DIRECTION('',(0.,1.,0.));
#25892=DIRECTION('center_axis',(0.,-1.,0.));
#25893=DIRECTION('ref_axis',(-1.,0.,0.));
#25894=DIRECTION('',(0.,1.,0.));
#25895=DIRECTION('center_axis',(0.,-1.,0.));
#25896=DIRECTION('ref_axis',(-1.,0.,0.));
#25897=DIRECTION('',(0.,1.,0.));
#25898=DIRECTION('center_axis',(0.,-1.,0.));
#25899=DIRECTION('ref_axis',(-1.,0.,0.));
#25900=DIRECTION('',(0.,1.,0.));
#25901=DIRECTION('center_axis',(0.,-1.,0.));
#25902=DIRECTION('ref_axis',(-1.,0.,0.));
#25903=DIRECTION('',(0.,1.,0.));
#25904=DIRECTION('center_axis',(0.,-1.,0.));
#25905=DIRECTION('ref_axis',(-1.,0.,0.));
#25906=DIRECTION('',(0.,1.,0.));
#25907=DIRECTION('center_axis',(0.,-1.,0.));
#25908=DIRECTION('ref_axis',(-1.,0.,0.));
#25909=DIRECTION('',(0.,1.,0.));
#25910=DIRECTION('center_axis',(0.,-1.,0.));
#25911=DIRECTION('ref_axis',(-1.,0.,0.));
#25912=DIRECTION('',(0.,1.,0.));
#25913=DIRECTION('center_axis',(0.,-1.,0.));
#25914=DIRECTION('ref_axis',(-1.,0.,0.));
#25915=DIRECTION('',(0.,1.,0.));
#25916=DIRECTION('center_axis',(0.,-1.,0.));
#25917=DIRECTION('ref_axis',(-1.,0.,0.));
#25918=DIRECTION('',(0.,1.,0.));
#25919=DIRECTION('center_axis',(0.,-1.,0.));
#25920=DIRECTION('ref_axis',(-1.,0.,0.));
#25921=DIRECTION('',(0.,1.,0.));
#25922=DIRECTION('center_axis',(0.,-1.,0.));
#25923=DIRECTION('ref_axis',(-1.,0.,0.));
#25924=DIRECTION('',(0.,1.,0.));
#25925=DIRECTION('center_axis',(0.,-1.,0.));
#25926=DIRECTION('ref_axis',(-1.,0.,0.));
#25927=DIRECTION('',(0.,1.,0.));
#25928=DIRECTION('center_axis',(0.,-1.,0.));
#25929=DIRECTION('ref_axis',(-1.,0.,0.));
#25930=DIRECTION('',(0.,1.,0.));
#25931=DIRECTION('center_axis',(0.,-1.,0.));
#25932=DIRECTION('ref_axis',(-1.,0.,0.));
#25933=DIRECTION('',(0.,1.,0.));
#25934=DIRECTION('center_axis',(0.,-1.,0.));
#25935=DIRECTION('ref_axis',(-1.,0.,0.));
#25936=DIRECTION('',(0.,1.,0.));
#25937=DIRECTION('center_axis',(0.,-1.,0.));
#25938=DIRECTION('ref_axis',(-1.,0.,0.));
#25939=DIRECTION('',(0.,1.,0.));
#25940=DIRECTION('center_axis',(0.,-1.,0.));
#25941=DIRECTION('ref_axis',(-1.,0.,0.));
#25942=DIRECTION('',(0.,1.,0.));
#25943=DIRECTION('center_axis',(0.,-1.,0.));
#25944=DIRECTION('ref_axis',(-1.,0.,0.));
#25945=DIRECTION('',(0.,1.,0.));
#25946=DIRECTION('center_axis',(0.,-1.,0.));
#25947=DIRECTION('ref_axis',(-1.,0.,0.));
#25948=DIRECTION('',(0.,1.,0.));
#25949=DIRECTION('center_axis',(0.,-1.,0.));
#25950=DIRECTION('ref_axis',(-1.,0.,0.));
#25951=DIRECTION('',(0.,1.,0.));
#25952=DIRECTION('center_axis',(0.,-1.,0.));
#25953=DIRECTION('ref_axis',(-1.,0.,0.));
#25954=DIRECTION('',(0.,1.,0.));
#25955=DIRECTION('center_axis',(0.,-1.,0.));
#25956=DIRECTION('ref_axis',(-1.,0.,0.));
#25957=DIRECTION('',(0.,1.,0.));
#25958=DIRECTION('center_axis',(0.,-1.,0.));
#25959=DIRECTION('ref_axis',(-1.,0.,0.));
#25960=DIRECTION('',(0.,1.,0.));
#25961=DIRECTION('center_axis',(0.,-1.,0.));
#25962=DIRECTION('ref_axis',(-1.,0.,0.));
#25963=DIRECTION('',(0.,1.,0.));
#25964=DIRECTION('center_axis',(0.,-1.,0.));
#25965=DIRECTION('ref_axis',(-1.,0.,0.));
#25966=DIRECTION('',(0.,1.,0.));
#25967=DIRECTION('center_axis',(0.,-1.,0.));
#25968=DIRECTION('ref_axis',(-1.,0.,0.));
#25969=DIRECTION('',(0.,1.,0.));
#25970=DIRECTION('center_axis',(0.,1.,0.));
#25971=DIRECTION('ref_axis',(-1.,0.,0.));
#25972=DIRECTION('center_axis',(0.,1.,0.));
#25973=DIRECTION('ref_axis',(1.,0.,0.));
#25974=DIRECTION('',(0.,-1.,0.));
#25975=DIRECTION('',(0.,-1.,0.));
#25976=DIRECTION('center_axis',(0.,1.,0.));
#25977=DIRECTION('ref_axis',(1.,0.,0.));
#25978=DIRECTION('center_axis',(0.,-1.,0.));
#25979=DIRECTION('ref_axis',(1.,0.,0.));
#25980=DIRECTION('center_axis',(0.,1.,0.));
#25981=DIRECTION('ref_axis',(1.,0.,0.));
#25982=DIRECTION('',(0.,-1.,0.));
#25983=DIRECTION('center_axis',(0.,1.,0.));
#25984=DIRECTION('ref_axis',(1.,0.,0.));
#25985=DIRECTION('',(0.,-1.,0.));
#25986=DIRECTION('center_axis',(0.,1.,0.));
#25987=DIRECTION('ref_axis',(1.,0.,0.));
#25988=DIRECTION('',(0.,-1.,0.));
#25989=DIRECTION('center_axis',(0.,1.,0.));
#25990=DIRECTION('ref_axis',(1.,0.,0.));
#25991=DIRECTION('',(0.,-1.,0.));
#25992=DIRECTION('center_axis',(0.,1.,0.));
#25993=DIRECTION('ref_axis',(1.,0.,0.));
#25994=DIRECTION('',(0.,-1.,0.));
#25995=DIRECTION('center_axis',(0.,1.,0.));
#25996=DIRECTION('ref_axis',(1.,0.,0.));
#25997=DIRECTION('',(0.,-1.,0.));
#25998=DIRECTION('center_axis',(0.,1.,0.));
#25999=DIRECTION('ref_axis',(1.,0.,0.));
#26000=DIRECTION('',(0.,-1.,0.));
#26001=DIRECTION('center_axis',(0.,1.,0.));
#26002=DIRECTION('ref_axis',(1.,0.,0.));
#26003=DIRECTION('',(0.,-1.,0.));
#26004=DIRECTION('center_axis',(0.,1.,0.));
#26005=DIRECTION('ref_axis',(1.,0.,0.));
#26006=DIRECTION('',(0.,-1.,0.));
#26007=DIRECTION('center_axis',(0.,-1.,0.));
#26008=DIRECTION('ref_axis',(1.,0.,0.));
#26009=DIRECTION('center_axis',(0.,1.,0.));
#26010=DIRECTION('ref_axis',(0.409697292977236,0.,0.912221534566645));
#26011=DIRECTION('',(0.,1.,0.));
#26012=DIRECTION('center_axis',(0.,1.,0.));
#26013=DIRECTION('ref_axis',(1.,0.,-6.50117889680365E-14));
#26014=DIRECTION('center_axis',(0.,1.,0.));
#26015=DIRECTION('ref_axis',(1.,0.,-6.50117889680365E-14));
#26016=DIRECTION('',(0.,1.,0.));
#26017=DIRECTION('center_axis',(0.,1.,0.));
#26018=DIRECTION('ref_axis',(1.,0.,-6.50117889680365E-14));
#26019=DIRECTION('',(0.,1.,0.));
#26020=DIRECTION('center_axis',(0.,1.,0.));
#26021=DIRECTION('ref_axis',(1.,0.,-6.50117889680365E-14));
#26022=DIRECTION('',(0.,1.,0.));
#26023=DIRECTION('center_axis',(0.,1.,0.));
#26024=DIRECTION('ref_axis',(1.,0.,-6.50117889680365E-14));
#26025=DIRECTION('',(0.,1.,0.));
#26026=DIRECTION('center_axis',(0.,1.,0.));
#26027=DIRECTION('ref_axis',(1.,0.,-6.50117889680365E-14));
#26028=DIRECTION('',(0.,1.,0.));
#26029=DIRECTION('center_axis',(0.,1.,0.));
#26030=DIRECTION('ref_axis',(1.,0.,-6.50117889680365E-14));
#26031=DIRECTION('',(0.,1.,0.));
#26032=DIRECTION('center_axis',(0.,1.,0.));
#26033=DIRECTION('ref_axis',(1.,0.,-6.50117889680365E-14));
#26034=DIRECTION('',(0.,1.,0.));
#26035=DIRECTION('center_axis',(0.,1.,0.));
#26036=DIRECTION('ref_axis',(1.,0.,-6.50117889680365E-14));
#26037=DIRECTION('',(0.,1.,0.));
#26038=DIRECTION('center_axis',(0.,1.,0.));
#26039=DIRECTION('ref_axis',(1.,0.,-6.50117889680365E-14));
#26040=DIRECTION('',(0.,1.,0.));
#26041=DIRECTION('center_axis',(0.,-1.,0.));
#26042=DIRECTION('ref_axis',(-1.,0.,2.36700689860723E-12));
#26043=DIRECTION('',(0.,-1.,0.));
#26044=DIRECTION('center_axis',(0.,1.,0.));
#26045=DIRECTION('ref_axis',(-1.,0.,2.36700689860723E-12));
#26046=DIRECTION('center_axis',(0.,-1.,0.));
#26047=DIRECTION('ref_axis',(-1.,0.,2.36700689860723E-12));
#26048=DIRECTION('',(0.,-1.,0.));
#26049=DIRECTION('center_axis',(0.,-1.,0.));
#26050=DIRECTION('ref_axis',(-1.,0.,2.36700689860723E-12));
#26051=DIRECTION('',(0.,-1.,0.));
#26052=DIRECTION('center_axis',(0.,-1.,0.));
#26053=DIRECTION('ref_axis',(-1.,0.,2.36700689860723E-12));
#26054=DIRECTION('',(0.,-1.,0.));
#26055=DIRECTION('center_axis',(0.,-1.,0.));
#26056=DIRECTION('ref_axis',(-1.,0.,2.36700689860723E-12));
#26057=DIRECTION('',(0.,-1.,0.));
#26058=DIRECTION('center_axis',(0.,-1.,0.));
#26059=DIRECTION('ref_axis',(-1.,0.,2.36700689860723E-12));
#26060=DIRECTION('',(0.,-1.,0.));
#26061=DIRECTION('center_axis',(0.,-1.,0.));
#26062=DIRECTION('ref_axis',(-1.,0.,2.36700689860723E-12));
#26063=DIRECTION('',(0.,-1.,0.));
#26064=DIRECTION('center_axis',(0.,-1.,0.));
#26065=DIRECTION('ref_axis',(-1.,0.,2.36700689860723E-12));
#26066=DIRECTION('',(0.,-1.,0.));
#26067=DIRECTION('center_axis',(0.,-1.,0.));
#26068=DIRECTION('ref_axis',(-1.,0.,2.36700689860723E-12));
#26069=DIRECTION('',(0.,-1.,0.));
#26070=DIRECTION('center_axis',(0.,-1.,0.));
#26071=DIRECTION('ref_axis',(-1.,0.,2.36700689860723E-12));
#26072=DIRECTION('',(0.,-1.,0.));
#26073=DIRECTION('center_axis',(0.,-1.,0.));
#26074=DIRECTION('ref_axis',(-1.,0.,2.36700689860723E-12));
#26075=DIRECTION('',(0.,-1.,0.));
#26076=DIRECTION('center_axis',(0.,-1.,0.));
#26077=DIRECTION('ref_axis',(-1.,0.,2.36700689860723E-12));
#26078=DIRECTION('',(0.,-1.,0.));
#26079=DIRECTION('center_axis',(0.,-1.,0.));
#26080=DIRECTION('ref_axis',(-1.,0.,2.36700689860723E-12));
#26081=DIRECTION('',(0.,-1.,0.));
#26082=DIRECTION('center_axis',(0.,-1.,0.));
#26083=DIRECTION('ref_axis',(-1.,0.,2.36700689860723E-12));
#26084=DIRECTION('',(0.,-1.,0.));
#26085=DIRECTION('center_axis',(0.,-1.,0.));
#26086=DIRECTION('ref_axis',(-1.,0.,2.36700689860723E-12));
#26087=DIRECTION('',(0.,-1.,0.));
#26088=DIRECTION('center_axis',(0.,-1.,0.));
#26089=DIRECTION('ref_axis',(-1.,0.,2.36700689860723E-12));
#26090=DIRECTION('',(0.,-1.,0.));
#26091=DIRECTION('center_axis',(0.,-1.,0.));
#26092=DIRECTION('ref_axis',(-1.,0.,2.36700689860723E-12));
#26093=DIRECTION('',(0.,-1.,0.));
#26094=DIRECTION('center_axis',(0.,-1.,0.));
#26095=DIRECTION('ref_axis',(-1.,0.,2.36700689860723E-12));
#26096=DIRECTION('',(0.,-1.,0.));
#26097=DIRECTION('center_axis',(0.,-1.,0.));
#26098=DIRECTION('ref_axis',(-1.,0.,2.36700689860723E-12));
#26099=DIRECTION('',(0.,-1.,0.));
#26100=DIRECTION('center_axis',(0.,-1.,0.));
#26101=DIRECTION('ref_axis',(-1.,0.,2.36700689860723E-12));
#26102=DIRECTION('',(0.,-1.,0.));
#26103=DIRECTION('center_axis',(0.,-1.,0.));
#26104=DIRECTION('ref_axis',(-1.,0.,2.36700689860723E-12));
#26105=DIRECTION('',(0.,-1.,0.));
#26106=DIRECTION('center_axis',(0.,-1.,0.));
#26107=DIRECTION('ref_axis',(-1.,0.,2.36700689860723E-12));
#26108=DIRECTION('',(0.,-1.,0.));
#26109=DIRECTION('center_axis',(0.,-1.,0.));
#26110=DIRECTION('ref_axis',(-1.,0.,2.36700689860723E-12));
#26111=DIRECTION('',(0.,-1.,0.));
#26112=DIRECTION('center_axis',(0.,-1.,0.));
#26113=DIRECTION('ref_axis',(-1.,0.,2.36700689860723E-12));
#26114=DIRECTION('',(0.,-1.,0.));
#26115=DIRECTION('center_axis',(0.,-1.,0.));
#26116=DIRECTION('ref_axis',(-1.,0.,2.36700689860723E-12));
#26117=DIRECTION('',(0.,-1.,0.));
#26118=DIRECTION('center_axis',(0.,-1.,0.));
#26119=DIRECTION('ref_axis',(-1.,0.,2.36700689860723E-12));
#26120=DIRECTION('',(0.,-1.,0.));
#26121=DIRECTION('center_axis',(0.,-1.,0.));
#26122=DIRECTION('ref_axis',(-1.,0.,2.36700689860723E-12));
#26123=DIRECTION('',(0.,-1.,0.));
#26124=DIRECTION('center_axis',(0.,-1.,0.));
#26125=DIRECTION('ref_axis',(-1.,0.,2.36700689860723E-12));
#26126=DIRECTION('',(0.,-1.,0.));
#26127=DIRECTION('center_axis',(0.,-1.,0.));
#26128=DIRECTION('ref_axis',(-1.,0.,2.36700689860723E-12));
#26129=DIRECTION('',(0.,-1.,0.));
#26130=DIRECTION('center_axis',(0.,-1.,0.));
#26131=DIRECTION('ref_axis',(-1.,0.,2.36700689860723E-12));
#26132=DIRECTION('',(0.,-1.,0.));
#26133=DIRECTION('center_axis',(0.,-1.,0.));
#26134=DIRECTION('ref_axis',(-1.,0.,2.36700689860723E-12));
#26135=DIRECTION('',(0.,-1.,0.));
#26136=DIRECTION('center_axis',(0.,-1.,0.));
#26137=DIRECTION('ref_axis',(-1.,0.,2.36700689860723E-12));
#26138=DIRECTION('',(0.,-1.,0.));
#26139=DIRECTION('center_axis',(0.,-1.,0.));
#26140=DIRECTION('ref_axis',(-1.,0.,2.36700689860723E-12));
#26141=DIRECTION('',(0.,-1.,0.));
#26142=DIRECTION('center_axis',(0.,-1.,0.));
#26143=DIRECTION('ref_axis',(-1.,0.,2.36700689860723E-12));
#26144=DIRECTION('',(0.,-1.,0.));
#26145=DIRECTION('center_axis',(0.,-1.,0.));
#26146=DIRECTION('ref_axis',(-1.,0.,2.36700689860723E-12));
#26147=DIRECTION('',(0.,-1.,0.));
#26148=DIRECTION('center_axis',(0.,-1.,0.));
#26149=DIRECTION('ref_axis',(-1.,0.,2.36700689860723E-12));
#26150=DIRECTION('',(0.,-1.,0.));
#26151=DIRECTION('center_axis',(0.,-1.,0.));
#26152=DIRECTION('ref_axis',(-1.,0.,2.36700689860723E-12));
#26153=DIRECTION('',(0.,-1.,0.));
#26154=DIRECTION('center_axis',(0.,-1.,0.));
#26155=DIRECTION('ref_axis',(-1.,0.,2.36700689860723E-12));
#26156=DIRECTION('',(0.,-1.,0.));
#26157=DIRECTION('center_axis',(0.,-1.,0.));
#26158=DIRECTION('ref_axis',(-1.,0.,2.36700689860723E-12));
#26159=DIRECTION('',(0.,-1.,0.));
#26160=DIRECTION('center_axis',(0.,-1.,0.));
#26161=DIRECTION('ref_axis',(-1.,0.,2.36700689860723E-12));
#26162=DIRECTION('',(0.,-1.,0.));
#26163=DIRECTION('center_axis',(0.,-1.,0.));
#26164=DIRECTION('ref_axis',(-1.,0.,2.36700689860723E-12));
#26165=DIRECTION('',(0.,-1.,0.));
#26166=DIRECTION('center_axis',(0.,-1.,0.));
#26167=DIRECTION('ref_axis',(-1.,0.,2.36700689860723E-12));
#26168=DIRECTION('',(0.,-1.,0.));
#26169=DIRECTION('center_axis',(0.,-1.,0.));
#26170=DIRECTION('ref_axis',(-1.,0.,2.36700689860723E-12));
#26171=DIRECTION('',(0.,-1.,0.));
#26172=DIRECTION('center_axis',(0.,-1.,0.));
#26173=DIRECTION('ref_axis',(-1.,0.,2.36700689860723E-12));
#26174=DIRECTION('',(0.,-1.,0.));
#26175=DIRECTION('center_axis',(0.,-1.,0.));
#26176=DIRECTION('ref_axis',(-1.,0.,2.36700689860723E-12));
#26177=DIRECTION('',(0.,-1.,0.));
#26178=DIRECTION('center_axis',(0.,-1.,0.));
#26179=DIRECTION('ref_axis',(-1.,0.,2.36700689860723E-12));
#26180=DIRECTION('',(0.,-1.,0.));
#26181=DIRECTION('center_axis',(0.,-1.,0.));
#26182=DIRECTION('ref_axis',(-1.,0.,2.36700689860723E-12));
#26183=DIRECTION('',(0.,-1.,0.));
#26184=DIRECTION('center_axis',(0.,-1.,0.));
#26185=DIRECTION('ref_axis',(-1.,0.,2.36700689860723E-12));
#26186=DIRECTION('',(0.,-1.,0.));
#26187=DIRECTION('center_axis',(0.,-1.,0.));
#26188=DIRECTION('ref_axis',(-1.,0.,2.36700689860723E-12));
#26189=DIRECTION('',(0.,-1.,0.));
#26190=DIRECTION('center_axis',(0.,-1.,0.));
#26191=DIRECTION('ref_axis',(-1.,0.,2.36700689860723E-12));
#26192=DIRECTION('',(0.,-1.,0.));
#26193=DIRECTION('center_axis',(0.,-1.,0.));
#26194=DIRECTION('ref_axis',(-1.,0.,2.36700689860723E-12));
#26195=DIRECTION('',(0.,-1.,0.));
#26196=DIRECTION('center_axis',(0.,-1.,0.));
#26197=DIRECTION('ref_axis',(-1.,0.,2.36700689860723E-12));
#26198=DIRECTION('',(0.,-1.,0.));
#26199=DIRECTION('center_axis',(0.,-1.,0.));
#26200=DIRECTION('ref_axis',(-1.,0.,2.36700689860723E-12));
#26201=DIRECTION('',(0.,-1.,0.));
#26202=DIRECTION('center_axis',(0.,-1.,0.));
#26203=DIRECTION('ref_axis',(-1.,0.,2.36700689860723E-12));
#26204=DIRECTION('',(0.,-1.,0.));
#26205=DIRECTION('center_axis',(0.,-1.,0.));
#26206=DIRECTION('ref_axis',(-1.,0.,2.36700689860723E-12));
#26207=DIRECTION('',(0.,-1.,0.));
#26208=DIRECTION('center_axis',(0.,-1.,0.));
#26209=DIRECTION('ref_axis',(-1.,0.,2.36700689860723E-12));
#26210=DIRECTION('',(0.,-1.,0.));
#26211=DIRECTION('center_axis',(0.,-1.,0.));
#26212=DIRECTION('ref_axis',(-1.,0.,2.36700689860723E-12));
#26213=DIRECTION('',(0.,-1.,0.));
#26214=DIRECTION('center_axis',(0.,-1.,0.));
#26215=DIRECTION('ref_axis',(-1.,0.,2.36700689860723E-12));
#26216=DIRECTION('',(0.,-1.,0.));
#26217=DIRECTION('center_axis',(0.,-1.,0.));
#26218=DIRECTION('ref_axis',(-1.,0.,2.36700689860723E-12));
#26219=DIRECTION('',(0.,-1.,0.));
#26220=DIRECTION('center_axis',(0.,-1.,0.));
#26221=DIRECTION('ref_axis',(-1.,0.,2.36700689860723E-12));
#26222=DIRECTION('',(0.,-1.,0.));
#26223=DIRECTION('center_axis',(0.,-1.,0.));
#26224=DIRECTION('ref_axis',(-1.,0.,2.36700689860723E-12));
#26225=DIRECTION('',(0.,-1.,0.));
#26226=DIRECTION('center_axis',(0.,-1.,0.));
#26227=DIRECTION('ref_axis',(-1.,0.,2.36700689860723E-12));
#26228=DIRECTION('',(0.,-1.,0.));
#26229=DIRECTION('center_axis',(0.,-1.,0.));
#26230=DIRECTION('ref_axis',(-1.,0.,2.36700689860723E-12));
#26231=DIRECTION('',(0.,-1.,0.));
#26232=DIRECTION('center_axis',(0.,-1.,0.));
#26233=DIRECTION('ref_axis',(-1.,0.,2.36700689860723E-12));
#26234=DIRECTION('',(0.,-1.,0.));
#26235=DIRECTION('center_axis',(0.,-1.,0.));
#26236=DIRECTION('ref_axis',(-1.,0.,2.36700689860723E-12));
#26237=DIRECTION('',(0.,-1.,0.));
#26238=DIRECTION('center_axis',(0.,-1.,0.));
#26239=DIRECTION('ref_axis',(-1.,0.,2.36700689860723E-12));
#26240=DIRECTION('',(0.,-1.,0.));
#26241=DIRECTION('center_axis',(0.,-1.,0.));
#26242=DIRECTION('ref_axis',(-1.,0.,2.36700689860723E-12));
#26243=DIRECTION('',(0.,-1.,0.));
#26244=DIRECTION('center_axis',(0.,-1.,0.));
#26245=DIRECTION('ref_axis',(-1.,0.,2.36700689860723E-12));
#26246=DIRECTION('',(0.,-1.,0.));
#26247=DIRECTION('center_axis',(0.,-1.,0.));
#26248=DIRECTION('ref_axis',(-1.,0.,2.36700689860723E-12));
#26249=DIRECTION('',(0.,-1.,0.));
#26250=DIRECTION('center_axis',(0.,-1.,0.));
#26251=DIRECTION('ref_axis',(-1.,0.,2.36700689860723E-12));
#26252=DIRECTION('',(0.,-1.,0.));
#26253=DIRECTION('center_axis',(0.,-1.,0.));
#26254=DIRECTION('ref_axis',(-1.,0.,2.36700689860723E-12));
#26255=DIRECTION('',(0.,-1.,0.));
#26256=DIRECTION('center_axis',(0.,-1.,0.));
#26257=DIRECTION('ref_axis',(-1.,0.,2.36700689860723E-12));
#26258=DIRECTION('',(0.,-1.,0.));
#26259=DIRECTION('center_axis',(0.,-1.,0.));
#26260=DIRECTION('ref_axis',(-1.,0.,2.36700689860723E-12));
#26261=DIRECTION('',(0.,-1.,0.));
#26262=DIRECTION('center_axis',(0.,-1.,0.));
#26263=DIRECTION('ref_axis',(-1.,0.,2.36700689860723E-12));
#26264=DIRECTION('',(0.,-1.,0.));
#26265=DIRECTION('center_axis',(0.,-1.,0.));
#26266=DIRECTION('ref_axis',(-1.,0.,2.36700689860723E-12));
#26267=DIRECTION('',(0.,-1.,0.));
#26268=DIRECTION('center_axis',(0.,-1.,0.));
#26269=DIRECTION('ref_axis',(-1.,0.,2.36700689860723E-12));
#26270=DIRECTION('',(0.,-1.,0.));
#26271=DIRECTION('center_axis',(0.,-1.,0.));
#26272=DIRECTION('ref_axis',(-1.,0.,2.36700689860723E-12));
#26273=DIRECTION('',(0.,-1.,0.));
#26274=DIRECTION('center_axis',(0.,-1.,0.));
#26275=DIRECTION('ref_axis',(-1.,0.,2.36700689860723E-12));
#26276=DIRECTION('',(0.,-1.,0.));
#26277=DIRECTION('center_axis',(0.,-1.,0.));
#26278=DIRECTION('ref_axis',(-1.,0.,2.36700689860723E-12));
#26279=DIRECTION('',(0.,-1.,0.));
#26280=DIRECTION('center_axis',(0.,-1.,0.));
#26281=DIRECTION('ref_axis',(-1.,0.,2.36700689860723E-12));
#26282=DIRECTION('',(0.,-1.,0.));
#26283=DIRECTION('center_axis',(0.,-1.,0.));
#26284=DIRECTION('ref_axis',(-1.,0.,2.36700689860723E-12));
#26285=DIRECTION('',(0.,-1.,0.));
#26286=DIRECTION('center_axis',(0.,-1.,0.));
#26287=DIRECTION('ref_axis',(-1.,0.,2.36700689860723E-12));
#26288=DIRECTION('',(0.,-1.,0.));
#26289=DIRECTION('center_axis',(0.,-1.,0.));
#26290=DIRECTION('ref_axis',(-1.,0.,2.36700689860723E-12));
#26291=DIRECTION('',(0.,-1.,0.));
#26292=DIRECTION('center_axis',(0.,-1.,0.));
#26293=DIRECTION('ref_axis',(-1.,0.,2.36700689860723E-12));
#26294=DIRECTION('',(0.,-1.,0.));
#26295=DIRECTION('center_axis',(0.,-1.,0.));
#26296=DIRECTION('ref_axis',(-1.,0.,2.36700689860723E-12));
#26297=DIRECTION('',(0.,-1.,0.));
#26298=DIRECTION('center_axis',(0.,-1.,0.));
#26299=DIRECTION('ref_axis',(-1.,0.,2.36700689860723E-12));
#26300=DIRECTION('',(0.,-1.,0.));
#26301=DIRECTION('center_axis',(0.,-1.,0.));
#26302=DIRECTION('ref_axis',(-1.,0.,2.36700689860723E-12));
#26303=DIRECTION('',(0.,-1.,0.));
#26304=DIRECTION('center_axis',(0.,-1.,0.));
#26305=DIRECTION('ref_axis',(-1.,0.,2.36700689860723E-12));
#26306=DIRECTION('',(0.,-1.,0.));
#26307=DIRECTION('center_axis',(0.,-1.,0.));
#26308=DIRECTION('ref_axis',(-1.,0.,2.36700689860723E-12));
#26309=DIRECTION('',(0.,-1.,0.));
#26310=DIRECTION('center_axis',(0.,-1.,0.));
#26311=DIRECTION('ref_axis',(-1.,0.,2.36700689860723E-12));
#26312=DIRECTION('',(0.,-1.,0.));
#26313=DIRECTION('center_axis',(0.,-1.,0.));
#26314=DIRECTION('ref_axis',(-1.,0.,2.36700689860723E-12));
#26315=DIRECTION('',(0.,-1.,0.));
#26316=DIRECTION('center_axis',(0.,-1.,0.));
#26317=DIRECTION('ref_axis',(-1.,0.,2.36700689860723E-12));
#26318=DIRECTION('',(0.,-1.,0.));
#26319=DIRECTION('center_axis',(0.,-1.,0.));
#26320=DIRECTION('ref_axis',(-1.,0.,2.36700689860723E-12));
#26321=DIRECTION('',(0.,-1.,0.));
#26322=DIRECTION('center_axis',(0.,-1.,0.));
#26323=DIRECTION('ref_axis',(-1.,0.,2.36700689860723E-12));
#26324=DIRECTION('',(0.,-1.,0.));
#26325=DIRECTION('center_axis',(0.,-1.,0.));
#26326=DIRECTION('ref_axis',(-1.,0.,2.36700689860723E-12));
#26327=DIRECTION('',(0.,-1.,0.));
#26328=DIRECTION('center_axis',(0.,-1.,0.));
#26329=DIRECTION('ref_axis',(-1.,0.,2.36700689860723E-12));
#26330=DIRECTION('',(0.,-1.,0.));
#26331=DIRECTION('center_axis',(0.,-1.,0.));
#26332=DIRECTION('ref_axis',(-1.,0.,2.36700689860723E-12));
#26333=DIRECTION('',(0.,-1.,0.));
#26334=DIRECTION('center_axis',(0.,-1.,0.));
#26335=DIRECTION('ref_axis',(-1.,0.,2.36700689860723E-12));
#26336=DIRECTION('',(0.,-1.,0.));
#26337=DIRECTION('center_axis',(0.,-1.,0.));
#26338=DIRECTION('ref_axis',(-1.,0.,2.36700689860723E-12));
#26339=DIRECTION('',(0.,-1.,0.));
#26340=DIRECTION('center_axis',(0.,-1.,0.));
#26341=DIRECTION('ref_axis',(-1.,0.,2.36700689860723E-12));
#26342=DIRECTION('',(0.,-1.,0.));
#26343=DIRECTION('center_axis',(0.,-1.,0.));
#26344=DIRECTION('ref_axis',(1.,0.,0.));
#26345=DIRECTION('center_axis',(0.,1.,0.));
#26346=DIRECTION('ref_axis',(1.,0.,0.));
#26347=DIRECTION('',(0.707106781186541,0.707106781186554,8.65956056235486E-17));
#26348=DIRECTION('center_axis',(0.,-1.,0.));
#26349=DIRECTION('ref_axis',(1.,0.,0.));
#26350=DIRECTION('center_axis',(0.,1.,0.));
#26351=DIRECTION('ref_axis',(1.,0.,0.));
#26352=DIRECTION('',(0.,-1.,0.));
#26353=DIRECTION('center_axis',(0.,1.,0.));
#26354=DIRECTION('ref_axis',(1.,0.,0.));
#26355=DIRECTION('center_axis',(0.,1.,0.));
#26356=DIRECTION('ref_axis',(1.,0.,0.));
#26357=DIRECTION('center_axis',(0.,1.,0.));
#26358=DIRECTION('ref_axis',(-1.,0.,0.));
#26359=DIRECTION('center_axis',(0.,1.,0.));
#26360=DIRECTION('ref_axis',(-1.,0.,0.));
#26361=DIRECTION('',(0.707106781186546,0.707106781186549,8.65956056235492E-17));
#26362=DIRECTION('center_axis',(0.,-1.,0.));
#26363=DIRECTION('ref_axis',(-1.,0.,0.));
#26364=DIRECTION('center_axis',(0.,1.,0.));
#26365=DIRECTION('ref_axis',(-1.,0.,0.));
#26366=DIRECTION('',(0.,1.,0.));
#26367=DIRECTION('center_axis',(0.,-1.,0.));
#26368=DIRECTION('ref_axis',(-1.,0.,0.));
#26369=DIRECTION('center_axis',(0.,-1.,0.));
#26370=DIRECTION('ref_axis',(-1.,0.,0.));
#26371=DIRECTION('center_axis',(0.,-1.,0.));
#26372=DIRECTION('ref_axis',(-1.,0.,0.));
#26373=DIRECTION('center_axis',(0.,1.,0.));
#26374=DIRECTION('ref_axis',(-1.,0.,0.));
#26375=DIRECTION('center_axis',(0.,-1.,0.));
#26376=DIRECTION('ref_axis',(-0.9659062825861,0.,-0.258891972182802));
#26377=DIRECTION('center_axis',(0.,1.,0.));
#26378=DIRECTION('ref_axis',(-1.,0.,2.36700689860723E-12));
#26379=DIRECTION('center_axis',(0.,1.,0.));
#26380=DIRECTION('ref_axis',(0.,0.,1.));
#26381=DIRECTION('center_axis',(0.,-1.,0.));
#26382=DIRECTION('ref_axis',(1.,0.,0.));
#26383=DIRECTION('center_axis',(0.,1.,0.));
#26384=DIRECTION('ref_axis',(0.,0.,1.));
#26385=DIRECTION('center_axis',(0.,-1.,0.));
#26386=DIRECTION('ref_axis',(1.,0.,-6.50117889680365E-14));
#26387=DIRECTION('center_axis',(0.,1.,0.));
#26388=DIRECTION('ref_axis',(-0.644123759008342,0.,-0.764921292082371));
#26389=DIRECTION('center_axis',(0.,1.,0.));
#26390=DIRECTION('ref_axis',(-0.0923927080499103,0.,0.995722645870427));
#26391=DIRECTION('center_axis',(0.,1.,0.));
#26392=DIRECTION('ref_axis',(1.,0.,0.));
#26393=DIRECTION('center_axis',(0.,-1.,0.));
#26394=DIRECTION('ref_axis',(-1.,0.,0.));
#30990=CARTESIAN_POINT('',(0.,0.,0.));
#30991=CARTESIAN_POINT('Origin',(74.9879498948689,255.,53.0228109606356));
#30992=CARTESIAN_POINT('',(82.9065970110875,414.278332223638,53.0282292646567));
#30993=CARTESIAN_POINT('',(82.9129498948689,415.721667776361,53.0228109606487));
#30994=CARTESIAN_POINT('',(82.9129498948689,255.,53.0228109606356));
#30995=CARTESIAN_POINT('',(67.8083803398704,416.,49.6673071229179));
#30996=CARTESIAN_POINT('Ctrl Pts',(82.9129498948689,414.278332223638,53.0228109606355));
#30997=CARTESIAN_POINT('Ctrl Pts',(82.9129498948689,414.455428795637,50.8182135007257));
#30998=CARTESIAN_POINT('Ctrl Pts',(81.9432795991106,414.632525367635,48.6308565362894));
#30999=CARTESIAN_POINT('Ctrl Pts',(80.3096882702542,414.809621939634,47.1504412801785));
#31000=CARTESIAN_POINT('Ctrl Pts',(78.6760969413978,414.986718511633,45.6700260240676));
#31001=CARTESIAN_POINT('Ctrl Pts',(76.4041347530445,415.163815083631,44.9197069006031));
#31002=CARTESIAN_POINT('Ctrl Pts',(74.210180011222,415.34091165563,45.136068983869));
#31003=CARTESIAN_POINT('Ctrl Pts',(72.0162252693994,415.518008227629,45.3524310671349));
#31004=CARTESIAN_POINT('Ctrl Pts',(69.934592507698,415.695104799628,46.5320903475013));
#31005=CARTESIAN_POINT('Ctrl Pts',(68.6216467656608,415.872201371626,48.3030853894784));
#31006=CARTESIAN_POINT('Ctrl Pts',(68.3058253599202,415.914800914418,48.7290878706236));
#31007=CARTESIAN_POINT('Ctrl Pts',(68.0329145681891,415.957400457209,49.1868847518951));
#31008=CARTESIAN_POINT('Ctrl Pts',(67.8083803398704,416.,49.6673071229179));
#31009=CARTESIAN_POINT('',(82.1675194498639,416.,49.6673071229103));
#31010=CARTESIAN_POINT('Origin',(74.9879498948689,416.,53.0228109606356));
#31011=CARTESIAN_POINT('Ctrl Pts',(82.1675194498639,416.000000000001,49.6673071229103));
#31012=CARTESIAN_POINT('Ctrl Pts',(82.6565318269656,415.907222592121,50.7136174668838));
#31013=CARTESIAN_POINT('Ctrl Pts',(82.9065122305317,415.814445184241,51.86425892299));
#31014=CARTESIAN_POINT('Ctrl Pts',(82.9078731907355,415.721667776361,53.0191031778888));
#31015=CARTESIAN_POINT('Origin',(74.9879498948689,255.,53.0228109606356));
#31016=CARTESIAN_POINT('',(82.9241352897681,410.278332223638,53.0251703538597));
#31017=CARTESIAN_POINT('',(82.9129145441845,411.721667776361,53.0231512301084));
#31018=CARTESIAN_POINT('',(82.9129498948689,255.,53.0228109606356));
#31019=CARTESIAN_POINT('Ctrl Pts',(82.9241352897681,410.278332223638,53.0251703538597));
#31020=CARTESIAN_POINT('Ctrl Pts',(82.9144087418507,410.479926090632,50.5264531396333));
#31021=CARTESIAN_POINT('Ctrl Pts',(81.6392328200664,410.681519957625,48.0190747435334));
#31022=CARTESIAN_POINT('Ctrl Pts',(79.6067374458105,410.883113824619,46.5659622102762));
#31023=CARTESIAN_POINT('Ctrl Pts',(77.4677531876784,411.095269834171,45.0367164991663));
#31024=CARTESIAN_POINT('Ctrl Pts',(74.4900138615837,411.307425843724,44.6751033274731));
#31025=CARTESIAN_POINT('Ctrl Pts',(72.0493789123074,411.519581853276,45.6477657875292));
#31026=CARTESIAN_POINT('Ctrl Pts',(69.6087439630311,411.731737862829,46.6204282475853));
#31027=CARTESIAN_POINT('Ctrl Pts',(67.7052133905732,411.94389387238,48.9273663393907));
#31028=CARTESIAN_POINT('Ctrl Pts',(67.1985039826836,412.156049881933,51.5089701657794));
#31029=CARTESIAN_POINT('Ctrl Pts',(66.9451492787388,412.262127886709,52.7997720789737));
#31030=CARTESIAN_POINT('Ctrl Pts',(67.040999865936,412.368205891486,54.1592404258139));
#31031=CARTESIAN_POINT('Ctrl Pts',(67.4422155137494,412.474283896262,55.4216291114888));
#31032=CARTESIAN_POINT('Ctrl Pts',(67.8434311615628,412.580361901038,56.6840177971637));
#31033=CARTESIAN_POINT('Ctrl Pts',(68.5500118699923,412.686439905814,57.8493268216733));
#31034=CARTESIAN_POINT('Ctrl Pts',(69.5022941704941,412.79251791059,58.7568510247251));
#31035=CARTESIAN_POINT('Ctrl Pts',(71.4068587714976,413.004673920142,60.5718994308287));
#31036=CARTESIAN_POINT('Ctrl Pts',(74.29422974079,413.216829929695,61.3558085511009));
#31037=CARTESIAN_POINT('Ctrl Pts',(76.8480876043277,413.428985939247,60.7407007216353));
#31038=CARTESIAN_POINT('Ctrl Pts',(79.4019454678654,413.6411419488,60.1255928921697));
#31039=CARTESIAN_POINT('Ctrl Pts',(81.6222902256485,413.853297958352,58.1114681129663));
#31040=CARTESIAN_POINT('Ctrl Pts',(82.4863699092025,414.065453967904,55.6275433329795));
#31041=CARTESIAN_POINT('Ctrl Pts',(82.7753770039315,414.136413386482,54.7967497177));
#31042=CARTESIAN_POINT('Ctrl Pts',(82.9126601982892,414.20737280506,53.913400086736));
#31043=CARTESIAN_POINT('Ctrl Pts',(82.9065970110875,414.278332223638,53.0282292646567));
#31044=CARTESIAN_POINT('Ctrl Pts',(82.9129498948689,415.721667776361,53.0228109606488));
#31045=CARTESIAN_POINT('Ctrl Pts',(82.9129498948652,415.544571204362,55.2274084205585));
#31046=CARTESIAN_POINT('Ctrl Pts',(81.9432795991034,415.367474632363,57.4147653849931));
#31047=CARTESIAN_POINT('Ctrl Pts',(80.3096882702446,415.190378060364,58.8951806411014));
#31048=CARTESIAN_POINT('Ctrl Pts',(78.6760969413858,415.013281488366,60.3755958972096));
#31049=CARTESIAN_POINT('Ctrl Pts',(76.4041347530313,414.836184916367,61.1259150206704));
#31050=CARTESIAN_POINT('Ctrl Pts',(74.2101800112091,414.659088344368,60.9095529374009));
#31051=CARTESIAN_POINT('Ctrl Pts',(72.016225269387,414.481991772369,60.6931908541314));
#31052=CARTESIAN_POINT('Ctrl Pts',(69.9345925076874,414.304895200371,59.5135315737616));
#31053=CARTESIAN_POINT('Ctrl Pts',(68.6216467656532,414.127798628372,57.7425365317824));
#31054=CARTESIAN_POINT('Ctrl Pts',(67.3087010236189,413.950702056373,55.9715414898033));
#31055=CARTESIAN_POINT('Ctrl Pts',(66.784977419823,413.773605484375,53.6369099216174));
#31056=CARTESIAN_POINT('Ctrl Pts',(67.215612605763,413.596508912376,51.4747805783839));
#31057=CARTESIAN_POINT('Ctrl Pts',(67.6462477917031,413.419412340377,49.3126512351505));
#31058=CARTESIAN_POINT('Ctrl Pts',(69.0245064208055,413.242315768378,47.3568408855388));
#31059=CARTESIAN_POINT('Ctrl Pts',(70.9158061804571,413.06521919638,46.224041177125));
#31060=CARTESIAN_POINT('Ctrl Pts',(72.8071059401087,412.888122624381,45.0912414687111));
#31061=CARTESIAN_POINT('Ctrl Pts',(75.1818659698228,412.711026052382,44.7991699473061));
#31062=CARTESIAN_POINT('Ctrl Pts',(77.2912945088783,412.533929480384,45.4399204438792));
#31063=CARTESIAN_POINT('Ctrl Pts',(79.4007230479338,412.356832908385,46.0806709404523));
#31064=CARTESIAN_POINT('Ctrl Pts',(81.2118275942158,412.179736336386,47.6442218014031));
#31065=CARTESIAN_POINT('Ctrl Pts',(82.1535440633151,412.002639764387,49.6375657386272));
#31066=CARTESIAN_POINT('Ctrl Pts',(82.6515697929947,411.908982435045,50.6917435101895));
#31067=CARTESIAN_POINT('Ctrl Pts',(82.9129498948708,411.815325105703,51.8569119935511));
#31068=CARTESIAN_POINT('Ctrl Pts',(82.9129498948689,411.721667776361,53.0228109606486));
#31069=CARTESIAN_POINT('Origin',(74.9879498948689,255.,53.0228109606356));
#31070=CARTESIAN_POINT('',(82.9129987951795,406.278332223638,53.022353166431));
#31071=CARTESIAN_POINT('',(82.9231891863576,407.721667776361,53.0235399778202));
#31072=CARTESIAN_POINT('',(82.9129498948689,255.,53.0228109606356));
#31073=CARTESIAN_POINT('Ctrl Pts',(82.9136411619662,406.278332223638,53.0163394665249));
#31074=CARTESIAN_POINT('Ctrl Pts',(82.9194890840726,406.328167357099,52.3962321856271));
#31075=CARTESIAN_POINT('Ctrl Pts',(82.8528804541948,406.37800249056,51.7772617381742));
#31076=CARTESIAN_POINT('Ctrl Pts',(82.7090801244942,406.427837624021,51.1765844418892));
#31077=CARTESIAN_POINT('Ctrl Pts',(82.0968994799793,406.639993633573,48.6194066165628));
#31078=CARTESIAN_POINT('Ctrl Pts',(80.0857435909802,406.852149643125,46.3937626956099));
#31079=CARTESIAN_POINT('Ctrl Pts',(77.605322558894,407.064305652678,45.5277522795078));
#31080=CARTESIAN_POINT('Ctrl Pts',(75.1249015268078,407.27646166223,44.6617418634056));
#31081=CARTESIAN_POINT('Ctrl Pts',(72.1752153516344,407.488617671782,45.1553649521542));
#31082=CARTESIAN_POINT('Ctrl Pts',(70.0996427799517,407.700773681334,46.7721254255252));
#31083=CARTESIAN_POINT('Ctrl Pts',(69.0618564941103,407.806851686111,47.5805056622108));
#31084=CARTESIAN_POINT('Ctrl Pts',(68.2425986091416,407.912929690887,48.6696702450519));
#31085=CARTESIAN_POINT('Ctrl Pts',(67.7178205322322,408.019007695663,49.8858983521605));
#31086=CARTESIAN_POINT('Ctrl Pts',(67.1930424553228,408.125085700439,51.102126459269));
#31087=CARTESIAN_POINT('Ctrl Pts',(66.9627441864726,408.231163705215,52.4454180906449));
#31088=CARTESIAN_POINT('Ctrl Pts',(67.0866534420349,408.337241709991,53.7550467932846));
#31089=CARTESIAN_POINT('Ctrl Pts',(67.3344719531597,408.549397719544,56.3743041985641));
#31090=CARTESIAN_POINT('Ctrl Pts',(68.9991205619347,408.761553729096,58.8589098888989));
#31091=CARTESIAN_POINT('Ctrl Pts',(71.3309510746786,408.973709738649,60.0692889110528));
#31092=CARTESIAN_POINT('Ctrl Pts',(73.6627815874224,409.185865748201,61.2796679332067));
#31093=CARTESIAN_POINT('Ctrl Pts',(76.6617940041351,409.398021757753,61.2158202871798));
#31094=CARTESIAN_POINT('Ctrl Pts',(78.9421958230637,409.610177767305,59.906728427714));
#31095=CARTESIAN_POINT('Ctrl Pts',(81.2225976419923,409.822333776857,58.5976365682483));
#31096=CARTESIAN_POINT('Ctrl Pts',(82.7843888631369,410.03448978641,56.0433004953437));
#31097=CARTESIAN_POINT('Ctrl Pts',(82.9151698786245,410.246645795963,53.4176933336282));
#31098=CARTESIAN_POINT('Ctrl Pts',(82.9216807841248,410.257207938521,53.2869780302849));
#31099=CARTESIAN_POINT('Ctrl Pts',(82.9246448944859,410.26777008108,53.156086079738));
#31100=CARTESIAN_POINT('Ctrl Pts',(82.9241352897681,410.278332223638,53.0251703538597));
#31101=CARTESIAN_POINT('Ctrl Pts',(82.9124186818494,411.721667776361,53.0279241726423));
#31102=CARTESIAN_POINT('Ctrl Pts',(82.9169360649469,411.662686450708,53.7626941830692));
#31103=CARTESIAN_POINT('Ctrl Pts',(82.8207774927491,411.603705125055,54.4960880068349));
#31104=CARTESIAN_POINT('Ctrl Pts',(82.6188780515908,411.544723799402,55.1990731318781));
#31105=CARTESIAN_POINT('Ctrl Pts',(81.8926451415501,411.33256778985,57.7277127860879));
#31106=CARTESIAN_POINT('Ctrl Pts',(79.7982912841655,411.120411780297,59.8629115870814));
#31107=CARTESIAN_POINT('Ctrl Pts',(77.2832349439534,410.908255770745,60.622689727324));
#31108=CARTESIAN_POINT('Ctrl Pts',(74.7681786037414,410.696099761193,61.3824678675665));
#31109=CARTESIAN_POINT('Ctrl Pts',(71.8324197807018,410.48394375164,60.7668253470583));
#31110=CARTESIAN_POINT('Ctrl Pts',(69.8324586031125,410.271787742088,59.0597807109634));
#31111=CARTESIAN_POINT('Ctrl Pts',(67.8324974255232,410.059631732536,57.3527360748685));
#31112=CARTESIAN_POINT('Ctrl Pts',(66.7683338933842,409.847475722983,54.554289323187));
#31113=CARTESIAN_POINT('Ctrl Pts',(67.1237968814133,409.635319713431,51.9495700089795));
#31114=CARTESIAN_POINT('Ctrl Pts',(67.4792598694425,409.423163703879,49.3448506947721));
#31115=CARTESIAN_POINT('Ctrl Pts',(69.2543493776398,409.211007694326,46.9338588180387));
#31116=CARTESIAN_POINT('Ctrl Pts',(71.638613990893,408.998851684774,45.8251495656732));
#31117=CARTESIAN_POINT('Ctrl Pts',(74.0228786041463,408.786695675222,44.7164403133077));
#31118=CARTESIAN_POINT('Ctrl Pts',(77.0163183224555,408.574539665669,44.9100136853101));
#31119=CARTESIAN_POINT('Ctrl Pts',(79.2357603254525,408.362383656117,46.3159041905652));
#31120=CARTESIAN_POINT('Ctrl Pts',(81.4552023284494,408.150227646565,47.7217946958203));
#31121=CARTESIAN_POINT('Ctrl Pts',(82.9006466161341,407.938071637013,50.3400023343282));
#31122=CARTESIAN_POINT('Ctrl Pts',(82.9229329658515,407.72591562746,52.970862780681));
#31123=CARTESIAN_POINT('Ctrl Pts',(82.9230817071722,407.724499677094,52.9884214056813));
#31124=CARTESIAN_POINT('Ctrl Pts',(82.9231670559047,407.723083726727,53.0059805942834));
#31125=CARTESIAN_POINT('Ctrl Pts',(82.9231891863576,407.721667776361,53.0235399778202));
#31126=CARTESIAN_POINT('Origin',(74.9879498948689,255.,53.0228109606356));
#31127=CARTESIAN_POINT('',(82.9129498948689,402.278332223638,53.0228109606356));
#31128=CARTESIAN_POINT('',(82.9110727027003,403.721667776361,53.0200287533551));
#31129=CARTESIAN_POINT('',(82.9129498948689,255.,53.0228109606356));
#31130=CARTESIAN_POINT('Ctrl Pts',(82.9129498948689,402.278332223638,53.0228109606358));
#31131=CARTESIAN_POINT('Ctrl Pts',(82.912949894869,402.455428795637,50.8182135007261));
#31132=CARTESIAN_POINT('Ctrl Pts',(81.9432795991109,402.632525367635,48.6308565362898));
#31133=CARTESIAN_POINT('Ctrl Pts',(80.3096882702546,402.809621939634,47.1504412801789));
#31134=CARTESIAN_POINT('Ctrl Pts',(78.6760969413983,402.986718511633,45.6700260240679));
#31135=CARTESIAN_POINT('Ctrl Pts',(76.4041347530452,403.163815083631,44.9197069006032));
#31136=CARTESIAN_POINT('Ctrl Pts',(74.2101800112226,403.34091165563,45.1360689838689));
#31137=CARTESIAN_POINT('Ctrl Pts',(72.0162252694001,403.518008227629,45.3524310671347));
#31138=CARTESIAN_POINT('Ctrl Pts',(69.9345925076986,403.695104799628,46.5320903475009));
#31139=CARTESIAN_POINT('Ctrl Pts',(68.6216467656613,403.872201371626,48.3030853894777));
#31140=CARTESIAN_POINT('Ctrl Pts',(67.308701023624,404.049297943625,50.0740804314546));
#31141=CARTESIAN_POINT('Ctrl Pts',(66.784977419824,404.226394515624,52.4087119996396));
#31142=CARTESIAN_POINT('Ctrl Pts',(67.2156126057604,404.403491087622,54.5708413428738));
#31143=CARTESIAN_POINT('Ctrl Pts',(67.6462477916967,404.580587659621,56.7329706861079));
#31144=CARTESIAN_POINT('Ctrl Pts',(69.0245064207957,404.75768423162,58.6887810357219));
#31145=CARTESIAN_POINT('Ctrl Pts',(70.9158061804453,404.934780803619,59.8215807441391));
#31146=CARTESIAN_POINT('Ctrl Pts',(72.8071059400949,405.111877375617,60.9543804525562));
#31147=CARTESIAN_POINT('Ctrl Pts',(75.1818659698084,405.288973947616,61.2464519739654));
#31148=CARTESIAN_POINT('Ctrl Pts',(77.2912945088651,405.466070519615,60.605701477396));
#31149=CARTESIAN_POINT('Ctrl Pts',(79.4007230479217,405.643167091614,59.9649509808265));
#31150=CARTESIAN_POINT('Ctrl Pts',(81.2118275942064,405.820263663612,58.4014001198789));
#31151=CARTESIAN_POINT('Ctrl Pts',(82.1535440633091,405.997360235611,56.4080561826565));
#31152=CARTESIAN_POINT('Ctrl Pts',(82.6515697929907,406.091017564953,55.3538784110949));
#31153=CARTESIAN_POINT('Ctrl Pts',(82.9129498948689,406.184674894295,54.1887099277337));
#31154=CARTESIAN_POINT('Ctrl Pts',(82.9129498948689,406.278332223638,53.022810960636));
#31155=CARTESIAN_POINT('Ctrl Pts',(82.9231891863576,407.721667776361,53.0235399778202));
#31156=CARTESIAN_POINT('Ctrl Pts',(82.9248249913466,407.617005721951,54.3214676443345));
#31157=CARTESIAN_POINT('Ctrl Pts',(82.5810585782997,407.512343667541,55.6204603650967));
#31158=CARTESIAN_POINT('Ctrl Pts',(81.9622851139255,407.407681613132,56.7716307635747));
#31159=CARTESIAN_POINT('Ctrl Pts',(81.3351403967737,407.301603608356,57.9383750981546));
#31160=CARTESIAN_POINT('Ctrl Pts',(80.4254972721032,407.19552560358,58.9532703421768));
#31161=CARTESIAN_POINT('Ctrl Pts',(79.3222099604759,407.089447598803,59.6696753185319));
#31162=CARTESIAN_POINT('Ctrl Pts',(77.1156353372214,406.877291589251,61.1024852712423));
#31163=CARTESIAN_POINT('Ctrl Pts',(74.1344839661398,406.665135579699,61.3413341532847));
#31164=CARTESIAN_POINT('Ctrl Pts',(71.7374668755085,406.452979570146,60.2658009811163));
#31165=CARTESIAN_POINT('Ctrl Pts',(69.3404497848772,406.240823560594,59.1902678089478));
#31166=CARTESIAN_POINT('Ctrl Pts',(67.5275669746961,406.028667551042,56.8003525825685));
#31167=CARTESIAN_POINT('Ctrl Pts',(67.1369370180655,405.81651154149,54.2000964780969));
#31168=CARTESIAN_POINT('Ctrl Pts',(66.7463070614349,405.604355531937,51.5998403736252));
#31169=CARTESIAN_POINT('Ctrl Pts',(67.7779299583547,405.392199522385,48.7892433910612));
#31170=CARTESIAN_POINT('Ctrl Pts',(69.7543007334193,405.180043512832,47.05577978859));
#31171=CARTESIAN_POINT('Ctrl Pts',(71.7306715084839,404.96788750328,45.3223161861188));
#31172=CARTESIAN_POINT('Ctrl Pts',(74.6517901616933,404.755731493728,44.6659859637404));
#31173=CARTESIAN_POINT('Ctrl Pts',(77.1789100392733,404.543575484176,45.3923390707145));
#31174=CARTESIAN_POINT('Ctrl Pts',(79.7060299168532,404.331419474623,46.1186921776886));
#31175=CARTESIAN_POINT('Ctrl Pts',(81.8391510188038,404.119263465071,48.2277286140151));
#31176=CARTESIAN_POINT('Ctrl Pts',(82.5929447446449,403.907107455519,50.7445233499528));
#31177=CARTESIAN_POINT('Ctrl Pts',(82.8125681355735,403.845294229133,51.4778101567128));
#31178=CARTESIAN_POINT('Ctrl Pts',(82.915101607755,403.783481002747,52.2457112160404));
#31179=CARTESIAN_POINT('Ctrl Pts',(82.9078799846978,403.721667776361,53.0152967906599));
#31180=CARTESIAN_POINT('Origin',(74.9879498948689,255.,53.0228109606356));
#31181=CARTESIAN_POINT('',(82.9129498948689,398.278332223638,53.0228109606356));
#31182=CARTESIAN_POINT('',(82.9080990005812,399.721667776361,53.0247995869528));
#31183=CARTESIAN_POINT('',(82.9129498948689,255.,53.0228109606356));
#31184=CARTESIAN_POINT('Ctrl Pts',(82.9129498948689,398.278332223638,53.0228109606356));
#31185=CARTESIAN_POINT('Ctrl Pts',(82.9129498948689,398.455428795637,50.8182135007258));
#31186=CARTESIAN_POINT('Ctrl Pts',(81.9432795991107,398.632525367635,48.6308565362895));
#31187=CARTESIAN_POINT('Ctrl Pts',(80.3096882702543,398.809621939634,47.1504412801786));
#31188=CARTESIAN_POINT('Ctrl Pts',(78.6760969413979,398.986718511633,45.6700260240676));
#31189=CARTESIAN_POINT('Ctrl Pts',(76.4041347530446,399.163815083631,44.9197069006031));
#31190=CARTESIAN_POINT('Ctrl Pts',(74.2101800112221,399.34091165563,45.136068983869));
#31191=CARTESIAN_POINT('Ctrl Pts',(72.0162252693995,399.518008227629,45.3524310671349));
#31192=CARTESIAN_POINT('Ctrl Pts',(69.934592507698,399.695104799628,46.5320903475013));
#31193=CARTESIAN_POINT('Ctrl Pts',(68.6216467656608,399.872201371626,48.3030853894784));
#31194=CARTESIAN_POINT('Ctrl Pts',(67.3087010236236,400.049297943625,50.0740804314554));
#31195=CARTESIAN_POINT('Ctrl Pts',(66.7849774198239,400.226394515624,52.4087119996406));
#31196=CARTESIAN_POINT('Ctrl Pts',(67.2156126057605,400.403491087623,54.5708413428747));
#31197=CARTESIAN_POINT('Ctrl Pts',(67.6462477916972,400.580587659621,56.7329706861089));
#31198=CARTESIAN_POINT('Ctrl Pts',(69.0245064207965,400.75768423162,58.6887810357228));
#31199=CARTESIAN_POINT('Ctrl Pts',(70.9158061804463,400.934780803619,59.8215807441397));
#31200=CARTESIAN_POINT('Ctrl Pts',(72.8071059400962,401.111877375617,60.9543804525566));
#31201=CARTESIAN_POINT('Ctrl Pts',(75.1818659698098,401.288973947616,61.2464519739654));
#31202=CARTESIAN_POINT('Ctrl Pts',(77.2912945088664,401.466070519615,60.6057014773956));
#31203=CARTESIAN_POINT('Ctrl Pts',(79.400723047923,401.643167091614,59.9649509808257));
#31204=CARTESIAN_POINT('Ctrl Pts',(81.2118275942074,401.820263663612,58.4014001198777));
#31205=CARTESIAN_POINT('Ctrl Pts',(82.1535440633098,401.997360235611,56.4080561826551));
#31206=CARTESIAN_POINT('Ctrl Pts',(82.651569792991,402.091017564953,55.3538784110938));
#31207=CARTESIAN_POINT('Ctrl Pts',(82.9129498948689,402.184674894296,54.188709927733));
#31208=CARTESIAN_POINT('Ctrl Pts',(82.9129498948689,402.278332223638,53.0228109606358));
#31209=CARTESIAN_POINT('Ctrl Pts',(82.9129498948689,403.721667776361,53.0228109606491));
#31210=CARTESIAN_POINT('Ctrl Pts',(82.9129498948652,403.544571204362,55.2274084205589));
#31211=CARTESIAN_POINT('Ctrl Pts',(81.9432795991032,403.367474632363,57.4147653849934));
#31212=CARTESIAN_POINT('Ctrl Pts',(80.3096882702443,403.190378060364,58.8951806411016));
#31213=CARTESIAN_POINT('Ctrl Pts',(78.6760969413854,403.013281488366,60.3755958972097));
#31214=CARTESIAN_POINT('Ctrl Pts',(76.4041347530309,402.836184916367,61.1259150206704));
#31215=CARTESIAN_POINT('Ctrl Pts',(74.2101800112088,402.659088344368,60.9095529374008));
#31216=CARTESIAN_POINT('Ctrl Pts',(72.0162252693866,402.481991772369,60.6931908541313));
#31217=CARTESIAN_POINT('Ctrl Pts',(69.9345925076871,402.304895200371,59.5135315737614));
#31218=CARTESIAN_POINT('Ctrl Pts',(68.6216467656529,402.127798628372,57.7425365317821));
#31219=CARTESIAN_POINT('Ctrl Pts',(67.3087010236187,401.950702056373,55.9715414898029));
#31220=CARTESIAN_POINT('Ctrl Pts',(66.7849774198229,401.773605484375,53.6369099216169));
#31221=CARTESIAN_POINT('Ctrl Pts',(67.2156126057631,401.596508912376,51.4747805783835));
#31222=CARTESIAN_POINT('Ctrl Pts',(67.6462477917033,401.419412340377,49.3126512351501));
#31223=CARTESIAN_POINT('Ctrl Pts',(69.0245064208058,401.242315768378,47.3568408855385));
#31224=CARTESIAN_POINT('Ctrl Pts',(70.9158061804575,401.06521919638,46.2240411771248));
#31225=CARTESIAN_POINT('Ctrl Pts',(72.8071059401091,400.888122624381,45.091241468711));
#31226=CARTESIAN_POINT('Ctrl Pts',(75.1818659698232,400.711026052382,44.7991699473061));
#31227=CARTESIAN_POINT('Ctrl Pts',(77.2912945088787,400.533929480384,45.4399204438793));
#31228=CARTESIAN_POINT('Ctrl Pts',(79.4007230479342,400.356832908385,46.0806709404525));
#31229=CARTESIAN_POINT('Ctrl Pts',(81.2118275942161,400.179736336386,47.6442218014035));
#31230=CARTESIAN_POINT('Ctrl Pts',(82.1535440633153,400.002639764387,49.6375657386276));
#31231=CARTESIAN_POINT('Ctrl Pts',(82.6515697929948,399.908982435045,50.6917435101899));
#31232=CARTESIAN_POINT('Ctrl Pts',(82.9129498948709,399.815325105703,51.8569119935514));
#31233=CARTESIAN_POINT('Ctrl Pts',(82.9129498948689,399.721667776361,53.0228109606489));
#31234=CARTESIAN_POINT('Origin',(74.9879498948689,255.,53.0228109606356));
#31235=CARTESIAN_POINT('',(82.9143243890985,394.278332223638,53.0219084888199));
#31236=CARTESIAN_POINT('',(82.9141514706698,395.72166777636,53.0235187303091));
#31237=CARTESIAN_POINT('',(82.9129498948689,255.,53.0228109606356));
#31238=CARTESIAN_POINT('Ctrl Pts',(82.9129498948689,394.278332223638,53.0228109606354));
#31239=CARTESIAN_POINT('Ctrl Pts',(82.9129498948689,394.455428795637,50.8182135007256));
#31240=CARTESIAN_POINT('Ctrl Pts',(81.9432795991106,394.632525367635,48.6308565362894));
#31241=CARTESIAN_POINT('Ctrl Pts',(80.3096882702542,394.809621939634,47.1504412801785));
#31242=CARTESIAN_POINT('Ctrl Pts',(78.6760969413978,394.986718511633,45.6700260240676));
#31243=CARTESIAN_POINT('Ctrl Pts',(76.4041347530445,395.163815083631,44.9197069006031));
#31244=CARTESIAN_POINT('Ctrl Pts',(74.210180011222,395.34091165563,45.136068983869));
#31245=CARTESIAN_POINT('Ctrl Pts',(72.0162252693995,395.518008227629,45.3524310671349));
#31246=CARTESIAN_POINT('Ctrl Pts',(69.934592507698,395.695104799628,46.5320903475013));
#31247=CARTESIAN_POINT('Ctrl Pts',(68.6216467656608,395.872201371626,48.3030853894784));
#31248=CARTESIAN_POINT('Ctrl Pts',(67.3087010236237,396.049297943625,50.0740804314554));
#31249=CARTESIAN_POINT('Ctrl Pts',(66.7849774198239,396.226394515624,52.4087119996405));
#31250=CARTESIAN_POINT('Ctrl Pts',(67.2156126057605,396.403491087623,54.5708413428747));
#31251=CARTESIAN_POINT('Ctrl Pts',(67.6462477916971,396.580587659621,56.7329706861088));
#31252=CARTESIAN_POINT('Ctrl Pts',(69.0245064207964,396.75768423162,58.6887810357227));
#31253=CARTESIAN_POINT('Ctrl Pts',(70.9158061804462,396.934780803619,59.8215807441396));
#31254=CARTESIAN_POINT('Ctrl Pts',(72.807105940096,397.111877375617,60.9543804525565));
#31255=CARTESIAN_POINT('Ctrl Pts',(75.1818659698097,397.288973947616,61.2464519739654));
#31256=CARTESIAN_POINT('Ctrl Pts',(77.2912945088662,397.466070519615,60.6057014773956));
#31257=CARTESIAN_POINT('Ctrl Pts',(79.4007230479228,397.643167091614,59.9649509808258));
#31258=CARTESIAN_POINT('Ctrl Pts',(81.2118275942073,397.820263663612,58.4014001198779));
#31259=CARTESIAN_POINT('Ctrl Pts',(82.1535440633097,397.997360235611,56.4080561826553));
#31260=CARTESIAN_POINT('Ctrl Pts',(82.651569792991,398.091017564953,55.3538784110939));
#31261=CARTESIAN_POINT('Ctrl Pts',(82.9129498948689,398.184674894296,54.188709927733));
#31262=CARTESIAN_POINT('Ctrl Pts',(82.9129498948689,398.278332223638,53.0228109606356));
#31263=CARTESIAN_POINT('Ctrl Pts',(82.9010717510546,399.721667776361,53.0276804110265));
#31264=CARTESIAN_POINT('Ctrl Pts',(82.9051844314699,399.631722269214,54.1519767949023));
#31265=CARTESIAN_POINT('Ctrl Pts',(82.682030927726,399.541776762067,55.2743640202701));
#31266=CARTESIAN_POINT('Ctrl Pts',(82.2236377097832,399.45183125492,56.2895162508407));
#31267=CARTESIAN_POINT('Ctrl Pts',(81.1424177688497,399.239675245368,58.6839732188166));
#31268=CARTESIAN_POINT('Ctrl Pts',(78.7524307261704,399.027519235815,60.4818233008151));
#31269=CARTESIAN_POINT('Ctrl Pts',(76.1506171505183,398.815363226263,60.8723217293589));
#31270=CARTESIAN_POINT('Ctrl Pts',(74.8497103626923,398.709285221487,61.0675709436308));
#31271=CARTESIAN_POINT('Ctrl Pts',(73.4958469416232,398.603207216711,60.9109822445391));
#31272=CARTESIAN_POINT('Ctrl Pts',(72.2527737980831,398.497129211935,60.4534117111886));
#31273=CARTESIAN_POINT('Ctrl Pts',(71.0097006545431,398.391051207159,59.9958411778381));
#31274=CARTESIAN_POINT('Ctrl Pts',(69.8774177885321,398.284973202383,59.2372888102288));
#31275=CARTESIAN_POINT('Ctrl Pts',(69.0135656461932,398.178895197606,58.2452000025176));
#31276=CARTESIAN_POINT('Ctrl Pts',(67.2858613615155,397.966739188054,56.2610223870953));
#31277=CARTESIAN_POINT('Ctrl Pts',(66.6318799715259,397.754583178501,53.3426990112652));
#31278=CARTESIAN_POINT('Ctrl Pts',(67.3611311303832,397.542427168949,50.8186836628596));
#31279=CARTESIAN_POINT('Ctrl Pts',(68.0903822892405,397.330271159396,48.294668314454));
#31280=CARTESIAN_POINT('Ctrl Pts',(70.2028659969447,397.118115149844,46.1649609934728));
#31281=CARTESIAN_POINT('Ctrl Pts',(72.7227932883516,396.905959140292,45.41403492531));
#31282=CARTESIAN_POINT('Ctrl Pts',(75.2427205797584,396.69380313074,44.6631088571472));
#31283=CARTESIAN_POINT('Ctrl Pts',(78.1700914548679,396.481647121188,45.2909640418026));
#31284=CARTESIAN_POINT('Ctrl Pts',(80.1632479148308,396.269491111635,47.0051009148426));
#31285=CARTESIAN_POINT('Ctrl Pts',(81.8788056026618,396.08688333321,48.4804997355617));
#31286=CARTESIAN_POINT('Ctrl Pts',(82.9022543906452,395.904275554785,50.7606658688838));
#31287=CARTESIAN_POINT('Ctrl Pts',(82.9211264258404,395.72166777636,53.027627219884));
#31288=CARTESIAN_POINT('Origin',(74.9879498948689,255.,53.0228109606356));
#31289=CARTESIAN_POINT('',(82.9098809662586,390.278332223638,53.0204521529043));
#31290=CARTESIAN_POINT('',(82.9135501799002,391.721667776361,53.0222178200602));
#31291=CARTESIAN_POINT('',(82.9129498948689,255.,53.0228109606356));
#31292=CARTESIAN_POINT('Ctrl Pts',(82.9082332267955,390.278332223638,53.0191856846757));
#31293=CARTESIAN_POINT('Ctrl Pts',(82.9121642338603,390.357600451624,52.0301359862952));
#31294=CARTESIAN_POINT('Ctrl Pts',(82.7366213310048,390.436868679611,51.0426507506166));
#31295=CARTESIAN_POINT('Ctrl Pts',(82.3762602245192,390.516136907597,50.1280769610102));
#31296=CARTESIAN_POINT('Ctrl Pts',(81.4117782839996,390.728292917149,47.6802825473726));
#31297=CARTESIAN_POINT('Ctrl Pts',(79.1233904318443,390.940448926702,45.7547737775995));
#31298=CARTESIAN_POINT('Ctrl Pts',(76.5473531371437,391.152604936254,45.2385445765189));
#31299=CARTESIAN_POINT('Ctrl Pts',(73.9713158424431,391.364760945806,44.7223153754382));
#31300=CARTESIAN_POINT('Ctrl Pts',(71.1076291051971,391.576916955359,45.6153657430501));
#31301=CARTESIAN_POINT('Ctrl Pts',(69.2797206269608,391.789072964911,47.5055176176273));
#31302=CARTESIAN_POINT('Ctrl Pts',(67.4518121487245,392.001228974463,49.3956694922046));
#31303=CARTESIAN_POINT('Ctrl Pts',(66.6596819294979,392.213384984015,52.2829228737472));
#31304=CARTESIAN_POINT('Ctrl Pts',(67.2621650360527,392.425540993568,54.8418195109206));
#31305=CARTESIAN_POINT('Ctrl Pts',(67.8646481426075,392.63769700312,57.400716148094));
#31306=CARTESIAN_POINT('Ctrl Pts',(69.8617445749438,392.849853012673,59.6312560408981));
#31307=CARTESIAN_POINT('Ctrl Pts',(72.34094729345,393.062009022225,60.5073139124612));
#31308=CARTESIAN_POINT('Ctrl Pts',(74.8201500119563,393.274165031777,61.3833717840243));
#31309=CARTESIAN_POINT('Ctrl Pts',(77.7814590166324,393.48632104133,60.9049476343463));
#31310=CARTESIAN_POINT('Ctrl Pts',(79.8565710669365,393.698477050882,59.2936218726151));
#31311=CARTESIAN_POINT('Ctrl Pts',(81.7471050800219,393.891762108467,57.8256210683852));
#31312=CARTESIAN_POINT('Ctrl Pts',(82.9020824215423,394.085047166052,55.4172950521791));
#31313=CARTESIAN_POINT('Ctrl Pts',(82.9194691672999,394.278332223638,53.0185305064141));
#31314=CARTESIAN_POINT('Ctrl Pts',(82.9129498948689,395.721667776361,53.0228109606487));
#31315=CARTESIAN_POINT('Ctrl Pts',(82.9129498948652,395.544571204362,55.2274084205586));
#31316=CARTESIAN_POINT('Ctrl Pts',(81.9432795991034,395.367474632363,57.4147653849932));
#31317=CARTESIAN_POINT('Ctrl Pts',(80.3096882702445,395.190378060364,58.8951806411014));
#31318=CARTESIAN_POINT('Ctrl Pts',(78.6760969413857,395.013281488366,60.3755958972096));
#31319=CARTESIAN_POINT('Ctrl Pts',(76.4041347530312,394.836184916367,61.1259150206704));
#31320=CARTESIAN_POINT('Ctrl Pts',(74.210180011209,394.659088344368,60.9095529374009));
#31321=CARTESIAN_POINT('Ctrl Pts',(72.0162252693868,394.481991772369,60.6931908541313));
#31322=CARTESIAN_POINT('Ctrl Pts',(69.9345925076872,394.304895200371,59.5135315737615));
#31323=CARTESIAN_POINT('Ctrl Pts',(68.621646765653,394.127798628372,57.7425365317822));
#31324=CARTESIAN_POINT('Ctrl Pts',(67.3087010236187,393.950702056373,55.971541489803));
#31325=CARTESIAN_POINT('Ctrl Pts',(66.7849774198229,393.773605484375,53.636909921617));
#31326=CARTESIAN_POINT('Ctrl Pts',(67.2156126057631,393.596508912376,51.4747805783835));
#31327=CARTESIAN_POINT('Ctrl Pts',(67.6462477917033,393.419412340377,49.31265123515));
#31328=CARTESIAN_POINT('Ctrl Pts',(69.0245064208059,393.242315768378,47.3568408855384));
#31329=CARTESIAN_POINT('Ctrl Pts',(70.9158061804576,393.06521919638,46.2240411771247));
#31330=CARTESIAN_POINT('Ctrl Pts',(72.8071059401093,392.888122624381,45.0912414687109));
#31331=CARTESIAN_POINT('Ctrl Pts',(75.1818659698234,392.711026052382,44.7991699473061));
#31332=CARTESIAN_POINT('Ctrl Pts',(77.291294508879,392.533929480383,45.4399204438794));
#31333=CARTESIAN_POINT('Ctrl Pts',(79.4007230479345,392.356832908385,46.0806709404527));
#31334=CARTESIAN_POINT('Ctrl Pts',(81.2118275942164,392.179736336386,47.6442218014037));
#31335=CARTESIAN_POINT('Ctrl Pts',(82.1535440633154,392.002639764387,49.6375657386279));
#31336=CARTESIAN_POINT('Ctrl Pts',(82.6515697929948,391.908982435045,50.6917435101901));
#31337=CARTESIAN_POINT('Ctrl Pts',(82.9129498948708,391.815325105703,51.8569119935513));
#31338=CARTESIAN_POINT('Ctrl Pts',(82.9129498948689,391.721667776361,53.0228109606485));
#31339=CARTESIAN_POINT('Origin',(74.9879498948689,255.,53.0228109606356));
#31340=CARTESIAN_POINT('',(82.90619017154,386.278332223638,53.0253308023074));
#31341=CARTESIAN_POINT('',(82.9082610542908,387.72166777636,53.0217421360302));
#31342=CARTESIAN_POINT('',(82.9129498948689,255.,53.0228109606356));
#31343=CARTESIAN_POINT('Ctrl Pts',(82.9129498948689,386.278332223638,53.022810960636));
#31344=CARTESIAN_POINT('Ctrl Pts',(82.912949894869,386.455428795637,50.8182135007262));
#31345=CARTESIAN_POINT('Ctrl Pts',(81.9432795991109,386.632525367635,48.6308565362899));
#31346=CARTESIAN_POINT('Ctrl Pts',(80.3096882702546,386.809621939634,47.1504412801789));
#31347=CARTESIAN_POINT('Ctrl Pts',(78.6760969413983,386.986718511633,45.6700260240679));
#31348=CARTESIAN_POINT('Ctrl Pts',(76.4041347530451,387.163815083631,44.9197069006032));
#31349=CARTESIAN_POINT('Ctrl Pts',(74.2101800112225,387.34091165563,45.136068983869));
#31350=CARTESIAN_POINT('Ctrl Pts',(72.0162252694,387.518008227629,45.3524310671347));
#31351=CARTESIAN_POINT('Ctrl Pts',(69.9345925076984,387.695104799628,46.532090347501));
#31352=CARTESIAN_POINT('Ctrl Pts',(68.6216467656611,387.872201371626,48.3030853894779));
#31353=CARTESIAN_POINT('Ctrl Pts',(67.3087010236239,388.049297943625,50.0740804314549));
#31354=CARTESIAN_POINT('Ctrl Pts',(66.784977419824,388.226394515624,52.40871199964));
#31355=CARTESIAN_POINT('Ctrl Pts',(67.2156126057604,388.403491087623,54.5708413428741));
#31356=CARTESIAN_POINT('Ctrl Pts',(67.6462477916969,388.580587659621,56.7329706861083));
#31357=CARTESIAN_POINT('Ctrl Pts',(69.024506420796,388.75768423162,58.6887810357223));
#31358=CARTESIAN_POINT('Ctrl Pts',(70.9158061804458,388.934780803619,59.8215807441393));
#31359=CARTESIAN_POINT('Ctrl Pts',(72.8071059400955,389.111877375617,60.9543804525564));
#31360=CARTESIAN_POINT('Ctrl Pts',(75.1818659698091,389.288973947616,61.2464519739654));
#31361=CARTESIAN_POINT('Ctrl Pts',(77.2912945088657,389.466070519615,60.6057014773958));
#31362=CARTESIAN_POINT('Ctrl Pts',(79.4007230479223,389.643167091614,59.9649509808262));
#31363=CARTESIAN_POINT('Ctrl Pts',(81.2118275942069,389.820263663612,58.4014001198783));
#31364=CARTESIAN_POINT('Ctrl Pts',(82.1535440633095,389.997360235611,56.4080561826558));
#31365=CARTESIAN_POINT('Ctrl Pts',(82.6515697929909,390.091017564953,55.3538784110942));
#31366=CARTESIAN_POINT('Ctrl Pts',(82.9129498948689,390.184674894296,54.1887099277329));
#31367=CARTESIAN_POINT('Ctrl Pts',(82.9129498948689,390.278332223638,53.0228109606353));
#31368=CARTESIAN_POINT('Ctrl Pts',(82.918916717821,391.721667776361,53.0169151530433));
#31369=CARTESIAN_POINT('Ctrl Pts',(82.9005549932558,391.5403608117,55.2681042080206));
#31370=CARTESIAN_POINT('Ctrl Pts',(81.8968913010544,391.35905384704,57.533901780382));
#31371=CARTESIAN_POINT('Ctrl Pts',(80.2020049922721,391.17774688238,59.0092987998488));
#31372=CARTESIAN_POINT('Ctrl Pts',(78.2187369110388,390.965590872827,60.7357318949143));
#31373=CARTESIAN_POINT('Ctrl Pts',(75.2890145455258,390.753434863275,61.3799116440399));
#31374=CARTESIAN_POINT('Ctrl Pts',(72.7667373037651,390.541278853723,60.6446713789343));
#31375=CARTESIAN_POINT('Ctrl Pts',(70.2444600620044,390.32912284417,59.9094311138287));
#31376=CARTESIAN_POINT('Ctrl Pts',(68.129627943996,390.116966834618,57.7947708344919));
#31377=CARTESIAN_POINT('Ctrl Pts',(67.3786141600463,389.904810825066,55.2732829401444));
#31378=CARTESIAN_POINT('Ctrl Pts',(67.0031072680715,389.79873282029,54.0125389929706));
#31379=CARTESIAN_POINT('Ctrl Pts',(66.9685549596114,389.692654815514,52.650088142044));
#31380=CARTESIAN_POINT('Ctrl Pts',(67.2475337798262,389.586576810738,51.3551856549928));
#31381=CARTESIAN_POINT('Ctrl Pts',(67.526512600041,389.480498805961,50.0602831679415));
#31382=CARTESIAN_POINT('Ctrl Pts',(68.1190225489307,389.374420801185,48.8329290447656));
#31383=CARTESIAN_POINT('Ctrl Pts',(68.9803591730895,389.268342796408,47.8386554676558));
#31384=CARTESIAN_POINT('Ctrl Pts',(70.7030324214069,389.056186786856,45.850108313436));
#31385=CARTESIAN_POINT('Ctrl Pts',(73.5010123708004,388.844030777304,44.7938833434809));
#31386=CARTESIAN_POINT('Ctrl Pts',(76.1022808095363,388.631874767752,45.162479655689));
#31387=CARTESIAN_POINT('Ctrl Pts',(78.7035492482722,388.4197187582,45.5310759678972));
#31388=CARTESIAN_POINT('Ctrl Pts',(81.1081061763504,388.207562748647,47.3244935622687));
#31389=CARTESIAN_POINT('Ctrl Pts',(82.2045282531435,387.995406739095,49.7144270641254));
#31390=CARTESIAN_POINT('Ctrl Pts',(82.6760891619508,387.904160418183,50.7423151721622));
#31391=CARTESIAN_POINT('Ctrl Pts',(82.9056739193359,387.812914097272,51.8805455919368));
#31392=CARTESIAN_POINT('Ctrl Pts',(82.9013757710113,387.72166777636,53.0201726307016));
#31393=CARTESIAN_POINT('Origin',(74.9879498948689,255.,53.0228109606356));
#31394=CARTESIAN_POINT('',(82.9169094223468,382.278332223638,53.0242849124606));
#31395=CARTESIAN_POINT('',(82.9129498948689,383.721667776361,53.0228109606488));
#31396=CARTESIAN_POINT('',(82.9129498948689,255.,53.0228109606356));
#31397=CARTESIAN_POINT('Ctrl Pts',(82.9257214576602,382.278332223638,53.0275652320441));
#31398=CARTESIAN_POINT('Ctrl Pts',(82.9150137442642,382.478395003663,50.5485677664457));
#31399=CARTESIAN_POINT('Ctrl Pts',(81.6577189855839,382.678457783688,48.0552956934044));
#31400=CARTESIAN_POINT('Ctrl Pts',(79.6514807652487,382.878520563714,46.5981796849265));
#31401=CARTESIAN_POINT('Ctrl Pts',(77.5239711156085,383.090676573266,45.0529851326245));
#31402=CARTESIAN_POINT('Ctrl Pts',(74.554238438814,383.302832582818,44.6729980251841));
#31403=CARTESIAN_POINT('Ctrl Pts',(72.1049313448895,383.514988592371,45.627897314676));
#31404=CARTESIAN_POINT('Ctrl Pts',(69.655624250965,383.727144601923,46.5827966041679));
#31405=CARTESIAN_POINT('Ctrl Pts',(67.7267427399103,383.939300611475,48.872582290592));
#31406=CARTESIAN_POINT('Ctrl Pts',(67.2065107590059,384.151456621028,51.4500388275331));
#31407=CARTESIAN_POINT('Ctrl Pts',(66.6862787781014,384.36361263058,54.0274953644742));
#31408=CARTESIAN_POINT('Ctrl Pts',(67.5746963273472,384.575768640132,56.8926227519322));
#31409=CARTESIAN_POINT('Ctrl Pts',(69.4607464568784,384.787924649684,58.7216322217361));
#31410=CARTESIAN_POINT('Ctrl Pts',(71.3467965864096,385.000080659237,60.55064169154));
#31411=CARTESIAN_POINT('Ctrl Pts',(74.2304792962261,385.212236668789,61.3435332436897));
#31412=CARTESIAN_POINT('Ctrl Pts',(76.7935642786192,385.424392678341,60.7498007466388));
#31413=CARTESIAN_POINT('Ctrl Pts',(78.0751067698158,385.530470683118,60.4529344981132));
#31414=CARTESIAN_POINT('Ctrl Pts',(79.2764998291565,385.636548687894,59.8094122372876));
#31415=CARTESIAN_POINT('Ctrl Pts',(80.2641755681491,385.74262669267,58.9267468036688));
#31416=CARTESIAN_POINT('Ctrl Pts',(81.2518513071416,385.848704697446,58.04408137005));
#31417=CARTESIAN_POINT('Ctrl Pts',(82.025809725786,385.954782702222,56.922272763638));
#31418=CARTESIAN_POINT('Ctrl Pts',(82.4642624635814,386.060860706998,55.6820147570218));
#31419=CARTESIAN_POINT('Ctrl Pts',(82.7638878259559,386.133351212545,54.8344598836305));
#31420=CARTESIAN_POINT('Ctrl Pts',(82.906833950516,386.205841718091,53.9315898164796));
#31421=CARTESIAN_POINT('Ctrl Pts',(82.9011087758377,386.278332223638,53.0272250089215));
#31422=CARTESIAN_POINT('Ctrl Pts',(82.9129498948689,387.721667776361,53.0228109606484));
#31423=CARTESIAN_POINT('Ctrl Pts',(82.9129498948653,387.544571204362,55.2274084205582));
#31424=CARTESIAN_POINT('Ctrl Pts',(81.9432795991036,387.367474632363,57.4147653849929));
#31425=CARTESIAN_POINT('Ctrl Pts',(80.3096882702448,387.190378060364,58.8951806411012));
#31426=CARTESIAN_POINT('Ctrl Pts',(78.676096941386,387.013281488366,60.3755958972095));
#31427=CARTESIAN_POINT('Ctrl Pts',(76.4041347530315,386.836184916367,61.1259150206703));
#31428=CARTESIAN_POINT('Ctrl Pts',(74.2101800112093,386.659088344368,60.9095529374009));
#31429=CARTESIAN_POINT('Ctrl Pts',(72.016225269387,386.48199177237,60.6931908541314));
#31430=CARTESIAN_POINT('Ctrl Pts',(69.9345925076875,386.304895200371,59.5135315737616));
#31431=CARTESIAN_POINT('Ctrl Pts',(68.6216467656532,386.127798628372,57.7425365317824));
#31432=CARTESIAN_POINT('Ctrl Pts',(67.3087010236189,385.950702056373,55.9715414898033));
#31433=CARTESIAN_POINT('Ctrl Pts',(66.7849774198229,385.773605484375,53.6369099216173));
#31434=CARTESIAN_POINT('Ctrl Pts',(67.2156126057631,385.596508912376,51.4747805783838));
#31435=CARTESIAN_POINT('Ctrl Pts',(67.6462477917032,385.419412340377,49.3126512351503));
#31436=CARTESIAN_POINT('Ctrl Pts',(69.0245064208057,385.242315768378,47.3568408855387));
#31437=CARTESIAN_POINT('Ctrl Pts',(70.9158061804574,385.06521919638,46.2240411771248));
#31438=CARTESIAN_POINT('Ctrl Pts',(72.807105940109,384.888122624381,45.091241468711));
#31439=CARTESIAN_POINT('Ctrl Pts',(75.1818659698231,384.711026052382,44.7991699473061));
#31440=CARTESIAN_POINT('Ctrl Pts',(77.2912945088787,384.533929480384,45.4399204438793));
#31441=CARTESIAN_POINT('Ctrl Pts',(79.4007230479342,384.356832908385,46.0806709404525));
#31442=CARTESIAN_POINT('Ctrl Pts',(81.2118275942162,384.179736336386,47.6442218014035));
#31443=CARTESIAN_POINT('Ctrl Pts',(82.1535440633153,384.002639764387,49.6375657386277));
#31444=CARTESIAN_POINT('Ctrl Pts',(82.6515697929949,383.908982435045,50.69174351019));
#31445=CARTESIAN_POINT('Ctrl Pts',(82.9129498948709,383.815325105703,51.8569119935516));
#31446=CARTESIAN_POINT('Ctrl Pts',(82.9129498948689,383.721667776361,53.0228109606491));
#31447=CARTESIAN_POINT('Origin',(74.9879498948689,255.,53.0228109606356));
#31448=CARTESIAN_POINT('',(82.9129498948689,378.278332223638,53.0228109606357));
#31449=CARTESIAN_POINT('',(82.917669415744,379.721667776361,53.0222330588015));
#31450=CARTESIAN_POINT('',(82.9129498948689,255.,53.0228109606356));
#31451=CARTESIAN_POINT('Ctrl Pts',(82.9129498948689,378.278332223638,53.0228109606356));
#31452=CARTESIAN_POINT('Ctrl Pts',(82.9129498948689,378.455428795637,50.8182135007257));
#31453=CARTESIAN_POINT('Ctrl Pts',(81.9432795991107,378.632525367635,48.6308565362895));
#31454=CARTESIAN_POINT('Ctrl Pts',(80.3096882702542,378.809621939634,47.1504412801785));
#31455=CARTESIAN_POINT('Ctrl Pts',(78.6760969413978,378.986718511633,45.6700260240676));
#31456=CARTESIAN_POINT('Ctrl Pts',(76.4041347530444,379.163815083631,44.9197069006031));
#31457=CARTESIAN_POINT('Ctrl Pts',(74.2101800112218,379.34091165563,45.136068983869));
#31458=CARTESIAN_POINT('Ctrl Pts',(72.0162252693992,379.518008227629,45.352431067135));
#31459=CARTESIAN_POINT('Ctrl Pts',(69.9345925076977,379.695104799628,46.5320903475015));
#31460=CARTESIAN_POINT('Ctrl Pts',(68.6216467656606,379.872201371626,48.3030853894787));
#31461=CARTESIAN_POINT('Ctrl Pts',(67.3087010236235,380.049297943625,50.0740804314558));
#31462=CARTESIAN_POINT('Ctrl Pts',(66.7849774198239,380.226394515624,52.408711999641));
#31463=CARTESIAN_POINT('Ctrl Pts',(67.2156126057606,380.403491087623,54.5708413428752));
#31464=CARTESIAN_POINT('Ctrl Pts',(67.6462477916974,380.580587659621,56.7329706861094));
#31465=CARTESIAN_POINT('Ctrl Pts',(69.0245064207969,380.75768423162,58.6887810357232));
#31466=CARTESIAN_POINT('Ctrl Pts',(70.9158061804468,380.934780803619,59.82158074414));
#31467=CARTESIAN_POINT('Ctrl Pts',(72.8071059400968,381.111877375617,60.9543804525568));
#31468=CARTESIAN_POINT('Ctrl Pts',(75.1818659698105,381.288973947616,61.2464519739654));
#31469=CARTESIAN_POINT('Ctrl Pts',(77.2912945088671,381.466070519615,60.6057014773954));
#31470=CARTESIAN_POINT('Ctrl Pts',(79.4007230479236,381.643167091614,59.9649509808253));
#31471=CARTESIAN_POINT('Ctrl Pts',(81.211827594208,381.820263663612,58.4014001198771));
#31472=CARTESIAN_POINT('Ctrl Pts',(82.1535440633102,381.997360235611,56.4080561826543));
#31473=CARTESIAN_POINT('Ctrl Pts',(82.6515697929911,382.091017564953,55.3538784110933));
#31474=CARTESIAN_POINT('Ctrl Pts',(82.9129498948689,382.184674894296,54.1887099277327));
#31475=CARTESIAN_POINT('Ctrl Pts',(82.9129498948689,382.278332223638,53.0228109606358));
#31476=CARTESIAN_POINT('Ctrl Pts',(82.9129498948689,383.721667776361,53.0228109606491));
#31477=CARTESIAN_POINT('Ctrl Pts',(82.9129498948652,383.544571204362,55.2274084205589));
#31478=CARTESIAN_POINT('Ctrl Pts',(81.9432795991032,383.367474632363,57.4147653849935));
#31479=CARTESIAN_POINT('Ctrl Pts',(80.3096882702443,383.190378060364,58.8951806411016));
#31480=CARTESIAN_POINT('Ctrl Pts',(78.6760969413854,383.013281488366,60.3755958972097));
#31481=CARTESIAN_POINT('Ctrl Pts',(76.4041347530309,382.836184916367,61.1259150206704));
#31482=CARTESIAN_POINT('Ctrl Pts',(74.2101800112088,382.659088344368,60.9095529374008));
#31483=CARTESIAN_POINT('Ctrl Pts',(72.0162252693866,382.481991772369,60.6931908541312));
#31484=CARTESIAN_POINT('Ctrl Pts',(69.9345925076871,382.304895200371,59.5135315737613));
#31485=CARTESIAN_POINT('Ctrl Pts',(68.6216467656529,382.127798628372,57.7425365317821));
#31486=CARTESIAN_POINT('Ctrl Pts',(67.3087010236187,381.950702056373,55.9715414898029));
#31487=CARTESIAN_POINT('Ctrl Pts',(66.7849774198229,381.773605484375,53.6369099216169));
#31488=CARTESIAN_POINT('Ctrl Pts',(67.2156126057631,381.596508912376,51.4747805783835));
#31489=CARTESIAN_POINT('Ctrl Pts',(67.6462477917033,381.419412340377,49.3126512351501));
#31490=CARTESIAN_POINT('Ctrl Pts',(69.0245064208058,381.242315768378,47.3568408855385));
#31491=CARTESIAN_POINT('Ctrl Pts',(70.9158061804575,381.06521919638,46.2240411771248));
#31492=CARTESIAN_POINT('Ctrl Pts',(72.8071059401092,380.888122624381,45.091241468711));
#31493=CARTESIAN_POINT('Ctrl Pts',(75.1818659698232,380.711026052382,44.7991699473061));
#31494=CARTESIAN_POINT('Ctrl Pts',(77.2912945088787,380.533929480384,45.4399204438793));
#31495=CARTESIAN_POINT('Ctrl Pts',(79.4007230479342,380.356832908385,46.0806709404526));
#31496=CARTESIAN_POINT('Ctrl Pts',(81.2118275942161,380.179736336386,47.6442218014035));
#31497=CARTESIAN_POINT('Ctrl Pts',(82.1535440633153,380.002639764387,49.6375657386276));
#31498=CARTESIAN_POINT('Ctrl Pts',(82.6515697929948,379.908982435045,50.69174351019));
#31499=CARTESIAN_POINT('Ctrl Pts',(82.9129498948709,379.815325105703,51.8569119935514));
#31500=CARTESIAN_POINT('Ctrl Pts',(82.9129498948689,379.721667776361,53.0228109606489));
#31501=CARTESIAN_POINT('Origin',(74.9879498948689,255.,53.0228109606356));
#31502=CARTESIAN_POINT('',(82.9087440841051,374.278332223638,53.0229220451327));
#31503=CARTESIAN_POINT('',(82.9105410465356,375.721667776361,53.0211223461501));
#31504=CARTESIAN_POINT('',(82.9129498948689,255.,53.0228109606356));
#31505=CARTESIAN_POINT('Ctrl Pts',(82.9129498948689,374.278332223638,53.0228109606354));
#31506=CARTESIAN_POINT('Ctrl Pts',(82.9129498948689,374.455428795637,50.8182135007257));
#31507=CARTESIAN_POINT('Ctrl Pts',(81.9432795991107,374.632525367635,48.6308565362895));
#31508=CARTESIAN_POINT('Ctrl Pts',(80.3096882702543,374.809621939634,47.1504412801786));
#31509=CARTESIAN_POINT('Ctrl Pts',(78.676096941398,374.986718511633,45.6700260240677));
#31510=CARTESIAN_POINT('Ctrl Pts',(76.4041347530448,375.163815083631,44.9197069006031));
#31511=CARTESIAN_POINT('Ctrl Pts',(74.2101800112223,375.34091165563,45.136068983869));
#31512=CARTESIAN_POINT('Ctrl Pts',(72.0162252693998,375.518008227629,45.3524310671348));
#31513=CARTESIAN_POINT('Ctrl Pts',(69.9345925076983,375.695104799628,46.5320903475011));
#31514=CARTESIAN_POINT('Ctrl Pts',(68.6216467656611,375.872201371626,48.303085389478));
#31515=CARTESIAN_POINT('Ctrl Pts',(67.3087010236239,376.049297943625,50.0740804314549));
#31516=CARTESIAN_POINT('Ctrl Pts',(66.784977419824,376.226394515624,52.4087119996399));
#31517=CARTESIAN_POINT('Ctrl Pts',(67.2156126057604,376.403491087623,54.570841342874));
#31518=CARTESIAN_POINT('Ctrl Pts',(67.6462477916968,376.580587659621,56.7329706861082));
#31519=CARTESIAN_POINT('Ctrl Pts',(69.0245064207959,376.75768423162,58.6887810357221));
#31520=CARTESIAN_POINT('Ctrl Pts',(70.9158061804455,376.934780803619,59.8215807441392));
#31521=CARTESIAN_POINT('Ctrl Pts',(72.8071059400951,377.111877375617,60.9543804525563));
#31522=CARTESIAN_POINT('Ctrl Pts',(75.1818659698087,377.288973947616,61.2464519739654));
#31523=CARTESIAN_POINT('Ctrl Pts',(77.2912945088653,377.466070519615,60.6057014773959));
#31524=CARTESIAN_POINT('Ctrl Pts',(79.4007230479219,377.643167091614,59.9649509808264));
#31525=CARTESIAN_POINT('Ctrl Pts',(81.2118275942065,377.820263663612,58.4014001198787));
#31526=CARTESIAN_POINT('Ctrl Pts',(82.1535440633092,377.997360235611,56.4080561826563));
#31527=CARTESIAN_POINT('Ctrl Pts',(82.6515697929908,378.091017564953,55.3538784110947));
#31528=CARTESIAN_POINT('Ctrl Pts',(82.9129498948689,378.184674894296,54.1887099277333));
#31529=CARTESIAN_POINT('Ctrl Pts',(82.9129498948689,378.278332223638,53.0228109606356));
#31530=CARTESIAN_POINT('Ctrl Pts',(82.9268750308129,379.721667776361,53.0211058379808));
#31531=CARTESIAN_POINT('Ctrl Pts',(82.9277596348217,379.509396630207,55.6497794910386));
#31532=CARTESIAN_POINT('Ctrl Pts',(81.4883940862173,379.297125484052,58.28388116542));
#31533=CARTESIAN_POINT('Ctrl Pts',(79.2743564499831,379.084854337897,59.7049607683006));
#31534=CARTESIAN_POINT('Ctrl Pts',(77.0615197154011,378.872698328345,61.1252695727021));
#31535=CARTESIAN_POINT('Ctrl Pts',(74.0748514262754,378.660542318793,61.3338718358065));
#31536=CARTESIAN_POINT('Ctrl Pts',(71.6845021330615,378.448386309241,60.2397200411031));
#31537=CARTESIAN_POINT('Ctrl Pts',(69.2941528398476,378.236230299689,59.1455682463996));
#31538=CARTESIAN_POINT('Ctrl Pts',(67.5001225425455,378.024074290136,56.7486623938882));
#31539=CARTESIAN_POINT('Ctrl Pts',(67.1289520079351,377.811918280584,54.1455573349225));
#31540=CARTESIAN_POINT('Ctrl Pts',(66.7577814733247,377.599762271031,51.5424522759567));
#31541=CARTESIAN_POINT('Ctrl Pts',(67.809470701406,377.387606261479,48.7331480105366));
#31542=CARTESIAN_POINT('Ctrl Pts',(69.7975664214702,377.175450251927,47.0156101973868));
#31543=CARTESIAN_POINT('Ctrl Pts',(71.7856621415344,376.963294242375,45.2980723842371));
#31544=CARTESIAN_POINT('Ctrl Pts',(74.7101643535816,376.751138232822,44.6723010233578));
#31545=CARTESIAN_POINT('Ctrl Pts',(77.2348699696133,376.53898222327,45.4124256462436));
#31546=CARTESIAN_POINT('Ctrl Pts',(78.4972227776292,376.432904218494,45.7824879576864));
#31547=CARTESIAN_POINT('Ctrl Pts',(79.6596264366412,376.326826213718,46.4940242650705));
#31548=CARTESIAN_POINT('Ctrl Pts',(80.5949158999949,376.220748208942,47.4320196023935));
#31549=CARTESIAN_POINT('Ctrl Pts',(81.5302053633485,376.114670204165,48.3700149397164));
#31550=CARTESIAN_POINT('Ctrl Pts',(82.2383806310438,376.008592199389,49.5344693069782));
#31551=CARTESIAN_POINT('Ctrl Pts',(82.6047945844103,375.902514194613,50.7978859211772));
#31552=CARTESIAN_POINT('Ctrl Pts',(82.8130207578564,375.842232055196,51.5158618733096));
#31553=CARTESIAN_POINT('Ctrl Pts',(82.9108773156051,375.781949915778,52.2657970458251));
#31554=CARTESIAN_POINT('Ctrl Pts',(82.9047414110188,375.721667776361,53.0170567732019));
#31555=CARTESIAN_POINT('Origin',(74.9879498948689,255.,53.0228109606356));
#31556=CARTESIAN_POINT('',(82.9146081634051,370.278332223638,53.029785282215));
#31557=CARTESIAN_POINT('',(82.9117595115795,371.72166777636,53.02320991057));
#31558=CARTESIAN_POINT('',(82.9129498948689,255.,53.0228109606356));
#31559=CARTESIAN_POINT('Ctrl Pts',(82.9146081634051,370.278332223638,53.029785282215));
#31560=CARTESIAN_POINT('Ctrl Pts',(82.895835554435,370.447430822169,50.9271921297301));
#31561=CARTESIAN_POINT('Ctrl Pts',(82.0366188183737,370.616529420701,48.8106954290504));
#31562=CARTESIAN_POINT('Ctrl Pts',(80.5375948247923,370.785628019232,47.3460294464692));
#31563=CARTESIAN_POINT('Ctrl Pts',(78.6568758155066,370.997784028784,45.5084169949747));
#31564=CARTESIAN_POINT('Ctrl Pts',(75.7690400495532,371.209940038336,44.6968473571427));
#31565=CARTESIAN_POINT('Ctrl Pts',(73.2086602687691,371.422096047889,45.2858432059296));
#31566=CARTESIAN_POINT('Ctrl Pts',(70.6482804879848,371.634252057441,45.8748390547165));
#31567=CARTESIAN_POINT('Ctrl Pts',(68.4153566923697,371.846408066993,47.8644003901223));
#31568=CARTESIAN_POINT('Ctrl Pts',(67.5206027772723,372.058564076546,50.3385342459275));
#31569=CARTESIAN_POINT('Ctrl Pts',(67.0732258197235,372.164642081322,51.5756011738301));
#31570=CARTESIAN_POINT('Ctrl Pts',(66.9603913323042,372.270720086098,52.9338112318324));
#31571=CARTESIAN_POINT('Ctrl Pts',(67.1644532117948,372.376798090874,54.2426123559298));
#31572=CARTESIAN_POINT('Ctrl Pts',(67.3685150912855,372.48287609565,55.5514134800272));
#31573=CARTESIAN_POINT('Ctrl Pts',(67.8894733376861,372.588954100426,56.8108056702197));
#31574=CARTESIAN_POINT('Ctrl Pts',(68.6922153662661,372.695032105203,57.8529601509983));
#31575=CARTESIAN_POINT('Ctrl Pts',(70.2976994234263,372.907188114755,59.9372691125558));
#31576=CARTESIAN_POINT('Ctrl Pts',(73.0303186093043,373.119344124307,61.1526272364583));
#31577=CARTESIAN_POINT('Ctrl Pts',(75.6484772999912,373.33150013386,60.9342106571487));
#31578=CARTESIAN_POINT('Ctrl Pts',(78.2666359906781,373.543656143412,60.7157940778391));
#31579=CARTESIAN_POINT('Ctrl Pts',(80.770334186174,373.755812152964,59.0636027953172));
#31580=CARTESIAN_POINT('Ctrl Pts',(82.0023607164196,373.967968162516,56.7406662609825));
#31581=CARTESIAN_POINT('Ctrl Pts',(82.6031399231037,374.071422849557,55.6079211990747));
#31582=CARTESIAN_POINT('Ctrl Pts',(82.9015310543615,374.174877536597,54.315681063604));
#31583=CARTESIAN_POINT('Ctrl Pts',(82.9001803294088,374.278332223638,53.0231482322911));
#31584=CARTESIAN_POINT('Ctrl Pts',(82.9129498948689,375.721667776361,53.0228109606487));
#31585=CARTESIAN_POINT('Ctrl Pts',(82.9129498948652,375.544571204362,55.2274084205585));
#31586=CARTESIAN_POINT('Ctrl Pts',(81.9432795991034,375.367474632363,57.4147653849932));
#31587=CARTESIAN_POINT('Ctrl Pts',(80.3096882702445,375.190378060364,58.8951806411014));
#31588=CARTESIAN_POINT('Ctrl Pts',(78.6760969413857,375.013281488366,60.3755958972096));
#31589=CARTESIAN_POINT('Ctrl Pts',(76.4041347530311,374.836184916367,61.1259150206704));
#31590=CARTESIAN_POINT('Ctrl Pts',(74.2101800112089,374.659088344368,60.9095529374008));
#31591=CARTESIAN_POINT('Ctrl Pts',(72.0162252693867,374.481991772369,60.6931908541313));
#31592=CARTESIAN_POINT('Ctrl Pts',(69.9345925076872,374.304895200371,59.5135315737614));
#31593=CARTESIAN_POINT('Ctrl Pts',(68.621646765653,374.127798628372,57.7425365317822));
#31594=CARTESIAN_POINT('Ctrl Pts',(67.3087010236187,373.950702056373,55.9715414898029));
#31595=CARTESIAN_POINT('Ctrl Pts',(66.7849774198229,373.773605484375,53.6369099216169));
#31596=CARTESIAN_POINT('Ctrl Pts',(67.2156126057631,373.596508912376,51.4747805783835));
#31597=CARTESIAN_POINT('Ctrl Pts',(67.6462477917033,373.419412340377,49.31265123515));
#31598=CARTESIAN_POINT('Ctrl Pts',(69.0245064208059,373.242315768378,47.3568408855384));
#31599=CARTESIAN_POINT('Ctrl Pts',(70.9158061804577,373.06521919638,46.2240411771247));
#31600=CARTESIAN_POINT('Ctrl Pts',(72.8071059401094,372.888122624381,45.0912414687109));
#31601=CARTESIAN_POINT('Ctrl Pts',(75.1818659698235,372.711026052382,44.7991699473061));
#31602=CARTESIAN_POINT('Ctrl Pts',(77.291294508879,372.533929480383,45.4399204438794));
#31603=CARTESIAN_POINT('Ctrl Pts',(79.4007230479345,372.356832908385,46.0806709404527));
#31604=CARTESIAN_POINT('Ctrl Pts',(81.2118275942164,372.179736336386,47.6442218014038));
#31605=CARTESIAN_POINT('Ctrl Pts',(82.1535440633154,372.002639764387,49.637565738628));
#31606=CARTESIAN_POINT('Ctrl Pts',(82.6515697929949,371.908982435045,50.6917435101901));
#31607=CARTESIAN_POINT('Ctrl Pts',(82.9129498948708,371.815325105703,51.8569119935514));
#31608=CARTESIAN_POINT('Ctrl Pts',(82.9129498948689,371.721667776361,53.0228109606486));
#31609=CARTESIAN_POINT('Origin',(74.9879498948689,255.,53.0228109606356));
#31610=CARTESIAN_POINT('',(82.9246351989638,366.278332223638,53.0200841918108));
#31611=CARTESIAN_POINT('',(82.9134155880036,367.721667776361,53.023873582756));
#31612=CARTESIAN_POINT('',(82.9129498948689,255.,53.0228109606356));
#31613=CARTESIAN_POINT('Ctrl Pts',(82.9246351989638,366.278332223638,53.0200841918108));
#31614=CARTESIAN_POINT('Ctrl Pts',(82.9259058467681,366.295672088636,52.8050527487061));
#31615=CARTESIAN_POINT('Ctrl Pts',(82.9179101534511,366.313011953635,52.590100792154));
#31616=CARTESIAN_POINT('Ctrl Pts',(82.9003407545765,366.330351818633,52.3759121346824));
#31617=CARTESIAN_POINT('Ctrl Pts',(82.6853763614975,366.542507828186,49.7552798019267));
#31618=CARTESIAN_POINT('Ctrl Pts',(81.0372366544246,366.754663837738,47.2489126711698));
#31619=CARTESIAN_POINT('Ctrl Pts',(78.7179356483762,366.96681984729,46.0146908211446));
#31620=CARTESIAN_POINT('Ctrl Pts',(76.3986346423277,367.178975856842,44.7804689711194));
#31621=CARTESIAN_POINT('Ctrl Pts',(73.4081723373038,367.391131866395,44.8183924018261));
#31622=CARTESIAN_POINT('Ctrl Pts',(71.110277134158,367.603287875947,46.0996420029512));
#31623=CARTESIAN_POINT('Ctrl Pts',(69.9613295325851,367.709365880723,46.7402668035138));
#31624=CARTESIAN_POINT('Ctrl Pts',(68.9855237064817,367.815443885499,47.691723146681));
#31625=CARTESIAN_POINT('Ctrl Pts',(68.2813726222647,367.921521890276,48.8136736285187));
#31626=CARTESIAN_POINT('Ctrl Pts',(67.5772215380476,368.027599895052,49.9356241103564));
#31627=CARTESIAN_POINT('Ctrl Pts',(67.1447251957169,368.133677899828,51.2280687308647));
#31628=CARTESIAN_POINT('Ctrl Pts',(67.0674236777374,368.239755904604,52.5412729044698));
#31629=CARTESIAN_POINT('Ctrl Pts',(66.9128206417784,368.451911914156,55.1676812516801));
#31630=CARTESIAN_POINT('Ctrl Pts',(68.1789969032245,368.664067923708,57.8771278112779));
#31631=CARTESIAN_POINT('Ctrl Pts',(70.2989217094926,368.876223933261,59.4290232805367));
#31632=CARTESIAN_POINT('Ctrl Pts',(72.4188465157607,369.088379942813,60.9809187497954));
#31633=CARTESIAN_POINT('Ctrl Pts',(75.3925198668508,369.300535952365,61.3752631287152));
#31634=CARTESIAN_POINT('Ctrl Pts',(77.8459107292913,369.512691961918,60.4293261382823));
#31635=CARTESIAN_POINT('Ctrl Pts',(80.2993015917319,369.72484797147,59.4833891478494));
#31636=CARTESIAN_POINT('Ctrl Pts',(82.2324099655229,369.937003981022,57.1971707880637));
#31637=CARTESIAN_POINT('Ctrl Pts',(82.7621630261094,370.149159990575,54.6222339755923));
#31638=CARTESIAN_POINT('Ctrl Pts',(82.8696772809139,370.192217401596,54.0996463151173));
#31639=CARTESIAN_POINT('Ctrl Pts',(82.9193882144959,370.235274812617,53.5651665234718));
#31640=CARTESIAN_POINT('Ctrl Pts',(82.9146081634051,370.278332223638,53.029785282215));
#31641=CARTESIAN_POINT('Ctrl Pts',(82.9066444346458,371.721667776361,53.0249241981763));
#31642=CARTESIAN_POINT('Ctrl Pts',(82.9091713020796,371.630191182245,54.1669385451946));
#31643=CARTESIAN_POINT('Ctrl Pts',(82.6734524996546,371.53871458813,55.3078024227671));
#31644=CARTESIAN_POINT('Ctrl Pts',(82.1975929589684,371.447237994014,56.3375751067078));
#31645=CARTESIAN_POINT('Ctrl Pts',(81.093961344394,371.235081984462,58.7258632309372));
#31646=CARTESIAN_POINT('Ctrl Pts',(78.6986449422475,371.02292597491,60.5166067407603));
#31647=CARTESIAN_POINT('Ctrl Pts',(76.0971869326856,370.810769965358,60.8838627226355));
#31648=CARTESIAN_POINT('Ctrl Pts',(73.4957289231237,370.598613955805,61.2511187045107));
#31649=CARTESIAN_POINT('Ctrl Pts',(70.6881293061464,370.386457946253,60.1948871584381));
#31650=CARTESIAN_POINT('Ctrl Pts',(68.9719265086356,370.1743019367,58.2027597851027));
#31651=CARTESIAN_POINT('Ctrl Pts',(67.2557237111248,369.962145927148,56.2106324117673));
#31652=CARTESIAN_POINT('Ctrl Pts',(66.6309177330805,369.749989917596,53.2826092111691));
#31653=CARTESIAN_POINT('Ctrl Pts',(67.3795376632359,369.537833908044,50.7625881609405));
#31654=CARTESIAN_POINT('Ctrl Pts',(68.1281575933913,369.325677898491,48.2425671107118));
#31655=CARTESIAN_POINT('Ctrl Pts',(70.2502034317463,369.113521888939,46.1305482108527));
#31656=CARTESIAN_POINT('Ctrl Pts',(72.7756768019202,368.901365879387,45.3984909929256));
#31657=CARTESIAN_POINT('Ctrl Pts',(75.3011501720939,368.689209869834,44.6664337749986));
#31658=CARTESIAN_POINT('Ctrl Pts',(78.2300510740863,368.477053860282,45.3143382390034));
#31659=CARTESIAN_POINT('Ctrl Pts',(80.2090806414343,368.26489785073,47.0423147154921));
#31660=CARTESIAN_POINT('Ctrl Pts',(81.8981967174103,368.083821159273,48.517155159264));
#31661=CARTESIAN_POINT('Ctrl Pts',(82.8953556346456,367.902744467817,50.778800650978));
#31662=CARTESIAN_POINT('Ctrl Pts',(82.9154483188492,367.72166777636,53.0285118833292));
#31663=CARTESIAN_POINT('Origin',(74.9879498948689,255.,53.0228109606356));
#31664=CARTESIAN_POINT('',(82.9101891893477,362.278332223638,53.0206763621601));
#31665=CARTESIAN_POINT('',(82.9152412871326,363.721667776361,53.0213275785589));
#31666=CARTESIAN_POINT('',(82.9129498948689,255.,53.0228109606356));
#31667=CARTESIAN_POINT('Ctrl Pts',(82.9036741822449,362.278332223638,53.0156389091875));
#31668=CARTESIAN_POINT('Ctrl Pts',(82.9096131525181,362.356069364656,52.0448043091272));
#31669=CARTESIAN_POINT('Ctrl Pts',(82.7445708386648,362.433806505673,51.0762468411838));
#31670=CARTESIAN_POINT('Ctrl Pts',(82.3994985579666,362.511543646691,50.1775538500318));
#31671=CARTESIAN_POINT('Ctrl Pts',(81.4577459141023,362.723699656244,47.7248894438173));
#31672=CARTESIAN_POINT('Ctrl Pts',(79.1750872235282,362.935855665796,45.7925922910192));
#31673=CARTESIAN_POINT('Ctrl Pts',(76.6000313647351,363.148011675349,45.2531386515664));
#31674=CARTESIAN_POINT('Ctrl Pts',(75.3125034353385,363.254089680125,44.98341183184));
#31675=CARTESIAN_POINT('Ctrl Pts',(73.9518762138872,363.360167684901,45.0618958904499));
#31676=CARTESIAN_POINT('Ctrl Pts',(72.6845498691734,363.466245689677,45.4472341432798));
#31677=CARTESIAN_POINT('Ctrl Pts',(71.4172235244595,363.572323694453,45.8325723961097));
#31678=CARTESIAN_POINT('Ctrl Pts',(70.243198056483,363.678401699229,46.5247648431596));
#31679=CARTESIAN_POINT('Ctrl Pts',(69.323731138859,363.784479704005,47.4655418165443));
#31680=CARTESIAN_POINT('Ctrl Pts',(67.484797303611,363.996635713558,49.3470957633138));
#31681=CARTESIAN_POINT('Ctrl Pts',(66.6640976697729,364.20879172311,52.2229878154227));
#31682=CARTESIAN_POINT('Ctrl Pts',(67.2470143817554,364.420947732662,54.7847584606265));
#31683=CARTESIAN_POINT('Ctrl Pts',(67.8299310937379,364.633103742214,57.3465291058304));
#31684=CARTESIAN_POINT('Ctrl Pts',(69.816464151541,364.845259751767,59.5941783441292));
#31685=CARTESIAN_POINT('Ctrl Pts',(72.2890450298562,365.057415761319,60.4887549556984));
#31686=CARTESIAN_POINT('Ctrl Pts',(74.7616259081713,365.269571770872,61.3833315672676));
#31687=CARTESIAN_POINT('Ctrl Pts',(77.7202546069985,365.481727780424,60.9248355521071));
#31688=CARTESIAN_POINT('Ctrl Pts',(79.8086744168695,365.693883789976,59.3281387771497));
#31689=CARTESIAN_POINT('Ctrl Pts',(81.7264041876525,365.88869993453,57.8619426963731));
#31690=CARTESIAN_POINT('Ctrl Pts',(82.9103592685377,366.083516079084,55.435996697892));
#31691=CARTESIAN_POINT('Ctrl Pts',(82.9246351989638,366.278332223638,53.0200841918108));
#31692=CARTESIAN_POINT('Ctrl Pts',(82.9129498948689,367.721667776361,53.0228109606493));
#31693=CARTESIAN_POINT('Ctrl Pts',(82.9129498948651,367.544571204362,55.2274084205591));
#31694=CARTESIAN_POINT('Ctrl Pts',(81.9432795991031,367.367474632363,57.4147653849936));
#31695=CARTESIAN_POINT('Ctrl Pts',(80.3096882702442,367.190378060364,58.8951806411017));
#31696=CARTESIAN_POINT('Ctrl Pts',(78.6760969413853,367.013281488366,60.3755958972098));
#31697=CARTESIAN_POINT('Ctrl Pts',(76.4041347530308,366.836184916367,61.1259150206705));
#31698=CARTESIAN_POINT('Ctrl Pts',(74.2101800112086,366.659088344368,60.9095529374008));
#31699=CARTESIAN_POINT('Ctrl Pts',(72.0162252693864,366.481991772369,60.6931908541312));
#31700=CARTESIAN_POINT('Ctrl Pts',(69.934592507687,366.304895200371,59.5135315737612));
#31701=CARTESIAN_POINT('Ctrl Pts',(68.6216467656528,366.127798628372,57.742536531782));
#31702=CARTESIAN_POINT('Ctrl Pts',(67.3087010236187,365.950702056373,55.9715414898028));
#31703=CARTESIAN_POINT('Ctrl Pts',(66.7849774198229,365.773605484375,53.6369099216168));
#31704=CARTESIAN_POINT('Ctrl Pts',(67.2156126057631,365.596508912376,51.4747805783834));
#31705=CARTESIAN_POINT('Ctrl Pts',(67.6462477917034,365.419412340377,49.31265123515));
#31706=CARTESIAN_POINT('Ctrl Pts',(69.024506420806,365.242315768378,47.3568408855384));
#31707=CARTESIAN_POINT('Ctrl Pts',(70.9158061804577,365.06521919638,46.2240411771247));
#31708=CARTESIAN_POINT('Ctrl Pts',(72.8071059401093,364.888122624381,45.091241468711));
#31709=CARTESIAN_POINT('Ctrl Pts',(75.1818659698234,364.711026052382,44.7991699473061));
#31710=CARTESIAN_POINT('Ctrl Pts',(77.2912945088789,364.533929480384,45.4399204438794));
#31711=CARTESIAN_POINT('Ctrl Pts',(79.4007230479344,364.356832908385,46.0806709404526));
#31712=CARTESIAN_POINT('Ctrl Pts',(81.2118275942163,364.179736336386,47.6442218014036));
#31713=CARTESIAN_POINT('Ctrl Pts',(82.1535440633153,364.002639764387,49.6375657386278));
#31714=CARTESIAN_POINT('Ctrl Pts',(82.6515697929949,363.908982435045,50.6917435101901));
#31715=CARTESIAN_POINT('Ctrl Pts',(82.9129498948709,363.815325105703,51.8569119935516));
#31716=CARTESIAN_POINT('Ctrl Pts',(82.9129498948689,363.721667776361,53.0228109606491));
#31717=CARTESIAN_POINT('Origin',(74.9879498948689,255.,53.0228109606356));
#31718=CARTESIAN_POINT('',(82.910167501573,358.278332223638,53.0247970047267));
#31719=CARTESIAN_POINT('',(82.9091777645014,359.721667776361,53.0220250865809));
#31720=CARTESIAN_POINT('',(82.9129498948689,255.,53.0228109606356));
#31721=CARTESIAN_POINT('Ctrl Pts',(82.9129498948689,358.278332223638,53.0228109606355));
#31722=CARTESIAN_POINT('Ctrl Pts',(82.9129498948689,358.455428795637,50.8182135007257));
#31723=CARTESIAN_POINT('Ctrl Pts',(81.9432795991106,358.632525367635,48.6308565362894));
#31724=CARTESIAN_POINT('Ctrl Pts',(80.3096882702542,358.809621939634,47.1504412801785));
#31725=CARTESIAN_POINT('Ctrl Pts',(78.6760969413977,358.986718511633,45.6700260240675));
#31726=CARTESIAN_POINT('Ctrl Pts',(76.4041347530443,359.163815083631,44.919706900603));
#31727=CARTESIAN_POINT('Ctrl Pts',(74.2101800112218,359.34091165563,45.136068983869));
#31728=CARTESIAN_POINT('Ctrl Pts',(72.0162252693992,359.518008227629,45.352431067135));
#31729=CARTESIAN_POINT('Ctrl Pts',(69.9345925076977,359.695104799628,46.5320903475016));
#31730=CARTESIAN_POINT('Ctrl Pts',(68.6216467656606,359.872201371626,48.3030853894787));
#31731=CARTESIAN_POINT('Ctrl Pts',(67.3087010236235,360.049297943625,50.0740804314559));
#31732=CARTESIAN_POINT('Ctrl Pts',(66.7849774198239,360.226394515624,52.4087119996411));
#31733=CARTESIAN_POINT('Ctrl Pts',(67.2156126057607,360.403491087623,54.5708413428753));
#31734=CARTESIAN_POINT('Ctrl Pts',(67.6462477916974,360.580587659621,56.7329706861094));
#31735=CARTESIAN_POINT('Ctrl Pts',(69.0245064207969,360.75768423162,58.6887810357233));
#31736=CARTESIAN_POINT('Ctrl Pts',(70.9158061804469,360.934780803619,59.82158074414));
#31737=CARTESIAN_POINT('Ctrl Pts',(72.8071059400968,361.111877375618,60.9543804525568));
#31738=CARTESIAN_POINT('Ctrl Pts',(75.1818659698106,361.288973947616,61.2464519739654));
#31739=CARTESIAN_POINT('Ctrl Pts',(77.2912945088671,361.466070519615,60.6057014773953));
#31740=CARTESIAN_POINT('Ctrl Pts',(79.4007230479237,361.643167091614,59.9649509808253));
#31741=CARTESIAN_POINT('Ctrl Pts',(81.211827594208,361.820263663612,58.4014001198771));
#31742=CARTESIAN_POINT('Ctrl Pts',(82.1535440633102,361.997360235611,56.4080561826543));
#31743=CARTESIAN_POINT('Ctrl Pts',(82.6515697929911,362.091017564953,55.3538784110932));
#31744=CARTESIAN_POINT('Ctrl Pts',(82.9129498948689,362.184674894296,54.1887099277327));
#31745=CARTESIAN_POINT('Ctrl Pts',(82.9129498948689,362.278332223638,53.0228109606358));
#31746=CARTESIAN_POINT('Ctrl Pts',(82.9208104299352,363.721667776361,53.0177222740361));
#31747=CARTESIAN_POINT('Ctrl Pts',(82.9006493036487,363.538829724732,55.2853910421037));
#31748=CARTESIAN_POINT('Ctrl Pts',(81.8727588800135,363.355991673103,57.5656941132477));
#31749=CARTESIAN_POINT('Ctrl Pts',(80.1547284126926,363.173153621474,59.0453531318087));
#31750=CARTESIAN_POINT('Ctrl Pts',(79.1579706672753,363.067075616698,59.9038138025483));
#31751=CARTESIAN_POINT('Ctrl Pts',(77.9289099623936,362.960997611922,60.4927755728916));
#31752=CARTESIAN_POINT('Ctrl Pts',(76.6332069362866,362.854919607146,60.7680123822706));
#31753=CARTESIAN_POINT('Ctrl Pts',(75.3375039101796,362.748841602369,61.0432491916497));
#31754=CARTESIAN_POINT('Ctrl Pts',(73.9751585628473,362.642763597593,61.0047610400644));
#31755=CARTESIAN_POINT('Ctrl Pts',(72.7155046793147,362.536685592817,60.6256135490307));
#31756=CARTESIAN_POINT('Ctrl Pts',(70.1961969122495,362.324529583265,59.8673185669634));
#31757=CARTESIAN_POINT('Ctrl Pts',(68.0876550003827,362.112373573713,57.7463862271029));
#31758=CARTESIAN_POINT('Ctrl Pts',(67.3597044157122,361.90021756416,55.2219954732745));
#31759=CARTESIAN_POINT('Ctrl Pts',(66.6317538310416,361.688061554608,52.697604719446));
#31760=CARTESIAN_POINT('Ctrl Pts',(67.2843945735672,361.475905545056,49.7697555516497));
#31761=CARTESIAN_POINT('Ctrl Pts',(69.0165499320151,361.263749535503,47.7914832427962));
#31762=CARTESIAN_POINT('Ctrl Pts',(70.748705290463,361.051593525951,45.8132109339427));
#31763=CARTESIAN_POINT('Ctrl Pts',(73.5603752648332,360.839437516399,44.7845154840321));
#31764=CARTESIAN_POINT('Ctrl Pts',(76.1604012109173,360.627281506846,45.1728490688669));
#31765=CARTESIAN_POINT('Ctrl Pts',(78.7604271570015,360.415125497294,45.5611826537016));
#31766=CARTESIAN_POINT('Ctrl Pts',(81.1488090747995,360.202969487742,47.3665452732815));
#31767=CARTESIAN_POINT('Ctrl Pts',(82.22732492823,359.99081347819,49.7646126342361));
#31768=CARTESIAN_POINT('Ctrl Pts',(82.6834011068206,359.901098244247,50.7786926725667));
#31769=CARTESIAN_POINT('Ctrl Pts',(82.9052440041322,359.811383010304,51.8987615445487));
#31770=CARTESIAN_POINT('Ctrl Pts',(82.9009763088175,359.721667776361,53.0203164204654));
#31771=CARTESIAN_POINT('Origin',(74.9879498948689,255.,53.0228109606356));
#31772=CARTESIAN_POINT('',(82.9154091900529,354.278332223638,53.0231896391828));
#31773=CARTESIAN_POINT('',(82.9122147864747,355.721667776361,53.0240094724492));
#31774=CARTESIAN_POINT('',(82.9129498948689,255.,53.0228109606356));
#31775=CARTESIAN_POINT('Ctrl Pts',(82.9228124950414,354.278332223638,53.0243295888637));
#31776=CARTESIAN_POINT('Ctrl Pts',(82.9198720468438,354.370785911918,51.8773028605082));
#31777=CARTESIAN_POINT('Ctrl Pts',(82.6535218078163,354.463239600199,50.7278473767095));
#31778=CARTESIAN_POINT('Ctrl Pts',(82.1663005056112,354.55569328848,49.6812098020159));
#31779=CARTESIAN_POINT('Ctrl Pts',(81.6072804753287,354.661771293256,48.4803358540751));
#31780=CARTESIAN_POINT('Ctrl Pts',(80.757496184371,354.767849298032,47.4148158673777));
#31781=CARTESIAN_POINT('Ctrl Pts',(79.6972259522975,354.873927302808,46.6361582011118));
#31782=CARTESIAN_POINT('Ctrl Pts',(77.5766854881505,355.086083312361,45.0788428685798));
#31783=CARTESIAN_POINT('Ctrl Pts',(74.6142012595406,355.298239321913,44.6689768177737));
#31784=CARTESIAN_POINT('Ctrl Pts',(72.1593083598743,355.510395331465,45.6049050110154));
#31785=CARTESIAN_POINT('Ctrl Pts',(69.7044154602081,355.722551341017,46.5408332042571));
#31786=CARTESIAN_POINT('Ctrl Pts',(67.7571138894853,355.93470735057,48.8225556415467));
#31787=CARTESIAN_POINT('Ctrl Pts',(67.2176183240624,356.146863360122,51.3960489966313));
#31788=CARTESIAN_POINT('Ctrl Pts',(66.6781227586394,356.359019369674,53.969542351716));
#31789=CARTESIAN_POINT('Ctrl Pts',(67.5464331985163,356.571175379227,56.8348066245959));
#31790=CARTESIAN_POINT('Ctrl Pts',(69.4198621488847,356.783331388779,58.6790413876732));
#31791=CARTESIAN_POINT('Ctrl Pts',(71.2932910992532,356.995487398331,60.5232761507505));
#31792=CARTESIAN_POINT('Ctrl Pts',(74.1718385601131,357.207643407883,61.3464814040251));
#31793=CARTESIAN_POINT('Ctrl Pts',(76.7365419224931,357.419799417436,60.7666364447703));
#31794=CARTESIAN_POINT('Ctrl Pts',(79.301245284873,357.631955426988,60.1867914855154));
#31795=CARTESIAN_POINT('Ctrl Pts',(81.5521045487729,357.844111436541,58.2038963137311));
#31796=CARTESIAN_POINT('Ctrl Pts',(82.4493639735543,358.056267446093,55.7346077003086));
#31797=CARTESIAN_POINT('Ctrl Pts',(82.7624193126962,358.130289038608,54.8730687039335));
#31798=CARTESIAN_POINT('Ctrl Pts',(82.9106976993204,358.204310631123,53.9523198681941));
#31799=CARTESIAN_POINT('Ctrl Pts',(82.9035224954183,358.278332223638,53.029540142668));
#31800=CARTESIAN_POINT('Ctrl Pts',(82.9129498948689,359.721667776361,53.0228109606489));
#31801=CARTESIAN_POINT('Ctrl Pts',(82.9129498948652,359.544571204362,55.2274084205588));
#31802=CARTESIAN_POINT('Ctrl Pts',(81.9432795991032,359.367474632363,57.4147653849934));
#31803=CARTESIAN_POINT('Ctrl Pts',(80.3096882702443,359.190378060364,58.8951806411016));
#31804=CARTESIAN_POINT('Ctrl Pts',(78.6760969413853,359.013281488366,60.3755958972098));
#31805=CARTESIAN_POINT('Ctrl Pts',(76.4041347530307,358.836184916367,61.1259150206705));
#31806=CARTESIAN_POINT('Ctrl Pts',(74.2101800112085,358.659088344368,60.9095529374008));
#31807=CARTESIAN_POINT('Ctrl Pts',(72.0162252693863,358.481991772369,60.6931908541311));
#31808=CARTESIAN_POINT('Ctrl Pts',(69.9345925076867,358.304895200371,59.5135315737611));
#31809=CARTESIAN_POINT('Ctrl Pts',(68.6216467656526,358.127798628372,57.7425365317817));
#31810=CARTESIAN_POINT('Ctrl Pts',(67.3087010236185,357.950702056373,55.9715414898024));
#31811=CARTESIAN_POINT('Ctrl Pts',(66.7849774198228,357.773605484375,53.6369099216163));
#31812=CARTESIAN_POINT('Ctrl Pts',(67.2156126057632,357.596508912376,51.4747805783828));
#31813=CARTESIAN_POINT('Ctrl Pts',(67.6462477917036,357.419412340377,49.3126512351494));
#31814=CARTESIAN_POINT('Ctrl Pts',(69.0245064208065,357.242315768378,47.3568408855378));
#31815=CARTESIAN_POINT('Ctrl Pts',(70.9158061804583,357.06521919638,46.2240411771243));
#31816=CARTESIAN_POINT('Ctrl Pts',(72.8071059401102,356.888122624381,45.0912414687107));
#31817=CARTESIAN_POINT('Ctrl Pts',(75.1818659698244,356.711026052382,44.7991699473061));
#31818=CARTESIAN_POINT('Ctrl Pts',(77.2912945088799,356.533929480383,45.4399204438797));
#31819=CARTESIAN_POINT('Ctrl Pts',(79.4007230479353,356.356832908385,46.0806709404532));
#31820=CARTESIAN_POINT('Ctrl Pts',(81.2118275942171,356.179736336386,47.6442218014045));
#31821=CARTESIAN_POINT('Ctrl Pts',(82.1535440633159,356.002639764387,49.6375657386289));
#31822=CARTESIAN_POINT('Ctrl Pts',(82.6515697929952,355.908982435045,50.6917435101911));
#31823=CARTESIAN_POINT('Ctrl Pts',(82.912949894871,355.815325105703,51.8569119935523));
#31824=CARTESIAN_POINT('Ctrl Pts',(82.9129498948689,355.721667776361,53.0228109606495));
#31825=CARTESIAN_POINT('Origin',(74.9879498948689,255.,53.0228109606356));
#31826=CARTESIAN_POINT('',(82.9131455474441,350.278332223638,53.0224568952625));
#31827=CARTESIAN_POINT('',(82.9249635206133,351.72166777636,53.0231874323186));
#31828=CARTESIAN_POINT('',(82.9129498948689,255.,53.0228109606356));
#31829=CARTESIAN_POINT('Ctrl Pts',(82.9129498948689,350.278332223638,53.0228109606361));
#31830=CARTESIAN_POINT('Ctrl Pts',(82.912949894869,350.455428795636,50.8182135007263));
#31831=CARTESIAN_POINT('Ctrl Pts',(81.943279599111,350.632525367635,48.63085653629));
#31832=CARTESIAN_POINT('Ctrl Pts',(80.3096882702547,350.809621939634,47.150441280179));
#31833=CARTESIAN_POINT('Ctrl Pts',(78.6760969413985,350.986718511633,45.6700260240679));
#31834=CARTESIAN_POINT('Ctrl Pts',(76.4041347530453,351.163815083631,44.9197069006032));
#31835=CARTESIAN_POINT('Ctrl Pts',(74.2101800112228,351.34091165563,45.1360689838689));
#31836=CARTESIAN_POINT('Ctrl Pts',(72.0162252694002,351.518008227629,45.3524310671346));
#31837=CARTESIAN_POINT('Ctrl Pts',(69.9345925076986,351.695104799628,46.5320903475008));
#31838=CARTESIAN_POINT('Ctrl Pts',(68.6216467656613,351.872201371626,48.3030853894777));
#31839=CARTESIAN_POINT('Ctrl Pts',(67.308701023624,352.049297943625,50.0740804314546));
#31840=CARTESIAN_POINT('Ctrl Pts',(66.784977419824,352.226394515624,52.4087119996397));
#31841=CARTESIAN_POINT('Ctrl Pts',(67.2156126057604,352.403491087622,54.5708413428738));
#31842=CARTESIAN_POINT('Ctrl Pts',(67.6462477916967,352.580587659621,56.732970686108));
#31843=CARTESIAN_POINT('Ctrl Pts',(69.0245064207958,352.75768423162,58.688781035722));
#31844=CARTESIAN_POINT('Ctrl Pts',(70.9158061804454,352.934780803619,59.8215807441392));
#31845=CARTESIAN_POINT('Ctrl Pts',(72.8071059400951,353.111877375617,60.9543804525563));
#31846=CARTESIAN_POINT('Ctrl Pts',(75.1818659698087,353.288973947616,61.2464519739654));
#31847=CARTESIAN_POINT('Ctrl Pts',(77.2912945088653,353.466070519615,60.6057014773959));
#31848=CARTESIAN_POINT('Ctrl Pts',(79.4007230479219,353.643167091614,59.9649509808264));
#31849=CARTESIAN_POINT('Ctrl Pts',(81.2118275942066,353.820263663612,58.4014001198787));
#31850=CARTESIAN_POINT('Ctrl Pts',(82.1535440633093,353.997360235611,56.4080561826562));
#31851=CARTESIAN_POINT('Ctrl Pts',(82.6515697929907,354.091017564953,55.3538784110948));
#31852=CARTESIAN_POINT('Ctrl Pts',(82.9129498948688,354.184674894296,54.1887099277338));
#31853=CARTESIAN_POINT('Ctrl Pts',(82.9129498948689,354.278332223638,53.0228109606363));
#31854=CARTESIAN_POINT('Ctrl Pts',(82.9091135838053,355.721667776361,53.0290656354458));
#31855=CARTESIAN_POINT('Ctrl Pts',(82.9157961825277,355.659624276771,53.8021586410643));
#31856=CARTESIAN_POINT('Ctrl Pts',(82.8118813088041,355.597580777181,54.5736419934824));
#31857=CARTESIAN_POINT('Ctrl Pts',(82.5901503636487,355.535537277591,55.3099391250131));
#31858=CARTESIAN_POINT('Ctrl Pts',(81.8319476054334,355.323381268038,57.8276865490433));
#31859=CARTESIAN_POINT('Ctrl Pts',(79.6961464125835,355.111225258486,59.9340089253166));
#31860=CARTESIAN_POINT('Ctrl Pts',(77.1700348613008,354.899069248934,60.6559654075322));
#31861=CARTESIAN_POINT('Ctrl Pts',(74.6439233100181,354.686913239382,61.3779218897477));
#31862=CARTESIAN_POINT('Ctrl Pts',(71.7275014003028,354.474757229829,60.7155124779055));
#31863=CARTESIAN_POINT('Ctrl Pts',(69.7483232334138,354.262601220277,58.9820833075226));
#31864=CARTESIAN_POINT('Ctrl Pts',(68.7587341499693,354.156523215501,58.1153687223312));
#31865=CARTESIAN_POINT('Ctrl Pts',(68.0034560022314,354.050445210725,56.9808991975047));
#31866=CARTESIAN_POINT('Ctrl Pts',(67.5494784950457,353.944367205949,55.7365093646672));
#31867=CARTESIAN_POINT('Ctrl Pts',(67.0955009878599,353.838289201172,54.4921195318297));
#31868=CARTESIAN_POINT('Ctrl Pts',(66.9428241212262,353.732211196396,53.1378093909812));
#31869=CARTESIAN_POINT('Ctrl Pts',(67.1418307132696,353.62613319162,51.8374720875944));
#31870=CARTESIAN_POINT('Ctrl Pts',(67.5398438973563,353.413977182067,49.2367974808209));
#31871=CARTESIAN_POINT('Ctrl Pts',(69.3445909161509,353.201821172515,46.8520142238943));
#31872=CARTESIAN_POINT('Ctrl Pts',(71.7421614310037,352.989665162963,45.7777161469878));
#31873=CARTESIAN_POINT('Ctrl Pts',(74.1397319458566,352.777509153411,44.7034180700812));
#31874=CARTESIAN_POINT('Ctrl Pts',(77.1301259567676,352.565353143858,44.9396051731948));
#31875=CARTESIAN_POINT('Ctrl Pts',(79.3314781915037,352.353197134306,46.3776496274446));
#31876=CARTESIAN_POINT('Ctrl Pts',(81.5157490438013,352.142687348324,47.8045355824324));
#31877=CARTESIAN_POINT('Ctrl Pts',(82.9231757438946,351.932177562342,50.4146996390436));
#31878=CARTESIAN_POINT('Ctrl Pts',(82.9249635206133,351.72166777636,53.0231874323186));
#31879=CARTESIAN_POINT('Origin',(74.9879498948689,255.,53.0228109606356));
#31880=CARTESIAN_POINT('',(82.9073270357724,346.278332223638,53.0223005851992));
#31881=CARTESIAN_POINT('',(82.9121137244291,347.721667776361,53.0207950825717));
#31882=CARTESIAN_POINT('',(82.9129498948689,255.,53.0228109606356));
#31883=CARTESIAN_POINT('Ctrl Pts',(82.8972748771451,346.278332223638,53.0213881712888));
#31884=CARTESIAN_POINT('Ctrl Pts',(82.8983129557911,346.385502459181,51.6828751929879));
#31885=CARTESIAN_POINT('Ctrl Pts',(82.5784150468752,346.492672694724,50.3448798377769));
#31886=CARTESIAN_POINT('Ctrl Pts',(81.9366274606094,346.599842930268,49.1832248243079));
#31887=CARTESIAN_POINT('Ctrl Pts',(80.6661339080663,346.81199893982,46.8835929266593));
#31888=CARTESIAN_POINT('Ctrl Pts',(78.1341923471884,347.024154949372,45.275018209567));
#31889=CARTESIAN_POINT('Ctrl Pts',(75.5105072571905,347.236310958925,45.1012365583537));
#31890=CARTESIAN_POINT('Ctrl Pts',(72.8868221671925,347.448466968477,44.9274549071403));
#31891=CARTESIAN_POINT('Ctrl Pts',(70.1713935480745,347.660622978029,46.1884663218059));
#31892=CARTESIAN_POINT('Ctrl Pts',(68.6076916836926,347.872778987582,48.301704210154));
#31893=CARTESIAN_POINT('Ctrl Pts',(67.0439898193109,348.084934997134,50.4149420985021));
#31894=CARTESIAN_POINT('Ctrl Pts',(66.6320147096651,348.297091006686,53.3804064605326));
#31895=CARTESIAN_POINT('Ctrl Pts',(67.5653121245716,348.509247016239,55.8386333518315));
#31896=CARTESIAN_POINT('Ctrl Pts',(68.4986095394781,348.721403025791,58.2968602431304));
#31897=CARTESIAN_POINT('Ctrl Pts',(70.7771794789368,348.933559035343,60.2478496636975));
#31898=CARTESIAN_POINT('Ctrl Pts',(73.3477887194659,349.145715044896,60.7904626604485));
#31899=CARTESIAN_POINT('Ctrl Pts',(75.918397959995,349.357871054448,61.3330756571995));
#31900=CARTESIAN_POINT('Ctrl Pts',(78.7810465015946,349.570027064,60.4673122301343));
#31901=CARTESIAN_POINT('Ctrl Pts',(80.633488508501,349.782183073552,58.5990559532621));
#31902=CARTESIAN_POINT('Ctrl Pts',(81.5597095119541,349.888261078329,57.664927814826));
#31903=CARTESIAN_POINT('Ctrl Pts',(82.233378881734,349.994339083105,56.4801764639381));
#31904=CARTESIAN_POINT('Ctrl Pts',(82.5987666386957,350.100417087881,55.2069547942504));
#31905=CARTESIAN_POINT('Ctrl Pts',(82.8030440240684,350.159722133134,54.4951345738729));
#31906=CARTESIAN_POINT('Ctrl Pts',(82.9109650860172,350.219027178386,53.755662121584));
#31907=CARTESIAN_POINT('Ctrl Pts',(82.9157605881844,350.278332223638,53.0177245508215));
#31908=CARTESIAN_POINT('Ctrl Pts',(82.9249635206133,351.72166777636,53.0231874323186));
#31909=CARTESIAN_POINT('Ctrl Pts',(82.9249775013419,351.72002155279,53.0435862658865));
#31910=CARTESIAN_POINT('Ctrl Pts',(82.924905520008,351.718375329219,53.0639849969422));
#31911=CARTESIAN_POINT('Ctrl Pts',(82.9247472758945,351.716729105649,53.0843830587884));
#31912=CARTESIAN_POINT('Ctrl Pts',(82.9043536669879,351.504573096097,55.7131702304965));
#31913=CARTESIAN_POINT('Ctrl Pts',(81.4512559906136,351.292417086545,58.3308427685267));
#31914=CARTESIAN_POINT('Ctrl Pts',(79.2278579260863,351.080261076992,59.7345608885324));
#31915=CARTESIAN_POINT('Ctrl Pts',(77.004459861559,350.86810506744,61.1382790085381));
#31916=CARTESIAN_POINT('Ctrl Pts',(74.0107614088787,350.655949057887,61.3280427105194));
#31917=CARTESIAN_POINT('Ctrl Pts',(71.6301468441837,350.443793048335,60.2166764225214));
#31918=CARTESIAN_POINT('Ctrl Pts',(69.2495322794886,350.231637038783,59.1053101345234));
#31919=CARTESIAN_POINT('Ctrl Pts',(67.4820016027788,350.019481029231,56.6928138565462));
#31920=CARTESIAN_POINT('Ctrl Pts',(67.1243849295486,349.807325019679,54.0862772233772));
#31921=CARTESIAN_POINT('Ctrl Pts',(66.9455765929335,349.701247014902,52.7830089067927));
#31922=CARTESIAN_POINT('Ctrl Pts',(67.1192467571882,349.595169010126,51.4312305014103));
#31923=CARTESIAN_POINT('Ctrl Pts',(67.5924759203216,349.48909100535,50.1940337538151));
#31924=CARTESIAN_POINT('Ctrl Pts',(68.065705083455,349.383013000574,48.95683700622));
#31925=CARTESIAN_POINT('Ctrl Pts',(68.8384932454669,349.276934995797,47.8342219164121));
#31926=CARTESIAN_POINT('Ctrl Pts',(69.8414100122834,349.170856991021,46.9829647959755));
#31927=CARTESIAN_POINT('Ctrl Pts',(71.8472435459166,348.958700981469,45.2804505551021));
#31928=CARTESIAN_POINT('Ctrl Pts',(74.7735914987686,348.746544971917,44.663368191714));
#31929=CARTESIAN_POINT('Ctrl Pts',(77.2881980920006,348.534388962364,45.4244295644106));
#31930=CARTESIAN_POINT('Ctrl Pts',(79.8028046852326,348.322232952812,46.1854909371071));
#31931=CARTESIAN_POINT('Ctrl Pts',(81.9056699188448,348.11007694326,48.3246960458882));
#31932=CARTESIAN_POINT('Ctrl Pts',(82.6247194016904,347.897920933707,50.8539036994817));
#31933=CARTESIAN_POINT('Ctrl Pts',(82.823841330733,347.839169881258,51.5543015426731));
#31934=CARTESIAN_POINT('Ctrl Pts',(82.9168428557268,347.78041882881,52.2846074336755));
#31935=CARTESIAN_POINT('Ctrl Pts',(82.910294861139,347.721667776361,53.0164100834644));
#31936=CARTESIAN_POINT('Origin',(74.9879498948689,255.,53.0228109606356));
#31937=CARTESIAN_POINT('',(82.9129498948689,342.278332223638,53.0228109606362));
#31938=CARTESIAN_POINT('',(82.9129498948689,343.721667776361,53.0228109606494));
#31939=CARTESIAN_POINT('',(82.9129498948689,255.,53.0228109606356));
#31940=CARTESIAN_POINT('Ctrl Pts',(82.9129498948689,342.278332223638,53.0228109606367));
#31941=CARTESIAN_POINT('Ctrl Pts',(82.9129498948692,342.455428795636,50.8182135007268));
#31942=CARTESIAN_POINT('Ctrl Pts',(81.9432795991113,342.632525367635,48.6308565362905));
#31943=CARTESIAN_POINT('Ctrl Pts',(80.3096882702551,342.809621939634,47.1504412801793));
#31944=CARTESIAN_POINT('Ctrl Pts',(78.6760969413989,342.986718511633,45.6700260240681));
#31945=CARTESIAN_POINT('Ctrl Pts',(76.4041347530457,343.163815083631,44.9197069006033));
#31946=CARTESIAN_POINT('Ctrl Pts',(74.2101800112231,343.34091165563,45.1360689838689));
#31947=CARTESIAN_POINT('Ctrl Pts',(72.0162252694005,343.518008227629,45.3524310671345));
#31948=CARTESIAN_POINT('Ctrl Pts',(69.9345925076989,343.695104799628,46.5320903475007));
#31949=CARTESIAN_POINT('Ctrl Pts',(68.6216467656614,343.872201371626,48.3030853894775));
#31950=CARTESIAN_POINT('Ctrl Pts',(67.308701023624,344.049297943625,50.0740804314544));
#31951=CARTESIAN_POINT('Ctrl Pts',(66.784977419824,344.226394515624,52.4087119996395));
#31952=CARTESIAN_POINT('Ctrl Pts',(67.2156126057603,344.403491087622,54.5708413428737));
#31953=CARTESIAN_POINT('Ctrl Pts',(67.6462477916967,344.580587659621,56.7329706861079));
#31954=CARTESIAN_POINT('Ctrl Pts',(69.0245064207958,344.75768423162,58.688781035722));
#31955=CARTESIAN_POINT('Ctrl Pts',(70.9158061804454,344.934780803619,59.8215807441392));
#31956=CARTESIAN_POINT('Ctrl Pts',(72.8071059400951,345.111877375617,60.9543804525563));
#31957=CARTESIAN_POINT('Ctrl Pts',(75.1818659698087,345.288973947616,61.2464519739654));
#31958=CARTESIAN_POINT('Ctrl Pts',(77.2912945088654,345.466070519615,60.6057014773959));
#31959=CARTESIAN_POINT('Ctrl Pts',(79.4007230479221,345.643167091614,59.9649509808263));
#31960=CARTESIAN_POINT('Ctrl Pts',(81.2118275942068,345.820263663612,58.4014001198785));
#31961=CARTESIAN_POINT('Ctrl Pts',(82.1535440633093,345.997360235611,56.408056182656));
#31962=CARTESIAN_POINT('Ctrl Pts',(82.6515697929908,346.091017564953,55.3538784110945));
#31963=CARTESIAN_POINT('Ctrl Pts',(82.9129498948689,346.184674894296,54.1887099277335));
#31964=CARTESIAN_POINT('Ctrl Pts',(82.9129498948689,346.278332223638,53.0228109606359));
#31965=CARTESIAN_POINT('Ctrl Pts',(82.9129498948689,347.721667776361,53.0228109606492));
#31966=CARTESIAN_POINT('Ctrl Pts',(82.9129498948651,347.544571204362,55.227408420559));
#31967=CARTESIAN_POINT('Ctrl Pts',(81.9432795991031,347.367474632363,57.4147653849935));
#31968=CARTESIAN_POINT('Ctrl Pts',(80.3096882702442,347.190378060364,58.8951806411017));
#31969=CARTESIAN_POINT('Ctrl Pts',(78.6760969413853,347.013281488366,60.3755958972098));
#31970=CARTESIAN_POINT('Ctrl Pts',(76.4041347530308,346.836184916367,61.1259150206704));
#31971=CARTESIAN_POINT('Ctrl Pts',(74.2101800112087,346.659088344368,60.9095529374008));
#31972=CARTESIAN_POINT('Ctrl Pts',(72.0162252693865,346.481991772369,60.6931908541312));
#31973=CARTESIAN_POINT('Ctrl Pts',(69.934592507687,346.304895200371,59.5135315737613));
#31974=CARTESIAN_POINT('Ctrl Pts',(68.6216467656529,346.127798628372,57.7425365317821));
#31975=CARTESIAN_POINT('Ctrl Pts',(67.3087010236187,345.950702056373,55.9715414898028));
#31976=CARTESIAN_POINT('Ctrl Pts',(66.7849774198229,345.773605484375,53.6369099216168));
#31977=CARTESIAN_POINT('Ctrl Pts',(67.2156126057631,345.596508912376,51.4747805783834));
#31978=CARTESIAN_POINT('Ctrl Pts',(67.6462477917033,345.419412340377,49.31265123515));
#31979=CARTESIAN_POINT('Ctrl Pts',(69.0245064208059,345.242315768378,47.3568408855384));
#31980=CARTESIAN_POINT('Ctrl Pts',(70.9158061804576,345.06521919638,46.2240411771247));
#31981=CARTESIAN_POINT('Ctrl Pts',(72.8071059401093,344.888122624381,45.091241468711));
#31982=CARTESIAN_POINT('Ctrl Pts',(75.1818659698233,344.711026052382,44.7991699473061));
#31983=CARTESIAN_POINT('Ctrl Pts',(77.2912945088788,344.533929480384,45.4399204438793));
#31984=CARTESIAN_POINT('Ctrl Pts',(79.4007230479343,344.356832908385,46.0806709404526));
#31985=CARTESIAN_POINT('Ctrl Pts',(81.2118275942162,344.179736336386,47.6442218014036));
#31986=CARTESIAN_POINT('Ctrl Pts',(82.1535440633153,344.002639764387,49.6375657386277));
#31987=CARTESIAN_POINT('Ctrl Pts',(82.6515697929949,343.908982435045,50.69174351019));
#31988=CARTESIAN_POINT('Ctrl Pts',(82.9129498948709,343.815325105703,51.8569119935515));
#31989=CARTESIAN_POINT('Ctrl Pts',(82.9129498948689,343.721667776361,53.022810960649));
#31990=CARTESIAN_POINT('Origin',(74.9879498948689,255.,53.0228109606356));
#31991=CARTESIAN_POINT('',(82.9170870675938,338.278332223638,53.0212355344904));
#31992=CARTESIAN_POINT('',(82.9129498948689,339.721667776361,53.0228109606494));
#31993=CARTESIAN_POINT('',(82.9129498948689,255.,53.0228109606356));
#31994=CARTESIAN_POINT('Ctrl Pts',(82.9129498948689,338.278332223638,53.0228109606365));
#31995=CARTESIAN_POINT('Ctrl Pts',(82.9129498948692,338.455428795636,50.8182135007266));
#31996=CARTESIAN_POINT('Ctrl Pts',(81.9432795991111,338.632525367635,48.6308565362901));
#31997=CARTESIAN_POINT('Ctrl Pts',(80.3096882702548,338.809621939634,47.150441280179));
#31998=CARTESIAN_POINT('Ctrl Pts',(78.6760969413984,338.986718511633,45.6700260240679));
#31999=CARTESIAN_POINT('Ctrl Pts',(76.4041347530451,339.163815083631,44.9197069006032));
#32000=CARTESIAN_POINT('Ctrl Pts',(74.2101800112225,339.34091165563,45.136068983869));
#32001=CARTESIAN_POINT('Ctrl Pts',(72.0162252693998,339.518008227629,45.3524310671347));
#32002=CARTESIAN_POINT('Ctrl Pts',(69.9345925076982,339.695104799628,46.5320903475011));
#32003=CARTESIAN_POINT('Ctrl Pts',(68.6216467656609,339.872201371626,48.3030853894782));
#32004=CARTESIAN_POINT('Ctrl Pts',(67.3087010236237,340.049297943625,50.0740804314553));
#32005=CARTESIAN_POINT('Ctrl Pts',(66.7849774198239,340.226394515624,52.4087119996405));
#32006=CARTESIAN_POINT('Ctrl Pts',(67.2156126057605,340.403491087623,54.5708413428748));
#32007=CARTESIAN_POINT('Ctrl Pts',(67.6462477916972,340.580587659621,56.732970686109));
#32008=CARTESIAN_POINT('Ctrl Pts',(69.0245064207966,340.75768423162,58.688781035723));
#32009=CARTESIAN_POINT('Ctrl Pts',(70.9158061804466,340.934780803619,59.8215807441398));
#32010=CARTESIAN_POINT('Ctrl Pts',(72.8071059400965,341.111877375617,60.9543804525567));
#32011=CARTESIAN_POINT('Ctrl Pts',(75.1818659698102,341.288973947616,61.2464519739654));
#32012=CARTESIAN_POINT('Ctrl Pts',(77.2912945088669,341.466070519615,60.6057014773954));
#32013=CARTESIAN_POINT('Ctrl Pts',(79.4007230479235,341.643167091614,59.9649509808254));
#32014=CARTESIAN_POINT('Ctrl Pts',(81.2118275942079,341.820263663612,58.4014001198772));
#32015=CARTESIAN_POINT('Ctrl Pts',(82.1535440633101,341.997360235611,56.4080561826544));
#32016=CARTESIAN_POINT('Ctrl Pts',(82.6515697929909,342.091017564953,55.3538784110936));
#32017=CARTESIAN_POINT('Ctrl Pts',(82.9129498948687,342.184674894296,54.1887099277334));
#32018=CARTESIAN_POINT('Ctrl Pts',(82.9129498948689,342.278332223638,53.0228109606367));
#32019=CARTESIAN_POINT('Ctrl Pts',(82.9129498948689,343.721667776361,53.022810960649));
#32020=CARTESIAN_POINT('Ctrl Pts',(82.9129498948652,343.544571204362,55.2274084205589));
#32021=CARTESIAN_POINT('Ctrl Pts',(81.9432795991032,343.367474632363,57.4147653849935));
#32022=CARTESIAN_POINT('Ctrl Pts',(80.3096882702443,343.190378060364,58.8951806411016));
#32023=CARTESIAN_POINT('Ctrl Pts',(78.6760969413854,343.013281488366,60.3755958972098));
#32024=CARTESIAN_POINT('Ctrl Pts',(76.4041347530308,342.836184916367,61.1259150206705));
#32025=CARTESIAN_POINT('Ctrl Pts',(74.2101800112086,342.659088344368,60.9095529374008));
#32026=CARTESIAN_POINT('Ctrl Pts',(72.0162252693864,342.481991772369,60.6931908541312));
#32027=CARTESIAN_POINT('Ctrl Pts',(69.9345925076869,342.304895200371,59.5135315737612));
#32028=CARTESIAN_POINT('Ctrl Pts',(68.6216467656528,342.127798628372,57.7425365317819));
#32029=CARTESIAN_POINT('Ctrl Pts',(67.3087010236186,341.950702056373,55.9715414898026));
#32030=CARTESIAN_POINT('Ctrl Pts',(66.7849774198229,341.773605484375,53.6369099216166));
#32031=CARTESIAN_POINT('Ctrl Pts',(67.2156126057632,341.596508912376,51.4747805783831));
#32032=CARTESIAN_POINT('Ctrl Pts',(67.6462477917035,341.419412340377,49.3126512351497));
#32033=CARTESIAN_POINT('Ctrl Pts',(69.0245064208062,341.242315768378,47.3568408855382));
#32034=CARTESIAN_POINT('Ctrl Pts',(70.9158061804579,341.06521919638,46.2240411771245));
#32035=CARTESIAN_POINT('Ctrl Pts',(72.8071059401097,340.888122624381,45.0912414687108));
#32036=CARTESIAN_POINT('Ctrl Pts',(75.1818659698238,340.711026052382,44.7991699473061));
#32037=CARTESIAN_POINT('Ctrl Pts',(77.2912945088793,340.533929480383,45.4399204438795));
#32038=CARTESIAN_POINT('Ctrl Pts',(79.4007230479348,340.356832908385,46.0806709404529));
#32039=CARTESIAN_POINT('Ctrl Pts',(81.2118275942166,340.179736336386,47.644221801404));
#32040=CARTESIAN_POINT('Ctrl Pts',(82.1535440633156,340.002639764387,49.6375657386283));
#32041=CARTESIAN_POINT('Ctrl Pts',(82.6515697929949,339.908982435045,50.6917435101904));
#32042=CARTESIAN_POINT('Ctrl Pts',(82.9129498948709,339.815325105703,51.8569119935516));
#32043=CARTESIAN_POINT('Ctrl Pts',(82.9129498948689,339.721667776361,53.0228109606489));
#32044=CARTESIAN_POINT('Origin',(74.9879498948689,255.,53.0228109606356));
#32045=CARTESIAN_POINT('',(82.9037265626259,334.278332223638,53.0173862307939));
#32046=CARTESIAN_POINT('',(82.913275875755,335.721667776361,53.0223309921515));
#32047=CARTESIAN_POINT('',(82.9129498948689,255.,53.0228109606356));
#32048=CARTESIAN_POINT('Ctrl Pts',(82.9037265626259,334.278332223638,53.0173862307939));
#32049=CARTESIAN_POINT('Ctrl Pts',(82.909334688827,334.354538277687,52.0664523593613));
#32050=CARTESIAN_POINT('Ctrl Pts',(82.7505377378628,334.430744331736,51.1174380195998));
#32051=CARTESIAN_POINT('Ctrl Pts',(82.4186752153905,334.506950385786,50.2333907696849));
#32052=CARTESIAN_POINT('Ctrl Pts',(81.494777116139,334.719106395338,47.7722223082382));
#32053=CARTESIAN_POINT('Ctrl Pts',(79.2295281067083,334.931262404891,45.8145836033915));
#32054=CARTESIAN_POINT('Ctrl Pts',(76.6588454982678,335.143418414443,45.2618499962738));
#32055=CARTESIAN_POINT('Ctrl Pts',(74.0881628898271,335.355574423995,44.7091163891561));
#32056=CARTESIAN_POINT('Ctrl Pts',(71.2120466823766,335.567730433547,45.5612878797677));
#32057=CARTESIAN_POINT('Ctrl Pts',(69.3593696430875,335.7798864431,47.4240945041463));
#32058=CARTESIAN_POINT('Ctrl Pts',(67.5066926037986,335.992042452652,49.2869011285248));
#32059=CARTESIAN_POINT('Ctrl Pts',(66.6774547326711,336.204198462204,52.1603428866702));
#32060=CARTESIAN_POINT('Ctrl Pts',(67.2387782634214,336.416354471757,54.7307200572133));
#32061=CARTESIAN_POINT('Ctrl Pts',(67.5194400287966,336.522432476533,56.0159086424849));
#32062=CARTESIAN_POINT('Ctrl Pts',(68.1477421446412,336.628510481309,57.2253310808559));
#32063=CARTESIAN_POINT('Ctrl Pts',(69.0178667763073,336.734588486085,58.2240726682886));
#32064=CARTESIAN_POINT('Ctrl Pts',(69.8879914079735,336.840666490862,59.2228142557214));
#32065=CARTESIAN_POINT('Ctrl Pts',(70.9999385554612,336.946744495638,60.0108749922159));
#32066=CARTESIAN_POINT('Ctrl Pts',(72.2345617728081,337.052822500414,60.4649523396405));
#32067=CARTESIAN_POINT('Ctrl Pts',(74.7038082075017,337.264978509966,61.3731070344896));
#32068=CARTESIAN_POINT('Ctrl Pts',(77.6637589216318,337.477134519518,60.9453281730592));
#32069=CARTESIAN_POINT('Ctrl Pts',(79.7628065854718,337.689290529071,59.3653093008097));
#32070=CARTESIAN_POINT('Ctrl Pts',(81.7054439799919,337.885637760593,57.9030253335823));
#32071=CARTESIAN_POINT('Ctrl Pts',(82.9106983513784,338.081984992116,55.4538216170673));
#32072=CARTESIAN_POINT('Ctrl Pts',(82.9246711232106,338.278332223638,53.018347543027));
#32073=CARTESIAN_POINT('Ctrl Pts',(82.9129498948689,339.721667776361,53.0228109606489));
#32074=CARTESIAN_POINT('Ctrl Pts',(82.9129498948652,339.544571204362,55.2274084205586));
#32075=CARTESIAN_POINT('Ctrl Pts',(81.9432795991034,339.367474632363,57.4147653849932));
#32076=CARTESIAN_POINT('Ctrl Pts',(80.3096882702446,339.190378060364,58.8951806411014));
#32077=CARTESIAN_POINT('Ctrl Pts',(78.6760969413858,339.013281488366,60.3755958972096));
#32078=CARTESIAN_POINT('Ctrl Pts',(76.4041347530314,338.836184916367,61.1259150206703));
#32079=CARTESIAN_POINT('Ctrl Pts',(74.2101800112092,338.659088344368,60.9095529374009));
#32080=CARTESIAN_POINT('Ctrl Pts',(72.0162252693871,338.48199177237,60.6931908541314));
#32081=CARTESIAN_POINT('Ctrl Pts',(69.9345925076876,338.304895200371,59.5135315737617));
#32082=CARTESIAN_POINT('Ctrl Pts',(68.6216467656533,338.127798628372,57.7425365317826));
#32083=CARTESIAN_POINT('Ctrl Pts',(67.308701023619,337.950702056373,55.9715414898035));
#32084=CARTESIAN_POINT('Ctrl Pts',(66.784977419823,337.773605484375,53.6369099216176));
#32085=CARTESIAN_POINT('Ctrl Pts',(67.215612605763,337.596508912376,51.4747805783842));
#32086=CARTESIAN_POINT('Ctrl Pts',(67.646247791703,337.419412340377,49.3126512351508));
#32087=CARTESIAN_POINT('Ctrl Pts',(69.0245064208053,337.242315768378,47.3568408855391));
#32088=CARTESIAN_POINT('Ctrl Pts',(70.9158061804568,337.06521919638,46.2240411771252));
#32089=CARTESIAN_POINT('Ctrl Pts',(72.8071059401083,336.888122624381,45.0912414687112));
#32090=CARTESIAN_POINT('Ctrl Pts',(75.1818659698223,336.711026052382,44.7991699473061));
#32091=CARTESIAN_POINT('Ctrl Pts',(77.2912945088779,336.533929480384,45.4399204438791));
#32092=CARTESIAN_POINT('Ctrl Pts',(79.4007230479334,336.356832908385,46.080670940452));
#32093=CARTESIAN_POINT('Ctrl Pts',(81.2118275942155,336.179736336386,47.6442218014027));
#32094=CARTESIAN_POINT('Ctrl Pts',(82.1535440633148,336.002639764387,49.6375657386267));
#32095=CARTESIAN_POINT('Ctrl Pts',(82.6515697929948,335.908982435045,50.6917435101894));
#32096=CARTESIAN_POINT('Ctrl Pts',(82.912949894871,335.815325105703,51.8569119935515));
#32097=CARTESIAN_POINT('Ctrl Pts',(82.9129498948689,335.721667776361,53.0228109606495));
#32098=CARTESIAN_POINT('Origin',(74.9879498948689,255.,53.0228109606356));
#32099=CARTESIAN_POINT('',(82.903889038595,330.278332223638,53.0283217876032));
#32100=CARTESIAN_POINT('',(82.9116685845283,331.721667776361,53.0222624917929));
#32101=CARTESIAN_POINT('',(82.9129498948689,255.,53.0228109606356));
#32102=CARTESIAN_POINT('Ctrl Pts',(82.903889038595,330.278332223638,53.0283217876032));
#32103=CARTESIAN_POINT('Ctrl Pts',(82.8936426485269,330.414935553707,51.3238139604592));
#32104=CARTESIAN_POINT('Ctrl Pts',(82.3548623019608,330.551538883775,49.6130285715222));
#32105=CARTESIAN_POINT('Ctrl Pts',(81.3385495151766,330.688142213844,48.2589583526772));
#32106=CARTESIAN_POINT('Ctrl Pts',(79.7601336362042,330.900298223397,46.1559778899091));
#32107=CARTESIAN_POINT('Ctrl Pts',(77.0298808687583,331.112454232949,44.9134158133818));
#32108=CARTESIAN_POINT('Ctrl Pts',(74.4096204600999,331.324610242501,45.1049781336692));
#32109=CARTESIAN_POINT('Ctrl Pts',(71.7893600514415,331.536766252054,45.2965404539567));
#32110=CARTESIAN_POINT('Ctrl Pts',(69.2790920015704,331.748922261606,46.9222271710588));
#32111=CARTESIAN_POINT('Ctrl Pts',(68.0174220572677,331.961078271158,49.230930672305));
#32112=CARTESIAN_POINT('Ctrl Pts',(67.3865870851163,332.067156275934,50.3852824229281));
#32113=CARTESIAN_POINT('Ctrl Pts',(67.0679016393569,332.17323428071,51.7103883695873));
#32114=CARTESIAN_POINT('Ctrl Pts',(67.0699408517118,332.279312285487,53.0350005674449));
#32115=CARTESIAN_POINT('Ctrl Pts',(67.0719800640667,332.385390290263,54.3596127653023));
#32116=CARTESIAN_POINT('Ctrl Pts',(67.3947439345357,332.491468295039,55.6837312143581));
#32117=CARTESIAN_POINT('Ctrl Pts',(68.0291301081419,332.597546299815,56.8361351838901));
#32118=CARTESIAN_POINT('Ctrl Pts',(69.2979024553544,332.809702309367,59.1409431229542));
#32119=CARTESIAN_POINT('Ctrl Pts',(71.8131640151158,333.02185831892,60.7588931439228));
#32120=CARTESIAN_POINT('Ctrl Pts',(74.4340018146482,333.234014328472,60.9423869047961));
#32121=CARTESIAN_POINT('Ctrl Pts',(77.0548396141805,333.446170338024,61.1258806656693));
#32122=CARTESIAN_POINT('Ctrl Pts',(79.7812536534837,333.658326347577,59.8749181664473));
#32123=CARTESIAN_POINT('Ctrl Pts',(81.3531870785991,333.870482357129,57.7670878078129));
#32124=CARTESIAN_POINT('Ctrl Pts',(82.3604848669058,334.006432312632,56.4163862930702));
#32125=CARTESIAN_POINT('Ctrl Pts',(82.8937217865357,334.142382268135,54.7138317313537));
#32126=CARTESIAN_POINT('Ctrl Pts',(82.9037265626259,334.278332223638,53.0173862307939));
#32127=CARTESIAN_POINT('Ctrl Pts',(82.9166114764614,335.721667776361,53.0174197121561));
#32128=CARTESIAN_POINT('Ctrl Pts',(82.8968976708308,335.537298637763,55.3072955719158));
#32129=CARTESIAN_POINT('Ctrl Pts',(81.8585861362189,335.352929499166,57.6087979274022));
#32130=CARTESIAN_POINT('Ctrl Pts',(80.1156668069684,335.168560360569,59.0835915110494));
#32131=CARTESIAN_POINT('Ctrl Pts',(78.1100664517325,334.956404351016,60.7806560197863));
#32132=CARTESIAN_POINT('Ctrl Pts',(75.1714660480381,334.744248341464,61.3830415737116));
#32133=CARTESIAN_POINT('Ctrl Pts',(72.6576542686765,334.532092331911,60.611890582194));
#32134=CARTESIAN_POINT('Ctrl Pts',(70.1438424893148,334.319936322359,59.8407395906763));
#32135=CARTESIAN_POINT('Ctrl Pts',(68.0548193342858,334.107780312807,57.6960520537159));
#32136=CARTESIAN_POINT('Ctrl Pts',(67.3453868006718,333.895624303255,55.164719721984));
#32137=CARTESIAN_POINT('Ctrl Pts',(66.6359542670578,333.683468293703,52.6333873902521));
#32138=CARTESIAN_POINT('Ctrl Pts',(67.3061123548589,333.47131228415,49.7154102637488));
#32139=CARTESIAN_POINT('Ctrl Pts',(69.0530157877858,333.259156274598,47.7501489809154));
#32140=CARTESIAN_POINT('Ctrl Pts',(70.7999192207128,333.047000265045,45.7848876980819));
#32141=CARTESIAN_POINT('Ctrl Pts',(73.6235679987656,332.834844255493,44.7723422589182));
#32142=CARTESIAN_POINT('Ctrl Pts',(76.2190150425094,332.622688245941,45.1799147983004));
#32143=CARTESIAN_POINT('Ctrl Pts',(78.8144620862531,332.410532236388,45.5874873376827));
#32144=CARTESIAN_POINT('Ctrl Pts',(81.1817073956878,332.198376226836,47.4151778556106));
#32145=CARTESIAN_POINT('Ctrl Pts',(82.2481526773765,331.986220217284,49.8203010055111));
#32146=CARTESIAN_POINT('Ctrl Pts',(82.6914282068279,331.898036070309,50.8200074658179));
#32147=CARTESIAN_POINT('Ctrl Pts',(82.9099634665863,331.809851923335,51.9194774275631));
#32148=CARTESIAN_POINT('Ctrl Pts',(82.9069840420526,331.72166777636,53.0202572588894));
#32149=CARTESIAN_POINT('Origin',(74.9879498948689,255.,53.0228109606356));
#32150=CARTESIAN_POINT('',(82.915920021327,326.278332223638,53.0238964569577));
#32151=CARTESIAN_POINT('',(82.9099077959009,327.721667776361,53.0246025132965));
#32152=CARTESIAN_POINT('',(82.9129498948689,255.,53.0228109606356));
#32153=CARTESIAN_POINT('Ctrl Pts',(82.9248220017562,326.278332223638,53.0271498763471));
#32154=CARTESIAN_POINT('Ctrl Pts',(82.9112391805045,326.475332829726,50.5837044358842));
#32155=CARTESIAN_POINT('Ctrl Pts',(81.6968655677976,326.672333435814,48.1267829301193));
#32156=CARTESIAN_POINT('Ctrl Pts',(79.74325571597,326.869334041903,46.6656411376162));
#32157=CARTESIAN_POINT('Ctrl Pts',(77.6393532020857,327.081490051455,45.0920926179295));
#32158=CARTESIAN_POINT('Ctrl Pts',(74.6780994082307,327.293646061007,44.6734293251219));
#32159=CARTESIAN_POINT('Ctrl Pts',(72.2116608408273,327.505802070559,45.5891824022388));
#32160=CARTESIAN_POINT('Ctrl Pts',(70.9784415571256,327.611880075336,46.0470589407973));
#32161=CARTESIAN_POINT('Ctrl Pts',(69.8689260800369,327.717958080112,46.8385395718368));
#32162=CARTESIAN_POINT('Ctrl Pts',(69.0018806483926,327.824036084888,47.839955495699));
#32163=CARTESIAN_POINT('Ctrl Pts',(68.1348352167483,327.930114089664,48.8413714195611));
#32164=CARTESIAN_POINT('Ctrl Pts',(67.5102598305485,328.03619209444,50.0527226362459));
#32165=CARTESIAN_POINT('Ctrl Pts',(67.2335564272066,328.142270099216,51.338769273361));
#32166=CARTESIAN_POINT('Ctrl Pts',(66.6801496205226,328.354426108769,53.910862547591));
#32167=CARTESIAN_POINT('Ctrl Pts',(67.5182307452699,328.566582118321,56.7817375035421));
#32168=CARTESIAN_POINT('Ctrl Pts',(69.3766344918117,328.778738127873,58.6388309978433));
#32169=CARTESIAN_POINT('Ctrl Pts',(71.2350382383536,328.990894137426,60.4959244921446));
#32170=CARTESIAN_POINT('Ctrl Pts',(74.1137646066901,329.203050146978,61.3392365247959));
#32171=CARTESIAN_POINT('Ctrl Pts',(76.6827331908784,329.41520615653,60.7785905337908));
#32172=CARTESIAN_POINT('Ctrl Pts',(79.2517017750665,329.627362166082,60.2179445427857));
#32173=CARTESIAN_POINT('Ctrl Pts',(81.5109125751065,329.839518175635,58.2533405281243));
#32174=CARTESIAN_POINT('Ctrl Pts',(82.4272284798771,330.051674185187,55.7893390962893));
#32175=CARTESIAN_POINT('Ctrl Pts',(82.7535455236642,330.127226864671,54.9118626070814));
#32176=CARTESIAN_POINT('Ctrl Pts',(82.9095561202415,330.202779544154,53.9710523453169));
#32177=CARTESIAN_POINT('Ctrl Pts',(82.903889038595,330.278332223638,53.0283217876032));
#32178=CARTESIAN_POINT('Ctrl Pts',(82.9129498948689,331.721667776361,53.0228109606494));
#32179=CARTESIAN_POINT('Ctrl Pts',(82.9129498948651,331.544571204362,55.2274084205592));
#32180=CARTESIAN_POINT('Ctrl Pts',(81.9432795991031,331.367474632363,57.4147653849937));
#32181=CARTESIAN_POINT('Ctrl Pts',(80.3096882702442,331.190378060364,58.8951806411017));
#32182=CARTESIAN_POINT('Ctrl Pts',(78.6760969413853,331.013281488366,60.3755958972098));
#32183=CARTESIAN_POINT('Ctrl Pts',(76.4041347530308,330.836184916367,61.1259150206704));
#32184=CARTESIAN_POINT('Ctrl Pts',(74.2101800112087,330.659088344368,60.9095529374008));
#32185=CARTESIAN_POINT('Ctrl Pts',(72.0162252693866,330.481991772369,60.6931908541312));
#32186=CARTESIAN_POINT('Ctrl Pts',(69.9345925076871,330.304895200371,59.5135315737613));
#32187=CARTESIAN_POINT('Ctrl Pts',(68.6216467656529,330.127798628372,57.7425365317822));
#32188=CARTESIAN_POINT('Ctrl Pts',(67.3087010236188,329.950702056373,55.971541489803));
#32189=CARTESIAN_POINT('Ctrl Pts',(66.7849774198229,329.773605484375,53.636909921617));
#32190=CARTESIAN_POINT('Ctrl Pts',(67.2156126057631,329.596508912376,51.4747805783836));
#32191=CARTESIAN_POINT('Ctrl Pts',(67.6462477917032,329.419412340377,49.3126512351503));
#32192=CARTESIAN_POINT('Ctrl Pts',(69.0245064208057,329.242315768378,47.3568408855387));
#32193=CARTESIAN_POINT('Ctrl Pts',(70.9158061804573,329.06521919638,46.2240411771249));
#32194=CARTESIAN_POINT('Ctrl Pts',(72.8071059401089,328.888122624381,45.0912414687111));
#32195=CARTESIAN_POINT('Ctrl Pts',(75.1818659698229,328.711026052382,44.7991699473061));
#32196=CARTESIAN_POINT('Ctrl Pts',(77.2912945088784,328.533929480384,45.4399204438792));
#32197=CARTESIAN_POINT('Ctrl Pts',(79.4007230479339,328.356832908385,46.0806709404524));
#32198=CARTESIAN_POINT('Ctrl Pts',(81.2118275942159,328.179736336386,47.6442218014032));
#32199=CARTESIAN_POINT('Ctrl Pts',(82.1535440633151,328.002639764387,49.6375657386272));
#32200=CARTESIAN_POINT('Ctrl Pts',(82.6515697929948,327.908982435045,50.6917435101897));
#32201=CARTESIAN_POINT('Ctrl Pts',(82.9129498948709,327.815325105703,51.8569119935515));
#32202=CARTESIAN_POINT('Ctrl Pts',(82.9129498948689,327.721667776361,53.0228109606492));
#32203=CARTESIAN_POINT('Origin',(74.9879498948689,255.,53.0228109606356));
#32204=CARTESIAN_POINT('',(82.9129498948689,322.278332223638,53.0228109606357));
#32205=CARTESIAN_POINT('',(82.9174913560738,323.721667776361,53.0236500017445));
#32206=CARTESIAN_POINT('',(82.9129498948689,255.,53.0228109606356));
#32207=CARTESIAN_POINT('Ctrl Pts',(82.9129498948689,322.278332223638,53.0228109606357));
#32208=CARTESIAN_POINT('Ctrl Pts',(82.9129498948689,322.455428795637,50.8182135007259));
#32209=CARTESIAN_POINT('Ctrl Pts',(81.9432795991108,322.632525367635,48.6308565362897));
#32210=CARTESIAN_POINT('Ctrl Pts',(80.3096882702545,322.809621939634,47.1504412801788));
#32211=CARTESIAN_POINT('Ctrl Pts',(78.6760969413982,322.986718511633,45.6700260240678));
#32212=CARTESIAN_POINT('Ctrl Pts',(76.4041347530451,323.163815083631,44.9197069006032));
#32213=CARTESIAN_POINT('Ctrl Pts',(74.2101800112226,323.34091165563,45.136068983869));
#32214=CARTESIAN_POINT('Ctrl Pts',(72.0162252694001,323.518008227629,45.3524310671347));
#32215=CARTESIAN_POINT('Ctrl Pts',(69.9345925076986,323.695104799628,46.5320903475009));
#32216=CARTESIAN_POINT('Ctrl Pts',(68.6216467656613,323.872201371626,48.3030853894778));
#32217=CARTESIAN_POINT('Ctrl Pts',(67.308701023624,324.049297943625,50.0740804314546));
#32218=CARTESIAN_POINT('Ctrl Pts',(66.784977419824,324.226394515624,52.4087119996396));
#32219=CARTESIAN_POINT('Ctrl Pts',(67.2156126057604,324.403491087622,54.5708413428738));
#32220=CARTESIAN_POINT('Ctrl Pts',(67.6462477916967,324.580587659621,56.7329706861079));
#32221=CARTESIAN_POINT('Ctrl Pts',(69.0245064207957,324.75768423162,58.6887810357219));
#32222=CARTESIAN_POINT('Ctrl Pts',(70.9158061804453,324.934780803619,59.8215807441391));
#32223=CARTESIAN_POINT('Ctrl Pts',(72.8071059400949,325.111877375617,60.9543804525562));
#32224=CARTESIAN_POINT('Ctrl Pts',(75.1818659698084,325.288973947616,61.2464519739654));
#32225=CARTESIAN_POINT('Ctrl Pts',(77.291294508865,325.466070519615,60.605701477396));
#32226=CARTESIAN_POINT('Ctrl Pts',(79.4007230479217,325.643167091614,59.9649509808266));
#32227=CARTESIAN_POINT('Ctrl Pts',(81.2118275942064,325.820263663612,58.401400119879));
#32228=CARTESIAN_POINT('Ctrl Pts',(82.1535440633091,325.997360235611,56.4080561826566));
#32229=CARTESIAN_POINT('Ctrl Pts',(82.6515697929907,326.091017564953,55.3538784110949));
#32230=CARTESIAN_POINT('Ctrl Pts',(82.9129498948689,326.184674894295,54.1887099277336));
#32231=CARTESIAN_POINT('Ctrl Pts',(82.9129498948689,326.278332223638,53.0228109606359));
#32232=CARTESIAN_POINT('Ctrl Pts',(82.9036744121771,327.721667776361,53.0282734770033));
#32233=CARTESIAN_POINT('Ctrl Pts',(82.909810152162,327.658093189802,53.8208117728148));
#32234=CARTESIAN_POINT('Ctrl Pts',(82.800678889337,327.594518603244,54.6119493203552));
#32235=CARTESIAN_POINT('Ctrl Pts',(82.569358847217,327.530944016685,55.3656410340849));
#32236=CARTESIAN_POINT('Ctrl Pts',(82.18338750456,327.424866011909,56.623220792551));
#32237=CARTESIAN_POINT('Ctrl Pts',(81.4572313483912,327.318788007133,57.776547901427));
#32238=CARTESIAN_POINT('Ctrl Pts',(80.5075017688919,327.212710002357,58.6999196353046));
#32239=CARTESIAN_POINT('Ctrl Pts',(79.5577721893926,327.106631997581,59.6232913691821));
#32240=CARTESIAN_POINT('Ctrl Pts',(78.3844691865628,327.000553992804,60.3167077280612));
#32241=CARTESIAN_POINT('Ctrl Pts',(77.1165269206526,326.894475988028,60.6671405127356));
#32242=CARTESIAN_POINT('Ctrl Pts',(74.5806423888323,326.682319978476,61.3680060820842));
#32243=CARTESIAN_POINT('Ctrl Pts',(71.6662008046903,326.470163968924,60.6969373546137));
#32244=CARTESIAN_POINT('Ctrl Pts',(69.7049914022054,326.258007959371,58.9487616164966));
#32245=CARTESIAN_POINT('Ctrl Pts',(67.7437819997204,326.045851949819,57.2005858783795));
#32246=CARTESIAN_POINT('Ctrl Pts',(66.7358047788924,325.833695940267,54.3753031296159));
#32247=CARTESIAN_POINT('Ctrl Pts',(67.1473169532818,325.621539930714,51.7782699676972));
#32248=CARTESIAN_POINT('Ctrl Pts',(67.5588291276712,325.409383921162,49.1812368057785));
#32249=CARTESIAN_POINT('Ctrl Pts',(69.3898306972781,325.19722791161,46.8124532307048));
#32250=CARTESIAN_POINT('Ctrl Pts',(71.7968676918125,324.985071902057,45.7555186062534));
#32251=CARTESIAN_POINT('Ctrl Pts',(74.2039046863469,324.772915892505,44.6985839818021));
#32252=CARTESIAN_POINT('Ctrl Pts',(77.1869771058089,324.560759882953,44.953498307973));
#32253=CARTESIAN_POINT('Ctrl Pts',(79.3775118827791,324.3486038734,46.4079675942286));
#32254=CARTESIAN_POINT('Ctrl Pts',(81.535240569327,324.139625174387,47.8406543224425));
#32255=CARTESIAN_POINT('Ctrl Pts',(82.9239924073639,323.930646475374,50.4372352852841));
#32256=CARTESIAN_POINT('Ctrl Pts',(82.926795049106,323.721667776361,53.0253688716062));
#32257=CARTESIAN_POINT('Origin',(74.9879498948689,255.,53.0228109606356));
#32258=CARTESIAN_POINT('',(82.9077404809001,318.278332223638,53.0233273752923));
#32259=CARTESIAN_POINT('',(82.9129498948689,319.721667776361,53.0228109606489));
#32260=CARTESIAN_POINT('',(82.9129498948689,255.,53.0228109606356));
#32261=CARTESIAN_POINT('Ctrl Pts',(82.9129498948689,318.278332223638,53.0228109606357));
#32262=CARTESIAN_POINT('Ctrl Pts',(82.9129498948689,318.455428795637,50.818213500726));
#32263=CARTESIAN_POINT('Ctrl Pts',(81.9432795991108,318.632525367635,48.6308565362898));
#32264=CARTESIAN_POINT('Ctrl Pts',(80.3096882702546,318.809621939634,47.1504412801788));
#32265=CARTESIAN_POINT('Ctrl Pts',(78.6760969413983,318.986718511633,45.6700260240679));
#32266=CARTESIAN_POINT('Ctrl Pts',(76.4041347530451,319.163815083631,44.9197069006032));
#32267=CARTESIAN_POINT('Ctrl Pts',(74.2101800112226,319.34091165563,45.1360689838689));
#32268=CARTESIAN_POINT('Ctrl Pts',(72.0162252694001,319.518008227629,45.3524310671347));
#32269=CARTESIAN_POINT('Ctrl Pts',(69.9345925076986,319.695104799628,46.5320903475009));
#32270=CARTESIAN_POINT('Ctrl Pts',(68.6216467656613,319.872201371626,48.3030853894777));
#32271=CARTESIAN_POINT('Ctrl Pts',(67.308701023624,320.049297943625,50.0740804314546));
#32272=CARTESIAN_POINT('Ctrl Pts',(66.784977419824,320.226394515624,52.4087119996396));
#32273=CARTESIAN_POINT('Ctrl Pts',(67.2156126057603,320.403491087623,54.5708413428737));
#32274=CARTESIAN_POINT('Ctrl Pts',(67.6462477916967,320.580587659621,56.7329706861079));
#32275=CARTESIAN_POINT('Ctrl Pts',(69.0245064207957,320.75768423162,58.6887810357219));
#32276=CARTESIAN_POINT('Ctrl Pts',(70.9158061804453,320.934780803619,59.821580744139));
#32277=CARTESIAN_POINT('Ctrl Pts',(72.8071059400948,321.111877375617,60.9543804525562));
#32278=CARTESIAN_POINT('Ctrl Pts',(75.1818659698083,321.288973947616,61.2464519739654));
#32279=CARTESIAN_POINT('Ctrl Pts',(77.291294508865,321.466070519615,60.605701477396));
#32280=CARTESIAN_POINT('Ctrl Pts',(79.4007230479216,321.643167091614,59.9649509808266));
#32281=CARTESIAN_POINT('Ctrl Pts',(81.2118275942063,321.820263663612,58.401400119879));
#32282=CARTESIAN_POINT('Ctrl Pts',(82.1535440633091,321.997360235611,56.4080561826566));
#32283=CARTESIAN_POINT('Ctrl Pts',(82.6515697929907,322.091017564953,55.3538784110949));
#32284=CARTESIAN_POINT('Ctrl Pts',(82.9129498948689,322.184674894295,54.1887099277335));
#32285=CARTESIAN_POINT('Ctrl Pts',(82.9129498948689,322.278332223638,53.0228109606357));
#32286=CARTESIAN_POINT('Ctrl Pts',(82.9129498948689,323.721667776361,53.0228109606491));
#32287=CARTESIAN_POINT('Ctrl Pts',(82.9129498948652,323.544571204362,55.2274084205588));
#32288=CARTESIAN_POINT('Ctrl Pts',(81.9432795991032,323.367474632363,57.4147653849934));
#32289=CARTESIAN_POINT('Ctrl Pts',(80.3096882702444,323.190378060364,58.8951806411015));
#32290=CARTESIAN_POINT('Ctrl Pts',(78.6760969413856,323.013281488366,60.3755958972097));
#32291=CARTESIAN_POINT('Ctrl Pts',(76.4041347530311,322.836184916367,61.1259150206704));
#32292=CARTESIAN_POINT('Ctrl Pts',(74.210180011209,322.659088344368,60.9095529374009));
#32293=CARTESIAN_POINT('Ctrl Pts',(72.0162252693869,322.48199177237,60.6931908541313));
#32294=CARTESIAN_POINT('Ctrl Pts',(69.9345925076874,322.304895200371,59.5135315737615));
#32295=CARTESIAN_POINT('Ctrl Pts',(68.6216467656531,322.127798628372,57.7425365317824));
#32296=CARTESIAN_POINT('Ctrl Pts',(67.3087010236189,321.950702056373,55.9715414898033));
#32297=CARTESIAN_POINT('Ctrl Pts',(66.784977419823,321.773605484375,53.6369099216174));
#32298=CARTESIAN_POINT('Ctrl Pts',(67.215612605763,321.596508912376,51.474780578384));
#32299=CARTESIAN_POINT('Ctrl Pts',(67.6462477917031,321.419412340377,49.3126512351506));
#32300=CARTESIAN_POINT('Ctrl Pts',(69.0245064208055,321.242315768378,47.3568408855389));
#32301=CARTESIAN_POINT('Ctrl Pts',(70.915806180457,321.06521919638,46.2240411771251));
#32302=CARTESIAN_POINT('Ctrl Pts',(72.8071059401085,320.888122624381,45.0912414687112));
#32303=CARTESIAN_POINT('Ctrl Pts',(75.1818659698225,320.711026052382,44.7991699473061));
#32304=CARTESIAN_POINT('Ctrl Pts',(77.2912945088781,320.533929480384,45.4399204438791));
#32305=CARTESIAN_POINT('Ctrl Pts',(79.4007230479336,320.356832908385,46.0806709404522));
#32306=CARTESIAN_POINT('Ctrl Pts',(81.2118275942156,320.179736336386,47.6442218014029));
#32307=CARTESIAN_POINT('Ctrl Pts',(82.1535440633149,320.002639764387,49.6375657386269));
#32308=CARTESIAN_POINT('Ctrl Pts',(82.6515697929947,319.908982435045,50.6917435101893));
#32309=CARTESIAN_POINT('Ctrl Pts',(82.9129498948708,319.815325105703,51.856911993551));
#32310=CARTESIAN_POINT('Ctrl Pts',(82.9129498948689,319.721667776361,53.0228109606487));
#32311=CARTESIAN_POINT('Origin',(74.9879498948689,255.,53.0228109606356));
#32312=CARTESIAN_POINT('',(82.9130547149714,314.278332223638,53.0229888658931));
#32313=CARTESIAN_POINT('',(82.9100618310243,315.721667776361,53.0233010180067));
#32314=CARTESIAN_POINT('',(82.9129498948689,255.,53.0228109606356));
#32315=CARTESIAN_POINT('Ctrl Pts',(82.9159347025624,314.278332223638,53.0278769066855));
#32316=CARTESIAN_POINT('Ctrl Pts',(82.9110875624937,314.338290643456,52.2818585047472));
#32317=CARTESIAN_POINT('Ctrl Pts',(82.8007484662297,314.398249063274,51.534267327686));
#32318=CARTESIAN_POINT('Ctrl Pts',(82.5920056934082,314.458207483092,50.8152441537794));
#32319=CARTESIAN_POINT('Ctrl Pts',(82.2226994822118,314.564285487869,49.5431535298568));
#32320=CARTESIAN_POINT('Ctrl Pts',(81.5453855151546,314.670363492644,48.3604819891323));
#32321=CARTESIAN_POINT('Ctrl Pts',(80.6162927679135,314.77644149742,47.4292100668239));
#32322=CARTESIAN_POINT('Ctrl Pts',(78.7581072734314,314.988597506973,45.5666662222072));
#32323=CARTESIAN_POINT('Ctrl Pts',(75.8928066582134,315.200753516525,44.7097208512549));
#32324=CARTESIAN_POINT('Ctrl Pts',(73.3238802807332,315.412909526078,45.2602460539687));
#32325=CARTESIAN_POINT('Ctrl Pts',(70.7549539032529,315.62506553563,45.8107712566825));
#32326=CARTESIAN_POINT('Ctrl Pts',(68.4824017635105,315.837221545182,47.7687670330626));
#32327=CARTESIAN_POINT('Ctrl Pts',(67.5566775306894,316.049377554734,50.229855848718));
#32328=CARTESIAN_POINT('Ctrl Pts',(66.6309532978684,316.261533564287,52.6909446643735));
#32329=CARTESIAN_POINT('Ctrl Pts',(67.0520569719687,316.473689573839,55.6551265193043));
#32330=CARTESIAN_POINT('Ctrl Pts',(68.6222579787399,316.685845583392,57.7635398307203));
#32331=CARTESIAN_POINT('Ctrl Pts',(70.1924589855109,316.898001592944,59.8719531421361));
#32332=CARTESIAN_POINT('Ctrl Pts',(72.9117573249526,317.110157602496,61.1245979100374));
#32333=CARTESIAN_POINT('Ctrl Pts',(75.5348949136829,317.322313612048,60.9427388867091));
#32334=CARTESIAN_POINT('Ctrl Pts',(78.1580325024134,317.534469621601,60.7608798633808));
#32335=CARTESIAN_POINT('Ctrl Pts',(80.6850093404324,317.746625631153,59.1445170488228));
#32336=CARTESIAN_POINT('Ctrl Pts',(81.9484164186813,317.958781640706,56.840984264952));
#32337=CARTESIAN_POINT('Ctrl Pts',(82.5827333838041,318.065298501683,55.6844528906374));
#32338=CARTESIAN_POINT('Ctrl Pts',(82.898538739761,318.17181536266,54.3547046353364));
#32339=CARTESIAN_POINT('Ctrl Pts',(82.8973003436811,318.278332223638,53.0243623170167));
#32340=CARTESIAN_POINT('Ctrl Pts',(82.9129498948689,319.721667776361,53.0228109606487));
#32341=CARTESIAN_POINT('Ctrl Pts',(82.9129498948653,319.544571204362,55.2274084205585));
#32342=CARTESIAN_POINT('Ctrl Pts',(81.9432795991034,319.367474632363,57.4147653849932));
#32343=CARTESIAN_POINT('Ctrl Pts',(80.3096882702445,319.190378060364,58.8951806411014));
#32344=CARTESIAN_POINT('Ctrl Pts',(78.6760969413857,319.013281488366,60.3755958972096));
#32345=CARTESIAN_POINT('Ctrl Pts',(76.4041347530312,318.836184916367,61.1259150206704));
#32346=CARTESIAN_POINT('Ctrl Pts',(74.210180011209,318.659088344368,60.9095529374009));
#32347=CARTESIAN_POINT('Ctrl Pts',(72.0162252693868,318.481991772369,60.6931908541313));
#32348=CARTESIAN_POINT('Ctrl Pts',(69.9345925076872,318.304895200371,59.5135315737614));
#32349=CARTESIAN_POINT('Ctrl Pts',(68.621646765653,318.127798628372,57.7425365317822));
#32350=CARTESIAN_POINT('Ctrl Pts',(67.3087010236187,317.950702056373,55.971541489803));
#32351=CARTESIAN_POINT('Ctrl Pts',(66.7849774198229,317.773605484375,53.6369099216169));
#32352=CARTESIAN_POINT('Ctrl Pts',(67.2156126057631,317.596508912376,51.4747805783835));
#32353=CARTESIAN_POINT('Ctrl Pts',(67.6462477917033,317.419412340377,49.31265123515));
#32354=CARTESIAN_POINT('Ctrl Pts',(69.0245064208059,317.242315768378,47.3568408855384));
#32355=CARTESIAN_POINT('Ctrl Pts',(70.9158061804576,317.06521919638,46.2240411771247));
#32356=CARTESIAN_POINT('Ctrl Pts',(72.8071059401093,316.888122624381,45.0912414687109));
#32357=CARTESIAN_POINT('Ctrl Pts',(75.1818659698235,316.711026052382,44.7991699473061));
#32358=CARTESIAN_POINT('Ctrl Pts',(77.291294508879,316.533929480384,45.4399204438794));
#32359=CARTESIAN_POINT('Ctrl Pts',(79.4007230479345,316.356832908385,46.0806709404527));
#32360=CARTESIAN_POINT('Ctrl Pts',(81.2118275942164,316.179736336386,47.6442218014038));
#32361=CARTESIAN_POINT('Ctrl Pts',(82.1535440633154,316.002639764387,49.637565738628));
#32362=CARTESIAN_POINT('Ctrl Pts',(82.6515697929949,315.908982435045,50.6917435101901));
#32363=CARTESIAN_POINT('Ctrl Pts',(82.9129498948708,315.815325105703,51.8569119935514));
#32364=CARTESIAN_POINT('Ctrl Pts',(82.9129498948689,315.721667776361,53.0228109606487));
#32365=CARTESIAN_POINT('Origin',(74.9879498948689,255.,53.0228109606356));
#32366=CARTESIAN_POINT('',(82.9151502769548,310.278332223638,53.0224445370273));
#32367=CARTESIAN_POINT('',(82.9178004843628,311.721667776361,53.029085373757));
#32368=CARTESIAN_POINT('',(82.9129498948689,255.,53.0228109606356));
#32369=CARTESIAN_POINT('Ctrl Pts',(82.9129498948689,310.278332223638,53.0228109606354));
#32370=CARTESIAN_POINT('Ctrl Pts',(82.9129498948688,310.455428795637,50.8182135007256));
#32371=CARTESIAN_POINT('Ctrl Pts',(81.9432795991106,310.632525367635,48.6308565362894));
#32372=CARTESIAN_POINT('Ctrl Pts',(80.3096882702541,310.809621939634,47.1504412801784));
#32373=CARTESIAN_POINT('Ctrl Pts',(78.6760969413977,310.986718511633,45.6700260240675));
#32374=CARTESIAN_POINT('Ctrl Pts',(76.4041347530444,311.163815083631,44.9197069006031));
#32375=CARTESIAN_POINT('Ctrl Pts',(74.2101800112218,311.34091165563,45.136068983869));
#32376=CARTESIAN_POINT('Ctrl Pts',(72.0162252693993,311.518008227629,45.352431067135));
#32377=CARTESIAN_POINT('Ctrl Pts',(69.9345925076978,311.695104799628,46.5320903475014));
#32378=CARTESIAN_POINT('Ctrl Pts',(68.6216467656607,311.872201371626,48.3030853894785));
#32379=CARTESIAN_POINT('Ctrl Pts',(67.3087010236236,312.049297943625,50.0740804314556));
#32380=CARTESIAN_POINT('Ctrl Pts',(66.7849774198239,312.226394515624,52.4087119996408));
#32381=CARTESIAN_POINT('Ctrl Pts',(67.2156126057606,312.403491087623,54.5708413428749));
#32382=CARTESIAN_POINT('Ctrl Pts',(67.6462477916973,312.580587659621,56.7329706861091));
#32383=CARTESIAN_POINT('Ctrl Pts',(69.0245064207967,312.75768423162,58.688781035723));
#32384=CARTESIAN_POINT('Ctrl Pts',(70.9158061804465,312.934780803619,59.8215807441398));
#32385=CARTESIAN_POINT('Ctrl Pts',(72.8071059400964,313.111877375617,60.9543804525566));
#32386=CARTESIAN_POINT('Ctrl Pts',(75.18186596981,313.288973947616,61.2464519739654));
#32387=CARTESIAN_POINT('Ctrl Pts',(77.2912945088666,313.466070519615,60.6057014773955));
#32388=CARTESIAN_POINT('Ctrl Pts',(79.4007230479232,313.643167091614,59.9649509808256));
#32389=CARTESIAN_POINT('Ctrl Pts',(81.2118275942076,313.820263663612,58.4014001198776));
#32390=CARTESIAN_POINT('Ctrl Pts',(82.1535440633099,313.997360235611,56.4080561826549));
#32391=CARTESIAN_POINT('Ctrl Pts',(82.6515697929911,314.091017564953,55.3538784110935));
#32392=CARTESIAN_POINT('Ctrl Pts',(82.9129498948689,314.184674894296,54.1887099277326));
#32393=CARTESIAN_POINT('Ctrl Pts',(82.9129498948689,314.278332223638,53.0228109606353));
#32394=CARTESIAN_POINT('Ctrl Pts',(82.9009180699073,315.721667776361,53.0248525651369));
#32395=CARTESIAN_POINT('Ctrl Pts',(82.9045269433347,315.627129008308,54.2057564279726));
#32396=CARTESIAN_POINT('Ctrl Pts',(82.6573714271191,315.532590240256,55.385490302401));
#32397=CARTESIAN_POINT('Ctrl Pts',(82.1523311861863,315.438051472203,56.4427594866264));
#32398=CARTESIAN_POINT('Ctrl Pts',(81.0189620468701,315.225895462651,58.8153947109755));
#32399=CARTESIAN_POINT('Ctrl Pts',(78.5868702499663,315.013739453099,60.5712905449027));
#32400=CARTESIAN_POINT('Ctrl Pts',(75.9801962493432,314.801583443546,60.8994846737545));
#32401=CARTESIAN_POINT('Ctrl Pts',(73.3735222487202,314.589427433994,61.2276788026062));
#32402=CARTESIAN_POINT('Ctrl Pts',(70.5922660443779,314.377271424442,60.1281712263825));
#32403=CARTESIAN_POINT('Ctrl Pts',(68.9006517877288,314.165115414889,58.1131367076396));
#32404=CARTESIAN_POINT('Ctrl Pts',(68.0548446594043,314.059037410113,57.1056194482682));
#32405=CARTESIAN_POINT('Ctrl Pts',(67.4814480180031,313.952959405337,55.869220453267));
#32406=CARTESIAN_POINT('Ctrl Pts',(67.2225927592744,313.846881400561,54.5701455562236));
#32407=CARTESIAN_POINT('Ctrl Pts',(66.9637375005457,313.740803395785,53.2710706591802));
#32408=CARTESIAN_POINT('Ctrl Pts',(67.0194236244894,313.634725391009,51.9093198600946));
#32409=CARTESIAN_POINT('Ctrl Pts',(67.4144453457865,313.528647386232,50.6545535209066));
#32410=CARTESIAN_POINT('Ctrl Pts',(68.2044887883807,313.31649137668,48.1450208425304));
#32411=CARTESIAN_POINT('Ctrl Pts',(70.351874620388,313.104335367128,46.0634260037446));
#32412=CARTESIAN_POINT('Ctrl Pts',(72.8852552910209,312.892179357576,45.3674065288727));
#32413=CARTESIAN_POINT('Ctrl Pts',(75.4186359616536,312.680023348023,44.6713870540009));
#32414=CARTESIAN_POINT('Ctrl Pts',(78.3380114709119,312.467867338471,45.360942943043));
#32415=CARTESIAN_POINT('Ctrl Pts',(80.2942558082632,312.255711328918,47.1179379932229));
#32416=CARTESIAN_POINT('Ctrl Pts',(81.935688886677,312.077696811399,48.5921862447881));
#32417=CARTESIAN_POINT('Ctrl Pts',(82.8990346722933,311.89968229388,50.8179592648528));
#32418=CARTESIAN_POINT('Ctrl Pts',(82.9178004843628,311.721667776361,53.029085373757));
#32419=CARTESIAN_POINT('Origin',(74.9879498948689,255.,53.0228109606356));
#32420=CARTESIAN_POINT('',(82.909363478242,306.278332223638,53.0203308108944));
#32421=CARTESIAN_POINT('',(82.9221877016763,307.721667776361,53.0184879124944));
#32422=CARTESIAN_POINT('',(82.9129498948689,255.,53.0228109606356));
#32423=CARTESIAN_POINT('Ctrl Pts',(82.9033131639287,306.278332223638,53.0161467779089));
#32424=CARTESIAN_POINT('Ctrl Pts',(82.9104530950279,306.353007190719,52.0851637795933));
#32425=CARTESIAN_POINT('Ctrl Pts',(82.7594722917077,306.427682157799,51.156220880406));
#32426=CARTESIAN_POINT('Ctrl Pts',(82.4409791193906,306.50235712488,50.288053752156));
#32427=CARTESIAN_POINT('Ctrl Pts',(81.5361211308319,306.714513134433,47.8215394602294));
#32428=CARTESIAN_POINT('Ctrl Pts',(79.2791673003925,306.926669143985,45.8455839709954));
#32429=CARTESIAN_POINT('Ctrl Pts',(76.7126907808753,307.138825153537,45.2736383542251));
#32430=CARTESIAN_POINT('Ctrl Pts',(74.146214261358,307.35098116309,44.7016927374548));
#32431=CARTESIAN_POINT('Ctrl Pts',(71.2702150527629,307.563137172642,45.5337569931483));
#32432=CARTESIAN_POINT('Ctrl Pts',(69.402473289473,307.775293182194,47.3837512091079));
#32433=CARTESIAN_POINT('Ctrl Pts',(67.5347315261831,307.987449191747,49.2337454250674));
#32434=CARTESIAN_POINT('Ctrl Pts',(66.6752472081982,308.199605201299,52.101669601293));
#32435=CARTESIAN_POINT('Ctrl Pts',(67.2226638744058,308.411761210851,54.6734896780741));
#32436=CARTESIAN_POINT('Ctrl Pts',(67.7700805406134,308.623917220403,57.2453097548552));
#32437=CARTESIAN_POINT('Ctrl Pts',(69.7243981910132,308.836073229956,59.5210257321916));
#32438=CARTESIAN_POINT('Ctrl Pts',(72.1821611308745,309.048229239508,60.4493909960724));
#32439=CARTESIAN_POINT('Ctrl Pts',(74.6399240707361,309.260385249061,61.3777562599533));
#32440=CARTESIAN_POINT('Ctrl Pts',(77.6011323000593,309.472541258613,60.9587708103782));
#32441=CARTESIAN_POINT('Ctrl Pts',(79.716867816474,309.684697268165,59.3949338209173));
#32442=CARTESIAN_POINT('Ctrl Pts',(80.7747355746812,309.790775272941,58.6130153261869));
#32443=CARTESIAN_POINT('Ctrl Pts',(81.6212351546614,309.896853277717,57.5448839464852));
#32444=CARTESIAN_POINT('Ctrl Pts',(82.1765551040712,310.002931282493,56.342294495805));
#32445=CARTESIAN_POINT('Ctrl Pts',(82.6571311261736,310.094731596208,55.3015689554307));
#32446=CARTESIAN_POINT('Ctrl Pts',(82.9196357860859,310.186531909923,54.1601445624674));
#32447=CARTESIAN_POINT('Ctrl Pts',(82.9227432920407,310.278332223638,53.021180093001));
#32448=CARTESIAN_POINT('Ctrl Pts',(82.9178004843628,311.721667776361,53.029085373757));
#32449=CARTESIAN_POINT('Ctrl Pts',(82.9213995887066,311.687526284328,53.4531583397328));
#32450=CARTESIAN_POINT('Ctrl Pts',(82.8902536476416,311.653384792295,53.8766925396881));
#32451=CARTESIAN_POINT('Ctrl Pts',(82.8224826236741,311.619243300262,54.2942828289855));
#32452=CARTESIAN_POINT('Ctrl Pts',(82.4013519362892,311.407087290709,56.8891984032508));
#32453=CARTESIAN_POINT('Ctrl Pts',(80.5659773960746,311.194931281157,59.2545953404634));
#32454=CARTESIAN_POINT('Ctrl Pts',(78.1544837942863,310.982775271605,60.3027471053861));
#32455=CARTESIAN_POINT('Ctrl Pts',(75.7429901924981,310.770619262052,61.3508988703087));
#32456=CARTESIAN_POINT('Ctrl Pts',(72.7553775291362,310.5584632525,61.0818054629415));
#32457=CARTESIAN_POINT('Ctrl Pts',(70.5721394437577,310.346307242948,59.6203225878146));
#32458=CARTESIAN_POINT('Ctrl Pts',(68.3889013583791,310.134151233396,58.1588397126877));
#32459=CARTESIAN_POINT('Ctrl Pts',(67.0100378509841,309.921995223843,55.5049673698008));
#32460=CARTESIAN_POINT('Ctrl Pts',(67.0541876334774,309.709839214291,52.8743830807635));
#32461=CARTESIAN_POINT('Ctrl Pts',(67.0762625247241,309.603761209515,51.5590909362448));
#32462=CARTESIAN_POINT('Ctrl Pts',(67.4540907384429,309.497683204738,50.2496208051885));
#32463=CARTESIAN_POINT('Ctrl Pts',(68.1104952068112,309.391605199962,49.0990840578369));
#32464=CARTESIAN_POINT('Ctrl Pts',(68.7668996751795,309.285527195186,47.9485473104855));
#32465=CARTESIAN_POINT('Ctrl Pts',(69.7018803981972,309.17944919041,46.9569439468388));
#32466=CARTESIAN_POINT('Ctrl Pts',(70.8229059287894,309.073371185634,46.2686253534415));
#32467=CARTESIAN_POINT('Ctrl Pts',(73.0649569899737,308.861215176081,44.891988166647));
#32468=CARTESIAN_POINT('Ctrl Pts',(76.0511872814558,308.649059166529,44.7284900608501));
#32469=CARTESIAN_POINT('Ctrl Pts',(78.4202823957525,308.436903156977,45.8642052853462));
#32470=CARTESIAN_POINT('Ctrl Pts',(80.7893775100491,308.224747147425,46.9999205098423));
#32471=CARTESIAN_POINT('Ctrl Pts',(82.5413374471603,308.012591137873,49.4348490646314));
#32472=CARTESIAN_POINT('Ctrl Pts',(82.8661863365622,307.80043512832,52.0441395261994));
#32473=CARTESIAN_POINT('Ctrl Pts',(82.9063886494091,307.774179344334,52.3670573962203));
#32474=CARTESIAN_POINT('Ctrl Pts',(82.9247336340708,307.747923560347,52.6926457559872));
#32475=CARTESIAN_POINT('Ctrl Pts',(82.9221877016763,307.721667776361,53.0184879124944));
#32476=CARTESIAN_POINT('Origin',(74.9879498948689,255.,53.0228109606356));
#32477=CARTESIAN_POINT('',(82.9095685911471,302.278332223638,53.0255146867421));
#32478=CARTESIAN_POINT('',(82.908600234471,303.721667776361,53.0206776223734));
#32479=CARTESIAN_POINT('',(82.9129498948689,255.,53.0228109606356));
#32480=CARTESIAN_POINT('Ctrl Pts',(82.9129498948689,302.278332223638,53.0228109606348));
#32481=CARTESIAN_POINT('Ctrl Pts',(82.9129498948687,302.455428795637,50.8182135007249));
#32482=CARTESIAN_POINT('Ctrl Pts',(81.9432795991102,302.632525367635,48.6308565362887));
#32483=CARTESIAN_POINT('Ctrl Pts',(80.3096882702535,302.809621939634,47.1504412801779));
#32484=CARTESIAN_POINT('Ctrl Pts',(78.6760969413969,302.986718511633,45.6700260240671));
#32485=CARTESIAN_POINT('Ctrl Pts',(76.4041347530434,303.163815083632,44.9197069006029));
#32486=CARTESIAN_POINT('Ctrl Pts',(74.2101800112208,303.34091165563,45.1360689838691));
#32487=CARTESIAN_POINT('Ctrl Pts',(72.0162252693982,303.518008227629,45.3524310671354));
#32488=CARTESIAN_POINT('Ctrl Pts',(69.9345925076968,303.695104799628,46.5320903475022));
#32489=CARTESIAN_POINT('Ctrl Pts',(68.6216467656599,303.872201371626,48.3030853894795));
#32490=CARTESIAN_POINT('Ctrl Pts',(67.308701023623,304.049297943625,50.0740804314569));
#32491=CARTESIAN_POINT('Ctrl Pts',(66.7849774198238,304.226394515624,52.4087119996423));
#32492=CARTESIAN_POINT('Ctrl Pts',(67.2156126057609,304.403491087623,54.5708413428764));
#32493=CARTESIAN_POINT('Ctrl Pts',(67.646247791698,304.580587659621,56.7329706861105));
#32494=CARTESIAN_POINT('Ctrl Pts',(69.0245064207978,304.75768423162,58.6887810357242));
#32495=CARTESIAN_POINT('Ctrl Pts',(70.915806180448,304.934780803619,59.8215807441407));
#32496=CARTESIAN_POINT('Ctrl Pts',(72.8071059400981,305.111877375618,60.9543804525571));
#32497=CARTESIAN_POINT('Ctrl Pts',(75.1818659698119,305.288973947616,61.2464519739654));
#32498=CARTESIAN_POINT('Ctrl Pts',(77.2912945088684,305.466070519615,60.6057014773949));
#32499=CARTESIAN_POINT('Ctrl Pts',(79.4007230479249,305.643167091614,59.9649509808245));
#32500=CARTESIAN_POINT('Ctrl Pts',(81.211827594209,305.820263663613,58.4014001198759));
#32501=CARTESIAN_POINT('Ctrl Pts',(82.1535440633108,305.997360235611,56.4080561826529));
#32502=CARTESIAN_POINT('Ctrl Pts',(82.6515697929914,306.091017564954,55.353878411092));
#32503=CARTESIAN_POINT('Ctrl Pts',(82.912949894869,306.184674894296,54.1887099277317));
#32504=CARTESIAN_POINT('Ctrl Pts',(82.9129498948689,306.278332223638,53.022810960635));
#32505=CARTESIAN_POINT('Ctrl Pts',(82.9221877016763,307.721667776361,53.0184879124944));
#32506=CARTESIAN_POINT('Ctrl Pts',(82.9041616009639,307.535767550795,55.3255654853793));
#32507=CARTESIAN_POINT('Ctrl Pts',(81.8388445351564,307.349867325229,57.6453662447269));
#32508=CARTESIAN_POINT('Ctrl Pts',(80.069262236979,307.163967099663,59.1200897530678));
#32509=CARTESIAN_POINT('Ctrl Pts',(78.0497514063015,306.95181109011,60.8030971500206));
#32510=CARTESIAN_POINT('Ctrl Pts',(75.112991903254,306.739655080558,61.3854595755789));
#32511=CARTESIAN_POINT('Ctrl Pts',(72.6050182791123,306.527499071006,60.5955280504543));
#32512=CARTESIAN_POINT('Ctrl Pts',(70.0970446549707,306.315343061454,59.8055965253297));
#32513=CARTESIAN_POINT('Ctrl Pts',(68.0178569097347,306.103187051901,57.6433710495224));
#32514=CARTESIAN_POINT('Ctrl Pts',(67.327852786392,305.891031042349,55.1083454004399));
#32515=CARTESIAN_POINT('Ctrl Pts',(66.6378486630492,305.678875032797,52.5733197513572));
#32516=CARTESIAN_POINT('Ctrl Pts',(67.3370281615999,305.466719023245,49.6654939289993));
#32517=CARTESIAN_POINT('Ctrl Pts',(69.0953083595857,305.254563013692,47.7083598890329));
#32518=CARTESIAN_POINT('Ctrl Pts',(69.9744484585786,305.148485008916,46.7297928690498));
#32519=CARTESIAN_POINT('Ctrl Pts',(71.1183637324302,305.04240700414,45.9888987946646));
#32520=CARTESIAN_POINT('Ctrl Pts',(72.3683863154353,304.936328999363,45.550669202924));
#32521=CARTESIAN_POINT('Ctrl Pts',(73.6184088984404,304.830250994587,45.1124396111834));
#32522=CARTESIAN_POINT('Ctrl Pts',(74.9745387905989,304.724172989811,44.9768745020875));
#32523=CARTESIAN_POINT('Ctrl Pts',(76.2722597746717,304.618094985035,45.1922833546281));
#32524=CARTESIAN_POINT('Ctrl Pts',(78.8677017428175,304.405938975483,45.6231010597095));
#32525=CARTESIAN_POINT('Ctrl Pts',(81.2295080786204,304.193782965931,47.4578146113376));
#32526=CARTESIAN_POINT('Ctrl Pts',(82.2734486764291,303.981626956378,49.8687581527721));
#32527=CARTESIAN_POINT('Ctrl Pts',(82.6998360667996,303.894973896372,50.8534846085884));
#32528=CARTESIAN_POINT('Ctrl Pts',(82.906372531569,303.808320836366,51.9343397465352));
#32529=CARTESIAN_POINT('Ctrl Pts',(82.9016479285953,303.721667776361,53.0172677883023));
#32530=CARTESIAN_POINT('Origin',(74.9879498948689,255.,53.0228109606356));
#32531=CARTESIAN_POINT('',(82.9247849645265,298.278332223638,53.0254077151713));
#32532=CARTESIAN_POINT('',(82.9107328264417,299.721667776361,53.0254029102435));
#32533=CARTESIAN_POINT('',(82.9129498948689,255.,53.0228109606356));
#32534=CARTESIAN_POINT('Ctrl Pts',(82.9247849645265,298.278332223638,53.0254077151713));
#32535=CARTESIAN_POINT('Ctrl Pts',(82.9108749806662,298.473801742758,50.6015025294555));
#32536=CARTESIAN_POINT('Ctrl Pts',(81.7179195953142,298.669271261877,48.1678523004493));
#32537=CARTESIAN_POINT('Ctrl Pts',(79.7892377761479,298.864740780997,46.7026702603182));
#32538=CARTESIAN_POINT('Ctrl Pts',(77.6959117154242,299.076896790549,45.112411194343));
#32539=CARTESIAN_POINT('Ctrl Pts',(74.735885354018,299.289052800102,44.6630268229847));
#32540=CARTESIAN_POINT('Ctrl Pts',(72.2660705525556,299.501208809654,45.5652121477675));
#32541=CARTESIAN_POINT('Ctrl Pts',(69.7962557510931,299.713364819206,46.4673974725502));
#32542=CARTESIAN_POINT('Ctrl Pts',(67.8166525095745,299.925520828759,48.721152493474));
#32543=CARTESIAN_POINT('Ctrl Pts',(67.2416261249463,300.137676838311,51.2847057674901));
#32544=CARTESIAN_POINT('Ctrl Pts',(66.6665997403182,300.349832847863,53.848259041506));
#32545=CARTESIAN_POINT('Ctrl Pts',(67.4961502125804,300.561988857416,56.7216105686142));
#32546=CARTESIAN_POINT('Ctrl Pts',(69.3408685422965,300.774144866968,58.5974936110859));
#32547=CARTESIAN_POINT('Ctrl Pts',(70.2632277071545,300.880222871744,59.5354351323217));
#32548=CARTESIAN_POINT('Ctrl Pts',(71.439378836376,300.98630087652,60.2240095323984));
#32549=CARTESIAN_POINT('Ctrl Pts',(72.7078856112961,301.092378881296,60.6054439239807));
#32550=CARTESIAN_POINT('Ctrl Pts',(73.9763923862162,301.198456886072,60.986878315563));
#32551=CARTESIAN_POINT('Ctrl Pts',(75.3372548068349,301.304534890849,61.0611726986508));
#32552=CARTESIAN_POINT('Ctrl Pts',(76.6239461579206,301.410612895625,60.7874829229971));
#32553=CARTESIAN_POINT('Ctrl Pts',(79.1973288600919,301.622768905177,60.2401033716898));
#32554=CARTESIAN_POINT('Ctrl Pts',(81.4740272841313,301.83492491473,58.3007871854165));
#32555=CARTESIAN_POINT('Ctrl Pts',(82.4082238324473,302.047080924282,55.8452347952502));
#32556=CARTESIAN_POINT('Ctrl Pts',(82.7476504115135,302.124164690734,54.9530459416149));
#32557=CARTESIAN_POINT('Ctrl Pts',(82.9098499119628,302.201248457186,53.9927074369835));
#32558=CARTESIAN_POINT('Ctrl Pts',(82.9038476214953,302.278332223638,53.0300892343956));
#32559=CARTESIAN_POINT('Ctrl Pts',(82.9129498948689,303.721667776361,53.0228109606482));
#32560=CARTESIAN_POINT('Ctrl Pts',(82.9129498948654,303.544571204362,55.227408420558));
#32561=CARTESIAN_POINT('Ctrl Pts',(81.9432795991037,303.367474632363,57.4147653849927));
#32562=CARTESIAN_POINT('Ctrl Pts',(80.3096882702449,303.190378060364,58.8951806411011));
#32563=CARTESIAN_POINT('Ctrl Pts',(78.6760969413861,303.013281488366,60.3755958972094));
#32564=CARTESIAN_POINT('Ctrl Pts',(76.4041347530316,302.836184916367,61.1259150206703));
#32565=CARTESIAN_POINT('Ctrl Pts',(74.2101800112094,302.659088344368,60.9095529374009));
#32566=CARTESIAN_POINT('Ctrl Pts',(72.0162252693872,302.48199177237,60.6931908541315));
#32567=CARTESIAN_POINT('Ctrl Pts',(69.9345925076876,302.304895200371,59.5135315737617));
#32568=CARTESIAN_POINT('Ctrl Pts',(68.6216467656533,302.127798628372,57.7425365317826));
#32569=CARTESIAN_POINT('Ctrl Pts',(67.3087010236189,301.950702056373,55.9715414898034));
#32570=CARTESIAN_POINT('Ctrl Pts',(66.7849774198229,301.773605484375,53.6369099216174));
#32571=CARTESIAN_POINT('Ctrl Pts',(67.215612605763,301.596508912376,51.4747805783839));
#32572=CARTESIAN_POINT('Ctrl Pts',(67.6462477917031,301.419412340377,49.3126512351505));
#32573=CARTESIAN_POINT('Ctrl Pts',(69.0245064208056,301.242315768378,47.3568408855388));
#32574=CARTESIAN_POINT('Ctrl Pts',(70.9158061804572,301.06521919638,46.2240411771249));
#32575=CARTESIAN_POINT('Ctrl Pts',(72.8071059401089,300.888122624381,45.0912414687111));
#32576=CARTESIAN_POINT('Ctrl Pts',(75.181865969823,300.711026052382,44.7991699473061));
#32577=CARTESIAN_POINT('Ctrl Pts',(77.2912945088786,300.533929480384,45.4399204438793));
#32578=CARTESIAN_POINT('Ctrl Pts',(79.4007230479341,300.356832908385,46.0806709404525));
#32579=CARTESIAN_POINT('Ctrl Pts',(81.2118275942161,300.179736336386,47.6442218014034));
#32580=CARTESIAN_POINT('Ctrl Pts',(82.1535440633152,300.002639764387,49.6375657386275));
#32581=CARTESIAN_POINT('Ctrl Pts',(82.6515697929947,299.908982435045,50.6917435101896));
#32582=CARTESIAN_POINT('Ctrl Pts',(82.9129498948707,299.815325105703,51.8569119935507));
#32583=CARTESIAN_POINT('Ctrl Pts',(82.9129498948689,299.721667776361,53.0228109606478));
#32584=CARTESIAN_POINT('Origin',(74.9879498948689,255.,53.0228109606356));
#32585=CARTESIAN_POINT('',(82.9143689269116,294.278332223638,53.0158045639297));
#32586=CARTESIAN_POINT('',(82.9232745335521,295.721667776361,53.0227066122654));
#32587=CARTESIAN_POINT('',(82.9129498948689,255.,53.0228109606356));
#32588=CARTESIAN_POINT('Ctrl Pts',(82.9143689269116,294.278332223638,53.0158045639297));
#32589=CARTESIAN_POINT('Ctrl Pts',(82.9192260453689,294.322043009225,52.4722564462004));
#32590=CARTESIAN_POINT('Ctrl Pts',(82.867980282346,294.365753794812,51.929638208115));
#32591=CARTESIAN_POINT('Ctrl Pts',(82.7572016326311,294.409464580398,51.399459111527));
#32592=CARTESIAN_POINT('Ctrl Pts',(82.2195229807472,294.621620589951,48.8261655875135));
#32593=CARTESIAN_POINT('Ctrl Pts',(80.2793846172819,294.833776599503,46.5459100088442));
#32594=CARTESIAN_POINT('Ctrl Pts',(77.823092890938,295.045932609055,45.6075313705159));
#32595=CARTESIAN_POINT('Ctrl Pts',(75.3668011645943,295.258088618608,44.6691527321877));
#32596=CARTESIAN_POINT('Ctrl Pts',(72.394356075372,295.47024462816,45.0726510342002));
#32597=CARTESIAN_POINT('Ctrl Pts',(70.2792195264287,295.682400637712,46.6310662904978));
#32598=CARTESIAN_POINT('Ctrl Pts',(68.1640829774853,295.894556647265,48.1894815467954));
#32599=CARTESIAN_POINT('Ctrl Pts',(66.9062549688212,296.106712656817,50.9028137573782));
#32600=CARTESIAN_POINT('Ctrl Pts',(67.0689438525749,296.318868666369,53.5287336404149));
#32601=CARTESIAN_POINT('Ctrl Pts',(67.1502882944518,296.424946671145,54.8416935819331));
#32602=CARTESIAN_POINT('Ctrl Pts',(67.5867619594331,296.531024675921,56.1328004415649));
#32603=CARTESIAN_POINT('Ctrl Pts',(68.2943641356939,296.637102680698,57.2525775592319));
#32604=CARTESIAN_POINT('Ctrl Pts',(69.0019663119547,296.743180685474,58.372354676899));
#32605=CARTESIAN_POINT('Ctrl Pts',(69.9806969994951,296.84925869025,59.3208020526014));
#32606=CARTESIAN_POINT('Ctrl Pts',(71.1316116069641,296.955336695026,59.9578862641231));
#32607=CARTESIAN_POINT('Ctrl Pts',(73.4334408219021,297.167492704579,61.2320546871664));
#32608=CARTESIAN_POINT('Ctrl Pts',(76.4240057165548,297.379648714131,61.2607704534866));
#32609=CARTESIAN_POINT('Ctrl Pts',(78.7394956215055,297.591804723683,60.0194134412586));
#32610=CARTESIAN_POINT('Ctrl Pts',(81.0549855264564,297.803960733235,58.7780564290305));
#32611=CARTESIAN_POINT('Ctrl Pts',(82.6954004417052,298.016116742788,56.2666266382539));
#32612=CARTESIAN_POINT('Ctrl Pts',(82.9022950193089,298.22827275234,53.6453448625695));
#32613=CARTESIAN_POINT('Ctrl Pts',(82.9185676876959,298.244959242773,53.4391758581496));
#32614=CARTESIAN_POINT('Ctrl Pts',(82.925972407017,298.261645733205,53.2323272946183));
#32615=CARTESIAN_POINT('Ctrl Pts',(82.9247849645265,298.278332223638,53.0254077151713));
#32616=CARTESIAN_POINT('Ctrl Pts',(82.9066314816043,299.721667776361,53.0301977459941));
#32617=CARTESIAN_POINT('Ctrl Pts',(82.9139510729998,299.656562102834,53.8410766346259));
#32618=CARTESIAN_POINT('Ctrl Pts',(82.7999589108879,299.591456429307,54.6501502598461));
#32619=CARTESIAN_POINT('Ctrl Pts',(82.5566825623697,299.52635075578,55.4188133435249));
#32620=CARTESIAN_POINT('Ctrl Pts',(81.7639323069155,299.314194746227,57.9236102942205));
#32621=CARTESIAN_POINT('Ctrl Pts',(79.5983468365648,299.102038736675,59.9992981943577));
#32622=CARTESIAN_POINT('Ctrl Pts',(77.0602620358863,298.889882727123,60.6863564585103));
#32623=CARTESIAN_POINT('Ctrl Pts',(74.5221772352076,298.67772671757,61.373414722663));
#32624=CARTESIAN_POINT('Ctrl Pts',(71.6115931042009,298.465570708018,60.6718433508309));
#32625=CARTESIAN_POINT('Ctrl Pts',(69.6623542357921,298.253414698466,58.9079256295904));
#32626=CARTESIAN_POINT('Ctrl Pts',(67.7131153673835,298.041258688913,57.14400790835));
#32627=CARTESIAN_POINT('Ctrl Pts',(66.7252217615726,297.829102679361,54.3177438377017));
#32628=CARTESIAN_POINT('Ctrl Pts',(67.156146985339,297.616946669809,51.7238612333232));
#32629=CARTESIAN_POINT('Ctrl Pts',(67.5870722091055,297.404790660256,49.1299786289446));
#32630=CARTESIAN_POINT('Ctrl Pts',(69.4368162624498,297.192634650704,46.768477490836));
#32631=CARTESIAN_POINT('Ctrl Pts',(71.8502309745856,296.980478641152,45.7302626002747));
#32632=CARTESIAN_POINT('Ctrl Pts',(74.2636456867215,296.7683226316,44.6920477097135));
#32633=CARTESIAN_POINT('Ctrl Pts',(77.240731057649,296.556166622047,44.9771190666996));
#32634=CARTESIAN_POINT('Ctrl Pts',(79.4248119076536,296.344010612495,46.4439911625783));
#32635=CARTESIAN_POINT('Ctrl Pts',(80.5168523326559,296.237932607719,47.1774272105176));
#32636=CARTESIAN_POINT('Ctrl Pts',(81.4106416274275,296.131854602943,48.20631344318));
#32637=CARTESIAN_POINT('Ctrl Pts',(82.0196085258,296.025776598167,49.382647132992));
#32638=CARTESIAN_POINT('Ctrl Pts',(82.6015457092702,295.924406990898,50.5067678628704));
#32639=CARTESIAN_POINT('Ctrl Pts',(82.9233837151354,295.823037383629,51.7655372820001));
#32640=CARTESIAN_POINT('Ctrl Pts',(82.9232745335521,295.721667776361,53.0227066122654));
#32641=CARTESIAN_POINT('Origin',(74.9879498948689,255.,53.0228109606356));
#32642=CARTESIAN_POINT('',(82.9071525502277,290.278332223638,53.0227160994365));
#32643=CARTESIAN_POINT('',(82.9129498948689,291.721667776361,53.0228109606475));
#32644=CARTESIAN_POINT('',(82.9129498948689,255.,53.0228109606356));
#32645=CARTESIAN_POINT('Ctrl Pts',(82.9001557306105,290.278332223638,53.022601611389));
#32646=CARTESIAN_POINT('Ctrl Pts',(82.9013200738902,290.382440285244,51.7218986273144));
#32647=CARTESIAN_POINT('Ctrl Pts',(82.5989606688327,290.48654834685,50.4214083906554));
#32648=CARTESIAN_POINT('Ctrl Pts',(81.9908803767954,290.590656408457,49.2833762609638));
#32649=CARTESIAN_POINT('Ctrl Pts',(80.7517074803303,290.802812418009,46.9642440856787));
#32650=CARTESIAN_POINT('Ctrl Pts',(78.2429341375652,291.014968427562,45.3197693966668));
#32651=CARTESIAN_POINT('Ctrl Pts',(75.6241153631151,291.227124437114,45.1094150329749));
#32652=CARTESIAN_POINT('Ctrl Pts',(73.005296588665,291.439280446666,44.8990606692829));
#32653=CARTESIAN_POINT('Ctrl Pts',(70.27643238253,291.651436456218,46.1228266309109));
#32654=CARTESIAN_POINT('Ctrl Pts',(68.6773734189062,291.86359246577,48.2120689184108));
#32655=CARTESIAN_POINT('Ctrl Pts',(67.8778439370942,291.969670470547,49.2566900621608));
#32656=CARTESIAN_POINT('Ctrl Pts',(67.3607657659101,292.075748475323,50.5176802873789));
#32657=CARTESIAN_POINT('Ctrl Pts',(67.1607345872029,292.181826480099,51.8271035041599));
#32658=CARTESIAN_POINT('Ctrl Pts',(66.9607034084957,292.287904484875,53.1365267209409));
#32659=CARTESIAN_POINT('Ctrl Pts',(67.0777192222654,292.393982489651,54.4943829292848));
#32660=CARTESIAN_POINT('Ctrl Pts',(67.528902926771,292.500060494428,55.7300665421262));
#32661=CARTESIAN_POINT('Ctrl Pts',(68.431270335782,292.71221650398,58.2014337678088));
#32662=CARTESIAN_POINT('Ctrl Pts',(70.6703093077364,292.924372513532,60.1841106114811));
#32663=CARTESIAN_POINT('Ctrl Pts',(73.2324904412851,293.136528523085,60.7652203865009));
#32664=CARTESIAN_POINT('Ctrl Pts',(75.7946715748338,293.348684532637,61.3463301615208));
#32665=CARTESIAN_POINT('Ctrl Pts',(78.6799948699769,293.560840542189,60.5258728678884));
#32666=CARTESIAN_POINT('Ctrl Pts',(80.5550470473972,293.772996551741,58.6824784863933));
#32667=CARTESIAN_POINT('Ctrl Pts',(82.0437797240675,293.941441775707,57.2188811077338));
#32668=CARTESIAN_POINT('Ctrl Pts',(82.8956513862547,294.109886999672,55.1104382612587));
#32669=CARTESIAN_POINT('Ctrl Pts',(82.9143689269116,294.278332223638,53.0158045639297));
#32670=CARTESIAN_POINT('Ctrl Pts',(82.9232745335521,295.721667776361,53.0227066122654));
#32671=CARTESIAN_POINT('Ctrl Pts',(82.9232694623053,295.716959378853,53.0810993899503));
#32672=CARTESIAN_POINT('Ctrl Pts',(82.9225698221323,295.712250981346,53.1394887156031));
#32673=CARTESIAN_POINT('Ctrl Pts',(82.921169415458,295.707542583838,53.1978609362051));
#32674=CARTESIAN_POINT('Ctrl Pts',(82.8580683940824,295.495386574286,55.8280588690849));
#32675=CARTESIAN_POINT('Ctrl Pts',(81.372187322062,295.283230564733,58.4235280798784));
#32676=CARTESIAN_POINT('Ctrl Pts',(79.1311979724809,295.071074555181,59.794814872202));
#32677=CARTESIAN_POINT('Ctrl Pts',(76.8902086228999,294.858918545629,61.1661016645256));
#32678=CARTESIAN_POINT('Ctrl Pts',(73.8941109957582,294.646762536076,61.3132060383795));
#32679=CARTESIAN_POINT('Ctrl Pts',(71.5273403904603,294.434606526524,60.1676404943475));
#32680=CARTESIAN_POINT('Ctrl Pts',(69.1605697851623,294.222450516972,59.0220749503154));
#32681=CARTESIAN_POINT('Ctrl Pts',(67.4231262017078,294.010294507419,56.5838394883976));
#32682=CARTESIAN_POINT('Ctrl Pts',(67.1081058109006,293.798138497867,53.9739161089098));
#32683=CARTESIAN_POINT('Ctrl Pts',(66.7930854200933,293.585982488315,51.363992729422));
#32684=CARTESIAN_POINT('Ctrl Pts',(67.9004882219333,293.373826478763,48.5823814323644));
#32685=CARTESIAN_POINT('Ctrl Pts',(69.9267165549782,293.16167046921,46.9065764746971));
#32686=CARTESIAN_POINT('Ctrl Pts',(71.952944888023,292.949514459658,45.2307715170298));
#32687=CARTESIAN_POINT('Ctrl Pts',(74.8979987522728,292.737358450105,44.6607728987527));
#32688=CARTESIAN_POINT('Ctrl Pts',(77.4009069250342,292.525202440553,45.4594664635574));
#32689=CARTESIAN_POINT('Ctrl Pts',(79.9038150977957,292.313046431001,46.2581600283622));
#32690=CARTESIAN_POINT('Ctrl Pts',(81.9645775790689,292.100890421449,48.4255457762487));
#32691=CARTESIAN_POINT('Ctrl Pts',(82.6516841256833,291.888734411896,50.9651928971345));
#32692=CARTESIAN_POINT('Ctrl Pts',(82.8320428771505,291.833045533384,51.6318254392738));
#32693=CARTESIAN_POINT('Ctrl Pts',(82.9177551992494,291.777356654873,52.324107206126));
#32694=CARTESIAN_POINT('Ctrl Pts',(82.9134059933203,291.721667776361,53.0176571633937));
#32695=CARTESIAN_POINT('Origin',(74.9879498948689,255.,53.0228109606356));
#32696=CARTESIAN_POINT('',(82.9129498948689,286.278332223638,53.0228109606342));
#32697=CARTESIAN_POINT('',(82.9078622521729,287.721667776361,53.0229211557408));
#32698=CARTESIAN_POINT('',(82.9129498948689,255.,53.0228109606356));
#32699=CARTESIAN_POINT('Ctrl Pts',(82.9129498948689,286.278332223638,53.0228109606342));
#32700=CARTESIAN_POINT('Ctrl Pts',(82.9129498948685,286.455428795637,50.8182135007243));
#32701=CARTESIAN_POINT('Ctrl Pts',(81.9432795991099,286.632525367635,48.6308565362883));
#32702=CARTESIAN_POINT('Ctrl Pts',(80.3096882702532,286.809621939634,47.1504412801776));
#32703=CARTESIAN_POINT('Ctrl Pts',(78.6760969413965,286.986718511633,45.670026024067));
#32704=CARTESIAN_POINT('Ctrl Pts',(76.4041347530431,287.163815083632,44.9197069006028));
#32705=CARTESIAN_POINT('Ctrl Pts',(74.2101800112206,287.34091165563,45.1360689838691));
#32706=CARTESIAN_POINT('Ctrl Pts',(72.0162252693981,287.518008227629,45.3524310671354));
#32707=CARTESIAN_POINT('Ctrl Pts',(69.9345925076968,287.695104799628,46.5320903475022));
#32708=CARTESIAN_POINT('Ctrl Pts',(68.6216467656599,287.872201371626,48.3030853894795));
#32709=CARTESIAN_POINT('Ctrl Pts',(67.3087010236231,288.049297943625,50.0740804314568));
#32710=CARTESIAN_POINT('Ctrl Pts',(66.7849774198238,288.226394515624,52.4087119996421));
#32711=CARTESIAN_POINT('Ctrl Pts',(67.2156126057608,288.403491087623,54.5708413428762));
#32712=CARTESIAN_POINT('Ctrl Pts',(67.6462477916978,288.580587659621,56.7329706861103));
#32713=CARTESIAN_POINT('Ctrl Pts',(69.0245064207976,288.75768423162,58.6887810357239));
#32714=CARTESIAN_POINT('Ctrl Pts',(70.9158061804476,288.934780803619,59.8215807441404));
#32715=CARTESIAN_POINT('Ctrl Pts',(72.8071059400976,289.111877375618,60.954380452557));
#32716=CARTESIAN_POINT('Ctrl Pts',(75.1818659698113,289.288973947616,61.2464519739654));
#32717=CARTESIAN_POINT('Ctrl Pts',(77.2912945088678,289.466070519615,60.6057014773951));
#32718=CARTESIAN_POINT('Ctrl Pts',(79.4007230479243,289.643167091614,59.9649509808249));
#32719=CARTESIAN_POINT('Ctrl Pts',(81.2118275942084,289.820263663613,58.4014001198766));
#32720=CARTESIAN_POINT('Ctrl Pts',(82.1535440633104,289.997360235611,56.4080561826538));
#32721=CARTESIAN_POINT('Ctrl Pts',(82.6515697929914,290.091017564953,55.3538784110924));
#32722=CARTESIAN_POINT('Ctrl Pts',(82.9129498948691,290.184674894296,54.1887099277315));
#32723=CARTESIAN_POINT('Ctrl Pts',(82.9129498948689,290.278332223638,53.0228109606343));
#32724=CARTESIAN_POINT('Ctrl Pts',(82.9129498948689,291.721667776361,53.0228109606475));
#32725=CARTESIAN_POINT('Ctrl Pts',(82.9129498948656,291.544571204362,55.2274084205573));
#32726=CARTESIAN_POINT('Ctrl Pts',(81.9432795991041,291.367474632363,57.4147653849921));
#32727=CARTESIAN_POINT('Ctrl Pts',(80.3096882702454,291.190378060365,58.8951806411006));
#32728=CARTESIAN_POINT('Ctrl Pts',(78.6760969413868,291.013281488366,60.3755958972091));
#32729=CARTESIAN_POINT('Ctrl Pts',(76.4041347530324,290.836184916367,61.1259150206702));
#32730=CARTESIAN_POINT('Ctrl Pts',(74.2101800112101,290.659088344368,60.909552937401));
#32731=CARTESIAN_POINT('Ctrl Pts',(72.0162252693879,290.48199177237,60.6931908541318));
#32732=CARTESIAN_POINT('Ctrl Pts',(69.9345925076882,290.304895200371,59.5135315737622));
#32733=CARTESIAN_POINT('Ctrl Pts',(68.6216467656537,290.127798628372,57.7425365317832));
#32734=CARTESIAN_POINT('Ctrl Pts',(67.3087010236192,289.950702056373,55.9715414898041));
#32735=CARTESIAN_POINT('Ctrl Pts',(66.784977419823,289.773605484375,53.6369099216182));
#32736=CARTESIAN_POINT('Ctrl Pts',(67.2156126057629,289.596508912376,51.4747805783847));
#32737=CARTESIAN_POINT('Ctrl Pts',(67.6462477917027,289.419412340377,49.3126512351511));
#32738=CARTESIAN_POINT('Ctrl Pts',(69.0245064208051,289.242315768378,47.3568408855393));
#32739=CARTESIAN_POINT('Ctrl Pts',(70.9158061804566,289.06521919638,46.2240411771253));
#32740=CARTESIAN_POINT('Ctrl Pts',(72.8071059401081,288.888122624381,45.0912414687113));
#32741=CARTESIAN_POINT('Ctrl Pts',(75.1818659698222,288.711026052382,44.799169947306));
#32742=CARTESIAN_POINT('Ctrl Pts',(77.2912945088778,288.533929480384,45.439920443879));
#32743=CARTESIAN_POINT('Ctrl Pts',(79.4007230479335,288.356832908385,46.080670940452));
#32744=CARTESIAN_POINT('Ctrl Pts',(81.2118275942156,288.179736336386,47.6442218014028));
#32745=CARTESIAN_POINT('Ctrl Pts',(82.1535440633149,288.002639764387,49.6375657386269));
#32746=CARTESIAN_POINT('Ctrl Pts',(82.6515697929945,287.908982435045,50.691743510189));
#32747=CARTESIAN_POINT('Ctrl Pts',(82.9129498948707,287.815325105703,51.8569119935502));
#32748=CARTESIAN_POINT('Ctrl Pts',(82.9129498948689,287.721667776361,53.0228109606475));
#32749=CARTESIAN_POINT('Origin',(74.9879498948689,255.,53.0228109606356));
#32750=CARTESIAN_POINT('',(82.9192650697738,282.278332223638,53.0203619272188));
#32751=CARTESIAN_POINT('',(82.9146235913291,283.721667776361,53.0253669122659));
#32752=CARTESIAN_POINT('',(82.9129498948689,255.,53.0228109606356));
#32753=CARTESIAN_POINT('Ctrl Pts',(82.9129498948689,282.278332223638,53.022810960634));
#32754=CARTESIAN_POINT('Ctrl Pts',(82.9129498948684,282.455428795637,50.8182135007241));
#32755=CARTESIAN_POINT('Ctrl Pts',(81.9432795991097,282.632525367635,48.630856536288));
#32756=CARTESIAN_POINT('Ctrl Pts',(80.3096882702529,282.809621939634,47.1504412801773));
#32757=CARTESIAN_POINT('Ctrl Pts',(78.6760969413961,282.986718511633,45.6700260240667));
#32758=CARTESIAN_POINT('Ctrl Pts',(76.4041347530426,283.163815083632,44.9197069006027));
#32759=CARTESIAN_POINT('Ctrl Pts',(74.21018001122,283.34091165563,45.1360689838692));
#32760=CARTESIAN_POINT('Ctrl Pts',(72.0162252693974,283.518008227629,45.3524310671357));
#32761=CARTESIAN_POINT('Ctrl Pts',(69.9345925076962,283.695104799628,46.5320903475027));
#32762=CARTESIAN_POINT('Ctrl Pts',(68.6216467656594,283.872201371627,48.3030853894802));
#32763=CARTESIAN_POINT('Ctrl Pts',(67.3087010236227,284.049297943625,50.0740804314577));
#32764=CARTESIAN_POINT('Ctrl Pts',(66.7849774198237,284.226394515624,52.4087119996431));
#32765=CARTESIAN_POINT('Ctrl Pts',(67.215612605761,284.403491087623,54.5708413428772));
#32766=CARTESIAN_POINT('Ctrl Pts',(67.6462477916984,284.580587659622,56.7329706861113));
#32767=CARTESIAN_POINT('Ctrl Pts',(69.0245064207984,284.75768423162,58.6887810357248));
#32768=CARTESIAN_POINT('Ctrl Pts',(70.9158061804487,284.934780803619,59.8215807441411));
#32769=CARTESIAN_POINT('Ctrl Pts',(72.807105940099,285.111877375618,60.9543804525574));
#32770=CARTESIAN_POINT('Ctrl Pts',(75.1818659698128,285.288973947616,61.2464519739653));
#32771=CARTESIAN_POINT('Ctrl Pts',(77.2912945088692,285.466070519615,60.6057014773947));
#32772=CARTESIAN_POINT('Ctrl Pts',(79.4007230479257,285.643167091614,59.9649509808241));
#32773=CARTESIAN_POINT('Ctrl Pts',(81.2118275942096,285.820263663613,58.4014001198753));
#32774=CARTESIAN_POINT('Ctrl Pts',(82.1535440633112,285.997360235611,56.4080561826522));
#32775=CARTESIAN_POINT('Ctrl Pts',(82.6515697929917,286.091017564954,55.3538784110912));
#32776=CARTESIAN_POINT('Ctrl Pts',(82.9129498948691,286.184674894296,54.1887099277309));
#32777=CARTESIAN_POINT('Ctrl Pts',(82.9129498948689,286.278332223638,53.0228109606342));
#32778=CARTESIAN_POINT('Ctrl Pts',(82.8973468488884,287.721667776361,53.0231489126204));
#32779=CARTESIAN_POINT('Ctrl Pts',(82.8989520065444,287.62559792134,54.2230004198988));
#32780=CARTESIAN_POINT('Ctrl Pts',(82.6424763919888,287.529528066319,55.4223533881397));
#32781=CARTESIAN_POINT('Ctrl Pts',(82.1232866064541,287.433458211298,56.49463821269));
#32782=CARTESIAN_POINT('Ctrl Pts',(81.5500098326146,287.327380206522,57.6786291192565));
#32783=CARTESIAN_POINT('Ctrl Pts',(80.6564308644769,287.221302201745,58.7076980240982));
#32784=CARTESIAN_POINT('Ctrl Pts',(79.5769703194514,287.115224196969,59.4754001569812));
#32785=CARTESIAN_POINT('Ctrl Pts',(78.497509774426,287.009146192193,60.2431022898643));
#32786=CARTESIAN_POINT('Ctrl Pts',(77.2321676525127,286.903068187417,60.7494376507887));
#32787=CARTESIAN_POINT('Ctrl Pts',(75.9256098672663,286.796990182641,60.9023673080429));
#32788=CARTESIAN_POINT('Ctrl Pts',(73.3124942967733,286.584834173088,61.2082266225512));
#32789=CARTESIAN_POINT('Ctrl Pts',(70.5345160729474,286.372678163536,60.1004631223783));
#32790=CARTESIAN_POINT('Ctrl Pts',(68.8629096503185,286.160522153984,58.0735954159003));
#32791=CARTESIAN_POINT('Ctrl Pts',(67.1913032276897,285.948366144431,56.0467277094226));
#32792=CARTESIAN_POINT('Ctrl Pts',(66.6260686062576,285.736210134879,53.10075579664));
#32793=CARTESIAN_POINT('Ctrl Pts',(67.4288976409122,285.524054125327,50.5968809884894));
#32794=CARTESIAN_POINT('Ctrl Pts',(68.2317266755669,285.311898115775,48.0930061803387));
#32795=CARTESIAN_POINT('Ctrl Pts',(70.4026193663083,285.099742106222,46.0312284768201));
#32796=CARTESIAN_POINT('Ctrl Pts',(72.9427072516828,284.88758609667,45.3538132216075));
#32797=CARTESIAN_POINT('Ctrl Pts',(75.4827951370574,284.675430087118,44.6763979663949));
#32798=CARTESIAN_POINT('Ctrl Pts',(78.3920782170651,284.463274077565,45.3833451594885));
#32799=CARTESIAN_POINT('Ctrl Pts',(80.335126355604,284.251118068013,47.1549228306892));
#32800=CARTESIAN_POINT('Ctrl Pts',(81.9514642662677,284.074634637462,48.6286218579301));
#32801=CARTESIAN_POINT('Ctrl Pts',(82.8991812941406,283.898151206912,50.8390300845257));
#32802=CARTESIAN_POINT('Ctrl Pts',(82.9187310422535,283.721667776361,53.0316395226755));
#32803=CARTESIAN_POINT('Origin',(74.9879498948689,255.,53.0228109606356));
#32804=CARTESIAN_POINT('',(82.909752682909,278.278332223638,53.0216597493918));
#32805=CARTESIAN_POINT('',(82.9157046094419,279.721667776361,53.0210340633603));
#32806=CARTESIAN_POINT('',(82.9129498948689,255.,53.0228109606356));
#32807=CARTESIAN_POINT('Ctrl Pts',(82.9009419360392,278.278332223638,53.0184872882153));
#32808=CARTESIAN_POINT('Ctrl Pts',(82.9066125316817,278.35147610375,52.1059266595105));
#32809=CARTESIAN_POINT('Ctrl Pts',(82.7609970955639,278.424619983862,51.1948597659628));
#32810=CARTESIAN_POINT('Ctrl Pts',(82.4560394698546,278.497763863975,50.340600574444));
#32811=CARTESIAN_POINT('Ctrl Pts',(82.0137701176292,278.603841868751,49.1016984207862));
#32812=CARTESIAN_POINT('Ctrl Pts',(81.2363613746537,278.709919873527,47.9822781111815));
#32813=CARTESIAN_POINT('Ctrl Pts',(80.2459726342748,278.815997878304,47.1026578658311));
#32814=CARTESIAN_POINT('Ctrl Pts',(79.2555838938957,278.92207588308,46.2230376204805));
#32815=CARTESIAN_POINT('Ctrl Pts',(78.0522151561131,279.028153887856,45.5832174393843));
#32816=CARTESIAN_POINT('Ctrl Pts',(76.7697647029933,279.134231892632,45.2902984035587));
#32817=CARTESIAN_POINT('Ctrl Pts',(74.204863796754,279.346387902184,44.7044603319075));
#32818=CARTESIAN_POINT('Ctrl Pts',(71.3236360291661,279.558543911736,45.5062268413383));
#32819=CARTESIAN_POINT('Ctrl Pts',(69.4432262686172,279.770699921289,47.3410346961746));
#32820=CARTESIAN_POINT('Ctrl Pts',(67.5628165080682,279.982855930841,49.1758425510109));
#32821=CARTESIAN_POINT('Ctrl Pts',(66.6832247545584,280.195011940393,52.0436917512528));
#32822=CARTESIAN_POINT('Ctrl Pts',(67.2113901299962,280.407167949946,54.6195343027231));
#32823=CARTESIAN_POINT('Ctrl Pts',(67.739555505434,280.619323959498,57.1953768541933));
#32824=CARTESIAN_POINT('Ctrl Pts',(69.6754780098195,280.83147996905,59.4792127568922));
#32825=CARTESIAN_POINT('Ctrl Pts',(72.1277135814771,281.043635978603,60.4265662255183));
#32826=CARTESIAN_POINT('Ctrl Pts',(74.5799491531347,281.255791988155,61.3739196941445));
#32827=CARTESIAN_POINT('Ctrl Pts',(77.5484977920643,281.467947997707,60.9847907286983));
#32828=CARTESIAN_POINT('Ctrl Pts',(79.6712397802176,281.68010400726,59.4330530042401));
#32829=CARTESIAN_POINT('Ctrl Pts',(81.6664447178233,281.879513412719,57.9745456646827));
#32830=CARTESIAN_POINT('Ctrl Pts',(82.9144241339818,282.078922818178,55.4889348666762));
#32831=CARTESIAN_POINT('Ctrl Pts',(82.9255991990642,282.278332223638,53.0179055432671));
#32832=CARTESIAN_POINT('Ctrl Pts',(82.9129498948689,283.721667776361,53.0228109606471));
#32833=CARTESIAN_POINT('Ctrl Pts',(82.9129498948657,283.544571204362,55.227408420557));
#32834=CARTESIAN_POINT('Ctrl Pts',(81.9432795991042,283.367474632363,57.414765384992));
#32835=CARTESIAN_POINT('Ctrl Pts',(80.3096882702455,283.190378060365,58.8951806411005));
#32836=CARTESIAN_POINT('Ctrl Pts',(78.6760969413868,283.013281488366,60.3755958972091));
#32837=CARTESIAN_POINT('Ctrl Pts',(76.4041347530324,282.836184916367,61.1259150206702));
#32838=CARTESIAN_POINT('Ctrl Pts',(74.21018001121,282.659088344368,60.909552937401));
#32839=CARTESIAN_POINT('Ctrl Pts',(72.0162252693877,282.48199177237,60.6931908541317));
#32840=CARTESIAN_POINT('Ctrl Pts',(69.934592507688,282.304895200371,59.513531573762));
#32841=CARTESIAN_POINT('Ctrl Pts',(68.6216467656535,282.127798628372,57.7425365317829));
#32842=CARTESIAN_POINT('Ctrl Pts',(67.308701023619,281.950702056373,55.9715414898037));
#32843=CARTESIAN_POINT('Ctrl Pts',(66.7849774198229,281.773605484375,53.6369099216177));
#32844=CARTESIAN_POINT('Ctrl Pts',(67.215612605763,281.596508912376,51.4747805783841));
#32845=CARTESIAN_POINT('Ctrl Pts',(67.646247791703,281.419412340377,49.3126512351505));
#32846=CARTESIAN_POINT('Ctrl Pts',(69.0245064208056,281.242315768378,47.3568408855388));
#32847=CARTESIAN_POINT('Ctrl Pts',(70.9158061804573,281.06521919638,46.2240411771249));
#32848=CARTESIAN_POINT('Ctrl Pts',(72.807105940109,280.888122624381,45.091241468711));
#32849=CARTESIAN_POINT('Ctrl Pts',(75.1818659698232,280.711026052382,44.799169947306));
#32850=CARTESIAN_POINT('Ctrl Pts',(77.2912945088788,280.533929480384,45.4399204438793));
#32851=CARTESIAN_POINT('Ctrl Pts',(79.4007230479344,280.356832908385,46.0806709404526));
#32852=CARTESIAN_POINT('Ctrl Pts',(81.2118275942164,280.179736336386,47.6442218014037));
#32853=CARTESIAN_POINT('Ctrl Pts',(82.1535440633154,280.002639764387,49.637565738628));
#32854=CARTESIAN_POINT('Ctrl Pts',(82.6515697929947,279.908982435045,50.6917435101897));
#32855=CARTESIAN_POINT('Ctrl Pts',(82.9129498948706,279.815325105703,51.8569119935504));
#32856=CARTESIAN_POINT('Ctrl Pts',(82.9129498948689,279.721667776361,53.0228109606472));
#32857=CARTESIAN_POINT('Origin',(74.9879498948689,255.,53.0228109606356));
#32858=CARTESIAN_POINT('',(82.9129498948689,274.278332223638,53.0228109606336));
#32859=CARTESIAN_POINT('',(82.9018331595289,275.721667776361,53.0187249907903));
#32860=CARTESIAN_POINT('',(82.9129498948689,255.,53.0228109606356));
#32861=CARTESIAN_POINT('Ctrl Pts',(82.9129498948689,274.278332223638,53.0228109606334));
#32862=CARTESIAN_POINT('Ctrl Pts',(82.9129498948683,274.455428795637,50.8182135007235));
#32863=CARTESIAN_POINT('Ctrl Pts',(81.9432795991094,274.632525367635,48.6308565362875));
#32864=CARTESIAN_POINT('Ctrl Pts',(80.3096882702525,274.809621939634,47.150441280177));
#32865=CARTESIAN_POINT('Ctrl Pts',(78.6760969413956,274.986718511633,45.6700260240665));
#32866=CARTESIAN_POINT('Ctrl Pts',(76.404134753042,275.163815083632,44.9197069006026));
#32867=CARTESIAN_POINT('Ctrl Pts',(74.2101800112194,275.34091165563,45.1360689838693));
#32868=CARTESIAN_POINT('Ctrl Pts',(72.0162252693968,275.518008227629,45.3524310671359));
#32869=CARTESIAN_POINT('Ctrl Pts',(69.9345925076957,275.695104799628,46.5320903475031));
#32870=CARTESIAN_POINT('Ctrl Pts',(68.6216467656591,275.872201371627,48.3030853894807));
#32871=CARTESIAN_POINT('Ctrl Pts',(67.3087010236225,276.049297943625,50.0740804314583));
#32872=CARTESIAN_POINT('Ctrl Pts',(66.7849774198237,276.226394515624,52.4087119996437));
#32873=CARTESIAN_POINT('Ctrl Pts',(67.2156126057612,276.403491087623,54.5708413428778));
#32874=CARTESIAN_POINT('Ctrl Pts',(67.6462477916986,276.580587659622,56.7329706861119));
#32875=CARTESIAN_POINT('Ctrl Pts',(69.0245064207988,276.75768423162,58.6887810357253));
#32876=CARTESIAN_POINT('Ctrl Pts',(70.9158061804492,276.934780803619,59.8215807441414));
#32877=CARTESIAN_POINT('Ctrl Pts',(72.8071059400995,277.111877375618,60.9543804525575));
#32878=CARTESIAN_POINT('Ctrl Pts',(75.1818659698134,277.288973947617,61.2464519739653));
#32879=CARTESIAN_POINT('Ctrl Pts',(77.2912945088698,277.466070519615,60.6057014773945));
#32880=CARTESIAN_POINT('Ctrl Pts',(79.4007230479262,277.643167091614,59.9649509808237));
#32881=CARTESIAN_POINT('Ctrl Pts',(81.21182759421,277.820263663613,58.4014001198748));
#32882=CARTESIAN_POINT('Ctrl Pts',(82.1535440633114,277.997360235611,56.4080561826517));
#32883=CARTESIAN_POINT('Ctrl Pts',(82.6515697929918,278.091017564954,55.3538784110907));
#32884=CARTESIAN_POINT('Ctrl Pts',(82.9129498948692,278.184674894296,54.1887099277304));
#32885=CARTESIAN_POINT('Ctrl Pts',(82.9129498948689,278.278332223638,53.0228109606338));
#32886=CARTESIAN_POINT('Ctrl Pts',(82.9221926362458,279.721667776361,53.01684903544));
#32887=CARTESIAN_POINT('Ctrl Pts',(82.9041921061136,279.534236463826,55.343761083048));
#32888=CARTESIAN_POINT('Ctrl Pts',(81.8191527316485,279.346805151292,57.6866115007869));
#32889=CARTESIAN_POINT('Ctrl Pts',(80.0249961549487,279.159373838757,59.1591540560566));
#32890=CARTESIAN_POINT('Ctrl Pts',(77.9941663289309,278.947217829205,60.825944669629));
#32891=CARTESIAN_POINT('Ctrl Pts',(75.0547957671856,278.735061819653,61.3776725782135));
#32892=CARTESIAN_POINT('Ctrl Pts',(72.5495833248604,278.5229058101,60.574034896268));
#32893=CARTESIAN_POINT('Ctrl Pts',(71.2969771036978,278.416827805324,60.1722160552952));
#32894=CARTESIAN_POINT('Ctrl Pts',(70.1529104123901,278.310749800548,59.43155581669));
#32895=CARTESIAN_POINT('Ctrl Pts',(69.2416036151328,278.204671795772,58.4702434042181));
#32896=CARTESIAN_POINT('Ctrl Pts',(68.3302968178754,278.098593790996,57.5089309917462));
#32897=CARTESIAN_POINT('Ctrl Pts',(67.6517499146684,277.99251578622,56.3269664054077));
#32898=CARTESIAN_POINT('Ctrl Pts',(67.3173541659037,277.886437781444,55.0547006275673));
#32899=CARTESIAN_POINT('Ctrl Pts',(66.6485626683742,277.674281771891,52.5101690718864));
#32900=CARTESIAN_POINT('Ctrl Pts',(67.3563757886142,277.462125762339,49.6044327501977));
#32901=CARTESIAN_POINT('Ctrl Pts',(69.1291745043439,277.249969752787,47.6654522332136));
#32902=CARTESIAN_POINT('Ctrl Pts',(70.9019732200736,277.037813743234,45.7264717162295));
#32903=CARTESIAN_POINT('Ctrl Pts',(73.7397575312933,276.825657733682,44.75424700395));
#32904=CARTESIAN_POINT('Ctrl Pts',(76.3313879059252,276.613501724129,45.1985166462418));
#32905=CARTESIAN_POINT('Ctrl Pts',(78.9230182805569,276.401345714577,45.6427862885337));
#32906=CARTESIAN_POINT('Ctrl Pts',(81.2684947186008,276.189189705025,47.5035502853966));
#32907=CARTESIAN_POINT('Ctrl Pts',(82.2949537237807,275.977033695473,49.9237403201058));
#32908=CARTESIAN_POINT('Ctrl Pts',(82.7067931807312,275.891911722436,50.8947773947302));
#32909=CARTESIAN_POINT('Ctrl Pts',(82.9062968379203,275.806789749398,51.9558710313029));
#32910=CARTESIAN_POINT('Ctrl Pts',(82.9018331595289,275.721667776361,53.0187249907903));
#32911=CARTESIAN_POINT('Origin',(74.9879498948689,255.,53.0228109606356));
#32912=CARTESIAN_POINT('',(82.913981855057,270.278332223638,53.0234548561531));
#32913=CARTESIAN_POINT('',(82.9063872485843,271.721667776361,53.029301811537));
#32914=CARTESIAN_POINT('',(82.9129498948689,255.,53.0228109606356));
#32915=CARTESIAN_POINT('Ctrl Pts',(82.9196569564088,270.278332223638,53.0269958574522));
#32916=CARTESIAN_POINT('Ctrl Pts',(82.9025226301854,270.472270655789,50.6202397052844));
#32917=CARTESIAN_POINT('Ctrl Pts',(81.7386913771929,270.66620908794,48.2041551979614));
#32918=CARTESIAN_POINT('Ctrl Pts',(79.8372404750172,270.860147520091,46.7370395298412));
#32919=CARTESIAN_POINT('Ctrl Pts',(77.7571770688595,271.072303529644,45.1321105725038));
#32920=CARTESIAN_POINT('Ctrl Pts',(74.7944090565747,271.284459539196,44.6628064136153));
#32921=CARTESIAN_POINT('Ctrl Pts',(72.3179154280297,271.496615548749,45.5464934744867));
#32922=CARTESIAN_POINT('Ctrl Pts',(69.8414217994845,271.708771558301,46.4301805353582));
#32923=CARTESIAN_POINT('Ctrl Pts',(67.8512025546794,271.920927567853,48.6668588159898));
#32924=CARTESIAN_POINT('Ctrl Pts',(67.2566010192954,272.133083577405,51.2275983395534));
#32925=CARTESIAN_POINT('Ctrl Pts',(66.6619994839114,272.345239586957,53.7883378631168));
#32926=CARTESIAN_POINT('Ctrl Pts',(67.4630156579487,272.55739559651,56.6731386296124));
#32927=CARTESIAN_POINT('Ctrl Pts',(69.296735155505,272.769551606062,58.5576535056635));
#32928=CARTESIAN_POINT('Ctrl Pts',(71.1304546530613,272.981707615615,60.4421683817145));
#32929=CARTESIAN_POINT('Ctrl Pts',(73.9968774741368,273.193863625167,61.3263973673213));
#32930=CARTESIAN_POINT('Ctrl Pts',(76.5713131144536,273.406019634719,60.8022391225105));
#32931=CARTESIAN_POINT('Ctrl Pts',(79.1457487547705,273.618175644271,60.2780808776997));
#32932=CARTESIAN_POINT('Ctrl Pts',(81.4281972143287,273.830331653824,58.3455354024713));
#32933=CARTESIAN_POINT('Ctrl Pts',(82.3851379460284,274.042487663376,55.8947829994249));
#32934=CARTESIAN_POINT('Ctrl Pts',(82.7397343372101,274.121102516797,54.986651566607));
#32935=CARTESIAN_POINT('Ctrl Pts',(82.9123267816282,274.199717370217,54.0073657345194));
#32936=CARTESIAN_POINT('Ctrl Pts',(82.9083427687154,274.278332223638,53.0265063581188));
#32937=CARTESIAN_POINT('Ctrl Pts',(82.9018331595289,275.721667776361,53.0187249907903));
#32938=CARTESIAN_POINT('Ctrl Pts',(82.8951716705674,275.594633739846,54.6049033168082));
#32939=CARTESIAN_POINT('Ctrl Pts',(82.4342366264749,275.467599703331,56.1950022124917));
#32940=CARTESIAN_POINT('Ctrl Pts',(81.5468431519361,275.340565666816,57.4955423912273));
#32941=CARTESIAN_POINT('Ctrl Pts',(80.0648320025961,275.128409657263,59.6675383550835));
#32942=CARTESIAN_POINT('Ctrl Pts',(77.3933681316007,274.916253647711,61.0319142102403));
#32943=CARTESIAN_POINT('Ctrl Pts',(74.7671359794171,274.704097638159,60.9586652199859));
#32944=CARTESIAN_POINT('Ctrl Pts',(72.1409038272333,274.491941628607,60.8854162297315));
#32945=CARTESIAN_POINT('Ctrl Pts',(69.5599033938615,274.279785619055,59.3745423940656));
#32946=CARTESIAN_POINT('Ctrl Pts',(68.1954420945736,274.067629609502,57.1250606164622));
#32947=CARTESIAN_POINT('Ctrl Pts',(67.5132114449297,273.961551604726,56.0003197276606));
#32948=CARTESIAN_POINT('Ctrl Pts',(67.1351155788067,273.855473599949,54.6909268533747));
#32949=CARTESIAN_POINT('Ctrl Pts',(67.0774405885565,273.749395595173,53.3675692945118));
#32950=CARTESIAN_POINT('Ctrl Pts',(67.0197655983062,273.643317590397,52.0442117356488));
#32951=CARTESIAN_POINT('Ctrl Pts',(67.2825114839288,273.537239585621,50.7068894922089));
#32952=CARTESIAN_POINT('Ctrl Pts',(67.8643035947425,273.431161580845,49.5270595612226));
#32953=CARTESIAN_POINT('Ctrl Pts',(69.0278878163698,273.219005571293,47.1673996992501));
#32954=CARTESIAN_POINT('Ctrl Pts',(71.4676569387615,273.00684956174,45.437709087092));
#32955=CARTESIAN_POINT('Ctrl Pts',(74.0775587598043,272.794693552188,45.1362572397698));
#32956=CARTESIAN_POINT('Ctrl Pts',(76.687460580847,272.582537542635,44.8348053924476));
#32957=CARTESIAN_POINT('Ctrl Pts',(79.4674951005409,272.370381533084,45.9615923099614));
#32958=CARTESIAN_POINT('Ctrl Pts',(81.1328493245277,272.158225523531,47.9964187945602));
#32959=CARTESIAN_POINT('Ctrl Pts',(82.2751271068042,272.012706274475,49.3921201118334));
#32960=CARTESIAN_POINT('Ctrl Pts',(82.8929833295828,271.867187025418,51.2150251104585));
#32961=CARTESIAN_POINT('Ctrl Pts',(82.9063872485843,271.721667776361,53.029301811537));
#32962=CARTESIAN_POINT('Origin',(74.9879498948689,255.,53.0228109606356));
#32963=CARTESIAN_POINT('',(82.9129498948689,266.278332223638,53.0228109606333));
#32964=CARTESIAN_POINT('',(82.918336458848,267.721667776361,53.0238104703768));
#32965=CARTESIAN_POINT('',(82.9129498948689,255.,53.0228109606356));
#32966=CARTESIAN_POINT('Ctrl Pts',(82.9129498948689,266.278332223638,53.0228109606331));
#32967=CARTESIAN_POINT('Ctrl Pts',(82.9129498948682,266.455428795637,50.8182135007232));
#32968=CARTESIAN_POINT('Ctrl Pts',(81.9432795991092,266.632525367635,48.6308565362872));
#32969=CARTESIAN_POINT('Ctrl Pts',(80.3096882702523,266.809621939634,47.1504412801767));
#32970=CARTESIAN_POINT('Ctrl Pts',(78.6760969413953,266.986718511633,45.6700260240663));
#32971=CARTESIAN_POINT('Ctrl Pts',(76.4041347530416,267.163815083632,44.9197069006026));
#32972=CARTESIAN_POINT('Ctrl Pts',(74.2101800112191,267.34091165563,45.1360689838693));
#32973=CARTESIAN_POINT('Ctrl Pts',(72.0162252693965,267.518008227629,45.352431067136));
#32974=CARTESIAN_POINT('Ctrl Pts',(69.9345925076954,267.695104799628,46.5320903475033));
#32975=CARTESIAN_POINT('Ctrl Pts',(68.6216467656589,267.872201371627,48.303085389481));
#32976=CARTESIAN_POINT('Ctrl Pts',(67.3087010236224,268.049297943625,50.0740804314586));
#32977=CARTESIAN_POINT('Ctrl Pts',(66.7849774198236,268.226394515624,52.4087119996441));
#32978=CARTESIAN_POINT('Ctrl Pts',(67.2156126057612,268.403491087623,54.5708413428781));
#32979=CARTESIAN_POINT('Ctrl Pts',(67.6462477916988,268.580587659622,56.7329706861122));
#32980=CARTESIAN_POINT('Ctrl Pts',(69.0245064207991,268.75768423162,58.6887810357255));
#32981=CARTESIAN_POINT('Ctrl Pts',(70.9158061804495,268.934780803619,59.8215807441416));
#32982=CARTESIAN_POINT('Ctrl Pts',(72.8071059400999,269.111877375618,60.9543804525576));
#32983=CARTESIAN_POINT('Ctrl Pts',(75.1818659698138,269.288973947617,61.2464519739653));
#32984=CARTESIAN_POINT('Ctrl Pts',(77.2912945088701,269.466070519615,60.6057014773944));
#32985=CARTESIAN_POINT('Ctrl Pts',(79.4007230479265,269.643167091614,59.9649509808236));
#32986=CARTESIAN_POINT('Ctrl Pts',(81.2118275942102,269.820263663613,58.4014001198745));
#32987=CARTESIAN_POINT('Ctrl Pts',(82.1535440633116,269.997360235611,56.4080561826513));
#32988=CARTESIAN_POINT('Ctrl Pts',(82.6515697929919,270.091017564954,55.3538784110904));
#32989=CARTESIAN_POINT('Ctrl Pts',(82.9129498948692,270.184674894296,54.1887099277301));
#32990=CARTESIAN_POINT('Ctrl Pts',(82.9129498948689,270.278332223638,53.0228109606335));
#32991=CARTESIAN_POINT('Ctrl Pts',(82.9063872485843,271.721667776361,53.029301811537));
#32992=CARTESIAN_POINT('Ctrl Pts',(82.9125252251475,271.655031015865,53.8601027041073));
#32993=CARTESIAN_POINT('Ctrl Pts',(82.7919129299211,271.588394255369,54.6890942908775));
#32994=CARTESIAN_POINT('Ctrl Pts',(82.5368654818679,271.521757494874,55.4744261937191));
#32995=CARTESIAN_POINT('Ctrl Pts',(81.7248534869414,271.309601485321,57.9747410565947));
#32996=CARTESIAN_POINT('Ctrl Pts',(79.5501555688087,271.097445475769,60.0325047306618));
#32997=CARTESIAN_POINT('Ctrl Pts',(77.0070028977421,270.885289466217,60.7005601216458));
#32998=CARTESIAN_POINT('Ctrl Pts',(74.4638502266754,270.673133456665,61.3686155126298));
#32999=CARTESIAN_POINT('Ctrl Pts',(71.5522428026749,270.460977447112,60.6469626205306));
#33000=CARTESIAN_POINT('Ctrl Pts',(69.6174757739374,270.24882143756,58.8695664136463));
#33001=CARTESIAN_POINT('Ctrl Pts',(67.6827087451997,270.036665428008,57.092170206762));
#33002=CARTESIAN_POINT('Ctrl Pts',(66.7247821117251,269.824509418456,54.2590306850926));
#33003=CARTESIAN_POINT('Ctrl Pts',(67.1696651073972,269.612353408903,51.6659626132545));
#33004=CARTESIAN_POINT('Ctrl Pts',(67.3921066052332,269.506275404127,50.3694285773356));
#33005=CARTESIAN_POINT('Ctrl Pts',(67.9652505103558,269.400197399351,49.1329124038745));
#33006=CARTESIAN_POINT('Ctrl Pts',(68.7894683730937,269.294119394575,48.0959618033907));
#33007=CARTESIAN_POINT('Ctrl Pts',(69.6136862358316,269.188041389799,47.0590112029069));
#33008=CARTESIAN_POINT('Ctrl Pts',(70.6889780561849,269.081963385022,46.2216261754004));
#33009=CARTESIAN_POINT('Ctrl Pts',(71.9018768584006,268.975885380246,45.7123549099239));
#33010=CARTESIAN_POINT('Ctrl Pts',(74.3276744628317,268.763729370694,44.693812378971));
#33011=CARTESIAN_POINT('Ctrl Pts',(77.3038999947122,268.551573361142,44.9877248961376));
#33012=CARTESIAN_POINT('Ctrl Pts',(79.4720394188731,268.339417351589,46.4715146956494));
#33013=CARTESIAN_POINT('Ctrl Pts',(81.5764141054351,268.133500826513,47.9116664033652));
#33014=CARTESIAN_POINT('Ctrl Pts',(82.9195351808777,267.927584301437,50.4727362525033));
#33015=CARTESIAN_POINT('Ctrl Pts',(82.9263548363187,267.721667776361,53.0252983291183));
#33016=CARTESIAN_POINT('Origin',(74.9879498948689,255.,53.0228109606356));
#33017=CARTESIAN_POINT('',(82.9129498948689,262.278332223638,53.0228109606331));
#33018=CARTESIAN_POINT('',(82.9129498948689,263.721667776361,53.0228109606465));
#33019=CARTESIAN_POINT('',(82.9129498948689,255.,53.0228109606356));
#33020=CARTESIAN_POINT('Ctrl Pts',(82.9129498948689,262.278332223638,53.0228109606331));
#33021=CARTESIAN_POINT('Ctrl Pts',(82.9129498948682,262.455428795637,50.8182135007233));
#33022=CARTESIAN_POINT('Ctrl Pts',(81.9432795991093,262.632525367635,48.6308565362874));
#33023=CARTESIAN_POINT('Ctrl Pts',(80.3096882702525,262.809621939634,47.1504412801769));
#33024=CARTESIAN_POINT('Ctrl Pts',(78.6760969413956,262.986718511633,45.6700260240665));
#33025=CARTESIAN_POINT('Ctrl Pts',(76.4041347530421,263.163815083632,44.9197069006027));
#33026=CARTESIAN_POINT('Ctrl Pts',(74.2101800112196,263.34091165563,45.1360689838692));
#33027=CARTESIAN_POINT('Ctrl Pts',(72.0162252693971,263.518008227629,45.3524310671358));
#33028=CARTESIAN_POINT('Ctrl Pts',(69.934592507696,263.695104799628,46.5320903475029));
#33029=CARTESIAN_POINT('Ctrl Pts',(68.6216467656593,263.872201371627,48.3030853894804));
#33030=CARTESIAN_POINT('Ctrl Pts',(67.3087010236227,264.049297943625,50.0740804314578));
#33031=CARTESIAN_POINT('Ctrl Pts',(66.7849774198237,264.226394515624,52.4087119996432));
#33032=CARTESIAN_POINT('Ctrl Pts',(67.215612605761,264.403491087623,54.5708413428772));
#33033=CARTESIAN_POINT('Ctrl Pts',(67.6462477916983,264.580587659622,56.7329706861112));
#33034=CARTESIAN_POINT('Ctrl Pts',(69.0245064207983,264.75768423162,58.6887810357247));
#33035=CARTESIAN_POINT('Ctrl Pts',(70.9158061804485,264.934780803619,59.821580744141));
#33036=CARTESIAN_POINT('Ctrl Pts',(72.8071059400987,265.111877375618,60.9543804525573));
#33037=CARTESIAN_POINT('Ctrl Pts',(75.1818659698124,265.288973947616,61.2464519739653));
#33038=CARTESIAN_POINT('Ctrl Pts',(77.2912945088688,265.466070519615,60.6057014773948));
#33039=CARTESIAN_POINT('Ctrl Pts',(79.4007230479252,265.643167091614,59.9649509808244));
#33040=CARTESIAN_POINT('Ctrl Pts',(81.2118275942092,265.820263663613,58.4014001198758));
#33041=CARTESIAN_POINT('Ctrl Pts',(82.1535440633109,265.997360235611,56.4080561826528));
#33042=CARTESIAN_POINT('Ctrl Pts',(82.6515697929918,266.091017564954,55.3538784110913));
#33043=CARTESIAN_POINT('Ctrl Pts',(82.9129498948693,266.184674894296,54.1887099277304));
#33044=CARTESIAN_POINT('Ctrl Pts',(82.9129498948689,266.278332223638,53.0228109606331));
#33045=CARTESIAN_POINT('Ctrl Pts',(82.9129498948689,267.721667776361,53.0228109606465));
#33046=CARTESIAN_POINT('Ctrl Pts',(82.9129498948659,267.544571204362,55.2274084205561));
#33047=CARTESIAN_POINT('Ctrl Pts',(81.9432795991048,267.367474632363,57.4147653849909));
#33048=CARTESIAN_POINT('Ctrl Pts',(80.3096882702465,267.190378060365,58.8951806410996));
#33049=CARTESIAN_POINT('Ctrl Pts',(78.6760969413883,267.013281488366,60.3755958972083));
#33050=CARTESIAN_POINT('Ctrl Pts',(76.4041347530342,266.836184916367,61.1259150206698));
#33051=CARTESIAN_POINT('Ctrl Pts',(74.2101800112121,266.659088344368,60.9095529374012));
#33052=CARTESIAN_POINT('Ctrl Pts',(72.0162252693899,266.48199177237,60.6931908541325));
#33053=CARTESIAN_POINT('Ctrl Pts',(69.9345925076901,266.304895200371,59.5135315737636));
#33054=CARTESIAN_POINT('Ctrl Pts',(68.6216467656551,266.127798628372,57.7425365317851));
#33055=CARTESIAN_POINT('Ctrl Pts',(67.3087010236202,265.950702056374,55.9715414898065));
#33056=CARTESIAN_POINT('Ctrl Pts',(66.7849774198232,265.773605484375,53.6369099216209));
#33057=CARTESIAN_POINT('Ctrl Pts',(67.2156126057623,265.596508912376,51.4747805783874));
#33058=CARTESIAN_POINT('Ctrl Pts',(67.6462477917014,265.419412340377,49.3126512351539));
#33059=CARTESIAN_POINT('Ctrl Pts',(69.0245064208028,265.242315768379,47.3568408855417));
#33060=CARTESIAN_POINT('Ctrl Pts',(70.9158061804538,265.06521919638,46.224041177127));
#33061=CARTESIAN_POINT('Ctrl Pts',(72.8071059401047,264.888122624381,45.0912414687123));
#33062=CARTESIAN_POINT('Ctrl Pts',(75.1818659698185,264.711026052383,44.799169947306));
#33063=CARTESIAN_POINT('Ctrl Pts',(77.2912945088743,264.533929480384,45.439920443878));
#33064=CARTESIAN_POINT('Ctrl Pts',(79.40072304793,264.356832908385,46.0806709404499));
#33065=CARTESIAN_POINT('Ctrl Pts',(81.2118275942128,264.179736336386,47.6442218013997));
#33066=CARTESIAN_POINT('Ctrl Pts',(82.1535440633131,264.002639764388,49.6375657386231));
#33067=CARTESIAN_POINT('Ctrl Pts',(82.6515697929937,263.908982435045,50.6917435101858));
#33068=CARTESIAN_POINT('Ctrl Pts',(82.9129498948705,263.815325105703,51.856911993548));
#33069=CARTESIAN_POINT('Ctrl Pts',(82.9129498948689,263.721667776361,53.0228109606463));
#33070=CARTESIAN_POINT('Origin',(74.9879498948689,255.,53.0228109606356));
#33071=CARTESIAN_POINT('',(82.9129854222471,258.278332223638,53.0230546176887));
#33072=CARTESIAN_POINT('',(82.9072183307991,259.721667776361,53.024065690185));
#33073=CARTESIAN_POINT('',(82.9129498948689,255.,53.0228109606356));
#33074=CARTESIAN_POINT('Ctrl Pts',(82.9129498948689,258.278332223638,53.0228109606327));
#33075=CARTESIAN_POINT('Ctrl Pts',(82.9129498948681,258.455428795637,50.8182135007229));
#33076=CARTESIAN_POINT('Ctrl Pts',(81.9432795991091,258.632525367635,48.630856536287));
#33077=CARTESIAN_POINT('Ctrl Pts',(80.3096882702522,258.809621939634,47.1504412801767));
#33078=CARTESIAN_POINT('Ctrl Pts',(78.6760969413952,258.986718511633,45.6700260240663));
#33079=CARTESIAN_POINT('Ctrl Pts',(76.4041347530417,259.163815083632,44.9197069006026));
#33080=CARTESIAN_POINT('Ctrl Pts',(74.2101800112192,259.34091165563,45.1360689838693));
#33081=CARTESIAN_POINT('Ctrl Pts',(72.0162252693967,259.518008227629,45.352431067136));
#33082=CARTESIAN_POINT('Ctrl Pts',(69.9345925076956,259.695104799628,46.5320903475032));
#33083=CARTESIAN_POINT('Ctrl Pts',(68.6216467656591,259.872201371627,48.3030853894807));
#33084=CARTESIAN_POINT('Ctrl Pts',(67.3087010236226,260.049297943625,50.0740804314582));
#33085=CARTESIAN_POINT('Ctrl Pts',(66.7849774198237,260.226394515624,52.4087119996436));
#33086=CARTESIAN_POINT('Ctrl Pts',(67.2156126057611,260.403491087623,54.5708413428776));
#33087=CARTESIAN_POINT('Ctrl Pts',(67.6462477916985,260.580587659622,56.7329706861116));
#33088=CARTESIAN_POINT('Ctrl Pts',(69.0245064207986,260.75768423162,58.688781035725));
#33089=CARTESIAN_POINT('Ctrl Pts',(70.9158061804488,260.934780803619,59.8215807441412));
#33090=CARTESIAN_POINT('Ctrl Pts',(72.807105940099,261.111877375618,60.9543804525574));
#33091=CARTESIAN_POINT('Ctrl Pts',(75.1818659698128,261.288973947616,61.2464519739653));
#33092=CARTESIAN_POINT('Ctrl Pts',(77.2912945088691,261.466070519615,60.6057014773947));
#33093=CARTESIAN_POINT('Ctrl Pts',(79.4007230479255,261.643167091614,59.9649509808241));
#33094=CARTESIAN_POINT('Ctrl Pts',(81.2118275942094,261.820263663613,58.4014001198754));
#33095=CARTESIAN_POINT('Ctrl Pts',(82.153544063311,261.997360235611,56.4080561826525));
#33096=CARTESIAN_POINT('Ctrl Pts',(82.6515697929918,262.091017564954,55.3538784110911));
#33097=CARTESIAN_POINT('Ctrl Pts',(82.9129498948693,262.184674894296,54.1887099277303));
#33098=CARTESIAN_POINT('Ctrl Pts',(82.9129498948689,262.278332223638,53.0228109606331));
#33099=CARTESIAN_POINT('Ctrl Pts',(82.9129498948689,263.721667776361,53.0228109606463));
#33100=CARTESIAN_POINT('Ctrl Pts',(82.9129498948659,263.544571204362,55.2274084205561));
#33101=CARTESIAN_POINT('Ctrl Pts',(81.9432795991047,263.367474632363,57.4147653849911));
#33102=CARTESIAN_POINT('Ctrl Pts',(80.3096882702463,263.190378060365,58.8951806410998));
#33103=CARTESIAN_POINT('Ctrl Pts',(78.6760969413879,263.013281488366,60.3755958972085));
#33104=CARTESIAN_POINT('Ctrl Pts',(76.4041347530336,262.836184916367,61.12591502067));
#33105=CARTESIAN_POINT('Ctrl Pts',(74.2101800112113,262.659088344368,60.9095529374011));
#33106=CARTESIAN_POINT('Ctrl Pts',(72.0162252693891,262.48199177237,60.6931908541322));
#33107=CARTESIAN_POINT('Ctrl Pts',(69.9345925076892,262.304895200371,59.513531573763));
#33108=CARTESIAN_POINT('Ctrl Pts',(68.6216467656544,262.127798628372,57.7425365317841));
#33109=CARTESIAN_POINT('Ctrl Pts',(67.3087010236196,261.950702056374,55.9715414898053));
#33110=CARTESIAN_POINT('Ctrl Pts',(66.7849774198231,261.773605484375,53.6369099216194));
#33111=CARTESIAN_POINT('Ctrl Pts',(67.2156126057626,261.596508912376,51.4747805783858));
#33112=CARTESIAN_POINT('Ctrl Pts',(67.6462477917022,261.419412340377,49.3126512351523));
#33113=CARTESIAN_POINT('Ctrl Pts',(69.0245064208042,261.242315768379,47.3568408855402));
#33114=CARTESIAN_POINT('Ctrl Pts',(70.9158061804556,261.06521919638,46.2240411771259));
#33115=CARTESIAN_POINT('Ctrl Pts',(72.8071059401069,260.888122624381,45.0912414687116));
#33116=CARTESIAN_POINT('Ctrl Pts',(75.181865969821,260.711026052382,44.799169947306));
#33117=CARTESIAN_POINT('Ctrl Pts',(77.2912945088767,260.533929480384,45.4399204438787));
#33118=CARTESIAN_POINT('Ctrl Pts',(79.4007230479324,260.356832908385,46.0806709404514));
#33119=CARTESIAN_POINT('Ctrl Pts',(81.2118275942148,260.179736336386,47.6442218014019));
#33120=CARTESIAN_POINT('Ctrl Pts',(82.1535440633144,260.002639764387,49.6375657386258));
#33121=CARTESIAN_POINT('Ctrl Pts',(82.6515697929941,259.908982435045,50.6917435101877));
#33122=CARTESIAN_POINT('Ctrl Pts',(82.9129498948705,259.815325105703,51.8569119935489));
#33123=CARTESIAN_POINT('Ctrl Pts',(82.9129498948689,259.721667776361,53.0228109606461));
#33124=CARTESIAN_POINT('Origin',(74.9879498948689,255.,53.0228109606356));
#33125=CARTESIAN_POINT('',(82.9240197340883,254.278332223638,53.020308991551));
#33126=CARTESIAN_POINT('',(82.9135245211875,255.721667776361,53.0233051945254));
#33127=CARTESIAN_POINT('',(82.9129498948689,255.,53.0228109606356));
#33128=CARTESIAN_POINT('Ctrl Pts',(82.9240197340883,254.278332223638,53.020308991551));
#33129=CARTESIAN_POINT('Ctrl Pts',(82.9245880973683,254.289547740762,52.8812896590367));
#33130=CARTESIAN_POINT('Ctrl Pts',(82.9212449384694,254.300763257887,52.7422985421507));
#33131=CARTESIAN_POINT('Ctrl Pts',(82.9139033389865,254.311978775011,52.6035189473502));
#33132=CARTESIAN_POINT('Ctrl Pts',(82.7750274911087,254.524134784563,49.9783234513351));
#33133=CARTESIAN_POINT('Ctrl Pts',(81.2054050595906,254.736290794115,47.4288160879574));
#33134=CARTESIAN_POINT('Ctrl Pts',(78.9209890990964,254.948446803668,46.1267534038997));
#33135=CARTESIAN_POINT('Ctrl Pts',(76.6365731386022,255.16060281322,44.8246907198419));
#33136=CARTESIAN_POINT('Ctrl Pts',(73.6373636491319,255.372758822773,44.7700727151041));
#33137=CARTESIAN_POINT('Ctrl Pts',(71.3092683796031,255.584914832325,45.9876248280484));
#33138=CARTESIAN_POINT('Ctrl Pts',(68.9811731100745,255.797070841877,47.2051769409925));
#33139=CARTESIAN_POINT('Ctrl Pts',(67.3241920604874,256.009226851429,49.6948991716185));
#33140=CARTESIAN_POINT('Ctrl Pts',(67.0844388701906,256.221382860982,52.3149070557222));
#33141=CARTESIAN_POINT('Ctrl Pts',(66.9645622750422,256.327460865758,53.6249109977741));
#33142=CARTESIAN_POINT('Ctrl Pts',(67.1989926447164,256.433538870534,54.9674863531954));
#33143=CARTESIAN_POINT('Ctrl Pts',(67.7275122687358,256.53961687531,56.182092725699));
#33144=CARTESIAN_POINT('Ctrl Pts',(68.2560318927553,256.645694880087,57.3966990982028));
#33145=CARTESIAN_POINT('Ctrl Pts',(69.0786407711201,256.751772884863,58.4833364877888));
#33146=CARTESIAN_POINT('Ctrl Pts',(70.118911778983,256.857850889639,59.2885178067825));
#33147=CARTESIAN_POINT('Ctrl Pts',(72.1994537947081,257.070006899191,60.8988804447697));
#33148=CARTESIAN_POINT('Ctrl Pts',(75.1506443284247,257.282162908743,61.3834188003888));
#33149=CARTESIAN_POINT('Ctrl Pts',(77.6283867922959,257.494318918295,60.5097752721314));
#33150=CARTESIAN_POINT('Ctrl Pts',(80.1061292561671,257.706474927848,59.636131743874));
#33151=CARTESIAN_POINT('Ctrl Pts',(82.1104236501927,257.918630937401,57.4043063317401));
#33152=CARTESIAN_POINT('Ctrl Pts',(82.7147281367444,258.130786946953,54.8452558044333));
#33153=CARTESIAN_POINT('Ctrl Pts',(82.8548172985812,258.179968705848,54.2520196934219));
#33154=CARTESIAN_POINT('Ctrl Pts',(82.9196710418623,258.229150464743,53.6411985138535));
#33155=CARTESIAN_POINT('Ctrl Pts',(82.913891463064,258.278332223638,53.0292685081989));
#33156=CARTESIAN_POINT('Ctrl Pts',(82.8980640920389,259.721667776361,53.0260696970247));
#33157=CARTESIAN_POINT('Ctrl Pts',(82.9017487919349,259.624066834371,54.2447780477463));
#33158=CARTESIAN_POINT('Ctrl Pts',(82.6388455870243,259.526465892382,55.462052251796));
#33159=CARTESIAN_POINT('Ctrl Pts',(82.1026481438308,259.428864950392,56.5452547766708));
#33160=CARTESIAN_POINT('Ctrl Pts',(80.9371111360811,259.21670894084,58.8998214491826));
#33161=CARTESIAN_POINT('Ctrl Pts',(78.4802563401325,259.004552931287,60.6208982051109));
#33162=CARTESIAN_POINT('Ctrl Pts',(75.867072311377,258.792396921735,60.9127761687082));
#33163=CARTESIAN_POINT('Ctrl Pts',(73.2538882826217,258.580240912183,61.2046541323055));
#33164=CARTESIAN_POINT('Ctrl Pts',(70.4843750210593,258.368084902631,60.0673333035724));
#33165=CARTESIAN_POINT('Ctrl Pts',(68.8270002240545,258.155928893078,58.026733716276));
#33166=CARTESIAN_POINT('Ctrl Pts',(67.1696254270496,257.943772883526,55.9861341289796));
#33167=CARTESIAN_POINT('Ctrl Pts',(66.6243890946025,257.731616873974,53.0422557831199));
#33168=CARTESIAN_POINT('Ctrl Pts',(67.445923452996,257.519460864421,50.5444557887738));
#33169=CARTESIAN_POINT('Ctrl Pts',(68.2674578113894,257.307304854869,48.0466557944278));
#33170=CARTESIAN_POINT('Ctrl Pts',(70.4557628606232,257.095148845317,45.9949341515953));
#33171=CARTESIAN_POINT('Ctrl Pts',(72.9992984648703,256.882992835764,45.3369923899906));
#33172=CARTESIAN_POINT('Ctrl Pts',(75.5428340691175,256.670836826212,44.6790506283859));
#33173=CARTESIAN_POINT('Ctrl Pts',(78.4416002283781,256.45868081666,45.4148887480092));
#33174=CARTESIAN_POINT('Ctrl Pts',(80.3763781282835,256.246524807107,47.197739662433));
#33175=CARTESIAN_POINT('Ctrl Pts',(81.3437670782363,256.140446802331,48.089165119645));
#33176=CARTESIAN_POINT('Ctrl Pts',(82.0701589633502,256.034368797555,49.2423437755571));
#33177=CARTESIAN_POINT('Ctrl Pts',(82.4925707755548,255.928290792779,50.4977998257677));
#33178=CARTESIAN_POINT('Ctrl Pts',(82.7668343642302,255.859416453973,51.3129424704724));
#33179=CARTESIAN_POINT('Ctrl Pts',(82.9129506957147,255.790542115167,52.1712016505031));
#33180=CARTESIAN_POINT('Ctrl Pts',(82.9182664199887,255.721667776361,53.0273836833877));
#33181=CARTESIAN_POINT('Origin',(74.9879498948689,255.,53.0228109606356));
#33182=CARTESIAN_POINT('',(82.9108136270844,250.278332223638,53.0211339884677));
#33183=CARTESIAN_POINT('',(82.9145920656403,251.721667776361,53.0222231462556));
#33184=CARTESIAN_POINT('',(82.9129498948689,255.,53.0228109606356));
#33185=CARTESIAN_POINT('Ctrl Pts',(82.905956915151,250.278332223638,53.0173214651763));
#33186=CARTESIAN_POINT('Ctrl Pts',(82.9125926517432,250.349945016782,52.124131973143));
#33187=CARTESIAN_POINT('Ctrl Pts',(82.7733011338671,250.421557809925,51.2327677033672));
#33188=CARTESIAN_POINT('Ctrl Pts',(82.4793208338808,250.493170603069,50.3953085987083));
#33189=CARTESIAN_POINT('Ctrl Pts',(81.6083914287547,250.705326612622,47.9142996335767));
#33190=CARTESIAN_POINT('Ctrl Pts',(79.379810627856,250.917482622174,45.9063981663636));
#33191=CARTESIAN_POINT('Ctrl Pts',(76.823722010962,251.129638631726,45.299050066571));
#33192=CARTESIAN_POINT('Ctrl Pts',(74.2676333940679,251.341794641279,44.6917019667784));
#33193=CARTESIAN_POINT('Ctrl Pts',(71.3840369611785,251.553950650831,45.4849072344063));
#33194=CARTESIAN_POINT('Ctrl Pts',(69.4850119429622,251.766106660383,47.3057935255329));
#33195=CARTESIAN_POINT('Ctrl Pts',(68.5354994338542,251.872184665159,48.2162366710961));
#33196=CARTESIAN_POINT('Ctrl Pts',(67.8321297784144,251.978262669935,49.383600072534));
#33197=CARTESIAN_POINT('Ctrl Pts',(67.4347095618133,252.084340674712,50.6471897229097));
#33198=CARTESIAN_POINT('Ctrl Pts',(67.0372893452122,252.190418679488,51.9107793732854));
#33199=CARTESIAN_POINT('Ctrl Pts',(66.9458185674498,252.296496684264,53.2705952725989));
#33200=CARTESIAN_POINT('Ctrl Pts',(67.2032406976284,252.40257468904,54.5606396800323));
#33201=CARTESIAN_POINT('Ctrl Pts',(67.7180849579855,252.614730698593,57.1407284948992));
#33202=CARTESIAN_POINT('Ctrl Pts',(69.6285008501065,252.826886708145,59.4417313422457));
#33203=CARTESIAN_POINT('Ctrl Pts',(72.0720622916857,253.039042717697,60.4068573510985));
#33204=CARTESIAN_POINT('Ctrl Pts',(74.515623733265,253.251198727249,61.3719833599513));
#33205=CARTESIAN_POINT('Ctrl Pts',(77.4923307243023,253.463354736802,61.0012325303105));
#33206=CARTESIAN_POINT('Ctrl Pts',(79.6266195877023,253.675510746354,59.4654153011639));
#33207=CARTESIAN_POINT('Ctrl Pts',(81.6480803801642,253.876451238782,58.0107882512143));
#33208=CARTESIAN_POINT('Ctrl Pts',(82.9138367709577,254.07739173121,55.5110201039194));
#33209=CARTESIAN_POINT('Ctrl Pts',(82.9240197340883,254.278332223638,53.020308991551));
#33210=CARTESIAN_POINT('Ctrl Pts',(82.9129498948689,255.721667776361,53.0228109606459));
#33211=CARTESIAN_POINT('Ctrl Pts',(82.912949894866,255.544571204362,55.2274084205558));
#33212=CARTESIAN_POINT('Ctrl Pts',(81.9432795991048,255.367474632363,57.4147653849909));
#33213=CARTESIAN_POINT('Ctrl Pts',(80.3096882702464,255.190378060365,58.8951806410997));
#33214=CARTESIAN_POINT('Ctrl Pts',(78.676096941388,255.013281488366,60.3755958972085));
#33215=CARTESIAN_POINT('Ctrl Pts',(76.4041347530336,254.836184916367,61.12591502067));
#33216=CARTESIAN_POINT('Ctrl Pts',(74.2101800112112,254.659088344368,60.9095529374011));
#33217=CARTESIAN_POINT('Ctrl Pts',(72.0162252693889,254.48199177237,60.6931908541322));
#33218=CARTESIAN_POINT('Ctrl Pts',(69.9345925076889,254.304895200371,59.5135315737628));
#33219=CARTESIAN_POINT('Ctrl Pts',(68.6216467656542,254.127798628372,57.7425365317838));
#33220=CARTESIAN_POINT('Ctrl Pts',(67.3087010236195,253.950702056374,55.9715414898049));
#33221=CARTESIAN_POINT('Ctrl Pts',(66.784977419823,253.773605484375,53.6369099216189));
#33222=CARTESIAN_POINT('Ctrl Pts',(67.2156126057627,253.596508912376,51.4747805783853));
#33223=CARTESIAN_POINT('Ctrl Pts',(67.6462477917025,253.419412340377,49.3126512351517));
#33224=CARTESIAN_POINT('Ctrl Pts',(69.0245064208047,253.242315768379,47.3568408855397));
#33225=CARTESIAN_POINT('Ctrl Pts',(70.9158061804562,253.06521919638,46.2240411771255));
#33226=CARTESIAN_POINT('Ctrl Pts',(72.8071059401077,252.888122624381,45.0912414687114));
#33227=CARTESIAN_POINT('Ctrl Pts',(75.1818659698218,252.711026052382,44.799169947306));
#33228=CARTESIAN_POINT('Ctrl Pts',(77.2912945088774,252.533929480384,45.4399204438789));
#33229=CARTESIAN_POINT('Ctrl Pts',(79.4007230479332,252.356832908385,46.0806709404519));
#33230=CARTESIAN_POINT('Ctrl Pts',(81.2118275942155,252.179736336386,47.6442218014027));
#33231=CARTESIAN_POINT('Ctrl Pts',(82.1535440633149,252.002639764387,49.6375657386269));
#33232=CARTESIAN_POINT('Ctrl Pts',(82.6515697929943,251.908982435045,50.6917435101885));
#33233=CARTESIAN_POINT('Ctrl Pts',(82.9129498948704,251.815325105703,51.8569119935492));
#33234=CARTESIAN_POINT('Ctrl Pts',(82.9129498948689,251.721667776361,53.022810960646));
#33235=CARTESIAN_POINT('Origin',(74.9879498948689,255.,53.0228109606356));
#33236=CARTESIAN_POINT('',(82.9094889824334,246.278332223638,53.0243238363652));
#33237=CARTESIAN_POINT('',(82.9070612414929,247.721667776361,53.0201181858126));
#33238=CARTESIAN_POINT('',(82.9129498948689,255.,53.0228109606356));
#33239=CARTESIAN_POINT('Ctrl Pts',(82.9129498948689,246.278332223638,53.0228109606324));
#33240=CARTESIAN_POINT('Ctrl Pts',(82.912949894868,246.455428795637,50.8182135007226));
#33241=CARTESIAN_POINT('Ctrl Pts',(81.9432795991089,246.632525367636,48.6308565362867));
#33242=CARTESIAN_POINT('Ctrl Pts',(80.3096882702519,246.809621939634,47.1504412801765));
#33243=CARTESIAN_POINT('Ctrl Pts',(78.676096941395,246.986718511633,45.6700260240662));
#33244=CARTESIAN_POINT('Ctrl Pts',(76.4041347530414,247.163815083632,44.9197069006025));
#33245=CARTESIAN_POINT('Ctrl Pts',(74.2101800112189,247.34091165563,45.1360689838693));
#33246=CARTESIAN_POINT('Ctrl Pts',(72.0162252693964,247.518008227629,45.3524310671361));
#33247=CARTESIAN_POINT('Ctrl Pts',(69.9345925076954,247.695104799628,46.5320903475033));
#33248=CARTESIAN_POINT('Ctrl Pts',(68.6216467656589,247.872201371627,48.3030853894809));
#33249=CARTESIAN_POINT('Ctrl Pts',(67.3087010236224,248.049297943625,50.0740804314585));
#33250=CARTESIAN_POINT('Ctrl Pts',(66.7849774198237,248.226394515624,52.4087119996439));
#33251=CARTESIAN_POINT('Ctrl Pts',(67.2156126057612,248.403491087623,54.5708413428779));
#33252=CARTESIAN_POINT('Ctrl Pts',(67.6462477916987,248.580587659622,56.7329706861118));
#33253=CARTESIAN_POINT('Ctrl Pts',(69.0245064207988,248.75768423162,58.6887810357252));
#33254=CARTESIAN_POINT('Ctrl Pts',(70.9158061804491,248.934780803619,59.8215807441413));
#33255=CARTESIAN_POINT('Ctrl Pts',(72.8071059400993,249.111877375618,60.9543804525574));
#33256=CARTESIAN_POINT('Ctrl Pts',(75.1818659698131,249.288973947616,61.2464519739653));
#33257=CARTESIAN_POINT('Ctrl Pts',(77.2912945088694,249.466070519615,60.6057014773946));
#33258=CARTESIAN_POINT('Ctrl Pts',(79.4007230479258,249.643167091614,59.964950980824));
#33259=CARTESIAN_POINT('Ctrl Pts',(81.2118275942096,249.820263663613,58.4014001198752));
#33260=CARTESIAN_POINT('Ctrl Pts',(82.1535440633112,249.997360235611,56.4080561826522));
#33261=CARTESIAN_POINT('Ctrl Pts',(82.6515697929919,250.091017564954,55.3538784110907));
#33262=CARTESIAN_POINT('Ctrl Pts',(82.9129498948693,250.184674894296,54.1887099277298));
#33263=CARTESIAN_POINT('Ctrl Pts',(82.9129498948689,250.278332223638,53.0228109606326));
#33264=CARTESIAN_POINT('Ctrl Pts',(82.9214093282576,251.721667776361,53.0197829096366));
#33265=CARTESIAN_POINT('Ctrl Pts',(82.916679486065,251.638783381634,54.048787391814));
#33266=CARTESIAN_POINT('Ctrl Pts',(82.7036892742198,251.555898986907,55.0803795699231));
#33267=CARTESIAN_POINT('Ctrl Pts',(82.3096390686196,251.47301459218,56.0374226167223));
#33268=CARTESIAN_POINT('Ctrl Pts',(81.8053214617955,251.366936587404,57.26227582611));
#33269=CARTESIAN_POINT('Ctrl Pts',(81.0044335625822,251.260858582628,58.3650200195222));
#33270=CARTESIAN_POINT('Ctrl Pts',(79.9803422437528,251.154780577852,59.1906819945182));
#33271=CARTESIAN_POINT('Ctrl Pts',(77.9321596060941,250.9426245683,60.8420059445101));
#33272=CARTESIAN_POINT('Ctrl Pts',(74.9911632899713,250.730468558747,61.3850010208379));
#33273=CARTESIAN_POINT('Ctrl Pts',(72.496575305283,250.518312549195,60.5606882656381));
#33274=CARTESIAN_POINT('Ctrl Pts',(70.0019873205946,250.306156539643,59.7363755104383));
#33275=CARTESIAN_POINT('Ctrl Pts',(67.9538076673407,250.09400053009,57.5447549237108));
#33276=CARTESIAN_POINT('Ctrl Pts',(67.2988501551073,249.881844520538,54.998197606283));
#33277=CARTESIAN_POINT('Ctrl Pts',(66.6438926428738,249.669688510986,52.4516402888551));
#33278=CARTESIAN_POINT('Ctrl Pts',(67.3821572716608,249.457532501433,49.5501462407268));
#33279=CARTESIAN_POINT('Ctrl Pts',(69.1705455751325,249.245376491881,47.623334062691));
#33280=CARTESIAN_POINT('Ctrl Pts',(70.9589338786041,249.033220482329,45.6965218846554));
#33281=CARTESIAN_POINT('Ctrl Pts',(73.7974458567604,248.821064472776,44.7443915767121));
#33282=CARTESIAN_POINT('Ctrl Pts',(76.3856808148585,248.608908463224,45.2080329418362));
#33283=CARTESIAN_POINT('Ctrl Pts',(78.9739157729569,248.396752453672,45.6716743069604));
#33284=CARTESIAN_POINT('Ctrl Pts',(81.311873710997,248.184596444119,47.5510873451521));
#33285=CARTESIAN_POINT('Ctrl Pts',(82.3195339490888,247.972440434567,49.97741823279));
#33286=CARTESIAN_POINT('Ctrl Pts',(82.7165588193061,247.888849548498,50.9334088230239));
#33287=CARTESIAN_POINT('Ctrl Pts',(82.9070665877906,247.80525866243,51.9743036336875));
#33288=CARTESIAN_POINT('Ctrl Pts',(82.9007584226264,247.721667776361,53.0172360205809));
#33289=CARTESIAN_POINT('Origin',(74.9879498948689,255.,53.0228109606356));
#33290=CARTESIAN_POINT('',(82.9161917637328,242.278332223638,53.0237563384547));
#33291=CARTESIAN_POINT('',(82.9098680058837,243.721667776361,53.0268864946943));
#33292=CARTESIAN_POINT('',(82.9129498948689,255.,53.0228109606356));
#33293=CARTESIAN_POINT('Ctrl Pts',(82.9238601319149,242.278332223638,53.0259925502159));
#33294=CARTESIAN_POINT('Ctrl Pts',(82.907066140212,242.470739568821,50.6417088931013));
#33295=CARTESIAN_POINT('Ctrl Pts',(81.7542886292362,242.663146914003,48.2474956051494));
#33296=CARTESIAN_POINT('Ctrl Pts',(79.8779861178407,242.855554259186,46.773478180744));
#33297=CARTESIAN_POINT('Ctrl Pts',(78.8435431417868,242.961632263962,45.9608229921502));
#33298=CARTESIAN_POINT('Ctrl Pts',(77.5891820870839,243.067710268738,45.4278647126812));
#33299=CARTESIAN_POINT('Ctrl Pts',(76.2823888503532,243.173788273514,45.2113166359524));
#33300=CARTESIAN_POINT('Ctrl Pts',(74.9755956136225,243.279866278291,44.9947685592237));
#33301=CARTESIAN_POINT('Ctrl Pts',(73.616370194864,243.385944283067,45.0946306852353));
#33302=CARTESIAN_POINT('Ctrl Pts',(72.375088412559,243.492022287843,45.5301766221626));
#33303=CARTESIAN_POINT('Ctrl Pts',(69.8925248479489,243.704178297395,46.4012684960171));
#33304=CARTESIAN_POINT('Ctrl Pts',(67.8817358291529,243.916334306947,48.615095613534));
#33305=CARTESIAN_POINT('Ctrl Pts',(67.2683221486002,244.1284903165,51.1697353901461));
#33306=CARTESIAN_POINT('Ctrl Pts',(66.6549084680477,244.340646326052,53.7243751667579));
#33307=CARTESIAN_POINT('Ctrl Pts',(67.4388701257386,244.552802335605,56.6198276024647));
#33308=CARTESIAN_POINT('Ctrl Pts',(69.2584430647217,244.764958345157,58.5180051056228));
#33309=CARTESIAN_POINT('Ctrl Pts',(71.078016003705,244.977114354709,60.4161826087811));
#33310=CARTESIAN_POINT('Ctrl Pts',(73.9332002239807,245.189270364261,61.3170851793908));
#33311=CARTESIAN_POINT('Ctrl Pts',(76.5130773837582,245.401426373813,60.8119399192136));
#33312=CARTESIAN_POINT('Ctrl Pts',(79.0929545435357,245.613582383366,60.3067946590365));
#33313=CARTESIAN_POINT('Ctrl Pts',(81.3975246428152,245.825738392919,58.3956015680724));
#33314=CARTESIAN_POINT('Ctrl Pts',(82.3668417432141,246.037894402471,55.9513536525265));
#33315=CARTESIAN_POINT('Ctrl Pts',(82.7330195889922,246.11804034286,55.0279928288149));
#33316=CARTESIAN_POINT('Ctrl Pts',(82.9086443675112,246.198186283249,54.0285601056758));
#33317=CARTESIAN_POINT('Ctrl Pts',(82.9028596079635,246.278332223638,53.0272217483888));
#33318=CARTESIAN_POINT('Ctrl Pts',(82.9129498948689,247.721667776361,53.0228109606458));
#33319=CARTESIAN_POINT('Ctrl Pts',(82.912949894866,247.544571204362,55.2274084205557));
#33320=CARTESIAN_POINT('Ctrl Pts',(81.943279599105,247.367474632363,57.4147653849906));
#33321=CARTESIAN_POINT('Ctrl Pts',(80.3096882702467,247.190378060365,58.8951806410995));
#33322=CARTESIAN_POINT('Ctrl Pts',(78.6760969413883,247.013281488366,60.3755958972083));
#33323=CARTESIAN_POINT('Ctrl Pts',(76.4041347530341,246.836184916367,61.1259150206699));
#33324=CARTESIAN_POINT('Ctrl Pts',(74.2101800112118,246.659088344368,60.9095529374011));
#33325=CARTESIAN_POINT('Ctrl Pts',(72.0162252693895,246.48199177237,60.6931908541324));
#33326=CARTESIAN_POINT('Ctrl Pts',(69.9345925076895,246.304895200371,59.5135315737633));
#33327=CARTESIAN_POINT('Ctrl Pts',(68.6216467656547,246.127798628372,57.7425365317845));
#33328=CARTESIAN_POINT('Ctrl Pts',(67.3087010236198,245.950702056374,55.9715414898057));
#33329=CARTESIAN_POINT('Ctrl Pts',(66.7849774198231,245.773605484375,53.6369099216199));
#33330=CARTESIAN_POINT('Ctrl Pts',(67.2156126057625,245.596508912376,51.4747805783863));
#33331=CARTESIAN_POINT('Ctrl Pts',(67.646247791702,245.419412340377,49.3126512351527));
#33332=CARTESIAN_POINT('Ctrl Pts',(69.0245064208039,245.242315768379,47.3568408855406));
#33333=CARTESIAN_POINT('Ctrl Pts',(70.9158061804552,245.06521919638,46.2240411771262));
#33334=CARTESIAN_POINT('Ctrl Pts',(72.8071059401065,244.888122624381,45.0912414687117));
#33335=CARTESIAN_POINT('Ctrl Pts',(75.1818659698205,244.711026052382,44.799169947306));
#33336=CARTESIAN_POINT('Ctrl Pts',(77.2912945088762,244.533929480384,45.4399204438786));
#33337=CARTESIAN_POINT('Ctrl Pts',(79.400723047932,244.356832908385,46.0806709404511));
#33338=CARTESIAN_POINT('Ctrl Pts',(81.2118275942144,244.179736336386,47.6442218014015));
#33339=CARTESIAN_POINT('Ctrl Pts',(82.1535440633142,244.002639764388,49.6375657386254));
#33340=CARTESIAN_POINT('Ctrl Pts',(82.6515697929939,243.908982435045,50.6917435101872));
#33341=CARTESIAN_POINT('Ctrl Pts',(82.9129498948703,243.815325105703,51.8569119935481));
#33342=CARTESIAN_POINT('Ctrl Pts',(82.9129498948689,243.721667776361,53.0228109606452));
#33343=CARTESIAN_POINT('Origin',(74.9879498948689,255.,53.0228109606356));
#33344=CARTESIAN_POINT('',(82.9128050499553,238.278332223638,53.0219540812206));
#33345=CARTESIAN_POINT('',(82.926321989507,239.721667776361,53.0235034425041));
#33346=CARTESIAN_POINT('',(82.9129498948689,255.,53.0228109606356));
#33347=CARTESIAN_POINT('Ctrl Pts',(82.9129498948689,238.278332223638,53.0228109606321));
#33348=CARTESIAN_POINT('Ctrl Pts',(82.9129498948679,238.455428795637,50.8182135007223));
#33349=CARTESIAN_POINT('Ctrl Pts',(81.9432795991088,238.632525367636,48.6308565362865));
#33350=CARTESIAN_POINT('Ctrl Pts',(80.3096882702517,238.809621939634,47.1504412801762));
#33351=CARTESIAN_POINT('Ctrl Pts',(78.6760969413946,238.986718511633,45.670026024066));
#33352=CARTESIAN_POINT('Ctrl Pts',(76.404134753041,239.163815083632,44.9197069006025));
#33353=CARTESIAN_POINT('Ctrl Pts',(74.2101800112185,239.34091165563,45.1360689838693));
#33354=CARTESIAN_POINT('Ctrl Pts',(72.0162252693961,239.518008227629,45.3524310671362));
#33355=CARTESIAN_POINT('Ctrl Pts',(69.9345925076951,239.695104799628,46.5320903475036));
#33356=CARTESIAN_POINT('Ctrl Pts',(68.6216467656587,239.872201371627,48.3030853894812));
#33357=CARTESIAN_POINT('Ctrl Pts',(67.3087010236223,240.049297943625,50.0740804314588));
#33358=CARTESIAN_POINT('Ctrl Pts',(66.7849774198236,240.226394515624,52.4087119996442));
#33359=CARTESIAN_POINT('Ctrl Pts',(67.2156126057612,240.403491087623,54.5708413428782));
#33360=CARTESIAN_POINT('Ctrl Pts',(67.6462477916988,240.580587659622,56.7329706861122));
#33361=CARTESIAN_POINT('Ctrl Pts',(69.024506420799,240.75768423162,58.6887810357255));
#33362=CARTESIAN_POINT('Ctrl Pts',(70.9158061804494,240.934780803619,59.8215807441415));
#33363=CARTESIAN_POINT('Ctrl Pts',(72.8071059400997,241.111877375618,60.9543804525575));
#33364=CARTESIAN_POINT('Ctrl Pts',(75.1818659698135,241.288973947617,61.2464519739653));
#33365=CARTESIAN_POINT('Ctrl Pts',(77.2912945088698,241.466070519615,60.6057014773945));
#33366=CARTESIAN_POINT('Ctrl Pts',(79.400723047926,241.643167091614,59.9649509808238));
#33367=CARTESIAN_POINT('Ctrl Pts',(81.2118275942098,241.820263663613,58.401400119875));
#33368=CARTESIAN_POINT('Ctrl Pts',(82.1535440633113,241.997360235611,56.4080561826519));
#33369=CARTESIAN_POINT('Ctrl Pts',(82.6515697929921,242.091017564954,55.3538784110903));
#33370=CARTESIAN_POINT('Ctrl Pts',(82.9129498948695,242.184674894296,54.1887099277292));
#33371=CARTESIAN_POINT('Ctrl Pts',(82.9129498948689,242.278332223638,53.0228109606318));
#33372=CARTESIAN_POINT('Ctrl Pts',(82.9065114310396,243.721667776361,53.0313252772196));
#33373=CARTESIAN_POINT('Ctrl Pts',(82.9130325787133,243.653499928897,53.8818329308789));
#33374=CARTESIAN_POINT('Ctrl Pts',(82.7869871502048,243.585332081433,54.7301656950663));
#33375=CARTESIAN_POINT('Ctrl Pts',(82.5202253887267,243.517164233968,55.5310708147046));
#33376=CARTESIAN_POINT('Ctrl Pts',(81.6899936457324,243.305008224416,58.0236951314963));
#33377=CARTESIAN_POINT('Ctrl Pts',(79.4967613740554,243.092852214864,60.0569278252234));
#33378=CARTESIAN_POINT('Ctrl Pts',(76.9486412513389,242.880696205312,60.711913890137));
#33379=CARTESIAN_POINT('Ctrl Pts',(75.6745811899807,242.774618200535,61.0394069225938));
#33380=CARTESIAN_POINT('Ctrl Pts',(74.3117991658626,242.668540195759,61.0223382978473));
#33381=CARTESIAN_POINT('Ctrl Pts',(73.0283905058894,242.562462190983,60.6945215127286));
#33382=CARTESIAN_POINT('Ctrl Pts',(71.7449818459162,242.456384186207,60.3667047276099));
#33383=CARTESIAN_POINT('Ctrl Pts',(70.5409465500878,242.350306181431,59.728139782119));
#33384=CARTESIAN_POINT('Ctrl Pts',(69.5800050974343,242.244228176655,58.8297677818719));
#33385=CARTESIAN_POINT('Ctrl Pts',(67.6581221921272,242.032072167102,57.0330237813775));
#33386=CARTESIAN_POINT('Ctrl Pts',(66.7086146595198,241.81991615755,54.1970515618584));
#33387=CARTESIAN_POINT('Ctrl Pts',(67.1754568585284,241.607760147998,51.6116078682225));
#33388=CARTESIAN_POINT('Ctrl Pts',(67.6422990575369,241.395604138445,49.0261641745868));
#33389=CARTESIAN_POINT('Ctrl Pts',(69.5254909881617,241.183448128893,46.6912490068345));
#33390=CARTESIAN_POINT('Ctrl Pts',(71.9552317322733,240.971292119341,45.6861204428294));
#33391=CARTESIAN_POINT('Ctrl Pts',(74.3849724763853,240.759136109789,44.6809918788241));
#33392=CARTESIAN_POINT('Ctrl Pts',(77.3612620339845,240.546980100236,45.0056499185663));
#33393=CARTESIAN_POINT('Ctrl Pts',(79.519536230537,240.334824090684,46.5065797590045));
#33394=CARTESIAN_POINT('Ctrl Pts',(81.5987599968093,240.130438652576,47.9525355141774));
#33395=CARTESIAN_POINT('Ctrl Pts',(82.9187934056723,239.926053214469,50.4901751805651));
#33396=CARTESIAN_POINT('Ctrl Pts',(82.926321989507,239.721667776361,53.0235034425041));
#33397=CARTESIAN_POINT('Origin',(74.9879498948689,255.,53.0228109606356));
#33398=CARTESIAN_POINT('',(82.91116743,234.278332223638,53.0226183020154));
#33399=CARTESIAN_POINT('',(82.9111139440083,235.721667776361,53.0156317204369));
#33400=CARTESIAN_POINT('',(82.9129498948689,255.,53.0228109606356));
#33401=CARTESIAN_POINT('Ctrl Pts',(82.9060478678828,234.278332223638,53.0220649515909));
#33402=CARTESIAN_POINT('Ctrl Pts',(82.9069987852815,234.379378111307,51.7603229420665));
#33403=CARTESIAN_POINT('Ctrl Pts',(82.6172193617369,234.480423998977,50.4990581479779));
#33404=CARTESIAN_POINT('Ctrl Pts',(82.0408377393029,234.581469886646,49.386413360037));
#33405=CARTESIAN_POINT('Ctrl Pts',(80.8306665209031,234.793625896198,47.0503036607335));
#33406=CARTESIAN_POINT('Ctrl Pts',(78.3570602913277,235.00578190575,45.3693589247679));
#33407=CARTESIAN_POINT('Ctrl Pts',(75.74169133811,235.217937915302,45.1197472858543));
#33408=CARTESIAN_POINT('Ctrl Pts',(73.1263223848922,235.430093924855,44.8701356469406));
#33409=CARTESIAN_POINT('Ctrl Pts',(70.3691907080321,235.642249934407,46.0518571050791));
#33410=CARTESIAN_POINT('Ctrl Pts',(68.7445355694784,235.85440594396,48.1193239596012));
#33411=CARTESIAN_POINT('Ctrl Pts',(67.1198804309247,236.066561953512,50.1867908141234));
#33412=CARTESIAN_POINT('Ctrl Pts',(66.6277018306775,236.278717963064,53.1400030650291));
#33413=CARTESIAN_POINT('Ctrl Pts',(67.489160642071,236.490873972616,55.6237153288983));
#33414=CARTESIAN_POINT('Ctrl Pts',(68.3506194534644,236.703029982169,58.1074275927673));
#33415=CARTESIAN_POINT('Ctrl Pts',(70.5657156764983,236.915185991721,60.1216398695997));
#33416=CARTESIAN_POINT('Ctrl Pts',(73.1216220916204,237.127342001274,60.7391072055076));
#33417=CARTESIAN_POINT('Ctrl Pts',(75.6775285067427,237.339498010826,61.3565745414155));
#33418=CARTESIAN_POINT('Ctrl Pts',(78.5742451139533,237.551654020378,60.5772969363989));
#33419=CARTESIAN_POINT('Ctrl Pts',(80.4733674854168,237.76381002993,58.7618644948182));
#33420=CARTESIAN_POINT('Ctrl Pts',(82.0086223052805,237.935317427833,57.2942648035324));
#33421=CARTESIAN_POINT('Ctrl Pts',(82.8919351099652,238.106824825735,55.1495231962438));
#33422=CARTESIAN_POINT('Ctrl Pts',(82.9118918566993,238.278332223638,53.0165517755375));
#33423=CARTESIAN_POINT('Ctrl Pts',(82.926321989507,239.721667776361,53.0235034425041));
#33424=CARTESIAN_POINT('Ctrl Pts',(82.9266082202634,239.713897204916,53.1198185637504));
#33425=CARTESIAN_POINT('Ctrl Pts',(82.9249972780706,239.706126633472,53.216127453035));
#33426=CARTESIAN_POINT('Ctrl Pts',(82.921458755405,239.698356062027,53.3123698796841));
#33427=CARTESIAN_POINT('Ctrl Pts',(82.8248482482147,239.486200052475,55.9400285187916));
#33428=CARTESIAN_POINT('Ctrl Pts',(81.2913683983285,239.274044042922,58.5181441558727));
#33429=CARTESIAN_POINT('Ctrl Pts',(79.0300625577341,239.06188803337,59.8556629882746));
#33430=CARTESIAN_POINT('Ctrl Pts',(76.7687567171396,238.849732023818,61.1931818206766));
#33431=CARTESIAN_POINT('Ctrl Pts',(73.779624885837,238.637576014265,61.2901038483994));
#33432=CARTESIAN_POINT('Ctrl Pts',(71.4263082709551,238.425420004713,60.1137434380047));
#33433=CARTESIAN_POINT('Ctrl Pts',(70.2496499635141,238.319341999937,59.5255632328073));
#33434=CARTESIAN_POINT('Ctrl Pts',(69.2319454601783,238.213263995161,58.6190624180804));
#33435=CARTESIAN_POINT('Ctrl Pts',(68.4779338448622,238.107185990385,57.5299948733117));
#33436=CARTESIAN_POINT('Ctrl Pts',(67.7239222295461,238.001107985608,56.440927328543));
#33437=CARTESIAN_POINT('Ctrl Pts',(67.2336035022498,237.895029980832,55.1692930537326));
#33438=CARTESIAN_POINT('Ctrl Pts',(67.0971826990598,237.788951976056,53.8609085190056));
#33439=CARTESIAN_POINT('Ctrl Pts',(66.8243410926796,237.576795966504,51.2441394495514));
#33440=CARTESIAN_POINT('Ctrl Pts',(67.9670911827251,237.364639956951,48.4803693404307));
#33441=CARTESIAN_POINT('Ctrl Pts',(70.0149031101221,237.152483947399,46.834487497239));
#33442=CARTESIAN_POINT('Ctrl Pts',(72.0627150375189,236.940327937847,45.1886056540473));
#33443=CARTESIAN_POINT('Ctrl Pts',(75.0155888022669,236.728171928295,44.6606120767842));
#33444=CARTESIAN_POINT('Ctrl Pts',(77.5091274627469,236.516015918742,45.4949911647695));
#33445=CARTESIAN_POINT('Ctrl Pts',(80.0026661232272,236.30385990919,46.3293702527549));
#33446=CARTESIAN_POINT('Ctrl Pts',(82.0368696794392,236.091703899637,48.5261220059891));
#33447=CARTESIAN_POINT('Ctrl Pts',(82.6821596603463,235.879547890085,51.0745604953318));
#33448=CARTESIAN_POINT('Ctrl Pts',(82.8422281178079,235.82692118551,51.7067175564894));
#33449=CARTESIAN_POINT('Ctrl Pts',(82.9168338184225,235.774294480936,52.3605146379828));
#33450=CARTESIAN_POINT('Ctrl Pts',(82.9111139440083,235.721667776361,53.0156317204369));
#33451=CARTESIAN_POINT('Origin',(74.9879498948689,255.,53.0228109606356));
#33452=CARTESIAN_POINT('',(82.9129498948689,230.278332223638,53.0228109606318));
#33453=CARTESIAN_POINT('',(82.9064065954961,231.721667776361,53.0236012027229));
#33454=CARTESIAN_POINT('',(82.9129498948689,255.,53.0228109606356));
#33455=CARTESIAN_POINT('Ctrl Pts',(82.9129498948689,230.278332223638,53.0228109606318));
#33456=CARTESIAN_POINT('Ctrl Pts',(82.9129498948678,230.455428795637,50.8182135007218));
#33457=CARTESIAN_POINT('Ctrl Pts',(81.9432795991084,230.632525367636,48.6308565362859));
#33458=CARTESIAN_POINT('Ctrl Pts',(80.3096882702511,230.809621939634,47.1504412801757));
#33459=CARTESIAN_POINT('Ctrl Pts',(78.6760969413938,230.986718511633,45.6700260240655));
#33460=CARTESIAN_POINT('Ctrl Pts',(76.4041347530399,231.163815083632,44.9197069006022));
#33461=CARTESIAN_POINT('Ctrl Pts',(74.2101800112173,231.340911655631,45.1360689838695));
#33462=CARTESIAN_POINT('Ctrl Pts',(72.0162252693947,231.518008227629,45.3524310671367));
#33463=CARTESIAN_POINT('Ctrl Pts',(69.9345925076938,231.695104799628,46.5320903475045));
#33464=CARTESIAN_POINT('Ctrl Pts',(68.6216467656577,231.872201371627,48.3030853894826));
#33465=CARTESIAN_POINT('Ctrl Pts',(67.3087010236216,232.049297943626,50.0740804314606));
#33466=CARTESIAN_POINT('Ctrl Pts',(66.7849774198234,232.226394515624,52.4087119996463));
#33467=CARTESIAN_POINT('Ctrl Pts',(67.2156126057616,232.403491087623,54.5708413428803));
#33468=CARTESIAN_POINT('Ctrl Pts',(67.6462477916998,232.580587659622,56.7329706861143));
#33469=CARTESIAN_POINT('Ctrl Pts',(69.0245064208007,232.757684231621,58.6887810357273));
#33470=CARTESIAN_POINT('Ctrl Pts',(70.9158061804516,232.934780803619,59.8215807441428));
#33471=CARTESIAN_POINT('Ctrl Pts',(72.8071059401024,233.111877375618,60.9543804525583));
#33472=CARTESIAN_POINT('Ctrl Pts',(75.1818659698165,233.288973947617,61.2464519739653));
#33473=CARTESIAN_POINT('Ctrl Pts',(77.2912945088727,233.466070519615,60.6057014773937));
#33474=CARTESIAN_POINT('Ctrl Pts',(79.4007230479289,233.643167091614,59.9649509808221));
#33475=CARTESIAN_POINT('Ctrl Pts',(81.2118275942122,233.820263663613,58.4014001198723));
#33476=CARTESIAN_POINT('Ctrl Pts',(82.1535440633128,233.997360235612,56.4080561826487));
#33477=CARTESIAN_POINT('Ctrl Pts',(82.6515697929926,234.091017564954,55.353878411088));
#33478=CARTESIAN_POINT('Ctrl Pts',(82.9129498948694,234.184674894296,54.1887099277281));
#33479=CARTESIAN_POINT('Ctrl Pts',(82.9129498948689,234.278332223638,53.0228109606319));
#33480=CARTESIAN_POINT('Ctrl Pts',(82.9111139440083,235.721667776361,53.0156317204369));
#33481=CARTESIAN_POINT('Ctrl Pts',(82.8937750739949,235.562138471383,55.0015127230071));
#33482=CARTESIAN_POINT('Ctrl Pts',(82.1383239120666,235.402609166406,56.9995232239856));
#33483=CARTESIAN_POINT('Ctrl Pts',(80.7878565684763,235.243079861428,58.4436494368539));
#33484=CARTESIAN_POINT('Ctrl Pts',(78.9918870900964,235.030923851876,60.3641746635835));
#33485=CARTESIAN_POINT('Ctrl Pts',(76.1435717277343,234.818767842324,61.3050998915916));
#33486=CARTESIAN_POINT('Ctrl Pts',(73.5592434434874,234.606611832771,60.8321220369526));
#33487=CARTESIAN_POINT('Ctrl Pts',(70.9749151592408,234.394455823219,60.3591441823135));
#33488=CARTESIAN_POINT('Ctrl Pts',(68.6545739531097,234.182299813667,58.4722632450275));
#33489=CARTESIAN_POINT('Ctrl Pts',(67.6491982592205,233.970143804114,56.0409790947974));
#33490=CARTESIAN_POINT('Ctrl Pts',(67.1465104122758,233.864065799338,54.8253370196822));
#33491=CARTESIAN_POINT('Ctrl Pts',(66.9725639433917,233.757987794562,53.4735941413305));
#33492=CARTESIAN_POINT('Ctrl Pts',(67.1174189961907,233.651909789786,52.156924613021));
#33493=CARTESIAN_POINT('Ctrl Pts',(67.2622740489897,233.54583178501,50.8402550847114));
#33494=CARTESIAN_POINT('Ctrl Pts',(67.7259306234716,233.439753780233,49.5586589064437));
#33495=CARTESIAN_POINT('Ctrl Pts',(68.4808773747036,233.333675775457,48.4813770821003));
#33496=CARTESIAN_POINT('Ctrl Pts',(69.9907708771672,233.121519765905,46.3268134334138));
#33497=CARTESIAN_POINT('Ctrl Pts',(72.66582508663,232.909363756353,44.9895072004247));
#33498=CARTESIAN_POINT('Ctrl Pts',(75.291168219243,232.697207746801,45.0896778936393));
#33499=CARTESIAN_POINT('Ctrl Pts',(77.9165113518563,232.485051737248,45.1898485868539));
#33500=CARTESIAN_POINT('Ctrl Pts',(80.4921434076196,232.272895727696,46.7274962062725));
#33501=CARTESIAN_POINT('Ctrl Pts',(81.8276330377482,232.060739718143,48.9925328420896));
#33502=CARTESIAN_POINT('Ctrl Pts',(82.5391017081758,231.947715737549,50.1992083320366));
#33503=CARTESIAN_POINT('Ctrl Pts',(82.8986032654198,231.834691756955,51.6123254426967));
#33504=CARTESIAN_POINT('Ctrl Pts',(82.9002267075262,231.721667776361,53.0243475551716));
#33505=CARTESIAN_POINT('Origin',(74.9879498948689,255.,53.0228109606356));
#33506=CARTESIAN_POINT('',(82.9129498948689,226.278332223638,53.0228109606316));
#33507=CARTESIAN_POINT('',(82.9129498948689,227.721667776361,53.022810960645));
#33508=CARTESIAN_POINT('',(82.9129498948689,255.,53.0228109606356));
#33509=CARTESIAN_POINT('Ctrl Pts',(82.9129498948689,226.278332223638,53.0228109606311));
#33510=CARTESIAN_POINT('Ctrl Pts',(82.9129498948677,226.455428795637,50.8182135007215));
#33511=CARTESIAN_POINT('Ctrl Pts',(81.9432795991084,226.632525367636,48.6308565362859));
#33512=CARTESIAN_POINT('Ctrl Pts',(80.3096882702513,226.809621939634,47.1504412801759));
#33513=CARTESIAN_POINT('Ctrl Pts',(78.6760969413943,226.986718511633,45.6700260240659));
#33514=CARTESIAN_POINT('Ctrl Pts',(76.4041347530408,227.163815083632,44.9197069006025));
#33515=CARTESIAN_POINT('Ctrl Pts',(74.2101800112185,227.34091165563,45.1360689838694));
#33516=CARTESIAN_POINT('Ctrl Pts',(72.0162252693962,227.518008227629,45.3524310671362));
#33517=CARTESIAN_POINT('Ctrl Pts',(69.9345925076953,227.695104799628,46.5320903475034));
#33518=CARTESIAN_POINT('Ctrl Pts',(68.621646765659,227.872201371627,48.3030853894809));
#33519=CARTESIAN_POINT('Ctrl Pts',(67.3087010236226,228.049297943625,50.0740804314583));
#33520=CARTESIAN_POINT('Ctrl Pts',(66.7849774198237,228.226394515624,52.4087119996435));
#33521=CARTESIAN_POINT('Ctrl Pts',(67.2156126057611,228.403491087623,54.5708413428774));
#33522=CARTESIAN_POINT('Ctrl Pts',(67.6462477916984,228.580587659622,56.7329706861112));
#33523=CARTESIAN_POINT('Ctrl Pts',(69.0245064207982,228.75768423162,58.6887810357246));
#33524=CARTESIAN_POINT('Ctrl Pts',(70.9158061804482,228.934780803619,59.8215807441408));
#33525=CARTESIAN_POINT('Ctrl Pts',(72.8071059400983,229.111877375618,60.9543804525571));
#33526=CARTESIAN_POINT('Ctrl Pts',(75.1818659698118,229.288973947616,61.2464519739653));
#33527=CARTESIAN_POINT('Ctrl Pts',(77.2912945088681,229.466070519615,60.6057014773951));
#33528=CARTESIAN_POINT('Ctrl Pts',(79.4007230479244,229.643167091614,59.9649509808248));
#33529=CARTESIAN_POINT('Ctrl Pts',(81.2118275942084,229.820263663613,58.4014001198765));
#33530=CARTESIAN_POINT('Ctrl Pts',(82.1535440633104,229.997360235611,56.4080561826539));
#33531=CARTESIAN_POINT('Ctrl Pts',(82.6515697929918,230.091017564954,55.3538784110917));
#33532=CARTESIAN_POINT('Ctrl Pts',(82.9129498948695,230.184674894296,54.1887099277299));
#33533=CARTESIAN_POINT('Ctrl Pts',(82.9129498948689,230.278332223638,53.0228109606318));
#33534=CARTESIAN_POINT('Ctrl Pts',(82.9129498948689,231.721667776361,53.0228109606451));
#33535=CARTESIAN_POINT('Ctrl Pts',(82.9129498948662,231.544571204362,55.227408420555));
#33536=CARTESIAN_POINT('Ctrl Pts',(81.9432795991054,231.367474632363,57.4147653849901));
#33537=CARTESIAN_POINT('Ctrl Pts',(80.3096882702472,231.190378060365,58.895180641099));
#33538=CARTESIAN_POINT('Ctrl Pts',(78.676096941389,231.013281488366,60.375595897208));
#33539=CARTESIAN_POINT('Ctrl Pts',(76.4041347530348,230.836184916367,61.1259150206698));
#33540=CARTESIAN_POINT('Ctrl Pts',(74.2101800112125,230.659088344369,60.9095529374012));
#33541=CARTESIAN_POINT('Ctrl Pts',(72.0162252693902,230.48199177237,60.6931908541326));
#33542=CARTESIAN_POINT('Ctrl Pts',(69.9345925076901,230.304895200371,59.5135315737637));
#33543=CARTESIAN_POINT('Ctrl Pts',(68.6216467656551,230.127798628372,57.742536531785));
#33544=CARTESIAN_POINT('Ctrl Pts',(67.30870102362,229.950702056374,55.9715414898064));
#33545=CARTESIAN_POINT('Ctrl Pts',(66.7849774198232,229.773605484375,53.6369099216206));
#33546=CARTESIAN_POINT('Ctrl Pts',(67.2156126057624,229.596508912376,51.474780578387));
#33547=CARTESIAN_POINT('Ctrl Pts',(67.6462477917017,229.419412340377,49.3126512351533));
#33548=CARTESIAN_POINT('Ctrl Pts',(69.0245064208034,229.242315768379,47.3568408855411));
#33549=CARTESIAN_POINT('Ctrl Pts',(70.9158061804546,229.06521919638,46.2240411771265));
#33550=CARTESIAN_POINT('Ctrl Pts',(72.8071059401058,228.888122624381,45.0912414687119));
#33551=CARTESIAN_POINT('Ctrl Pts',(75.1818659698198,228.711026052382,44.799169947306));
#33552=CARTESIAN_POINT('Ctrl Pts',(77.2912945088756,228.533929480384,45.4399204438784));
#33553=CARTESIAN_POINT('Ctrl Pts',(79.4007230479314,228.356832908385,46.0806709404508));
#33554=CARTESIAN_POINT('Ctrl Pts',(81.211827594214,228.179736336386,47.644221801401));
#33555=CARTESIAN_POINT('Ctrl Pts',(82.1535440633139,228.002639764388,49.6375657386248));
#33556=CARTESIAN_POINT('Ctrl Pts',(82.6515697929938,227.908982435045,50.6917435101865));
#33557=CARTESIAN_POINT('Ctrl Pts',(82.9129498948702,227.815325105703,51.8569119935475));
#33558=CARTESIAN_POINT('Ctrl Pts',(82.9129498948689,227.721667776361,53.0228109606445));
#33559=CARTESIAN_POINT('Origin',(74.9879498948689,255.,53.0228109606356));
#33560=CARTESIAN_POINT('',(82.9129498948689,222.278332223638,53.0228109606314));
#33561=CARTESIAN_POINT('',(82.9158285778574,223.721667776361,53.0209513109217));
#33562=CARTESIAN_POINT('',(82.9129498948689,255.,53.0228109606356));
#33563=CARTESIAN_POINT('Ctrl Pts',(82.9129498948689,222.278332223638,53.022810960631));
#33564=CARTESIAN_POINT('Ctrl Pts',(82.9129498948676,222.455428795637,50.8182135007211));
#33565=CARTESIAN_POINT('Ctrl Pts',(81.9432795991081,222.632525367636,48.6308565362855));
#33566=CARTESIAN_POINT('Ctrl Pts',(80.3096882702508,222.809621939634,47.1504412801755));
#33567=CARTESIAN_POINT('Ctrl Pts',(78.6760969413936,222.986718511633,45.6700260240655));
#33568=CARTESIAN_POINT('Ctrl Pts',(76.4041347530399,223.163815083632,44.9197069006023));
#33569=CARTESIAN_POINT('Ctrl Pts',(74.2101800112174,223.340911655631,45.1360689838695));
#33570=CARTESIAN_POINT('Ctrl Pts',(72.016225269395,223.518008227629,45.3524310671366));
#33571=CARTESIAN_POINT('Ctrl Pts',(69.9345925076942,223.695104799628,46.5320903475043));
#33572=CARTESIAN_POINT('Ctrl Pts',(68.621646765658,223.872201371627,48.3030853894821));
#33573=CARTESIAN_POINT('Ctrl Pts',(67.3087010236219,224.049297943625,50.0740804314599));
#33574=CARTESIAN_POINT('Ctrl Pts',(66.7849774198236,224.226394515624,52.4087119996454));
#33575=CARTESIAN_POINT('Ctrl Pts',(67.2156126057615,224.403491087623,54.5708413428793));
#33576=CARTESIAN_POINT('Ctrl Pts',(67.6462477916993,224.580587659622,56.7329706861132));
#33577=CARTESIAN_POINT('Ctrl Pts',(69.0245064207998,224.75768423162,58.6887810357263));
#33578=CARTESIAN_POINT('Ctrl Pts',(70.9158061804503,224.934780803619,59.8215807441421));
#33579=CARTESIAN_POINT('Ctrl Pts',(72.8071059401008,225.111877375618,60.9543804525578));
#33580=CARTESIAN_POINT('Ctrl Pts',(75.1818659698146,225.288973947617,61.2464519739653));
#33581=CARTESIAN_POINT('Ctrl Pts',(77.2912945088708,225.466070519615,60.6057014773942));
#33582=CARTESIAN_POINT('Ctrl Pts',(79.400723047927,225.643167091614,59.9649509808232));
#33583=CARTESIAN_POINT('Ctrl Pts',(81.2118275942106,225.820263663613,58.4014001198741));
#33584=CARTESIAN_POINT('Ctrl Pts',(82.1535440633118,225.997360235611,56.4080561826509));
#33585=CARTESIAN_POINT('Ctrl Pts',(82.6515697929923,226.091017564954,55.3538784110893));
#33586=CARTESIAN_POINT('Ctrl Pts',(82.9129498948696,226.184674894296,54.1887099277284));
#33587=CARTESIAN_POINT('Ctrl Pts',(82.9129498948689,226.278332223638,53.0228109606311));
#33588=CARTESIAN_POINT('Ctrl Pts',(82.9129498948689,227.721667776361,53.0228109606445));
#33589=CARTESIAN_POINT('Ctrl Pts',(82.9129498948664,227.544571204362,55.2274084205545));
#33590=CARTESIAN_POINT('Ctrl Pts',(81.9432795991056,227.367474632363,57.4147653849898));
#33591=CARTESIAN_POINT('Ctrl Pts',(80.3096882702473,227.190378060365,58.8951806410989));
#33592=CARTESIAN_POINT('Ctrl Pts',(78.676096941389,227.013281488366,60.375595897208));
#33593=CARTESIAN_POINT('Ctrl Pts',(76.4041347530346,226.836184916367,61.1259150206698));
#33594=CARTESIAN_POINT('Ctrl Pts',(74.2101800112122,226.659088344369,60.9095529374012));
#33595=CARTESIAN_POINT('Ctrl Pts',(72.0162252693897,226.48199177237,60.6931908541325));
#33596=CARTESIAN_POINT('Ctrl Pts',(69.9345925076896,226.304895200371,59.5135315737633));
#33597=CARTESIAN_POINT('Ctrl Pts',(68.6216467656546,226.127798628372,57.7425365317845));
#33598=CARTESIAN_POINT('Ctrl Pts',(67.3087010236197,225.950702056374,55.9715414898056));
#33599=CARTESIAN_POINT('Ctrl Pts',(66.7849774198231,225.773605484375,53.6369099216195));
#33600=CARTESIAN_POINT('Ctrl Pts',(67.2156126057626,225.596508912376,51.4747805783858));
#33601=CARTESIAN_POINT('Ctrl Pts',(67.6462477917023,225.419412340377,49.3126512351521));
#33602=CARTESIAN_POINT('Ctrl Pts',(69.0245064208044,225.242315768379,47.3568408855399));
#33603=CARTESIAN_POINT('Ctrl Pts',(70.915806180456,225.06521919638,46.2240411771257));
#33604=CARTESIAN_POINT('Ctrl Pts',(72.8071059401075,224.888122624381,45.0912414687114));
#33605=CARTESIAN_POINT('Ctrl Pts',(75.1818659698218,224.711026052382,44.799169947306));
#33606=CARTESIAN_POINT('Ctrl Pts',(77.2912945088776,224.533929480384,45.439920443879));
#33607=CARTESIAN_POINT('Ctrl Pts',(79.4007230479334,224.356832908385,46.080670940452));
#33608=CARTESIAN_POINT('Ctrl Pts',(81.2118275942156,224.179736336386,47.6442218014028));
#33609=CARTESIAN_POINT('Ctrl Pts',(82.153544063315,224.002639764387,49.6375657386271));
#33610=CARTESIAN_POINT('Ctrl Pts',(82.6515697929941,223.908982435045,50.6917435101881));
#33611=CARTESIAN_POINT('Ctrl Pts',(82.9129498948702,223.815325105703,51.8569119935482));
#33612=CARTESIAN_POINT('Ctrl Pts',(82.9129498948689,223.721667776361,53.0228109606443));
#33613=CARTESIAN_POINT('Origin',(74.9879498948689,255.,53.0228109606356));
#33614=CARTESIAN_POINT('',(82.9088343949514,218.278332223638,53.0245926135986));
#33615=CARTESIAN_POINT('',(82.9093646881469,219.721667776361,53.0220566607781));
#33616=CARTESIAN_POINT('',(82.9129498948689,255.,53.0228109606356));
#33617=CARTESIAN_POINT('Ctrl Pts',(82.9129498948689,218.278332223638,53.0228109606313));
#33618=CARTESIAN_POINT('Ctrl Pts',(82.9129498948677,218.455428795637,50.8182135007216));
#33619=CARTESIAN_POINT('Ctrl Pts',(81.9432795991084,218.632525367636,48.630856536286));
#33620=CARTESIAN_POINT('Ctrl Pts',(80.3096882702514,218.809621939634,47.150441280176));
#33621=CARTESIAN_POINT('Ctrl Pts',(78.6760969413944,218.986718511633,45.6700260240659));
#33622=CARTESIAN_POINT('Ctrl Pts',(76.4041347530409,219.163815083632,44.9197069006025));
#33623=CARTESIAN_POINT('Ctrl Pts',(74.2101800112186,219.34091165563,45.1360689838693));
#33624=CARTESIAN_POINT('Ctrl Pts',(72.0162252693963,219.518008227629,45.3524310671362));
#33625=CARTESIAN_POINT('Ctrl Pts',(69.9345925076954,219.695104799628,46.5320903475034));
#33626=CARTESIAN_POINT('Ctrl Pts',(68.621646765659,219.872201371627,48.3030853894808));
#33627=CARTESIAN_POINT('Ctrl Pts',(67.3087010236226,220.049297943625,50.0740804314582));
#33628=CARTESIAN_POINT('Ctrl Pts',(66.7849774198237,220.226394515624,52.4087119996434));
#33629=CARTESIAN_POINT('Ctrl Pts',(67.215612605761,220.403491087623,54.5708413428773));
#33630=CARTESIAN_POINT('Ctrl Pts',(67.6462477916983,220.580587659622,56.7329706861111));
#33631=CARTESIAN_POINT('Ctrl Pts',(69.0245064207981,220.75768423162,58.6887810357245));
#33632=CARTESIAN_POINT('Ctrl Pts',(70.9158061804481,220.934780803619,59.8215807441408));
#33633=CARTESIAN_POINT('Ctrl Pts',(72.8071059400982,221.111877375618,60.9543804525571));
#33634=CARTESIAN_POINT('Ctrl Pts',(75.1818659698117,221.288973947616,61.2464519739653));
#33635=CARTESIAN_POINT('Ctrl Pts',(77.291294508868,221.466070519615,60.6057014773951));
#33636=CARTESIAN_POINT('Ctrl Pts',(79.4007230479243,221.643167091614,59.9649509808249));
#33637=CARTESIAN_POINT('Ctrl Pts',(81.2118275942083,221.820263663612,58.4014001198766));
#33638=CARTESIAN_POINT('Ctrl Pts',(82.1535440633103,221.997360235611,56.408056182654));
#33639=CARTESIAN_POINT('Ctrl Pts',(82.6515697929919,222.091017564954,55.3538784110915));
#33640=CARTESIAN_POINT('Ctrl Pts',(82.9129498948696,222.184674894296,54.1887099277294));
#33641=CARTESIAN_POINT('Ctrl Pts',(82.9129498948689,222.278332223638,53.022810960631));
#33642=CARTESIAN_POINT('Ctrl Pts',(82.9234447883723,223.721667776361,53.0160311846121));
#33643=CARTESIAN_POINT('Ctrl Pts',(82.907270754594,223.531174289889,55.3785973853056));
#33644=CARTESIAN_POINT('Ctrl Pts',(81.7821471756311,223.340680803418,57.758561145984));
#33645=CARTESIAN_POINT('Ctrl Pts',(79.9363556092803,223.150187316946,59.230684047091));
#33646=CARTESIAN_POINT('Ctrl Pts',(77.8806644650022,222.938031307394,60.8702137026943));
#33647=CARTESIAN_POINT('Ctrl Pts',(74.9310800947544,222.725875297841,61.3836869650193));
#33648=CARTESIAN_POINT('Ctrl Pts',(72.4412170677322,222.513719288289,60.5401705955808));
#33649=CARTESIAN_POINT('Ctrl Pts',(69.9513540407098,222.301563278737,59.6966542261423));
#33650=CARTESIAN_POINT('Ctrl Pts',(67.9212123569129,222.089407269185,57.4961482249402));
#33651=CARTESIAN_POINT('Ctrl Pts',(67.285320134102,221.877251259632,54.944763374811));
#33652=CARTESIAN_POINT('Ctrl Pts',(66.6494279112911,221.66509525008,52.3933785246817));
#33653=CARTESIAN_POINT('Ctrl Pts',(67.407785149466,221.452939240528,49.4911148256255));
#33654=CARTESIAN_POINT('Ctrl Pts',(69.2094682792691,221.240783230975,47.5789435076261));
#33655=CARTESIAN_POINT('Ctrl Pts',(71.0111514090722,221.028627221423,45.6667721896267));
#33656=CARTESIAN_POINT('Ctrl Pts',(73.8561604305038,220.816471211871,44.7446932526844));
#33657=CARTESIAN_POINT('Ctrl Pts',(76.4434042330216,220.604315202319,45.2222810130445));
#33658=CARTESIAN_POINT('Ctrl Pts',(77.7370261342805,220.498237197542,45.4610748932245));
#33659=CARTESIAN_POINT('Ctrl Pts',(78.9662067308111,220.392159192766,46.0497854477303));
#33660=CARTESIAN_POINT('Ctrl Pts',(79.992668284066,220.28608118799,46.8870301906149));
#33661=CARTESIAN_POINT('Ctrl Pts',(81.0191298373208,220.180003183214,47.7242749334995));
#33662=CARTESIAN_POINT('Ctrl Pts',(81.8428723473001,220.073925178438,48.8100538647629));
#33663=CARTESIAN_POINT('Ctrl Pts',(82.336788967223,219.967847173662,50.0292860659892));
#33664=CARTESIAN_POINT('Ctrl Pts',(82.7188728750852,219.885787374561,50.9724594382655));
#33665=CARTESIAN_POINT('Ctrl Pts',(82.9035805041128,219.803727575461,51.995494672869));
#33666=CARTESIAN_POINT('Ctrl Pts',(82.8989973990194,219.721667776361,53.0198754630378));
#33667=CARTESIAN_POINT('Origin',(74.9879498948689,255.,53.0228109606356));
#33668=CARTESIAN_POINT('',(82.9155886507495,214.278332223638,53.0240128735546));
#33669=CARTESIAN_POINT('',(82.9129498948689,215.721667776361,53.0228109606445));
#33670=CARTESIAN_POINT('',(82.9129498948689,255.,53.0228109606356));
#33671=CARTESIAN_POINT('Ctrl Pts',(82.9225333537804,214.278332223638,53.0271760795405));
#33672=CARTESIAN_POINT('Ctrl Pts',(82.906990815689,214.469208481852,50.6594335019644));
#33673=CARTESIAN_POINT('Ctrl Pts',(81.7792862151741,214.660084740066,48.278630556164));
#33674=CARTESIAN_POINT('Ctrl Pts',(79.9265027100333,214.85096099828,46.8074088927466));
#33675=CARTESIAN_POINT('Ctrl Pts',(77.8671624930109,215.063117007833,45.1721687628427));
#33676=CARTESIAN_POINT('Ctrl Pts',(74.912061336723,215.275273017385,44.6606234179444));
#33677=CARTESIAN_POINT('Ctrl Pts',(72.4256081920683,215.487429026937,45.5088026735112));
#33678=CARTESIAN_POINT('Ctrl Pts',(69.9391550474136,215.69958503649,46.3569819290781));
#33679=CARTESIAN_POINT('Ctrl Pts',(67.9213499143921,215.911741046042,48.5648857851099));
#33680=CARTESIAN_POINT('Ctrl Pts',(67.2847849840505,216.123897055594,51.1176627810452));
#33681=CARTESIAN_POINT('Ctrl Pts',(66.9665025188798,216.22997506037,52.3940512790129));
#33682=CARTESIAN_POINT('Ctrl Pts',(66.993530104379,216.336053065147,53.7566580619564));
#33683=CARTESIAN_POINT('Ctrl Pts',(67.3306293105148,216.442131069923,55.0376640357496));
#33684=CARTESIAN_POINT('Ctrl Pts',(67.6677285166505,216.548209074699,56.318670009543));
#33685=CARTESIAN_POINT('Ctrl Pts',(68.3148993434228,216.654287079475,57.5180751741862));
#33686=CARTESIAN_POINT('Ctrl Pts',(69.2201496857532,216.760365084251,58.4725139703031));
#33687=CARTESIAN_POINT('Ctrl Pts',(71.0306503704139,216.972521093803,60.3813915625367));
#33688=CARTESIAN_POINT('Ctrl Pts',(73.8734691173067,217.184677103356,61.3104036806656));
#33689=CARTESIAN_POINT('Ctrl Pts',(76.4554961749134,217.396833112908,60.8249171391498));
#33690=CARTESIAN_POINT('Ctrl Pts',(79.0375232325201,217.60898912246,60.3394305976341));
#33691=CARTESIAN_POINT('Ctrl Pts',(81.3587586008407,217.821145132013,58.4394453964739));
#33692=CARTESIAN_POINT('Ctrl Pts',(82.3463226381038,218.033301141565,56.0025168924015));
#33693=CARTESIAN_POINT('Ctrl Pts',(82.7265206586982,218.114978168923,55.0643342950013));
#33694=CARTESIAN_POINT('Ctrl Pts',(82.9090499430764,218.19665519628,54.0465691935503));
#33695=CARTESIAN_POINT('Ctrl Pts',(82.9032295534682,218.278332223638,53.0270190217289));
#33696=CARTESIAN_POINT('Ctrl Pts',(82.9129498948689,219.721667776361,53.0228109606442));
#33697=CARTESIAN_POINT('Ctrl Pts',(82.9129498948665,219.544571204362,55.2274084205539));
#33698=CARTESIAN_POINT('Ctrl Pts',(81.943279599106,219.367474632364,57.4147653849889));
#33699=CARTESIAN_POINT('Ctrl Pts',(80.3096882702482,219.190378060365,58.8951806410981));
#33700=CARTESIAN_POINT('Ctrl Pts',(78.6760969413904,219.013281488366,60.3755958972072));
#33701=CARTESIAN_POINT('Ctrl Pts',(76.4041347530365,218.836184916367,61.1259150206694));
#33702=CARTESIAN_POINT('Ctrl Pts',(74.2101800112143,218.659088344369,60.9095529374014));
#33703=CARTESIAN_POINT('Ctrl Pts',(72.0162252693921,218.48199177237,60.6931908541333));
#33704=CARTESIAN_POINT('Ctrl Pts',(69.9345925076919,218.304895200371,59.513531573765));
#33705=CARTESIAN_POINT('Ctrl Pts',(68.6216467656565,218.127798628373,57.7425365317869));
#33706=CARTESIAN_POINT('Ctrl Pts',(67.308701023621,217.950702056374,55.9715414898088));
#33707=CARTESIAN_POINT('Ctrl Pts',(66.7849774198234,217.773605484375,53.6369099216233));
#33708=CARTESIAN_POINT('Ctrl Pts',(67.2156126057619,217.596508912376,51.4747805783897));
#33709=CARTESIAN_POINT('Ctrl Pts',(67.6462477917003,217.419412340378,49.312651235156));
#33710=CARTESIAN_POINT('Ctrl Pts',(69.0245064208012,217.242315768379,47.3568408855434));
#33711=CARTESIAN_POINT('Ctrl Pts',(70.9158061804518,217.06521919638,46.2240411771282));
#33712=CARTESIAN_POINT('Ctrl Pts',(72.8071059401024,216.888122624381,45.0912414687129));
#33713=CARTESIAN_POINT('Ctrl Pts',(75.1818659698161,216.711026052383,44.7991699473059));
#33714=CARTESIAN_POINT('Ctrl Pts',(77.2912945088721,216.533929480384,45.4399204438773));
#33715=CARTESIAN_POINT('Ctrl Pts',(79.4007230479281,216.356832908385,46.0806709404487));
#33716=CARTESIAN_POINT('Ctrl Pts',(81.2118275942113,216.179736336387,47.6442218013979));
#33717=CARTESIAN_POINT('Ctrl Pts',(82.1535440633122,216.002639764388,49.637565738621));
#33718=CARTESIAN_POINT('Ctrl Pts',(82.6515697929931,215.908982435046,50.6917435101838));
#33719=CARTESIAN_POINT('Ctrl Pts',(82.9129498948702,215.815325105703,51.856911993546));
#33720=CARTESIAN_POINT('Ctrl Pts',(82.9129498948689,215.721667776361,53.0228109606445));
#33721=CARTESIAN_POINT('Origin',(74.9879498948689,255.,53.0228109606356));
#33722=CARTESIAN_POINT('',(82.9128963053489,210.278332223638,53.0220763034151));
#33723=CARTESIAN_POINT('',(82.9259067049454,211.721667776361,53.0240434941313));
#33724=CARTESIAN_POINT('',(82.9129498948689,255.,53.0228109606356));
#33725=CARTESIAN_POINT('Ctrl Pts',(82.9129498948689,210.278332223638,53.0228109606305));
#33726=CARTESIAN_POINT('Ctrl Pts',(82.9129498948675,210.455428795637,50.8182135007206));
#33727=CARTESIAN_POINT('Ctrl Pts',(81.9432795991078,210.632525367636,48.630856536285));
#33728=CARTESIAN_POINT('Ctrl Pts',(80.3096882702505,210.809621939634,47.1504412801751));
#33729=CARTESIAN_POINT('Ctrl Pts',(78.6760969413931,210.986718511633,45.6700260240652));
#33730=CARTESIAN_POINT('Ctrl Pts',(76.4041347530393,211.163815083632,44.9197069006022));
#33731=CARTESIAN_POINT('Ctrl Pts',(74.2101800112169,211.340911655631,45.1360689838695));
#33732=CARTESIAN_POINT('Ctrl Pts',(72.0162252693945,211.518008227629,45.3524310671368));
#33733=CARTESIAN_POINT('Ctrl Pts',(69.9345925076938,211.695104799628,46.5320903475046));
#33734=CARTESIAN_POINT('Ctrl Pts',(68.6216467656577,211.872201371627,48.3030853894825));
#33735=CARTESIAN_POINT('Ctrl Pts',(67.3087010236217,212.049297943626,50.0740804314604));
#33736=CARTESIAN_POINT('Ctrl Pts',(66.7849774198235,212.226394515624,52.4087119996459));
#33737=CARTESIAN_POINT('Ctrl Pts',(67.2156126057615,212.403491087623,54.5708413428798));
#33738=CARTESIAN_POINT('Ctrl Pts',(67.6462477916996,212.580587659622,56.7329706861137));
#33739=CARTESIAN_POINT('Ctrl Pts',(69.0245064208002,212.75768423162,58.6887810357267));
#33740=CARTESIAN_POINT('Ctrl Pts',(70.9158061804508,212.934780803619,59.8215807441423));
#33741=CARTESIAN_POINT('Ctrl Pts',(72.8071059401013,213.111877375618,60.954380452558));
#33742=CARTESIAN_POINT('Ctrl Pts',(75.1818659698152,213.288973947617,61.2464519739653));
#33743=CARTESIAN_POINT('Ctrl Pts',(77.2912945088713,213.466070519615,60.6057014773941));
#33744=CARTESIAN_POINT('Ctrl Pts',(79.4007230479275,213.643167091614,59.9649509808229));
#33745=CARTESIAN_POINT('Ctrl Pts',(81.2118275942109,213.820263663613,58.4014001198737));
#33746=CARTESIAN_POINT('Ctrl Pts',(82.153544063312,213.997360235612,56.4080561826504));
#33747=CARTESIAN_POINT('Ctrl Pts',(82.6515697929924,214.091017564954,55.3538784110889));
#33748=CARTESIAN_POINT('Ctrl Pts',(82.9129498948696,214.184674894296,54.1887099277282));
#33749=CARTESIAN_POINT('Ctrl Pts',(82.9129498948689,214.278332223638,53.0228109606311));
#33750=CARTESIAN_POINT('Ctrl Pts',(82.9100628360345,215.721667776361,53.0273218344214));
#33751=CARTESIAN_POINT('Ctrl Pts',(82.9145791607339,215.651968841928,53.8964065984667));
#33752=CARTESIAN_POINT('Ctrl Pts',(82.7796363005651,215.582269907496,54.7639078768016));
#33753=CARTESIAN_POINT('Ctrl Pts',(82.4993576186766,215.512570973063,55.581539792728));
#33754=CARTESIAN_POINT('Ctrl Pts',(81.6462196590214,215.300414963511,58.0703228132649));
#33755=CARTESIAN_POINT('Ctrl Pts',(79.4465050799532,215.088258953958,60.097052386485));
#33756=CARTESIAN_POINT('Ctrl Pts',(76.8964746196261,214.876102944406,60.7288766829011));
#33757=CARTESIAN_POINT('Ctrl Pts',(74.346444159299,214.663946934854,61.3607009793171));
#33758=CARTESIAN_POINT('Ctrl Pts',(71.446097817713,214.451790925301,60.597619998929));
#33759=CARTESIAN_POINT('Ctrl Pts',(69.5345770260846,214.239634915749,58.7918014379804));
#33760=CARTESIAN_POINT('Ctrl Pts',(67.6230562344562,214.027478906197,56.9859828770317));
#33761=CARTESIAN_POINT('Ctrl Pts',(66.7003609927855,213.815322896644,54.1374267355225));
#33762=CARTESIAN_POINT('Ctrl Pts',(67.1874014817734,213.603166887092,51.5539497122178));
#33763=CARTESIAN_POINT('Ctrl Pts',(67.6744419707613,213.39101087754,48.9704726889132));
#33764=CARTESIAN_POINT('Ctrl Pts',(69.5712181904076,213.178854867988,46.6520747838132));
#33765=CARTESIAN_POINT('Ctrl Pts',(72.0073869599948,212.966698858435,45.6651863848547));
#33766=CARTESIAN_POINT('Ctrl Pts',(74.4435557295822,212.754542848883,44.6782979858962));
#33767=CARTESIAN_POINT('Ctrl Pts',(77.4191170491105,212.54238683933,45.0229190930795));
#33768=CARTESIAN_POINT('Ctrl Pts',(79.5668964072261,212.330230829778,46.5390344569979));
#33769=CARTESIAN_POINT('Ctrl Pts',(81.6205096374134,212.127376478639,47.9886780426244));
#33770=CARTESIAN_POINT('Ctrl Pts',(82.9173353903022,211.9245221275,50.5093430137754));
#33771=CARTESIAN_POINT('Ctrl Pts',(82.9259067049454,211.721667776361,53.0240434941313));
#33772=CARTESIAN_POINT('Origin',(74.9879498948689,255.,53.0228109606356));
#33773=CARTESIAN_POINT('',(82.910875927569,206.278332223638,53.0225169327894));
#33774=CARTESIAN_POINT('',(82.9116710970601,207.721667776361,53.0156229854146));
#33775=CARTESIAN_POINT('',(82.9129498948689,255.,53.0228109606356));
#33776=CARTESIAN_POINT('Ctrl Pts',(82.9061037343352,206.278332223638,53.0218403755537));
#33777=CARTESIAN_POINT('Ctrl Pts',(82.9073297587047,206.377847024339,51.7792408097306));
#33778=CARTESIAN_POINT('Ctrl Pts',(82.6266185356372,206.47736182504,50.5372467636587));
#33779=CARTESIAN_POINT('Ctrl Pts',(82.0668914032528,206.57687662574,49.4373940912735));
#33780=CARTESIAN_POINT('Ctrl Pts',(80.8736068464957,206.789032635293,47.0926136925203));
#33781=CARTESIAN_POINT('Ctrl Pts',(78.4121907958689,207.001188644845,45.3938679696944));
#33782=CARTESIAN_POINT('Ctrl Pts',(75.7986914495842,207.213344654397,45.1253922903185));
#33783=CARTESIAN_POINT('Ctrl Pts',(73.1851921032995,207.425500663949,44.8569166109425));
#33784=CARTESIAN_POINT('Ctrl Pts',(70.4196094613566,207.637656673502,46.0187109750167));
#33785=CARTESIAN_POINT('Ctrl Pts',(68.780078490162,207.849812683054,48.0744034917667));
#33786=CARTESIAN_POINT('Ctrl Pts',(67.1405475189675,208.061968692606,50.1300960085167));
#33787=CARTESIAN_POINT('Ctrl Pts',(66.6270682185208,208.274124702159,53.0796866779427));
#33788=CARTESIAN_POINT('Ctrl Pts',(67.4705872150538,208.486280711711,55.5695469642904));
#33789=CARTESIAN_POINT('Ctrl Pts',(68.3141062115868,208.698436721263,58.0594072506382));
#33790=CARTESIAN_POINT('Ctrl Pts',(70.5146235050995,208.910592730815,60.0895371539075));
#33791=CARTESIAN_POINT('Ctrl Pts',(73.0660029762825,209.122748740368,60.7254349882198));
#33792=CARTESIAN_POINT('Ctrl Pts',(75.6173824474655,209.33490474992,61.3613328225322));
#33793=CARTESIAN_POINT('Ctrl Pts',(78.5196240963186,209.547060759473,60.6029985878876));
#33794=CARTESIAN_POINT('Ctrl Pts',(80.4318085557769,209.759216769025,58.8013017484574));
#33795=CARTESIAN_POINT('Ctrl Pts',(81.9914226452245,209.932255253896,57.3318034676876));
#33796=CARTESIAN_POINT('Ctrl Pts',(82.8924165854151,210.105293738767,55.1682244390036));
#33797=CARTESIAN_POINT('Ctrl Pts',(82.9124953745832,210.278332223638,53.0165799548811));
#33798=CARTESIAN_POINT('Ctrl Pts',(82.9259067049454,211.721667776361,53.0240434941313));
#33799=CARTESIAN_POINT('Ctrl Pts',(82.9262997329505,211.712366117948,53.1393522599951));
#33800=CARTESIAN_POINT('Ctrl Pts',(82.9239841054999,211.703064459535,53.2546484850516));
#33801=CARTESIAN_POINT('Ctrl Pts',(82.9189085831446,211.693762801121,53.3698283356355));
#33802=CARTESIAN_POINT('Ctrl Pts',(82.8031440042447,211.481606791569,55.9968972297008));
#33803=CARTESIAN_POINT('Ctrl Pts',(81.2516174497423,211.269450782017,58.563425397178));
#33804=CARTESIAN_POINT('Ctrl Pts',(78.9808078930308,211.057294772464,59.8845163279184));
#33805=CARTESIAN_POINT('Ctrl Pts',(76.7099983363191,210.845138762912,61.205607258659));
#33806=CARTESIAN_POINT('Ctrl Pts',(73.7199057773981,210.63298275336,61.2812609526625));
#33807=CARTESIAN_POINT('Ctrl Pts',(71.3751524852751,210.420826743807,60.0879389925039));
#33808=CARTESIAN_POINT('Ctrl Pts',(70.2027758392138,210.314748739031,59.4912780124247));
#33809=CARTESIAN_POINT('Ctrl Pts',(69.1917340098519,210.208670734255,58.5773731188052));
#33810=CARTESIAN_POINT('Ctrl Pts',(68.4456231577739,210.102592729479,57.4828728784752));
#33811=CARTESIAN_POINT('Ctrl Pts',(67.6995123056957,209.996514724703,56.3883726381449));
#33812=CARTESIAN_POINT('Ctrl Pts',(67.2183324309016,209.890436719926,55.1132770511039));
#33813=CARTESIAN_POINT('Ctrl Pts',(67.0913314365078,209.78435871515,53.8039633586506));
#33814=CARTESIAN_POINT('Ctrl Pts',(66.8373294477203,209.572202705598,51.1853359737447));
#33815=CARTESIAN_POINT('Ctrl Pts',(68.0000429805332,209.360046696046,48.4298361671897));
#33816=CARTESIAN_POINT('Ctrl Pts',(70.05969095471,209.147890686494,46.7987594888346));
#33817=CARTESIAN_POINT('Ctrl Pts',(72.1193389288871,208.935734676941,45.1676828104792));
#33818=CARTESIAN_POINT('Ctrl Pts',(75.0759213444285,208.723578667389,44.6610292603245));
#33819=CARTESIAN_POINT('Ctrl Pts',(77.5633691966018,208.511422657836,45.5133827341697));
#33820=CARTESIAN_POINT('Ctrl Pts',(80.050817048775,208.299266648284,46.3657362080148));
#33821=CARTESIAN_POINT('Ctrl Pts',(82.0691303375802,208.087110638732,48.5770967058599));
#33822=CARTESIAN_POINT('Ctrl Pts',(82.6960193572198,207.87495462918,51.1301221072413));
#33823=CARTESIAN_POINT('Ctrl Pts',(82.84699920312,207.823859011574,51.7449923148922));
#33824=CARTESIAN_POINT('Ctrl Pts',(82.9172711199504,207.772763393967,52.3796803936349));
#33825=CARTESIAN_POINT('Ctrl Pts',(82.9116710970601,207.721667776361,53.0156229854146));
#33826=CARTESIAN_POINT('Origin',(74.9879498948689,255.,53.0228109606356));
#33827=CARTESIAN_POINT('',(82.9129498948689,202.278332223638,53.0228109606306));
#33828=CARTESIAN_POINT('',(82.9084421270908,203.721667776361,53.0232477115732));
#33829=CARTESIAN_POINT('',(82.9129498948689,255.,53.0228109606356));
#33830=CARTESIAN_POINT('Ctrl Pts',(82.9129498948689,202.278332223638,53.0228109606301));
#33831=CARTESIAN_POINT('Ctrl Pts',(82.9129498948674,202.455428795637,50.8182135007201));
#33832=CARTESIAN_POINT('Ctrl Pts',(81.9432795991075,202.632525367636,48.6308565362844));
#33833=CARTESIAN_POINT('Ctrl Pts',(80.3096882702499,202.809621939634,47.1504412801746));
#33834=CARTESIAN_POINT('Ctrl Pts',(78.6760969413923,202.986718511633,45.6700260240648));
#33835=CARTESIAN_POINT('Ctrl Pts',(76.4041347530382,203.163815083632,44.9197069006019));
#33836=CARTESIAN_POINT('Ctrl Pts',(74.2101800112157,203.340911655631,45.1360689838696));
#33837=CARTESIAN_POINT('Ctrl Pts',(72.0162252693931,203.518008227629,45.3524310671373));
#33838=CARTESIAN_POINT('Ctrl Pts',(69.9345925076925,203.695104799628,46.5320903475056));
#33839=CARTESIAN_POINT('Ctrl Pts',(68.6216467656567,203.872201371627,48.3030853894839));
#33840=CARTESIAN_POINT('Ctrl Pts',(67.308701023621,204.049297943626,50.0740804314622));
#33841=CARTESIAN_POINT('Ctrl Pts',(66.7849774198233,204.226394515624,52.408711999648));
#33842=CARTESIAN_POINT('Ctrl Pts',(67.215612605762,204.403491087623,54.5708413428819));
#33843=CARTESIAN_POINT('Ctrl Pts',(67.6462477917006,204.580587659622,56.7329706861158));
#33844=CARTESIAN_POINT('Ctrl Pts',(69.0245064208019,204.757684231621,58.6887810357286));
#33845=CARTESIAN_POINT('Ctrl Pts',(70.915806180453,204.934780803619,59.8215807441437));
#33846=CARTESIAN_POINT('Ctrl Pts',(72.8071059401041,205.111877375618,60.9543804525588));
#33847=CARTESIAN_POINT('Ctrl Pts',(75.1818659698182,205.288973947617,61.2464519739652));
#33848=CARTESIAN_POINT('Ctrl Pts',(77.2912945088742,205.466070519616,60.6057014773932));
#33849=CARTESIAN_POINT('Ctrl Pts',(79.4007230479303,205.643167091614,59.9649509808211));
#33850=CARTESIAN_POINT('Ctrl Pts',(81.2118275942133,205.820263663613,58.4014001198711));
#33851=CARTESIAN_POINT('Ctrl Pts',(82.1535440633135,205.997360235612,56.4080561826472));
#33852=CARTESIAN_POINT('Ctrl Pts',(82.6515697929931,206.091017564954,55.3538784110864));
#33853=CARTESIAN_POINT('Ctrl Pts',(82.9129498948697,206.184674894296,54.1887099277265));
#33854=CARTESIAN_POINT('Ctrl Pts',(82.9129498948689,206.278332223638,53.0228109606303));
#33855=CARTESIAN_POINT('Ctrl Pts',(82.9116710970601,207.721667776361,53.0156229854146));
#33856=CARTESIAN_POINT('Ctrl Pts',(82.8940190571418,207.560607384415,55.0202012229607));
#33857=CARTESIAN_POINT('Ctrl Pts',(82.1225058291152,207.399546992469,57.0372442622787));
#33858=CARTESIAN_POINT('Ctrl Pts',(80.7485923473629,207.238486600523,58.4853563737063));
#33859=CARTESIAN_POINT('Ctrl Pts',(78.938811567392,207.02633059097,60.3928749338722));
#33860=CARTESIAN_POINT('Ctrl Pts',(76.0837852569762,206.814174581418,61.3132217492859));
#33861=CARTESIAN_POINT('Ctrl Pts',(73.5029374125956,206.602018571866,60.8216096790478));
#33862=CARTESIAN_POINT('Ctrl Pts',(70.9220895682152,206.389862562313,60.3299976088097));
#33863=CARTESIAN_POINT('Ctrl Pts',(68.6154201898701,206.177706552761,58.4264266529199));
#33864=CARTESIAN_POINT('Ctrl Pts',(67.6276125205348,205.965550543209,55.9879518918911));
#33865=CARTESIAN_POINT('Ctrl Pts',(67.1337086858671,205.859472538433,54.7687145113765));
#33866=CARTESIAN_POINT('Ctrl Pts',(66.969520278452,205.753394533656,53.4157511795768));
#33867=CARTESIAN_POINT('Ctrl Pts',(67.1238715200474,205.64731652888,52.1001609036867));
#33868=CARTESIAN_POINT('Ctrl Pts',(67.2782227616428,205.541238524104,50.7845706277968));
#33869=CARTESIAN_POINT('Ctrl Pts',(67.7511136522486,205.435160519328,49.5063534078162));
#33870=CARTESIAN_POINT('Ctrl Pts',(68.5138131866417,205.329082514552,48.4345467270829));
#33871=CARTESIAN_POINT('Ctrl Pts',(70.039212255428,205.116926504999,46.2909333656162));
#33872=CARTESIAN_POINT('Ctrl Pts',(72.7238458993632,204.904770495447,44.9729621611391));
#33873=CARTESIAN_POINT('Ctrl Pts',(75.3483980678444,204.692614485895,45.0920720453542));
#33874=CARTESIAN_POINT('Ctrl Pts',(77.9729502363255,204.480458476343,45.2111819295692));
#33875=CARTESIAN_POINT('Ctrl Pts',(80.5374209293524,204.26830246679,46.7673729024763));
#33876=CARTESIAN_POINT('Ctrl Pts',(81.8565334837811,204.056146457238,49.0419861973571));
#33877=CARTESIAN_POINT('Ctrl Pts',(82.5497576635792,203.944653563612,50.2373481324761));
#33878=CARTESIAN_POINT('Ctrl Pts',(82.8990455859946,203.833160669987,51.631120048613));
#33879=CARTESIAN_POINT('Ctrl Pts',(82.9001606972016,203.721667776361,53.0240500870242));
#33880=CARTESIAN_POINT('Origin',(74.9879498948689,255.,53.0228109606356));
#33881=CARTESIAN_POINT('',(82.9129498948689,198.278332223638,53.0228109606304));
#33882=CARTESIAN_POINT('',(82.9129498948689,199.721667776361,53.0228109606438));
#33883=CARTESIAN_POINT('',(82.9129498948689,255.,53.0228109606356));
#33884=CARTESIAN_POINT('Ctrl Pts',(82.9129498948689,198.278332223638,53.0228109606304));
#33885=CARTESIAN_POINT('Ctrl Pts',(82.9129498948675,198.455428795637,50.8182135007206));
#33886=CARTESIAN_POINT('Ctrl Pts',(81.9432795991078,198.632525367636,48.630856536285));
#33887=CARTESIAN_POINT('Ctrl Pts',(80.3096882702504,198.809621939634,47.1504412801751));
#33888=CARTESIAN_POINT('Ctrl Pts',(78.676096941393,198.986718511633,45.6700260240652));
#33889=CARTESIAN_POINT('Ctrl Pts',(76.4041347530393,199.163815083632,44.9197069006022));
#33890=CARTESIAN_POINT('Ctrl Pts',(74.2101800112168,199.340911655631,45.1360689838695));
#33891=CARTESIAN_POINT('Ctrl Pts',(72.0162252693944,199.518008227629,45.3524310671369));
#33892=CARTESIAN_POINT('Ctrl Pts',(69.9345925076937,199.695104799628,46.5320903475046));
#33893=CARTESIAN_POINT('Ctrl Pts',(68.6216467656577,199.872201371627,48.3030853894826));
#33894=CARTESIAN_POINT('Ctrl Pts',(67.3087010236217,200.049297943626,50.0740804314605));
#33895=CARTESIAN_POINT('Ctrl Pts',(66.7849774198235,200.226394515624,52.408711999646));
#33896=CARTESIAN_POINT('Ctrl Pts',(67.2156126057616,200.403491087623,54.5708413428799));
#33897=CARTESIAN_POINT('Ctrl Pts',(67.6462477916996,200.580587659622,56.7329706861138));
#33898=CARTESIAN_POINT('Ctrl Pts',(69.0245064208002,200.75768423162,58.6887810357267));
#33899=CARTESIAN_POINT('Ctrl Pts',(70.9158061804508,200.934780803619,59.8215807441424));
#33900=CARTESIAN_POINT('Ctrl Pts',(72.8071059401014,201.111877375618,60.954380452558));
#33901=CARTESIAN_POINT('Ctrl Pts',(75.1818659698152,201.288973947617,61.2464519739653));
#33902=CARTESIAN_POINT('Ctrl Pts',(77.2912945088714,201.466070519615,60.605701477394));
#33903=CARTESIAN_POINT('Ctrl Pts',(79.4007230479275,201.643167091614,59.9649509808228));
#33904=CARTESIAN_POINT('Ctrl Pts',(81.211827594211,201.820263663613,58.4014001198736));
#33905=CARTESIAN_POINT('Ctrl Pts',(82.153544063312,201.997360235612,56.4080561826503));
#33906=CARTESIAN_POINT('Ctrl Pts',(82.6515697929926,202.091017564954,55.3538784110886));
#33907=CARTESIAN_POINT('Ctrl Pts',(82.9129498948697,202.184674894296,54.1887099277275));
#33908=CARTESIAN_POINT('Ctrl Pts',(82.9129498948689,202.278332223638,53.0228109606301));
#33909=CARTESIAN_POINT('Ctrl Pts',(82.9129498948689,203.721667776361,53.0228109606435));
#33910=CARTESIAN_POINT('Ctrl Pts',(82.9129498948667,203.544571204362,55.2274084205535));
#33911=CARTESIAN_POINT('Ctrl Pts',(81.9432795991061,203.367474632364,57.4147653849889));
#33912=CARTESIAN_POINT('Ctrl Pts',(80.3096882702481,203.190378060365,58.8951806410982));
#33913=CARTESIAN_POINT('Ctrl Pts',(78.67609694139,203.013281488366,60.3755958972075));
#33914=CARTESIAN_POINT('Ctrl Pts',(76.4041347530357,202.836184916367,61.1259150206696));
#33915=CARTESIAN_POINT('Ctrl Pts',(74.2101800112132,202.659088344369,60.9095529374013));
#33916=CARTESIAN_POINT('Ctrl Pts',(72.0162252693907,202.48199177237,60.6931908541329));
#33917=CARTESIAN_POINT('Ctrl Pts',(69.9345925076904,202.304895200371,59.513531573764));
#33918=CARTESIAN_POINT('Ctrl Pts',(68.6216467656553,202.127798628372,57.7425365317853));
#33919=CARTESIAN_POINT('Ctrl Pts',(67.3087010236201,201.950702056374,55.9715414898066));
#33920=CARTESIAN_POINT('Ctrl Pts',(66.7849774198231,201.773605484375,53.6369099216206));
#33921=CARTESIAN_POINT('Ctrl Pts',(67.2156126057624,201.596508912376,51.4747805783868));
#33922=CARTESIAN_POINT('Ctrl Pts',(67.6462477917018,201.419412340377,49.312651235153));
#33923=CARTESIAN_POINT('Ctrl Pts',(69.0245064208037,201.242315768379,47.3568408855407));
#33924=CARTESIAN_POINT('Ctrl Pts',(70.9158061804551,201.06521919638,46.2240411771262));
#33925=CARTESIAN_POINT('Ctrl Pts',(72.8071059401065,200.888122624381,45.0912414687117));
#33926=CARTESIAN_POINT('Ctrl Pts',(75.1818659698207,200.711026052382,44.799169947306));
#33927=CARTESIAN_POINT('Ctrl Pts',(77.2912945088766,200.533929480384,45.4399204438787));
#33928=CARTESIAN_POINT('Ctrl Pts',(79.4007230479325,200.356832908385,46.0806709404514));
#33929=CARTESIAN_POINT('Ctrl Pts',(81.2118275942149,200.179736336386,47.644221801402));
#33930=CARTESIAN_POINT('Ctrl Pts',(82.1535440633146,200.002639764387,49.6375657386261));
#33931=CARTESIAN_POINT('Ctrl Pts',(82.6515697929939,199.908982435045,50.6917435101873));
#33932=CARTESIAN_POINT('Ctrl Pts',(82.9129498948701,199.815325105703,51.8569119935475));
#33933=CARTESIAN_POINT('Ctrl Pts',(82.9129498948689,199.721667776361,53.0228109606438));
#33934=CARTESIAN_POINT('Origin',(74.9879498948689,255.,53.0228109606356));
#33935=CARTESIAN_POINT('',(82.9129498948689,194.278332223638,53.0228109606302));
#33936=CARTESIAN_POINT('',(82.9158434391062,195.721667776361,53.0210929467476));
#33937=CARTESIAN_POINT('',(82.9129498948689,255.,53.0228109606356));
#33938=CARTESIAN_POINT('Ctrl Pts',(82.9129498948689,194.278332223638,53.0228109606302));
#33939=CARTESIAN_POINT('Ctrl Pts',(82.9129498948674,194.455428795637,50.8182135007204));
#33940=CARTESIAN_POINT('Ctrl Pts',(81.9432795991077,194.632525367636,48.6308565362848));
#33941=CARTESIAN_POINT('Ctrl Pts',(80.3096882702503,194.809621939634,47.150441280175));
#33942=CARTESIAN_POINT('Ctrl Pts',(78.6760969413929,194.986718511633,45.6700260240651));
#33943=CARTESIAN_POINT('Ctrl Pts',(76.4041347530391,195.163815083632,44.9197069006021));
#33944=CARTESIAN_POINT('Ctrl Pts',(74.2101800112167,195.340911655631,45.1360689838695));
#33945=CARTESIAN_POINT('Ctrl Pts',(72.0162252693943,195.518008227629,45.3524310671369));
#33946=CARTESIAN_POINT('Ctrl Pts',(69.9345925076936,195.695104799628,46.5320903475048));
#33947=CARTESIAN_POINT('Ctrl Pts',(68.6216467656576,195.872201371627,48.3030853894827));
#33948=CARTESIAN_POINT('Ctrl Pts',(67.3087010236216,196.049297943626,50.0740804314607));
#33949=CARTESIAN_POINT('Ctrl Pts',(66.7849774198235,196.226394515624,52.4087119996462));
#33950=CARTESIAN_POINT('Ctrl Pts',(67.2156126057616,196.403491087623,54.57084134288));
#33951=CARTESIAN_POINT('Ctrl Pts',(67.6462477916997,196.580587659622,56.7329706861139));
#33952=CARTESIAN_POINT('Ctrl Pts',(69.0245064208004,196.75768423162,58.6887810357269));
#33953=CARTESIAN_POINT('Ctrl Pts',(70.915806180451,196.934780803619,59.8215807441425));
#33954=CARTESIAN_POINT('Ctrl Pts',(72.8071059401016,197.111877375618,60.954380452558));
#33955=CARTESIAN_POINT('Ctrl Pts',(75.1818659698154,197.288973947617,61.2464519739653));
#33956=CARTESIAN_POINT('Ctrl Pts',(77.2912945088716,197.466070519615,60.605701477394));
#33957=CARTESIAN_POINT('Ctrl Pts',(79.4007230479277,197.643167091614,59.9649509808227));
#33958=CARTESIAN_POINT('Ctrl Pts',(81.2118275942111,197.820263663613,58.4014001198735));
#33959=CARTESIAN_POINT('Ctrl Pts',(82.1535440633121,197.997360235612,56.4080561826502));
#33960=CARTESIAN_POINT('Ctrl Pts',(82.6515697929926,198.091017564954,55.3538784110886));
#33961=CARTESIAN_POINT('Ctrl Pts',(82.9129498948697,198.184674894296,54.1887099277276));
#33962=CARTESIAN_POINT('Ctrl Pts',(82.9129498948689,198.278332223638,53.0228109606304));
#33963=CARTESIAN_POINT('Ctrl Pts',(82.9129498948689,199.721667776361,53.0228109606438));
#33964=CARTESIAN_POINT('Ctrl Pts',(82.9129498948666,199.544571204362,55.2274084205536));
#33965=CARTESIAN_POINT('Ctrl Pts',(81.9432795991061,199.367474632364,57.4147653849889));
#33966=CARTESIAN_POINT('Ctrl Pts',(80.3096882702482,199.190378060365,58.8951806410981));
#33967=CARTESIAN_POINT('Ctrl Pts',(78.6760969413902,199.013281488366,60.3755958972073));
#33968=CARTESIAN_POINT('Ctrl Pts',(76.4041347530362,198.836184916367,61.1259150206695));
#33969=CARTESIAN_POINT('Ctrl Pts',(74.2101800112138,198.659088344369,60.9095529374013));
#33970=CARTESIAN_POINT('Ctrl Pts',(72.0162252693915,198.48199177237,60.6931908541332));
#33971=CARTESIAN_POINT('Ctrl Pts',(69.9345925076912,198.304895200371,59.5135315737646));
#33972=CARTESIAN_POINT('Ctrl Pts',(68.6216467656559,198.127798628372,57.7425365317861));
#33973=CARTESIAN_POINT('Ctrl Pts',(67.3087010236206,197.950702056374,55.9715414898077));
#33974=CARTESIAN_POINT('Ctrl Pts',(66.7849774198233,197.773605484375,53.636909921622));
#33975=CARTESIAN_POINT('Ctrl Pts',(67.2156126057621,197.596508912376,51.4747805783883));
#33976=CARTESIAN_POINT('Ctrl Pts',(67.646247791701,197.419412340378,49.3126512351546));
#33977=CARTESIAN_POINT('Ctrl Pts',(69.0245064208024,197.242315768379,47.3568408855421));
#33978=CARTESIAN_POINT('Ctrl Pts',(70.9158061804534,197.06521919638,46.2240411771272));
#33979=CARTESIAN_POINT('Ctrl Pts',(72.8071059401044,196.888122624381,45.0912414687123));
#33980=CARTESIAN_POINT('Ctrl Pts',(75.1818659698184,196.711026052383,44.7991699473059));
#33981=CARTESIAN_POINT('Ctrl Pts',(77.2912945088743,196.533929480384,45.439920443878));
#33982=CARTESIAN_POINT('Ctrl Pts',(79.4007230479302,196.356832908385,46.08067094045));
#33983=CARTESIAN_POINT('Ctrl Pts',(81.211827594213,196.179736336386,47.6442218013999));
#33984=CARTESIAN_POINT('Ctrl Pts',(82.1535440633133,196.002639764388,49.6375657386235));
#33985=CARTESIAN_POINT('Ctrl Pts',(82.6515697929934,195.908982435045,50.6917435101853));
#33986=CARTESIAN_POINT('Ctrl Pts',(82.9129498948701,195.815325105703,51.8569119935464));
#33987=CARTESIAN_POINT('Ctrl Pts',(82.9129498948689,195.721667776361,53.0228109606436));
#33988=CARTESIAN_POINT('Origin',(74.9879498948689,255.,53.0228109606356));
#33989=CARTESIAN_POINT('',(82.9085809447878,190.278332223638,53.0245374982806));
#33990=CARTESIAN_POINT('',(82.9093019423321,191.721667776361,53.0219586769292));
#33991=CARTESIAN_POINT('',(82.9129498948689,255.,53.0228109606356));
#33992=CARTESIAN_POINT('Ctrl Pts',(82.9129498948689,190.278332223638,53.0228109606296));
#33993=CARTESIAN_POINT('Ctrl Pts',(82.9129498948673,190.455428795637,50.8182135007196));
#33994=CARTESIAN_POINT('Ctrl Pts',(81.9432795991072,190.632525367636,48.630856536284));
#33995=CARTESIAN_POINT('Ctrl Pts',(80.3096882702495,190.809621939634,47.1504412801742));
#33996=CARTESIAN_POINT('Ctrl Pts',(78.6760969413918,190.986718511633,45.6700260240645));
#33997=CARTESIAN_POINT('Ctrl Pts',(76.4041347530377,191.163815083632,44.9197069006019));
#33998=CARTESIAN_POINT('Ctrl Pts',(74.2101800112152,191.340911655631,45.1360689838697));
#33999=CARTESIAN_POINT('Ctrl Pts',(72.0162252693926,191.518008227629,45.3524310671375));
#34000=CARTESIAN_POINT('Ctrl Pts',(69.934592507692,191.695104799628,46.5320903475059));
#34001=CARTESIAN_POINT('Ctrl Pts',(68.6216467656564,191.872201371627,48.3030853894843));
#34002=CARTESIAN_POINT('Ctrl Pts',(67.3087010236208,192.049297943626,50.0740804314627));
#34003=CARTESIAN_POINT('Ctrl Pts',(66.7849774198233,192.226394515624,52.4087119996485));
#34004=CARTESIAN_POINT('Ctrl Pts',(67.2156126057621,192.403491087623,54.5708413428824));
#34005=CARTESIAN_POINT('Ctrl Pts',(67.6462477917009,192.580587659622,56.7329706861163));
#34006=CARTESIAN_POINT('Ctrl Pts',(69.0245064208023,192.757684231621,58.688781035729));
#34007=CARTESIAN_POINT('Ctrl Pts',(70.9158061804534,192.934780803619,59.8215807441439));
#34008=CARTESIAN_POINT('Ctrl Pts',(72.8071059401046,193.111877375618,60.9543804525589));
#34009=CARTESIAN_POINT('Ctrl Pts',(75.1818659698187,193.288973947617,61.2464519739652));
#34010=CARTESIAN_POINT('Ctrl Pts',(77.2912945088747,193.466070519616,60.605701477393));
#34011=CARTESIAN_POINT('Ctrl Pts',(79.4007230479308,193.643167091614,59.9649509808209));
#34012=CARTESIAN_POINT('Ctrl Pts',(81.2118275942136,193.820263663613,58.4014001198706));
#34013=CARTESIAN_POINT('Ctrl Pts',(82.1535440633137,193.997360235612,56.4080561826468));
#34014=CARTESIAN_POINT('Ctrl Pts',(82.6515697929932,194.091017564954,55.353878411086));
#34015=CARTESIAN_POINT('Ctrl Pts',(82.9129498948697,194.184674894296,54.1887099277262));
#34016=CARTESIAN_POINT('Ctrl Pts',(82.9129498948689,194.278332223638,53.0228109606302));
#34017=CARTESIAN_POINT('Ctrl Pts',(82.923873025696,195.721667776361,53.0163254573511));
#34018=CARTESIAN_POINT('Ctrl Pts',(82.9083833277983,195.529643202921,55.3974887847026));
#34019=CARTESIAN_POINT('Ctrl Pts',(81.7627222847989,195.337618629481,57.7957333087917));
#34020=CARTESIAN_POINT('Ctrl Pts',(79.8914368959041,195.145594056041,59.2662252860257));
#34021=CARTESIAN_POINT('Ctrl Pts',(77.8239700413806,194.933438046488,60.8908804245823));
#34022=CARTESIAN_POINT('Ctrl Pts',(74.8707577904796,194.721282036936,61.3830590248267));
#34023=CARTESIAN_POINT('Ctrl Pts',(72.3870455266111,194.509126027384,60.5216002134336));
#34024=CARTESIAN_POINT('Ctrl Pts',(69.9033332627425,194.296970017831,59.6601414020404));
#34025=CARTESIAN_POINT('Ctrl Pts',(67.8891209859066,194.084814008279,57.4450451790096));
#34026=CARTESIAN_POINT('Ctrl Pts',(67.271653649997,193.872657998727,54.8891387638881));
#34027=CARTESIAN_POINT('Ctrl Pts',(66.6541863140874,193.660501989174,52.3332323487668));
#34028=CARTESIAN_POINT('Ctrl Pts',(67.4334639191042,193.448345979622,49.4365157415545));
#34029=CARTESIAN_POINT('Ctrl Pts',(69.248896360684,193.23618997007,47.5373933700901));
#34030=CARTESIAN_POINT('Ctrl Pts',(71.0643288022642,193.024033960517,45.6382709986253));
#34031=CARTESIAN_POINT('Ctrl Pts',(73.9159160804077,192.811877950965,44.7367428629084));
#34032=CARTESIAN_POINT('Ctrl Pts',(76.499647194539,192.599721941413,45.2329851776049));
#34033=CARTESIAN_POINT('Ctrl Pts',(77.7915127516044,192.493643936637,45.4811063349531));
#34034=CARTESIAN_POINT('Ctrl Pts',(79.0164142676668,192.387565931861,46.0786701049046));
#34035=CARTESIAN_POINT('Ctrl Pts',(80.0368081446007,192.281487927084,46.9232989991627));
#34036=CARTESIAN_POINT('Ctrl Pts',(81.0572020215346,192.175409922308,47.7679278934208));
#34037=CARTESIAN_POINT('Ctrl Pts',(81.87308825934,192.069331917532,48.8596219119855));
#34038=CARTESIAN_POINT('Ctrl Pts',(82.3581951748484,191.963253912756,50.0823859966649));
#34039=CARTESIAN_POINT('Ctrl Pts',(82.7264622367569,191.882725200624,51.0106426808646));
#34040=CARTESIAN_POINT('Ctrl Pts',(82.9041002083746,191.802196488493,52.0144354272772));
#34041=CARTESIAN_POINT('Ctrl Pts',(82.89928520713,191.721667776361,53.0196184325889));
#34042=CARTESIAN_POINT('Origin',(74.9879498948689,255.,53.0228109606356));
#34043=CARTESIAN_POINT('',(82.9141190436509,186.278332223638,53.0234646524037));
#34044=CARTESIAN_POINT('',(82.9129498948689,187.721667776361,53.0228109606433));
#34045=CARTESIAN_POINT('',(82.9129498948689,255.,53.0228109606356));
#34046=CARTESIAN_POINT('Ctrl Pts',(82.9213928923929,186.278332223638,53.0275315900476));
#34047=CARTESIAN_POINT('Ctrl Pts',(82.9050897166817,186.467677394884,50.6784741063503));
#34048=CARTESIAN_POINT('Ctrl Pts',(81.7986655277071,186.657022566129,48.3158326354731));
#34049=CARTESIAN_POINT('Ctrl Pts',(79.9715559132873,186.846367737375,46.8431606257875));
#34050=CARTESIAN_POINT('Ctrl Pts',(77.9243302974441,187.058523746927,45.19307250947));
#34051=CARTESIAN_POINT('Ctrl Pts',(74.9723143575872,187.27067975648,44.6603037237834));
#34052=CARTESIAN_POINT('Ctrl Pts',(72.4796900407957,187.482835766032,45.4905354667791));
#34053=CARTESIAN_POINT('Ctrl Pts',(69.9870657240046,187.694991775584,46.3207672097748));
#34054=CARTESIAN_POINT('Ctrl Pts',(67.9538330302788,187.907147785136,48.5139994814526));
#34055=CARTESIAN_POINT('Ctrl Pts',(67.2988469653665,188.119303794689,51.0621196041693));
#34056=CARTESIAN_POINT('Ctrl Pts',(66.9713539329103,188.225381799465,52.3361796655279));
#34057=CARTESIAN_POINT('Ctrl Pts',(66.9884225576576,188.331459804241,53.6989616896462));
#34058=CARTESIAN_POINT('Ctrl Pts',(67.3162393427771,188.437537809017,54.9823703496194));
#34059=CARTESIAN_POINT('Ctrl Pts',(67.6440561278964,188.543615813793,56.2657790095924));
#34060=CARTESIAN_POINT('Ctrl Pts',(68.2826210733879,188.64969381857,57.4698143054203));
#34061=CARTESIAN_POINT('Ctrl Pts',(69.1809930736355,188.755771823346,58.4307557580733));
#34062=CARTESIAN_POINT('Ctrl Pts',(70.9777370741309,188.967927832898,60.3526386633794));
#34063=CARTESIAN_POINT('Ctrl Pts',(73.8137092936511,189.18008384245,61.3021461959855));
#34064=CARTESIAN_POINT('Ctrl Pts',(76.3991529872867,189.392239852003,60.8353039969753));
#34065=CARTESIAN_POINT('Ctrl Pts',(78.9845966809222,189.604395861555,60.3684617979652));
#34066=CARTESIAN_POINT('Ctrl Pts',(81.3195118486733,189.816551871107,58.485269867339));
#34067=CARTESIAN_POINT('Ctrl Pts',(82.3246404126769,190.02870788066,56.0555291232267));
#34068=CARTESIAN_POINT('Ctrl Pts',(82.7188543340392,190.111915994986,55.1025787635085));
#34069=CARTESIAN_POINT('Ctrl Pts',(82.9085167700725,190.195124109312,54.0655567404961));
#34070=CARTESIAN_POINT('Ctrl Pts',(82.9028892198067,190.278332223638,53.0267867749482));
#34071=CARTESIAN_POINT('Ctrl Pts',(82.9129498948689,191.721667776361,53.022810960643));
#34072=CARTESIAN_POINT('Ctrl Pts',(82.9129498948669,191.544571204362,55.2274084205527));
#34073=CARTESIAN_POINT('Ctrl Pts',(81.9432795991067,191.367474632364,57.4147653849879));
#34074=CARTESIAN_POINT('Ctrl Pts',(80.3096882702491,191.190378060365,58.8951806410973));
#34075=CARTESIAN_POINT('Ctrl Pts',(78.6760969413915,191.013281488366,60.3755958972067));
#34076=CARTESIAN_POINT('Ctrl Pts',(76.4041347530378,190.836184916368,61.1259150206692));
#34077=CARTESIAN_POINT('Ctrl Pts',(74.2101800112155,190.659088344369,60.9095529374015));
#34078=CARTESIAN_POINT('Ctrl Pts',(72.0162252693933,190.48199177237,60.6931908541338));
#34079=CARTESIAN_POINT('Ctrl Pts',(69.9345925076929,190.304895200371,59.5135315737658));
#34080=CARTESIAN_POINT('Ctrl Pts',(68.6216467656572,190.127798628373,57.7425365317879));
#34081=CARTESIAN_POINT('Ctrl Pts',(67.3087010236215,189.950702056374,55.9715414898099));
#34082=CARTESIAN_POINT('Ctrl Pts',(66.7849774198235,189.773605484375,53.6369099216246));
#34083=CARTESIAN_POINT('Ctrl Pts',(67.2156126057616,189.596508912376,51.4747805783908));
#34084=CARTESIAN_POINT('Ctrl Pts',(67.6462477916998,189.419412340378,49.3126512351571));
#34085=CARTESIAN_POINT('Ctrl Pts',(69.0245064208004,189.242315768379,47.3568408855443));
#34086=CARTESIAN_POINT('Ctrl Pts',(70.9158061804508,189.06521919638,46.2240411771288));
#34087=CARTESIAN_POINT('Ctrl Pts',(72.8071059401013,188.888122624382,45.0912414687132));
#34088=CARTESIAN_POINT('Ctrl Pts',(75.1818659698149,188.711026052383,44.7991699473059));
#34089=CARTESIAN_POINT('Ctrl Pts',(77.2912945088709,188.533929480384,45.4399204438769));
#34090=CARTESIAN_POINT('Ctrl Pts',(79.400723047927,188.356832908385,46.080670940448));
#34091=CARTESIAN_POINT('Ctrl Pts',(81.2118275942104,188.179736336387,47.6442218013969));
#34092=CARTESIAN_POINT('Ctrl Pts',(82.1535440633116,188.002639764388,49.63756573862));
#34093=CARTESIAN_POINT('Ctrl Pts',(82.6515697929927,187.908982435046,50.6917435101825));
#34094=CARTESIAN_POINT('Ctrl Pts',(82.91294989487,187.815325105703,51.8569119935445));
#34095=CARTESIAN_POINT('Ctrl Pts',(82.9129498948689,187.721667776361,53.0228109606428));
#34096=CARTESIAN_POINT('Origin',(74.9879498948689,255.,53.0228109606356));
#34097=CARTESIAN_POINT('',(82.9129498948689,182.278332223638,53.0228109606297));
#34098=CARTESIAN_POINT('',(82.9148398491843,183.721667776361,53.0234719832117));
#34099=CARTESIAN_POINT('',(82.9129498948689,255.,53.0228109606356));
#34100=CARTESIAN_POINT('Ctrl Pts',(82.9129498948689,182.278332223638,53.0228109606297));
#34101=CARTESIAN_POINT('Ctrl Pts',(82.9129498948673,182.455428795637,50.8182135007202));
#34102=CARTESIAN_POINT('Ctrl Pts',(81.9432795991077,182.632525367636,48.6308565362849));
#34103=CARTESIAN_POINT('Ctrl Pts',(80.3096882702506,182.809621939634,47.1504412801752));
#34104=CARTESIAN_POINT('Ctrl Pts',(78.6760969413935,182.986718511633,45.6700260240655));
#34105=CARTESIAN_POINT('Ctrl Pts',(76.4041347530401,183.163815083632,44.9197069006024));
#34106=CARTESIAN_POINT('Ctrl Pts',(74.210180011218,183.340911655631,45.1360689838694));
#34107=CARTESIAN_POINT('Ctrl Pts',(72.0162252693958,183.518008227629,45.3524310671364));
#34108=CARTESIAN_POINT('Ctrl Pts',(69.9345925076952,183.695104799628,46.5320903475036));
#34109=CARTESIAN_POINT('Ctrl Pts',(68.6216467656589,183.872201371627,48.3030853894809));
#34110=CARTESIAN_POINT('Ctrl Pts',(67.3087010236226,184.049297943625,50.0740804314583));
#34111=CARTESIAN_POINT('Ctrl Pts',(66.7849774198238,184.226394515624,52.4087119996433));
#34112=CARTESIAN_POINT('Ctrl Pts',(67.215612605761,184.403491087623,54.570841342877));
#34113=CARTESIAN_POINT('Ctrl Pts',(67.6462477916982,184.580587659621,56.7329706861107));
#34114=CARTESIAN_POINT('Ctrl Pts',(69.0245064207978,184.75768423162,58.688781035724));
#34115=CARTESIAN_POINT('Ctrl Pts',(70.9158061804475,184.934780803619,59.8215807441404));
#34116=CARTESIAN_POINT('Ctrl Pts',(72.8071059400973,185.111877375618,60.9543804525568));
#34117=CARTESIAN_POINT('Ctrl Pts',(75.1818659698106,185.288973947616,61.2464519739653));
#34118=CARTESIAN_POINT('Ctrl Pts',(77.2912945088669,185.466070519615,60.6057014773954));
#34119=CARTESIAN_POINT('Ctrl Pts',(79.4007230479231,185.643167091614,59.9649509808256));
#34120=CARTESIAN_POINT('Ctrl Pts',(81.2118275942073,185.820263663612,58.4014001198778));
#34121=CARTESIAN_POINT('Ctrl Pts',(82.1535440633096,185.997360235611,56.4080561826554));
#34122=CARTESIAN_POINT('Ctrl Pts',(82.6515697929918,186.091017564953,55.3538784110921));
#34123=CARTESIAN_POINT('Ctrl Pts',(82.9129498948698,186.184674894296,54.1887099277289));
#34124=CARTESIAN_POINT('Ctrl Pts',(82.9129498948689,186.278332223638,53.0228109606294));
#34125=CARTESIAN_POINT('Ctrl Pts',(82.9097357579327,187.721667776361,53.0272021174371));
#34126=CARTESIAN_POINT('Ctrl Pts',(82.9141531006835,187.65043775496,53.9154826081945));
#34127=CARTESIAN_POINT('Ctrl Pts',(82.7730477508649,187.579207733559,54.8021676263194));
#34128=CARTESIAN_POINT('Ctrl Pts',(82.4805842333433,187.507977712157,55.6356724429414));
#34129=CARTESIAN_POINT('Ctrl Pts',(81.6094923594901,187.295821702605,58.1182360075521));
#34130=CARTESIAN_POINT('Ctrl Pts',(79.3956652419737,187.083665693053,60.1290250263497));
#34131=CARTESIAN_POINT('Ctrl Pts',(76.8410254653617,186.8715096835,60.7424387069034));
#34132=CARTESIAN_POINT('Ctrl Pts',(74.2863856887502,186.659353673948,61.3558523874571));
#34133=CARTESIAN_POINT('Ctrl Pts',(71.3909332530432,186.447197664396,60.5718907297675));
#34134=CARTESIAN_POINT('Ctrl Pts',(69.4927557498842,186.235041654843,58.7523177907851));
#34135=CARTESIAN_POINT('Ctrl Pts',(67.5945782467252,186.022885645291,56.9327448518028));
#34136=CARTESIAN_POINT('Ctrl Pts',(66.6936756761142,185.810729635739,54.0775606315278));
#34137=CARTESIAN_POINT('Ctrl Pts',(67.1988209362901,185.598573626187,51.4976834717501));
#34138=CARTESIAN_POINT('Ctrl Pts',(67.703966196466,185.386417616634,48.9178063119723));
#34139=CARTESIAN_POINT('Ctrl Pts',(69.6151592874289,185.174261607082,46.6132362126918));
#34140=CARTESIAN_POINT('Ctrl Pts',(72.0594072029743,184.96210559753,45.6439191122917));
#34141=CARTESIAN_POINT('Ctrl Pts',(74.5036551185198,184.749949587977,44.6746020118916));
#34142=CARTESIAN_POINT('Ctrl Pts',(77.4809578586477,184.537793578425,45.0405379103718));
#34143=CARTESIAN_POINT('Ctrl Pts',(79.6156024351346,184.325637568872,46.5721231230884));
#34144=CARTESIAN_POINT('Ctrl Pts',(81.6412514605336,184.124314304702,48.0255051650586));
#34145=CARTESIAN_POINT('Ctrl Pts',(82.9080981087541,183.922991040532,50.5285387843388));
#34146=CARTESIAN_POINT('Ctrl Pts',(82.9215114273086,183.721667776361,53.0258054066561));
#34147=CARTESIAN_POINT('Origin',(74.9879498948689,255.,53.0228109606356));
#34148=CARTESIAN_POINT('',(82.9129498948689,178.278332223638,53.0228109606295));
#34149=CARTESIAN_POINT('',(82.9129498948689,179.721667776361,53.0228109606429));
#34150=CARTESIAN_POINT('',(82.9129498948689,255.,53.0228109606356));
#34151=CARTESIAN_POINT('Ctrl Pts',(82.9129498948689,178.278332223638,53.0228109606295));
#34152=CARTESIAN_POINT('Ctrl Pts',(82.9129498948672,178.455428795637,50.8182135007197));
#34153=CARTESIAN_POINT('Ctrl Pts',(81.9432795991073,178.632525367636,48.6308565362842));
#34154=CARTESIAN_POINT('Ctrl Pts',(80.3096882702498,178.809621939634,47.1504412801745));
#34155=CARTESIAN_POINT('Ctrl Pts',(78.6760969413923,178.986718511633,45.6700260240648));
#34156=CARTESIAN_POINT('Ctrl Pts',(76.4041347530384,179.163815083632,44.919706900602));
#34157=CARTESIAN_POINT('Ctrl Pts',(74.210180011216,179.340911655631,45.1360689838696));
#34158=CARTESIAN_POINT('Ctrl Pts',(72.0162252693936,179.518008227629,45.3524310671372));
#34159=CARTESIAN_POINT('Ctrl Pts',(69.934592507693,179.695104799628,46.5320903475052));
#34160=CARTESIAN_POINT('Ctrl Pts',(68.6216467656572,179.872201371627,48.3030853894833));
#34161=CARTESIAN_POINT('Ctrl Pts',(67.3087010236214,180.049297943626,50.0740804314613));
#34162=CARTESIAN_POINT('Ctrl Pts',(66.7849774198234,180.226394515624,52.4087119996469));
#34163=CARTESIAN_POINT('Ctrl Pts',(67.2156126057617,180.403491087623,54.5708413428807));
#34164=CARTESIAN_POINT('Ctrl Pts',(67.6462477917,180.580587659622,56.7329706861145));
#34165=CARTESIAN_POINT('Ctrl Pts',(69.0245064208009,180.75768423162,58.6887810357274));
#34166=CARTESIAN_POINT('Ctrl Pts',(70.9158061804516,180.934780803619,59.8215807441428));
#34167=CARTESIAN_POINT('Ctrl Pts',(72.8071059401022,181.111877375618,60.9543804525582));
#34168=CARTESIAN_POINT('Ctrl Pts',(75.1818659698161,181.288973947617,61.2464519739652));
#34169=CARTESIAN_POINT('Ctrl Pts',(77.2912945088722,181.466070519615,60.6057014773938));
#34170=CARTESIAN_POINT('Ctrl Pts',(79.4007230479283,181.643167091614,59.9649509808224));
#34171=CARTESIAN_POINT('Ctrl Pts',(81.2118275942116,181.820263663613,58.4014001198729));
#34172=CARTESIAN_POINT('Ctrl Pts',(82.1535440633124,181.997360235612,56.4080561826496));
#34173=CARTESIAN_POINT('Ctrl Pts',(82.6515697929928,182.091017564954,55.3538784110879));
#34174=CARTESIAN_POINT('Ctrl Pts',(82.9129498948698,182.184674894296,54.1887099277269));
#34175=CARTESIAN_POINT('Ctrl Pts',(82.9129498948689,182.278332223638,53.0228109606297));
#34176=CARTESIAN_POINT('Ctrl Pts',(82.9129498948689,183.721667776361,53.0228109606431));
#34177=CARTESIAN_POINT('Ctrl Pts',(82.9129498948668,183.544571204362,55.2274084205531));
#34178=CARTESIAN_POINT('Ctrl Pts',(81.9432795991064,183.367474632364,57.4147653849885));
#34179=CARTESIAN_POINT('Ctrl Pts',(80.3096882702484,183.190378060365,58.8951806410979));
#34180=CARTESIAN_POINT('Ctrl Pts',(78.6760969413904,183.013281488366,60.3755958972073));
#34181=CARTESIAN_POINT('Ctrl Pts',(76.4041347530361,182.836184916367,61.1259150206696));
#34182=CARTESIAN_POINT('Ctrl Pts',(74.2101800112136,182.659088344369,60.9095529374013));
#34183=CARTESIAN_POINT('Ctrl Pts',(72.0162252693911,182.48199177237,60.6931908541331));
#34184=CARTESIAN_POINT('Ctrl Pts',(69.9345925076908,182.304895200371,59.5135315737643));
#34185=CARTESIAN_POINT('Ctrl Pts',(68.6216467656555,182.127798628372,57.7425365317856));
#34186=CARTESIAN_POINT('Ctrl Pts',(67.3087010236202,181.950702056374,55.9715414898069));
#34187=CARTESIAN_POINT('Ctrl Pts',(66.7849774198232,181.773605484375,53.636909921621));
#34188=CARTESIAN_POINT('Ctrl Pts',(67.2156126057624,181.596508912376,51.4747805783872));
#34189=CARTESIAN_POINT('Ctrl Pts',(67.6462477917016,181.419412340377,49.3126512351534));
#34190=CARTESIAN_POINT('Ctrl Pts',(69.0245064208034,181.242315768379,47.356840885541));
#34191=CARTESIAN_POINT('Ctrl Pts',(70.9158061804548,181.06521919638,46.2240411771264));
#34192=CARTESIAN_POINT('Ctrl Pts',(72.8071059401061,180.888122624381,45.0912414687118));
#34193=CARTESIAN_POINT('Ctrl Pts',(75.1818659698203,180.711026052382,44.7991699473059));
#34194=CARTESIAN_POINT('Ctrl Pts',(77.2912945088762,180.533929480384,45.4399204438786));
#34195=CARTESIAN_POINT('Ctrl Pts',(79.4007230479321,180.356832908385,46.0806709404512));
#34196=CARTESIAN_POINT('Ctrl Pts',(81.2118275942147,180.179736336386,47.6442218014017));
#34197=CARTESIAN_POINT('Ctrl Pts',(82.1535440633144,180.002639764387,49.6375657386258));
#34198=CARTESIAN_POINT('Ctrl Pts',(82.6515697929937,179.908982435045,50.6917435101869));
#34199=CARTESIAN_POINT('Ctrl Pts',(82.9129498948701,179.815325105703,51.8569119935471));
#34200=CARTESIAN_POINT('Ctrl Pts',(82.9129498948689,179.721667776361,53.0228109606434));
#34201=CARTESIAN_POINT('Origin',(74.9879498948689,255.,53.0228109606356));
#34202=CARTESIAN_POINT('',(82.9129498948689,174.278332223638,53.0228109606294));
#34203=CARTESIAN_POINT('',(82.9129498948689,175.721667776361,53.0228109606428));
#34204=CARTESIAN_POINT('',(82.9129498948689,255.,53.0228109606356));
#34205=CARTESIAN_POINT('Ctrl Pts',(82.9129498948689,174.278332223638,53.0228109606289));
#34206=CARTESIAN_POINT('Ctrl Pts',(82.9129498948671,174.455428795637,50.8182135007192));
#34207=CARTESIAN_POINT('Ctrl Pts',(81.9432795991071,174.632525367636,48.630856536284));
#34208=CARTESIAN_POINT('Ctrl Pts',(80.3096882702497,174.809621939634,47.1504412801744));
#34209=CARTESIAN_POINT('Ctrl Pts',(78.6760969413922,174.986718511633,45.6700260240648));
#34210=CARTESIAN_POINT('Ctrl Pts',(76.4041347530385,175.163815083632,44.9197069006021));
#34211=CARTESIAN_POINT('Ctrl Pts',(74.2101800112163,175.340911655631,45.1360689838696));
#34212=CARTESIAN_POINT('Ctrl Pts',(72.016225269394,175.518008227629,45.3524310671371));
#34213=CARTESIAN_POINT('Ctrl Pts',(69.9345925076935,175.695104799628,46.5320903475048));
#34214=CARTESIAN_POINT('Ctrl Pts',(68.6216467656576,175.872201371627,48.3030853894827));
#34215=CARTESIAN_POINT('Ctrl Pts',(67.3087010236217,176.049297943626,50.0740804314605));
#34216=CARTESIAN_POINT('Ctrl Pts',(66.7849774198236,176.226394515624,52.4087119996458));
#34217=CARTESIAN_POINT('Ctrl Pts',(67.2156126057615,176.403491087623,54.5708413428795));
#34218=CARTESIAN_POINT('Ctrl Pts',(67.6462477916994,176.580587659622,56.7329706861133));
#34219=CARTESIAN_POINT('Ctrl Pts',(69.0245064207998,176.75768423162,58.6887810357262));
#34220=CARTESIAN_POINT('Ctrl Pts',(70.9158061804501,176.934780803619,59.821580744142));
#34221=CARTESIAN_POINT('Ctrl Pts',(72.8071059401005,177.111877375618,60.9543804525577));
#34222=CARTESIAN_POINT('Ctrl Pts',(75.1818659698141,177.288973947617,61.2464519739653));
#34223=CARTESIAN_POINT('Ctrl Pts',(77.2912945088702,177.466070519615,60.6057014773944));
#34224=CARTESIAN_POINT('Ctrl Pts',(79.4007230479263,177.643167091614,59.9649509808236));
#34225=CARTESIAN_POINT('Ctrl Pts',(81.2118275942099,177.820263663613,58.4014001198748));
#34226=CARTESIAN_POINT('Ctrl Pts',(82.1535440633113,177.997360235611,56.4080561826519));
#34227=CARTESIAN_POINT('Ctrl Pts',(82.6515697929924,178.091017564954,55.3538784110896));
#34228=CARTESIAN_POINT('Ctrl Pts',(82.9129498948698,178.184674894296,54.1887099277277));
#34229=CARTESIAN_POINT('Ctrl Pts',(82.9129498948689,178.278332223638,53.0228109606295));
#34230=CARTESIAN_POINT('Ctrl Pts',(82.9129498948689,179.721667776361,53.0228109606434));
#34231=CARTESIAN_POINT('Ctrl Pts',(82.9129498948667,179.544571204362,55.2274084205531));
#34232=CARTESIAN_POINT('Ctrl Pts',(81.9432795991065,179.367474632364,57.4147653849882));
#34233=CARTESIAN_POINT('Ctrl Pts',(80.3096882702488,179.190378060365,58.8951806410975));
#34234=CARTESIAN_POINT('Ctrl Pts',(78.6760969413912,179.013281488366,60.3755958972069));
#34235=CARTESIAN_POINT('Ctrl Pts',(76.4041347530373,178.836184916368,61.1259150206693));
#34236=CARTESIAN_POINT('Ctrl Pts',(74.2101800112151,178.659088344369,60.9095529374015));
#34237=CARTESIAN_POINT('Ctrl Pts',(72.0162252693929,178.48199177237,60.6931908541337));
#34238=CARTESIAN_POINT('Ctrl Pts',(69.9345925076926,178.304895200371,59.5135315737656));
#34239=CARTESIAN_POINT('Ctrl Pts',(68.6216467656569,178.127798628373,57.7425365317875));
#34240=CARTESIAN_POINT('Ctrl Pts',(67.3087010236213,177.950702056374,55.9715414898095));
#34241=CARTESIAN_POINT('Ctrl Pts',(66.7849774198235,177.773605484375,53.6369099216241));
#34242=CARTESIAN_POINT('Ctrl Pts',(67.2156126057617,177.596508912376,51.4747805783905));
#34243=CARTESIAN_POINT('Ctrl Pts',(67.6462477917,177.419412340378,49.3126512351568));
#34244=CARTESIAN_POINT('Ctrl Pts',(69.0245064208006,177.242315768379,47.356840885544));
#34245=CARTESIAN_POINT('Ctrl Pts',(70.9158061804511,177.06521919638,46.2240411771286));
#34246=CARTESIAN_POINT('Ctrl Pts',(72.8071059401016,176.888122624382,45.0912414687131));
#34247=CARTESIAN_POINT('Ctrl Pts',(75.1818659698153,176.711026052383,44.7991699473059));
#34248=CARTESIAN_POINT('Ctrl Pts',(77.2912945088713,176.533929480384,45.4399204438771));
#34249=CARTESIAN_POINT('Ctrl Pts',(79.4007230479273,176.356832908385,46.0806709404482));
#34250=CARTESIAN_POINT('Ctrl Pts',(81.2118275942107,176.179736336387,47.6442218013973));
#34251=CARTESIAN_POINT('Ctrl Pts',(82.1535440633118,176.002639764388,49.6375657386203));
#34252=CARTESIAN_POINT('Ctrl Pts',(82.6515697929928,175.908982435046,50.6917435101827));
#34253=CARTESIAN_POINT('Ctrl Pts',(82.91294989487,175.815325105703,51.8569119935446));
#34254=CARTESIAN_POINT('Ctrl Pts',(82.9129498948689,175.721667776361,53.0228109606428));
#34255=CARTESIAN_POINT('Origin',(74.9879498948689,255.,53.0228109606356));
#34256=CARTESIAN_POINT('',(82.9158840595049,170.278332223638,53.0221079210748));
#34257=CARTESIAN_POINT('',(82.9129498948689,171.721667776361,53.0228109606426));
#34258=CARTESIAN_POINT('',(82.9129498948689,255.,53.0228109606356));
#34259=CARTESIAN_POINT('Ctrl Pts',(82.9129498948689,170.278332223638,53.0228109606287));
#34260=CARTESIAN_POINT('Ctrl Pts',(82.912949894867,170.455428795637,50.8182135007189));
#34261=CARTESIAN_POINT('Ctrl Pts',(81.9432795991069,170.632525367636,48.6308565362835));
#34262=CARTESIAN_POINT('Ctrl Pts',(80.3096882702492,170.809621939635,47.150441280174));
#34263=CARTESIAN_POINT('Ctrl Pts',(78.6760969413915,170.986718511633,45.6700260240644));
#34264=CARTESIAN_POINT('Ctrl Pts',(76.4041347530376,171.163815083632,44.9197069006019));
#34265=CARTESIAN_POINT('Ctrl Pts',(74.2101800112152,171.340911655631,45.1360689838697));
#34266=CARTESIAN_POINT('Ctrl Pts',(72.0162252693928,171.518008227629,45.3524310671375));
#34267=CARTESIAN_POINT('Ctrl Pts',(69.9345925076924,171.695104799628,46.5320903475057));
#34268=CARTESIAN_POINT('Ctrl Pts',(68.6216467656567,171.872201371627,48.3030853894839));
#34269=CARTESIAN_POINT('Ctrl Pts',(67.3087010236211,172.049297943626,50.0740804314621));
#34270=CARTESIAN_POINT('Ctrl Pts',(66.7849774198234,172.226394515624,52.4087119996477));
#34271=CARTESIAN_POINT('Ctrl Pts',(67.2156126057619,172.403491087623,54.5708413428815));
#34272=CARTESIAN_POINT('Ctrl Pts',(67.6462477917004,172.580587659622,56.7329706861153));
#34273=CARTESIAN_POINT('Ctrl Pts',(69.0245064208014,172.757684231621,58.688781035728));
#34274=CARTESIAN_POINT('Ctrl Pts',(70.9158061804522,172.934780803619,59.8215807441432));
#34275=CARTESIAN_POINT('Ctrl Pts',(72.807105940103,173.111877375618,60.9543804525585));
#34276=CARTESIAN_POINT('Ctrl Pts',(75.1818659698169,173.288973947617,61.2464519739652));
#34277=CARTESIAN_POINT('Ctrl Pts',(77.291294508873,173.466070519615,60.6057014773936));
#34278=CARTESIAN_POINT('Ctrl Pts',(79.400723047929,173.643167091614,59.9649509808219));
#34279=CARTESIAN_POINT('Ctrl Pts',(81.2118275942121,173.820263663613,58.4014001198723));
#34280=CARTESIAN_POINT('Ctrl Pts',(82.1535440633127,173.997360235612,56.4080561826489));
#34281=CARTESIAN_POINT('Ctrl Pts',(82.651569792993,174.091017564954,55.3538784110872));
#34282=CARTESIAN_POINT('Ctrl Pts',(82.9129498948699,174.184674894296,54.1887099277261));
#34283=CARTESIAN_POINT('Ctrl Pts',(82.9129498948689,174.278332223638,53.0228109606289));
#34284=CARTESIAN_POINT('Ctrl Pts',(82.9129498948689,175.721667776361,53.0228109606428));
#34285=CARTESIAN_POINT('Ctrl Pts',(82.9129498948669,175.544571204362,55.2274084205527));
#34286=CARTESIAN_POINT('Ctrl Pts',(81.9432795991065,175.367474632364,57.4147653849882));
#34287=CARTESIAN_POINT('Ctrl Pts',(80.3096882702486,175.190378060365,58.8951806410977));
#34288=CARTESIAN_POINT('Ctrl Pts',(78.6760969413907,175.013281488366,60.3755958972072));
#34289=CARTESIAN_POINT('Ctrl Pts',(76.4041347530364,174.836184916367,61.1259150206695));
#34290=CARTESIAN_POINT('Ctrl Pts',(74.210180011214,174.659088344369,60.9095529374013));
#34291=CARTESIAN_POINT('Ctrl Pts',(72.0162252693915,174.48199177237,60.6931908541332));
#34292=CARTESIAN_POINT('Ctrl Pts',(69.9345925076911,174.304895200371,59.5135315737645));
#34293=CARTESIAN_POINT('Ctrl Pts',(68.6216467656557,174.127798628372,57.7425365317859));
#34294=CARTESIAN_POINT('Ctrl Pts',(67.3087010236203,173.950702056374,55.9715414898073));
#34295=CARTESIAN_POINT('Ctrl Pts',(66.7849774198232,173.773605484375,53.6369099216214));
#34296=CARTESIAN_POINT('Ctrl Pts',(67.2156126057623,173.596508912376,51.4747805783875));
#34297=CARTESIAN_POINT('Ctrl Pts',(67.6462477917014,173.419412340377,49.3126512351537));
#34298=CARTESIAN_POINT('Ctrl Pts',(69.0245064208031,173.242315768379,47.3568408855413));
#34299=CARTESIAN_POINT('Ctrl Pts',(70.9158061804545,173.06521919638,46.2240411771266));
#34300=CARTESIAN_POINT('Ctrl Pts',(72.8071059401058,172.888122624381,45.0912414687119));
#34301=CARTESIAN_POINT('Ctrl Pts',(75.18186596982,172.711026052382,44.7991699473059));
#34302=CARTESIAN_POINT('Ctrl Pts',(77.2912945088759,172.533929480384,45.4399204438785));
#34303=CARTESIAN_POINT('Ctrl Pts',(79.4007230479318,172.356832908385,46.080670940451));
#34304=CARTESIAN_POINT('Ctrl Pts',(81.2118275942144,172.179736336386,47.6442218014014));
#34305=CARTESIAN_POINT('Ctrl Pts',(82.1535440633142,172.002639764388,49.6375657386255));
#34306=CARTESIAN_POINT('Ctrl Pts',(82.6515697929936,171.908982435045,50.6917435101864));
#34307=CARTESIAN_POINT('Ctrl Pts',(82.9129498948699,171.815325105703,51.8569119935464));
#34308=CARTESIAN_POINT('Ctrl Pts',(82.9129498948689,171.721667776361,53.0228109606426));
#34309=CARTESIAN_POINT('Origin',(74.9879498948689,255.,53.0228109606356));
#34310=CARTESIAN_POINT('',(82.9129498948689,166.278332223638,53.0228109606286));
#34311=CARTESIAN_POINT('',(82.9144547577616,167.721667776361,53.022184232359));
#34312=CARTESIAN_POINT('',(82.9129498948689,255.,53.0228109606356));
#34313=CARTESIAN_POINT('Ctrl Pts',(82.9106451661498,166.278332223638,53.018111936927));
#34314=CARTESIAN_POINT('Ctrl Pts',(82.9151724908915,166.345351755876,52.1826111629703));
#34315=CARTESIAN_POINT('Ctrl Pts',(82.7905111495548,166.412371288115,51.3486593970808));
#34316=CARTESIAN_POINT('Ctrl Pts',(82.5309490101129,166.479390820353,50.5591188525927));
#34317=CARTESIAN_POINT('Ctrl Pts',(81.7092830584731,166.691546829905,48.0597613413635));
#34318=CARTESIAN_POINT('Ctrl Pts',(79.5357860780612,166.903702839457,46.0054454307733));
#34319=CARTESIAN_POINT('Ctrl Pts',(76.9938193710111,167.11585884901,45.341468027555));
#34320=CARTESIAN_POINT('Ctrl Pts',(74.4518526639606,167.328014858562,44.6774906243366));
#34321=CARTESIAN_POINT('Ctrl Pts',(71.5414162302718,167.540170868114,45.4038517284906));
#34322=CARTESIAN_POINT('Ctrl Pts',(69.6075117357223,167.752326877667,47.1854063641216));
#34323=CARTESIAN_POINT('Ctrl Pts',(67.6736072411727,167.964482887219,48.9669609997525));
#34324=CARTESIAN_POINT('Ctrl Pts',(66.7162346857625,168.176638896771,51.8037091668605));
#34325=CARTESIAN_POINT('Ctrl Pts',(67.1700953375757,168.388794906323,54.3931006788104));
#34326=CARTESIAN_POINT('Ctrl Pts',(67.6239559893889,168.600950915876,56.9824921907597));
#34327=CARTESIAN_POINT('Ctrl Pts',(69.4890498484247,168.813106925428,59.3245270475509));
#34328=CARTESIAN_POINT('Ctrl Pts',(71.9135852423216,169.02526293498,60.3421476239523));
#34329=CARTESIAN_POINT('Ctrl Pts',(74.338120636219,169.237418944533,61.3597682003539));
#34330=CARTESIAN_POINT('Ctrl Pts',(77.3220975649777,169.449574954085,61.052974496365));
#34331=CARTESIAN_POINT('Ctrl Pts',(79.4867088649507,169.661730963637,59.5640424456095));
#34332=CARTESIAN_POINT('Ctrl Pts',(81.58375379868,169.867264716971,58.1215860499773));
#34333=CARTESIAN_POINT('Ctrl Pts',(82.9117862805714,170.072798470305,55.569638266714));
#34334=CARTESIAN_POINT('Ctrl Pts',(82.9223099933314,170.278332223639,53.0205682373108));
#34335=CARTESIAN_POINT('Ctrl Pts',(82.9129498948689,171.721667776361,53.0228109606426));
#34336=CARTESIAN_POINT('Ctrl Pts',(82.912949894867,171.544571204362,55.2274084205524));
#34337=CARTESIAN_POINT('Ctrl Pts',(81.9432795991068,171.367474632364,57.4147653849878));
#34338=CARTESIAN_POINT('Ctrl Pts',(80.3096882702491,171.190378060365,58.8951806410973));
#34339=CARTESIAN_POINT('Ctrl Pts',(78.6760969413914,171.013281488366,60.3755958972068));
#34340=CARTESIAN_POINT('Ctrl Pts',(76.4041347530374,170.836184916367,61.1259150206693));
#34341=CARTESIAN_POINT('Ctrl Pts',(74.210180011215,170.659088344369,60.9095529374015));
#34342=CARTESIAN_POINT('Ctrl Pts',(72.0162252693926,170.48199177237,60.6931908541336));
#34343=CARTESIAN_POINT('Ctrl Pts',(69.9345925076922,170.304895200371,59.5135315737653));
#34344=CARTESIAN_POINT('Ctrl Pts',(68.6216467656566,170.127798628373,57.7425365317871));
#34345=CARTESIAN_POINT('Ctrl Pts',(67.308701023621,169.950702056374,55.9715414898089));
#34346=CARTESIAN_POINT('Ctrl Pts',(66.7849774198234,169.773605484375,53.6369099216232));
#34347=CARTESIAN_POINT('Ctrl Pts',(67.2156126057619,169.596508912376,51.4747805783895));
#34348=CARTESIAN_POINT('Ctrl Pts',(67.6462477917005,169.419412340378,49.3126512351557));
#34349=CARTESIAN_POINT('Ctrl Pts',(69.0245064208016,169.242315768379,47.356840885543));
#34350=CARTESIAN_POINT('Ctrl Pts',(70.9158061804524,169.06521919638,46.2240411771278));
#34351=CARTESIAN_POINT('Ctrl Pts',(72.8071059401032,168.888122624381,45.0912414687126));
#34352=CARTESIAN_POINT('Ctrl Pts',(75.1818659698171,168.711026052383,44.7991699473059));
#34353=CARTESIAN_POINT('Ctrl Pts',(77.2912945088732,168.533929480384,45.4399204438776));
#34354=CARTESIAN_POINT('Ctrl Pts',(79.4007230479292,168.356832908385,46.0806709404493));
#34355=CARTESIAN_POINT('Ctrl Pts',(81.2118275942122,168.179736336386,47.644221801399));
#34356=CARTESIAN_POINT('Ctrl Pts',(82.1535440633128,168.002639764388,49.6375657386224));
#34357=CARTESIAN_POINT('Ctrl Pts',(82.6515697929931,167.908982435046,50.6917435101842));
#34358=CARTESIAN_POINT('Ctrl Pts',(82.9129498948699,167.815325105703,51.8569119935452));
#34359=CARTESIAN_POINT('Ctrl Pts',(82.9129498948689,167.721667776361,53.0228109606424));
#34360=CARTESIAN_POINT('Origin',(74.9879498948689,255.,53.0228109606356));
#34361=CARTESIAN_POINT('',(82.9094046261903,162.278332223638,53.0234187658783));
#34362=CARTESIAN_POINT('',(82.9093059554942,163.721667776361,53.0209644405026));
#34363=CARTESIAN_POINT('',(82.9129498948689,255.,53.0228109606356));
#34364=CARTESIAN_POINT('Ctrl Pts',(82.9129498948689,162.278332223638,53.0228109606289));
#34365=CARTESIAN_POINT('Ctrl Pts',(82.912949894867,162.455428795637,50.8182135007193));
#34366=CARTESIAN_POINT('Ctrl Pts',(81.9432795991072,162.632525367636,48.6308565362842));
#34367=CARTESIAN_POINT('Ctrl Pts',(80.3096882702499,162.809621939634,47.1504412801746));
#34368=CARTESIAN_POINT('Ctrl Pts',(78.6760969413927,162.986718511633,45.6700260240651));
#34369=CARTESIAN_POINT('Ctrl Pts',(76.4041347530392,163.163815083632,44.9197069006022));
#34370=CARTESIAN_POINT('Ctrl Pts',(74.2101800112171,163.340911655631,45.1360689838695));
#34371=CARTESIAN_POINT('Ctrl Pts',(72.016225269395,163.518008227629,45.3524310671367));
#34372=CARTESIAN_POINT('Ctrl Pts',(69.9345925076945,163.695104799628,46.5320903475041));
#34373=CARTESIAN_POINT('Ctrl Pts',(68.6216467656584,163.872201371627,48.3030853894816));
#34374=CARTESIAN_POINT('Ctrl Pts',(67.3087010236223,164.049297943625,50.0740804314591));
#34375=CARTESIAN_POINT('Ctrl Pts',(66.7849774198237,164.226394515624,52.4087119996442));
#34376=CARTESIAN_POINT('Ctrl Pts',(67.2156126057612,164.403491087623,54.5708413428778));
#34377=CARTESIAN_POINT('Ctrl Pts',(67.6462477916986,164.580587659622,56.7329706861115));
#34378=CARTESIAN_POINT('Ctrl Pts',(69.0245064207984,164.75768423162,58.6887810357247));
#34379=CARTESIAN_POINT('Ctrl Pts',(70.9158061804483,164.934780803619,59.8215807441408));
#34380=CARTESIAN_POINT('Ctrl Pts',(72.8071059400982,165.111877375618,60.954380452557));
#34381=CARTESIAN_POINT('Ctrl Pts',(75.1818659698115,165.288973947616,61.2464519739653));
#34382=CARTESIAN_POINT('Ctrl Pts',(77.2912945088677,165.466070519615,60.6057014773952));
#34383=CARTESIAN_POINT('Ctrl Pts',(79.4007230479239,165.643167091614,59.9649509808251));
#34384=CARTESIAN_POINT('Ctrl Pts',(81.2118275942079,165.820263663612,58.4014001198771));
#34385=CARTESIAN_POINT('Ctrl Pts',(82.15354406331,165.997360235611,56.4080561826547));
#34386=CARTESIAN_POINT('Ctrl Pts',(82.6515697929921,166.091017564954,55.3538784110913));
#34387=CARTESIAN_POINT('Ctrl Pts',(82.9129498948699,166.184674894296,54.1887099277281));
#34388=CARTESIAN_POINT('Ctrl Pts',(82.9129498948689,166.278332223638,53.0228109606286));
#34389=CARTESIAN_POINT('Ctrl Pts',(82.9224999886125,167.721667776361,53.0188336454937));
#34390=CARTESIAN_POINT('Ctrl Pts',(82.9079541551392,167.528112115953,55.4192369642975));
#34391=CARTESIAN_POINT('Ctrl Pts',(81.7452090935466,167.334556455544,57.8320530567318));
#34392=CARTESIAN_POINT('Ctrl Pts',(79.8479697065302,167.141000795135,59.3001204669499));
#34393=CARTESIAN_POINT('Ctrl Pts',(77.7684090433854,166.928844785583,60.9092665019874));
#34394=CARTESIAN_POINT('Ctrl Pts',(74.8064039462386,166.71668877603,61.3833619487564));
#34395=CARTESIAN_POINT('Ctrl Pts',(72.3307421974144,166.504532766478,60.5038395572588));
#34396=CARTESIAN_POINT('Ctrl Pts',(69.85508044859,166.292376756926,59.6243171657612));
#34397=CARTESIAN_POINT('Ctrl Pts',(67.8657620480882,166.080220747374,57.3911769359969));
#34398=CARTESIAN_POINT('Ctrl Pts',(67.2614600207839,165.868064737821,54.8305633445269));
#34399=CARTESIAN_POINT('Ctrl Pts',(66.9593090071318,165.761986733045,53.5502565487921));
#34400=CARTESIAN_POINT('Ctrl Pts',(67.0034120867789,165.655908728269,52.1880814126309));
#34401=CARTESIAN_POINT('Ctrl Pts',(67.3566273802562,165.549830723493,50.911429310626));
#34402=CARTESIAN_POINT('Ctrl Pts',(67.7098426737335,165.443752718716,49.6347772086211));
#34403=CARTESIAN_POINT('Ctrl Pts',(68.3721701810411,165.33767471394,48.4436481407725));
#34404=CARTESIAN_POINT('Ctrl Pts',(69.2894305829301,165.231596709164,47.500719680399));
#34405=CARTESIAN_POINT('Ctrl Pts',(71.1239513867081,165.019440699612,45.614862759652));
#34406=CARTESIAN_POINT('Ctrl Pts',(73.978203768812,164.80728469006,44.7218082688056));
#34407=CARTESIAN_POINT('Ctrl Pts',(76.553876331361,164.595128680507,45.2398541956007));
#34408=CARTESIAN_POINT('Ctrl Pts',(79.12954889391,164.382972670955,45.7579001223958));
#34409=CARTESIAN_POINT('Ctrl Pts',(81.4266416369042,164.170816661403,47.6870464668322));
#34410=CARTESIAN_POINT('Ctrl Pts',(82.3833659087906,163.95866065185,50.1362508644599));
#34411=CARTESIAN_POINT('Ctrl Pts',(82.7396082116808,163.879663026687,51.0482275337036));
#34412=CARTESIAN_POINT('Ctrl Pts',(82.9100094867986,163.800665401524,52.0323098404564));
#34413=CARTESIAN_POINT('Ctrl Pts',(82.9038913724499,163.721667776361,53.0182206691028));
#34414=CARTESIAN_POINT('Origin',(74.9879498948689,255.,53.0228109606356));
#34415=CARTESIAN_POINT('',(82.9156111860663,158.278332223638,53.0248046760933));
#34416=CARTESIAN_POINT('',(82.9097002693887,159.721667776361,53.0250701739541));
#34417=CARTESIAN_POINT('',(82.9129498948689,255.,53.0228109606356));
#34418=CARTESIAN_POINT('Ctrl Pts',(82.9226459731562,158.278332223638,53.0300748111075));
#34419=CARTESIAN_POINT('Ctrl Pts',(82.905435742135,158.466146307915,50.7000344004891));
#34420=CARTESIAN_POINT('Ctrl Pts',(81.8157007576566,158.653960392192,48.3521897248115));
#34421=CARTESIAN_POINT('Ctrl Pts',(80.0143420609404,158.841774476469,46.8779115309736));
#34422=CARTESIAN_POINT('Ctrl Pts',(77.9795155763405,159.053930486022,45.2125573069881));
#34423=CARTESIAN_POINT('Ctrl Pts',(75.0366495246558,159.266086495574,44.6618833787099));
#34424=CARTESIAN_POINT('Ctrl Pts',(72.5363346617808,159.478242505126,45.473895373638));
#34425=CARTESIAN_POINT('Ctrl Pts',(70.0360197989058,159.690398514678,46.285907368566));
#34426=CARTESIAN_POINT('Ctrl Pts',(67.97825612484,159.902554524231,48.4606052867));
#34427=CARTESIAN_POINT('Ctrl Pts',(67.3102007338575,160.114710533783,51.0037579577669));
#34428=CARTESIAN_POINT('Ctrl Pts',(66.642145342875,160.326866543336,53.5469106288341));
#34429=CARTESIAN_POINT('Ctrl Pts',(67.3637982349759,160.539022552888,56.4585180528339));
#34430=CARTESIAN_POINT('Ctrl Pts',(69.1411944418614,160.75117856244,58.3932850815706));
#34431=CARTESIAN_POINT('Ctrl Pts',(70.9185906487468,160.963334571992,60.328052110307));
#34432=CARTESIAN_POINT('Ctrl Pts',(73.7517301704166,161.175490581545,61.2859787437801));
#34433=CARTESIAN_POINT('Ctrl Pts',(76.3447982422542,161.387646591097,60.8410957481066));
#34434=CARTESIAN_POINT('Ctrl Pts',(77.6413322781732,161.493724595873,60.6186542502698));
#34435=CARTESIAN_POINT('Ctrl Pts',(78.8778484516341,161.599802600649,60.0455103451463));
#34436=CARTESIAN_POINT('Ctrl Pts',(79.9147990521175,161.705880605426,59.2212924824077));
#34437=CARTESIAN_POINT('Ctrl Pts',(80.9517496526007,161.811958610202,58.3970746196692));
#34438=CARTESIAN_POINT('Ctrl Pts',(81.7891346801065,161.918036614978,57.3217827993156));
#34439=CARTESIAN_POINT('Ctrl Pts',(82.2984059455822,162.024114619754,56.1088839970999));
#34440=CARTESIAN_POINT('Ctrl Pts',(82.7052314733612,162.108853821049,55.1399736563743));
#34441=CARTESIAN_POINT('Ctrl Pts',(82.9026734824335,162.193593022343,54.0832503757628));
#34442=CARTESIAN_POINT('Ctrl Pts',(82.8985428315738,162.278332223638,53.0252809253887));
#34443=CARTESIAN_POINT('Ctrl Pts',(82.9129498948689,163.721667776361,53.0228109606422));
#34444=CARTESIAN_POINT('Ctrl Pts',(82.9129498948671,163.544571204362,55.2274084205519));
#34445=CARTESIAN_POINT('Ctrl Pts',(81.9432795991071,163.367474632364,57.4147653849872));
#34446=CARTESIAN_POINT('Ctrl Pts',(80.3096882702497,163.190378060365,58.8951806410968));
#34447=CARTESIAN_POINT('Ctrl Pts',(78.6760969413922,163.013281488366,60.3755958972063));
#34448=CARTESIAN_POINT('Ctrl Pts',(76.4041347530385,162.836184916368,61.1259150206691));
#34449=CARTESIAN_POINT('Ctrl Pts',(74.2101800112163,162.659088344369,60.9095529374016));
#34450=CARTESIAN_POINT('Ctrl Pts',(72.016225269394,162.48199177237,60.6931908541341));
#34451=CARTESIAN_POINT('Ctrl Pts',(69.9345925076935,162.304895200371,59.5135315737663));
#34452=CARTESIAN_POINT('Ctrl Pts',(68.6216467656576,162.127798628373,57.7425365317885));
#34453=CARTESIAN_POINT('Ctrl Pts',(67.3087010236217,161.950702056374,55.9715414898106));
#34454=CARTESIAN_POINT('Ctrl Pts',(66.7849774198236,161.773605484375,53.6369099216253));
#34455=CARTESIAN_POINT('Ctrl Pts',(67.2156126057615,161.596508912377,51.4747805783916));
#34456=CARTESIAN_POINT('Ctrl Pts',(67.6462477916994,161.419412340378,49.3126512351578));
#34457=CARTESIAN_POINT('Ctrl Pts',(69.0245064207998,161.242315768379,47.3568408855449));
#34458=CARTESIAN_POINT('Ctrl Pts',(70.9158061804502,161.06521919638,46.2240411771292));
#34459=CARTESIAN_POINT('Ctrl Pts',(72.8071059401005,160.888122624382,45.0912414687134));
#34460=CARTESIAN_POINT('Ctrl Pts',(75.1818659698141,160.711026052383,44.7991699473059));
#34461=CARTESIAN_POINT('Ctrl Pts',(77.2912945088702,160.533929480384,45.4399204438767));
#34462=CARTESIAN_POINT('Ctrl Pts',(79.4007230479263,160.356832908385,46.0806709404476));
#34463=CARTESIAN_POINT('Ctrl Pts',(81.2118275942099,160.179736336387,47.6442218013964));
#34464=CARTESIAN_POINT('Ctrl Pts',(82.1535440633113,160.002639764388,49.6375657386193));
#34465=CARTESIAN_POINT('Ctrl Pts',(82.6515697929925,159.908982435046,50.6917435101817));
#34466=CARTESIAN_POINT('Ctrl Pts',(82.9129498948699,159.815325105703,51.8569119935438));
#34467=CARTESIAN_POINT('Ctrl Pts',(82.9129498948689,159.721667776361,53.0228109606421));
#34468=CARTESIAN_POINT('Origin',(74.9879498948689,255.,53.0228109606356));
#34469=CARTESIAN_POINT('',(82.9129498948689,154.278332223638,53.0228109606285));
#34470=CARTESIAN_POINT('',(82.9174930945309,155.721667776361,53.0233296472211));
#34471=CARTESIAN_POINT('',(82.9129498948689,255.,53.0228109606356));
#34472=CARTESIAN_POINT('Ctrl Pts',(82.9129498948689,154.278332223638,53.0228109606281));
#34473=CARTESIAN_POINT('Ctrl Pts',(82.9129498948668,154.455428795637,50.8182135007182));
#34474=CARTESIAN_POINT('Ctrl Pts',(81.9432795991065,154.632525367636,48.6308565362829));
#34475=CARTESIAN_POINT('Ctrl Pts',(80.3096882702487,154.809621939635,47.1504412801735));
#34476=CARTESIAN_POINT('Ctrl Pts',(78.6760969413909,154.986718511633,45.6700260240641));
#34477=CARTESIAN_POINT('Ctrl Pts',(76.4041347530369,155.163815083632,44.9197069006018));
#34478=CARTESIAN_POINT('Ctrl Pts',(74.2101800112145,155.340911655631,45.1360689838697));
#34479=CARTESIAN_POINT('Ctrl Pts',(72.0162252693922,155.518008227629,45.3524310671377));
#34480=CARTESIAN_POINT('Ctrl Pts',(69.9345925076918,155.695104799628,46.5320903475061));
#34481=CARTESIAN_POINT('Ctrl Pts',(68.6216467656563,155.872201371627,48.3030853894844));
#34482=CARTESIAN_POINT('Ctrl Pts',(67.3087010236208,156.049297943626,50.0740804314627));
#34483=CARTESIAN_POINT('Ctrl Pts',(66.7849774198233,156.226394515624,52.4087119996484));
#34484=CARTESIAN_POINT('Ctrl Pts',(67.215612605762,156.403491087623,54.5708413428822));
#34485=CARTESIAN_POINT('Ctrl Pts',(67.6462477917007,156.580587659622,56.7329706861159));
#34486=CARTESIAN_POINT('Ctrl Pts',(69.0245064208019,156.757684231621,58.6887810357285));
#34487=CARTESIAN_POINT('Ctrl Pts',(70.9158061804528,156.934780803619,59.8215807441436));
#34488=CARTESIAN_POINT('Ctrl Pts',(72.8071059401037,157.111877375618,60.9543804525586));
#34489=CARTESIAN_POINT('Ctrl Pts',(75.1818659698177,157.288973947617,61.2464519739652));
#34490=CARTESIAN_POINT('Ctrl Pts',(77.2912945088736,157.466070519616,60.6057014773934));
#34491=CARTESIAN_POINT('Ctrl Pts',(79.4007230479296,157.643167091614,59.9649509808215));
#34492=CARTESIAN_POINT('Ctrl Pts',(81.2118275942126,157.820263663613,58.4014001198718));
#34493=CARTESIAN_POINT('Ctrl Pts',(82.153544063313,157.997360235612,56.4080561826482));
#34494=CARTESIAN_POINT('Ctrl Pts',(82.6515697929932,158.091017564954,55.3538784110865));
#34495=CARTESIAN_POINT('Ctrl Pts',(82.91294989487,158.184674894296,54.1887099277255));
#34496=CARTESIAN_POINT('Ctrl Pts',(82.9129498948689,158.278332223638,53.0228109606282));
#34497=CARTESIAN_POINT('Ctrl Pts',(82.9048209325127,159.721667776361,53.0284623995511));
#34498=CARTESIAN_POINT('Ctrl Pts',(82.9112653993961,159.648906667991,53.9369704888767));
#34499=CARTESIAN_POINT('Ctrl Pts',(82.7673370425225,159.576145559622,54.8435061998724));
#34500=CARTESIAN_POINT('Ctrl Pts',(82.4642673810189,159.503384451252,55.6928454274716));
#34501=CARTESIAN_POINT('Ctrl Pts',(81.5805803201484,159.291228441699,58.1693390560172));
#34502=CARTESIAN_POINT('Ctrl Pts',(79.3439020395175,159.079072432147,60.1595583008234));
#34503=CARTESIAN_POINT('Ctrl Pts',(76.783162515954,158.866916422595,60.7541598362084));
#34504=CARTESIAN_POINT('Ctrl Pts',(74.222422992391,158.654760413043,61.3487613715933));
#34505=CARTESIAN_POINT('Ctrl Pts',(71.3376222258955,158.44260440349,60.5477451975575));
#34506=CARTESIAN_POINT('Ctrl Pts',(69.4531073498438,158.230448393938,58.7140257000022));
#34507=CARTESIAN_POINT('Ctrl Pts',(67.5685924737917,158.018292384386,56.8803062024467));
#34508=CARTESIAN_POINT('Ctrl Pts',(66.6843634881836,157.806136374833,54.0138833813717));
#34509=CARTESIAN_POINT('Ctrl Pts',(67.2085217329933,157.593980365281,51.4394477410545));
#34510=CARTESIAN_POINT('Ctrl Pts',(67.7326799778029,157.381824355729,48.8650121007375));
#34511=CARTESIAN_POINT('Ctrl Pts',(69.6652254530304,157.169668346176,46.5825636411782));
#34512=CARTESIAN_POINT('Ctrl Pts',(72.1159778560763,156.957512336624,45.6256229094774));
#34513=CARTESIAN_POINT('Ctrl Pts',(73.3413540575996,156.851434331848,45.1471525436269));
#34514=CARTESIAN_POINT('Ctrl Pts',(74.6962819910771,156.745356327072,45.0000591097411));
#34515=CARTESIAN_POINT('Ctrl Pts',(76.0098184047083,156.639278322295,45.1710085852169));
#34516=CARTESIAN_POINT('Ctrl Pts',(77.3233548183392,156.533200317519,45.3419580606926));
#34517=CARTESIAN_POINT('Ctrl Pts',(78.5954997121234,156.427122312743,45.8309504455298));
#34518=CARTESIAN_POINT('Ctrl Pts',(79.6575912243027,156.321044307967,46.6071220412562));
#34519=CARTESIAN_POINT('Ctrl Pts',(81.6579830685288,156.121252130765,48.0689992072128));
#34520=CARTESIAN_POINT('Ctrl Pts',(82.9132382168655,155.921459953563,50.5496067868154));
#34521=CARTESIAN_POINT('Ctrl Pts',(82.9256064713947,155.721667776361,53.0242559326596));
#34522=CARTESIAN_POINT('Origin',(74.9879498948689,255.,53.0228109606356));
#34523=CARTESIAN_POINT('',(82.908722947904,150.278332223638,53.0221202519349));
#34524=CARTESIAN_POINT('',(82.9129498948689,151.721667776361,53.0228109606417));
#34525=CARTESIAN_POINT('',(82.9129498948689,255.,53.0228109606356));
#34526=CARTESIAN_POINT('Ctrl Pts',(82.9129498948689,150.278332223638,53.0228109606279));
#34527=CARTESIAN_POINT('Ctrl Pts',(82.9129498948668,150.455428795637,50.8182135007181));
#34528=CARTESIAN_POINT('Ctrl Pts',(81.9432795991064,150.632525367636,48.6308565362828));
#34529=CARTESIAN_POINT('Ctrl Pts',(80.3096882702486,150.809621939635,47.1504412801734));
#34530=CARTESIAN_POINT('Ctrl Pts',(78.6760969413907,150.986718511633,45.670026024064));
#34531=CARTESIAN_POINT('Ctrl Pts',(76.4041347530367,151.163815083632,44.9197069006017));
#34532=CARTESIAN_POINT('Ctrl Pts',(74.2101800112144,151.340911655631,45.1360689838698));
#34533=CARTESIAN_POINT('Ctrl Pts',(72.016225269392,151.51800822763,45.3524310671378));
#34534=CARTESIAN_POINT('Ctrl Pts',(69.9345925076917,151.695104799628,46.5320903475062));
#34535=CARTESIAN_POINT('Ctrl Pts',(68.6216467656562,151.872201371627,48.3030853894846));
#34536=CARTESIAN_POINT('Ctrl Pts',(67.3087010236208,152.049297943626,50.0740804314629));
#34537=CARTESIAN_POINT('Ctrl Pts',(66.7849774198233,152.226394515624,52.4087119996486));
#34538=CARTESIAN_POINT('Ctrl Pts',(67.2156126057621,152.403491087623,54.5708413428823));
#34539=CARTESIAN_POINT('Ctrl Pts',(67.6462477917008,152.580587659622,56.7329706861161));
#34540=CARTESIAN_POINT('Ctrl Pts',(69.024506420802,152.757684231621,58.6887810357286));
#34541=CARTESIAN_POINT('Ctrl Pts',(70.915806180453,152.934780803619,59.8215807441437));
#34542=CARTESIAN_POINT('Ctrl Pts',(72.8071059401039,153.111877375618,60.9543804525587));
#34543=CARTESIAN_POINT('Ctrl Pts',(75.1818659698178,153.288973947617,61.2464519739652));
#34544=CARTESIAN_POINT('Ctrl Pts',(77.2912945088738,153.466070519616,60.6057014773933));
#34545=CARTESIAN_POINT('Ctrl Pts',(79.4007230479297,153.643167091614,59.9649509808214));
#34546=CARTESIAN_POINT('Ctrl Pts',(81.2118275942127,153.820263663613,58.4014001198717));
#34547=CARTESIAN_POINT('Ctrl Pts',(82.1535440633131,153.997360235612,56.4080561826481));
#34548=CARTESIAN_POINT('Ctrl Pts',(82.6515697929933,154.091017564954,55.3538784110863));
#34549=CARTESIAN_POINT('Ctrl Pts',(82.91294989487,154.184674894296,54.1887099277253));
#34550=CARTESIAN_POINT('Ctrl Pts',(82.9129498948689,154.278332223638,53.0228109606281));
#34551=CARTESIAN_POINT('Ctrl Pts',(82.9129498948689,155.721667776361,53.0228109606419));
#34552=CARTESIAN_POINT('Ctrl Pts',(82.9129498948672,155.544571204362,55.2274084205516));
#34553=CARTESIAN_POINT('Ctrl Pts',(81.9432795991073,155.367474632364,57.4147653849869));
#34554=CARTESIAN_POINT('Ctrl Pts',(80.3096882702499,155.190378060365,58.8951806410965));
#34555=CARTESIAN_POINT('Ctrl Pts',(78.6760969413925,155.013281488366,60.3755958972062));
#34556=CARTESIAN_POINT('Ctrl Pts',(76.4041347530389,154.836184916368,61.125915020669));
#34557=CARTESIAN_POINT('Ctrl Pts',(74.2101800112166,154.659088344369,60.9095529374016));
#34558=CARTESIAN_POINT('Ctrl Pts',(72.0162252693943,154.48199177237,60.6931908541342));
#34559=CARTESIAN_POINT('Ctrl Pts',(69.9345925076938,154.304895200371,59.5135315737665));
#34560=CARTESIAN_POINT('Ctrl Pts',(68.6216467656578,154.127798628373,57.7425365317887));
#34561=CARTESIAN_POINT('Ctrl Pts',(67.3087010236219,153.950702056374,55.971541489811));
#34562=CARTESIAN_POINT('Ctrl Pts',(66.7849774198236,153.773605484375,53.6369099216257));
#34563=CARTESIAN_POINT('Ctrl Pts',(67.2156126057614,153.596508912377,51.4747805783919));
#34564=CARTESIAN_POINT('Ctrl Pts',(67.6462477916993,153.419412340378,49.3126512351581));
#34565=CARTESIAN_POINT('Ctrl Pts',(69.0245064207996,153.242315768379,47.3568408855451));
#34566=CARTESIAN_POINT('Ctrl Pts',(70.9158061804499,153.06521919638,46.2240411771293));
#34567=CARTESIAN_POINT('Ctrl Pts',(72.8071059401002,152.888122624382,45.0912414687135));
#34568=CARTESIAN_POINT('Ctrl Pts',(75.1818659698138,152.711026052383,44.7991699473059));
#34569=CARTESIAN_POINT('Ctrl Pts',(77.2912945088699,152.533929480384,45.4399204438766));
#34570=CARTESIAN_POINT('Ctrl Pts',(79.400723047926,152.356832908386,46.0806709404474));
#34571=CARTESIAN_POINT('Ctrl Pts',(81.2118275942097,152.179736336387,47.6442218013961));
#34572=CARTESIAN_POINT('Ctrl Pts',(82.1535440633112,152.002639764388,49.637565738619));
#34573=CARTESIAN_POINT('Ctrl Pts',(82.6515697929924,151.908982435046,50.6917435101814));
#34574=CARTESIAN_POINT('Ctrl Pts',(82.9129498948698,151.815325105703,51.8569119935435));
#34575=CARTESIAN_POINT('Ctrl Pts',(82.9129498948689,151.721667776361,53.0228109606417));
#34576=CARTESIAN_POINT('Origin',(74.9879498948689,255.,53.0228109606356));
#34577=CARTESIAN_POINT('',(82.9101577115551,146.278332223638,53.0299467479158));
#34578=CARTESIAN_POINT('',(82.9129498948689,147.721667776361,53.0228109606416));
#34579=CARTESIAN_POINT('',(82.9129498948689,255.,53.0228109606356));
#34580=CARTESIAN_POINT('Ctrl Pts',(82.9101577115551,146.278332223638,53.0299467479158));
#34581=CARTESIAN_POINT('Ctrl Pts',(82.8934310719895,146.435182126421,51.0768094606804));
#34582=CARTESIAN_POINT('Ctrl Pts',(82.1655901552695,146.592032029204,49.1121571431887));
#34583=CARTESIAN_POINT('Ctrl Pts',(80.8558380248122,146.748881931987,47.6756344998972));
#34584=CARTESIAN_POINT('Ctrl Pts',(79.0842603536104,146.96103794154,45.7325863613593));
#34585=CARTESIAN_POINT('Ctrl Pts',(76.248052204302,147.173193951092,44.7557731642908));
#34586=CARTESIAN_POINT('Ctrl Pts',(73.657958079385,147.385349960644,45.1960834592049));
#34587=CARTESIAN_POINT('Ctrl Pts',(71.067863954468,147.597505970197,45.6363937541189));
#34588=CARTESIAN_POINT('Ctrl Pts',(68.7238838539422,147.809661979749,47.4938275410156));
#34589=CARTESIAN_POINT('Ctrl Pts',(67.6878907853398,148.021817989301,49.9122239656804));
#34590=CARTESIAN_POINT('Ctrl Pts',(67.1698942510386,148.127895994077,51.1214221780127));
#34591=CARTESIAN_POINT('Ctrl Pts',(66.9788944747182,148.233973998854,52.4708610497871));
#34592=CARTESIAN_POINT('Ctrl Pts',(67.1071136457221,148.34005200363,53.7892545711937));
#34593=CARTESIAN_POINT('Ctrl Pts',(67.235332816726,148.446130008406,55.1076480926003));
#34594=CARTESIAN_POINT('Ctrl Pts',(67.6827709350543,148.552208013182,56.3949962636391));
#34595=CARTESIAN_POINT('Ctrl Pts',(68.4240556941093,148.658286017958,57.4817242113098));
#34596=CARTESIAN_POINT('Ctrl Pts',(69.9066252122194,148.87044202751,59.6551801066513));
#34597=CARTESIAN_POINT('Ctrl Pts',(72.5645812932367,149.082598037063,61.0261551085201));
#34598=CARTESIAN_POINT('Ctrl Pts',(75.1909799153373,149.294754046615,60.9591401134426));
#34599=CARTESIAN_POINT('Ctrl Pts',(77.8173785374379,149.506910056167,60.8921251183651));
#34600=CARTESIAN_POINT('Ctrl Pts',(80.4122197006218,149.71906606572,59.3871201263413));
#34601=CARTESIAN_POINT('Ctrl Pts',(81.7762013420966,149.931222075272,57.1391259992369));
#34602=CARTESIAN_POINT('Ctrl Pts',(82.5200751089225,150.046925458061,55.9131389270623));
#34603=CARTESIAN_POINT('Ctrl Pts',(82.8978571389894,150.16262884085,54.4661662931259));
#34604=CARTESIAN_POINT('Ctrl Pts',(82.9003953240663,150.278332223638,53.0207594678455));
#34605=CARTESIAN_POINT('Ctrl Pts',(82.9129498948689,151.721667776361,53.0228109606417));
#34606=CARTESIAN_POINT('Ctrl Pts',(82.9129498948672,151.544571204362,55.2274084205517));
#34607=CARTESIAN_POINT('Ctrl Pts',(81.9432795991071,151.367474632364,57.4147653849873));
#34608=CARTESIAN_POINT('Ctrl Pts',(80.3096882702494,151.190378060365,58.895180641097));
#34609=CARTESIAN_POINT('Ctrl Pts',(78.6760969413916,151.013281488366,60.3755958972067));
#34610=CARTESIAN_POINT('Ctrl Pts',(76.4041347530375,150.836184916367,61.1259150206693));
#34611=CARTESIAN_POINT('Ctrl Pts',(74.210180011215,150.659088344369,60.9095529374014));
#34612=CARTESIAN_POINT('Ctrl Pts',(72.0162252693925,150.48199177237,60.6931908541336));
#34613=CARTESIAN_POINT('Ctrl Pts',(69.9345925076919,150.304895200371,59.5135315737651));
#34614=CARTESIAN_POINT('Ctrl Pts',(68.6216467656563,150.127798628372,57.7425365317867));
#34615=CARTESIAN_POINT('Ctrl Pts',(67.3087010236207,149.950702056374,55.9715414898083));
#34616=CARTESIAN_POINT('Ctrl Pts',(66.7849774198233,149.773605484375,53.6369099216224));
#34617=CARTESIAN_POINT('Ctrl Pts',(67.2156126057621,149.596508912376,51.4747805783885));
#34618=CARTESIAN_POINT('Ctrl Pts',(67.6462477917009,149.419412340378,49.3126512351547));
#34619=CARTESIAN_POINT('Ctrl Pts',(69.0245064208024,149.242315768379,47.356840885542));
#34620=CARTESIAN_POINT('Ctrl Pts',(70.9158061804536,149.06521919638,46.2240411771271));
#34621=CARTESIAN_POINT('Ctrl Pts',(72.8071059401047,148.888122624381,45.0912414687122));
#34622=CARTESIAN_POINT('Ctrl Pts',(75.1818659698189,148.711026052383,44.7991699473059));
#34623=CARTESIAN_POINT('Ctrl Pts',(77.2912945088749,148.533929480384,45.4399204438782));
#34624=CARTESIAN_POINT('Ctrl Pts',(79.4007230479309,148.356832908385,46.0806709404504));
#34625=CARTESIAN_POINT('Ctrl Pts',(81.2118275942137,148.179736336386,47.6442218014006));
#34626=CARTESIAN_POINT('Ctrl Pts',(82.1535440633138,148.002639764388,49.6375657386245));
#34627=CARTESIAN_POINT('Ctrl Pts',(82.6515697929933,147.908982435045,50.6917435101854));
#34628=CARTESIAN_POINT('Ctrl Pts',(82.9129498948698,147.815325105703,51.8569119935454));
#34629=CARTESIAN_POINT('Ctrl Pts',(82.9129498948689,147.721667776361,53.0228109606416));
#34630=CARTESIAN_POINT('Origin',(74.9879498948689,255.,53.0228109606356));
#34631=CARTESIAN_POINT('',(82.9265740259991,142.278332223638,53.0227242078164));
#34632=CARTESIAN_POINT('',(82.9129498948689,143.721667776361,53.0228109606414));
#34633=CARTESIAN_POINT('',(82.9129498948689,255.,53.0228109606356));
#34634=CARTESIAN_POINT('Ctrl Pts',(82.9265740259991,142.278332223638,53.0227242078164));
#34635=CARTESIAN_POINT('Ctrl Pts',(82.9266987001804,142.283423392889,52.959623945468));
#34636=CARTESIAN_POINT('Ctrl Pts',(82.926004395604,142.288514562139,52.8965249331533));
#34637=CARTESIAN_POINT('Ctrl Pts',(82.9244823469275,142.293605731389,52.8334440014662));
#34638=CARTESIAN_POINT('Ctrl Pts',(82.8610564897863,142.505761740941,50.2047750085305));
#34639=CARTESIAN_POINT('Ctrl Pts',(81.3602502928963,142.717917750493,47.6075030844636));
#34640=CARTESIAN_POINT('Ctrl Pts',(79.1160122844355,142.930073760046,46.241539507674));
#34641=CARTESIAN_POINT('Ctrl Pts',(76.8717742759746,143.142229769598,44.8755759308844));
#34642=CARTESIAN_POINT('Ctrl Pts',(73.8841044559424,143.35438577915,44.7409207013721));
#34643=CARTESIAN_POINT('Ctrl Pts',(71.5161226428102,143.566541788703,45.8874742490525));
#34644=CARTESIAN_POINT('Ctrl Pts',(70.3321317362438,143.672619793479,46.4607510228928));
#34645=CARTESIAN_POINT('Ctrl Pts',(69.3030628314027,143.778697798255,47.3543299910311));
#34646=CARTESIAN_POINT('Ctrl Pts',(68.5353606985202,143.884775803031,48.4337905360573));
#34647=CARTESIAN_POINT('Ctrl Pts',(67.7676585656378,143.990853807807,49.5132510810832));
#34648=CARTESIAN_POINT('Ctrl Pts',(67.2613232047143,144.096931812583,50.7785932029967));
#34649=CARTESIAN_POINT('Ctrl Pts',(67.108393547461,144.20300981736,52.0851509882432));
#34650=CARTESIAN_POINT('Ctrl Pts',(66.8025342329545,144.415165826912,54.6982665587361));
#34651=CARTESIAN_POINT('Ctrl Pts',(67.910297733129,144.627321836464,57.4762447825611));
#34652=CARTESIAN_POINT('Ctrl Pts',(69.9371654396076,144.839477846017,59.1478512051887));
#34653=CARTESIAN_POINT('Ctrl Pts',(71.9640331460865,145.051633855569,60.8194576278166));
#34654=CARTESIAN_POINT('Ctrl Pts',(74.9100050588693,145.263789865121,61.384692249247));
#34655=CARTESIAN_POINT('Ctrl Pts',(77.4138798670197,145.475945874673,60.5818632145908));
#34656=CARTESIAN_POINT('Ctrl Pts',(79.9177546751699,145.688101884226,59.7790341799346));
#34657=CARTESIAN_POINT('Ctrl Pts',(81.9795323786876,145.900257893778,57.6081414891914));
#34658=CARTESIAN_POINT('Ctrl Pts',(82.6569476338984,146.11241390333,55.0680536038164));
#34659=CARTESIAN_POINT('Ctrl Pts',(82.8335403239236,146.1677200101,54.4058881903149));
#34660=CARTESIAN_POINT('Ctrl Pts',(82.9160556132897,146.223026116869,53.7186333038295));
#34661=CARTESIAN_POINT('Ctrl Pts',(82.9101577115551,146.278332223638,53.0299467479158));
#34662=CARTESIAN_POINT('Ctrl Pts',(82.9129498948689,147.721667776361,53.0228109606416));
#34663=CARTESIAN_POINT('Ctrl Pts',(82.9129498948672,147.544571204362,55.2274084205511));
#34664=CARTESIAN_POINT('Ctrl Pts',(81.9432795991076,147.367474632364,57.4147653849863));
#34665=CARTESIAN_POINT('Ctrl Pts',(80.3096882702505,147.190378060365,58.895180641096));
#34666=CARTESIAN_POINT('Ctrl Pts',(78.6760969413934,147.013281488366,60.3755958972057));
#34667=CARTESIAN_POINT('Ctrl Pts',(76.40413475304,146.836184916368,61.1259150206688));
#34668=CARTESIAN_POINT('Ctrl Pts',(74.2101800112178,146.659088344369,60.9095529374017));
#34669=CARTESIAN_POINT('Ctrl Pts',(72.0162252693957,146.48199177237,60.6931908541347));
#34670=CARTESIAN_POINT('Ctrl Pts',(69.9345925076951,146.304895200372,59.5135315737675));
#34671=CARTESIAN_POINT('Ctrl Pts',(68.6216467656588,146.127798628373,57.7425365317901));
#34672=CARTESIAN_POINT('Ctrl Pts',(67.3087010236226,145.950702056374,55.9715414898127));
#34673=CARTESIAN_POINT('Ctrl Pts',(66.7849774198238,145.773605484375,53.6369099216277));
#34674=CARTESIAN_POINT('Ctrl Pts',(67.215612605761,145.596508912377,51.474780578394));
#34675=CARTESIAN_POINT('Ctrl Pts',(67.6462477916982,145.419412340378,49.3126512351603));
#34676=CARTESIAN_POINT('Ctrl Pts',(69.0245064207979,145.242315768379,47.356840885547));
#34677=CARTESIAN_POINT('Ctrl Pts',(70.9158061804476,145.065219196381,46.2240411771307));
#34678=CARTESIAN_POINT('Ctrl Pts',(72.8071059400974,144.888122624382,45.0912414687143));
#34679=CARTESIAN_POINT('Ctrl Pts',(75.1818659698108,144.711026052383,44.7991699473058));
#34680=CARTESIAN_POINT('Ctrl Pts',(77.291294508867,144.533929480384,45.4399204438757));
#34681=CARTESIAN_POINT('Ctrl Pts',(79.4007230479233,144.356832908386,46.0806709404456));
#34682=CARTESIAN_POINT('Ctrl Pts',(81.2118275942074,144.179736336387,47.6442218013935));
#34683=CARTESIAN_POINT('Ctrl Pts',(82.1535440633097,144.002639764388,49.6375657386158));
#34684=CARTESIAN_POINT('Ctrl Pts',(82.6515697929918,143.908982435046,50.691743510179));
#34685=CARTESIAN_POINT('Ctrl Pts',(82.9129498948698,143.815325105704,51.8569119935421));
#34686=CARTESIAN_POINT('Ctrl Pts',(82.9129498948689,143.721667776361,53.0228109606414));
#34687=CARTESIAN_POINT('Origin',(74.9879498948689,255.,53.0228109606356));
#34688=CARTESIAN_POINT('',(82.911308479162,138.278332223639,53.0202043904445));
#34689=CARTESIAN_POINT('',(82.9151797848103,139.721667776361,53.0223168535823));
#34690=CARTESIAN_POINT('',(82.9129498948689,255.,53.0228109606356));
#34691=CARTESIAN_POINT('Ctrl Pts',(82.9074078591984,138.278332223639,53.0140102011414));
#34692=CARTESIAN_POINT('Ctrl Pts',(82.9139627399995,138.343820668908,52.1971816301529));
#34693=CARTESIAN_POINT('Ctrl Pts',(82.7978356043124,138.409309114178,51.3824531381546));
#34694=CARTESIAN_POINT('Ctrl Pts',(82.5512943919456,138.474797559447,50.6098539304659));
#34695=CARTESIAN_POINT('Ctrl Pts',(81.7526008271395,138.686953568999,48.1069457577048));
#34696=CARTESIAN_POINT('Ctrl Pts',(79.5852150792516,138.899109578552,46.0461832764327));
#34697=CARTESIAN_POINT('Ctrl Pts',(77.0455679583654,139.111265588104,45.3590767298199));
#34698=CARTESIAN_POINT('Ctrl Pts',(75.7757443979224,139.21734359288,45.0155234565135));
#34699=CARTESIAN_POINT('Ctrl Pts',(74.4128554942297,139.323421597656,45.0153841668718));
#34700=CARTESIAN_POINT('Ctrl Pts',(73.1254101059182,139.429499602433,45.3269704393795));
#34701=CARTESIAN_POINT('Ctrl Pts',(71.8379647176066,139.535577607209,45.6385567118871));
#34702=CARTESIAN_POINT('Ctrl Pts',(70.625962844676,139.641655611985,46.2618685465441));
#34703=CARTESIAN_POINT('Ctrl Pts',(69.6537551006523,139.747733616761,47.1480360412744));
#34704=CARTESIAN_POINT('Ctrl Pts',(67.7093396126049,139.959889626313,48.9203710307349));
#34705=CARTESIAN_POINT('Ctrl Pts',(66.7241006401847,140.172045635866,51.744128660488));
#34706=CARTESIAN_POINT('Ctrl Pts',(67.1582616853377,140.384201645418,54.3352606367889));
#34707=CARTESIAN_POINT('Ctrl Pts',(67.5924227304907,140.59635765497,56.9263926130896));
#34708=CARTESIAN_POINT('Ctrl Pts',(69.4459837932168,140.808513664523,59.2848989359379));
#34709=CARTESIAN_POINT('Ctrl Pts',(71.8628400550648,141.020669674075,60.3206254072329));
#34710=CARTESIAN_POINT('Ctrl Pts',(74.2796963169129,141.232825683627,61.3563518785279));
#34711=CARTESIAN_POINT('Ctrl Pts',(77.2598477778832,141.444981693179,61.0692984982696));
#34712=CARTESIAN_POINT('Ctrl Pts',(79.436900749672,141.657137702732,59.5957387772383));
#34713=CARTESIAN_POINT('Ctrl Pts',(81.5617103503248,141.864202543034,58.1575404959124));
#34714=CARTESIAN_POINT('Ctrl Pts',(82.9215033559457,142.071267383336,55.5890984735887));
#34715=CARTESIAN_POINT('Ctrl Pts',(82.9265740259991,142.278332223638,53.0227242078164));
#34716=CARTESIAN_POINT('Ctrl Pts',(82.9129498948689,143.721667776361,53.0228109606414));
#34717=CARTESIAN_POINT('Ctrl Pts',(82.9129498948673,143.544571204362,55.2274084205511));
#34718=CARTESIAN_POINT('Ctrl Pts',(81.9432795991076,143.367474632364,57.4147653849865));
#34719=CARTESIAN_POINT('Ctrl Pts',(80.3096882702503,143.190378060365,58.8951806410962));
#34720=CARTESIAN_POINT('Ctrl Pts',(78.676096941393,143.013281488366,60.3755958972059));
#34721=CARTESIAN_POINT('Ctrl Pts',(76.4041347530394,142.836184916368,61.1259150206689));
#34722=CARTESIAN_POINT('Ctrl Pts',(74.2101800112171,142.659088344369,60.9095529374017));
#34723=CARTESIAN_POINT('Ctrl Pts',(72.0162252693948,142.48199177237,60.6931908541344));
#34724=CARTESIAN_POINT('Ctrl Pts',(69.9345925076942,142.304895200371,59.5135315737668));
#34725=CARTESIAN_POINT('Ctrl Pts',(68.6216467656581,142.127798628373,57.7425365317891));
#34726=CARTESIAN_POINT('Ctrl Pts',(67.308701023622,141.950702056374,55.9715414898115));
#34727=CARTESIAN_POINT('Ctrl Pts',(66.7849774198236,141.773605484375,53.6369099216262));
#34728=CARTESIAN_POINT('Ctrl Pts',(67.2156126057613,141.596508912377,51.4747805783924));
#34729=CARTESIAN_POINT('Ctrl Pts',(67.646247791699,141.419412340378,49.3126512351586));
#34730=CARTESIAN_POINT('Ctrl Pts',(69.0245064207992,141.242315768379,47.3568408855455));
#34731=CARTESIAN_POINT('Ctrl Pts',(70.9158061804494,141.06521919638,46.2240411771296));
#34732=CARTESIAN_POINT('Ctrl Pts',(72.8071059400996,140.888122624382,45.0912414687136));
#34733=CARTESIAN_POINT('Ctrl Pts',(75.1818659698132,140.711026052383,44.7991699473059));
#34734=CARTESIAN_POINT('Ctrl Pts',(77.2912945088694,140.533929480384,45.4399204438765));
#34735=CARTESIAN_POINT('Ctrl Pts',(79.4007230479256,140.356832908386,46.0806709404471));
#34736=CARTESIAN_POINT('Ctrl Pts',(81.2118275942094,140.179736336387,47.6442218013957));
#34737=CARTESIAN_POINT('Ctrl Pts',(82.153544063311,140.002639764388,49.6375657386185));
#34738=CARTESIAN_POINT('Ctrl Pts',(82.6515697929922,139.908982435046,50.6917435101809));
#34739=CARTESIAN_POINT('Ctrl Pts',(82.9129498948697,139.815325105704,51.8569119935429));
#34740=CARTESIAN_POINT('Ctrl Pts',(82.9129498948689,139.721667776361,53.0228109606412));
#34741=CARTESIAN_POINT('Origin',(74.9879498948689,255.,53.0228109606356));
#34742=CARTESIAN_POINT('',(82.9084961307343,134.278332223638,53.0246083443181));
#34743=CARTESIAN_POINT('',(82.9105909927084,135.721667776361,53.0215876101194));
#34744=CARTESIAN_POINT('',(82.9129498948689,255.,53.0228109606356));
#34745=CARTESIAN_POINT('Ctrl Pts',(82.9129498948689,134.278332223638,53.0228109606272));
#34746=CARTESIAN_POINT('Ctrl Pts',(82.9129498948666,134.455428795637,50.8182135007174));
#34747=CARTESIAN_POINT('Ctrl Pts',(81.943279599106,134.632525367636,48.6308565362822));
#34748=CARTESIAN_POINT('Ctrl Pts',(80.3096882702481,134.809621939635,47.1504412801729));
#34749=CARTESIAN_POINT('Ctrl Pts',(78.6760969413901,134.986718511633,45.6700260240637));
#34750=CARTESIAN_POINT('Ctrl Pts',(76.404134753036,135.163815083632,44.9197069006016));
#34751=CARTESIAN_POINT('Ctrl Pts',(74.2101800112137,135.340911655631,45.1360689838698));
#34752=CARTESIAN_POINT('Ctrl Pts',(72.0162252693913,135.51800822763,45.352431067138));
#34753=CARTESIAN_POINT('Ctrl Pts',(69.9345925076911,135.695104799628,46.5320903475067));
#34754=CARTESIAN_POINT('Ctrl Pts',(68.6216467656558,135.872201371627,48.3030853894851));
#34755=CARTESIAN_POINT('Ctrl Pts',(67.3087010236205,136.049297943626,50.0740804314636));
#34756=CARTESIAN_POINT('Ctrl Pts',(66.7849774198233,136.226394515624,52.4087119996493));
#34757=CARTESIAN_POINT('Ctrl Pts',(67.2156126057622,136.403491087623,54.570841342883));
#34758=CARTESIAN_POINT('Ctrl Pts',(67.6462477917011,136.580587659622,56.7329706861167));
#34759=CARTESIAN_POINT('Ctrl Pts',(69.0245064208025,136.757684231621,58.6887810357291));
#34760=CARTESIAN_POINT('Ctrl Pts',(70.9158061804535,136.934780803619,59.821580744144));
#34761=CARTESIAN_POINT('Ctrl Pts',(72.8071059401046,137.111877375618,60.9543804525589));
#34762=CARTESIAN_POINT('Ctrl Pts',(75.1818659698185,137.288973947617,61.2464519739652));
#34763=CARTESIAN_POINT('Ctrl Pts',(77.2912945088744,137.466070519616,60.6057014773931));
#34764=CARTESIAN_POINT('Ctrl Pts',(79.4007230479303,137.643167091614,59.9649509808211));
#34765=CARTESIAN_POINT('Ctrl Pts',(81.2118275942132,137.820263663613,58.4014001198711));
#34766=CARTESIAN_POINT('Ctrl Pts',(82.1535440633134,137.997360235612,56.4080561826475));
#34767=CARTESIAN_POINT('Ctrl Pts',(82.6515697929935,138.091017564954,55.3538784110857));
#34768=CARTESIAN_POINT('Ctrl Pts',(82.9129498948701,138.184674894296,54.1887099277246));
#34769=CARTESIAN_POINT('Ctrl Pts',(82.9129498948689,138.278332223638,53.0228109606274));
#34770=CARTESIAN_POINT('Ctrl Pts',(82.9245648731632,139.721667776361,53.0202372717949));
#34771=CARTESIAN_POINT('Ctrl Pts',(82.909178717574,139.526581028984,55.437258796622));
#34772=CARTESIAN_POINT('Ctrl Pts',(81.7198417702367,139.331494281607,57.8629826494013));
#34773=CARTESIAN_POINT('Ctrl Pts',(79.7986919370961,139.13640753423,59.3333874365964));
#34774=CARTESIAN_POINT('Ctrl Pts',(78.7540707933465,139.030329529453,60.1329169184087));
#34775=CARTESIAN_POINT('Ctrl Pts',(77.4930805681288,138.924251524677,60.6499950895933));
#34776=CARTESIAN_POINT('Ctrl Pts',(76.183657351348,138.818173519901,60.8500262683011));
#34777=CARTESIAN_POINT('Ctrl Pts',(74.874234134567,138.712095515125,61.0500574470088));
#34778=CARTESIAN_POINT('Ctrl Pts',(73.5163779262234,138.606017510349,60.9330416332398));
#34779=CARTESIAN_POINT('Ctrl Pts',(72.2806943133818,138.499939505573,60.4818579287348));
#34780=CARTESIAN_POINT('Ctrl Pts',(69.8093270876987,138.28778349602,59.5794905197248));
#34781=CARTESIAN_POINT('Ctrl Pts',(67.8266502440253,138.075627486468,57.3404515477713));
#34782=CARTESIAN_POINT('Ctrl Pts',(67.2455404690043,137.863471476916,54.7782704142227));
#34783=CARTESIAN_POINT('Ctrl Pts',(66.6644306939832,137.651315467363,52.2160892806742));
#34784=CARTESIAN_POINT('Ctrl Pts',(67.4848879876146,137.439159457811,49.3307659855306));
#34785=CARTESIAN_POINT('Ctrl Pts',(69.3282823691089,137.227003448259,47.4557138081096));
#34786=CARTESIAN_POINT('Ctrl Pts',(71.1716767506032,137.014847438706,45.5806616306886));
#34787=CARTESIAN_POINT('Ctrl Pts',(74.0380082199606,136.802691429154,44.71588057099));
#34788=CARTESIAN_POINT('Ctrl Pts',(76.6113017439743,136.590535419602,45.2535592228728));
#34789=CARTESIAN_POINT('Ctrl Pts',(79.1845952679878,136.378379410049,45.7912378747556));
#34790=CARTESIAN_POINT('Ctrl Pts',(81.4648508466579,136.166223400497,47.7313762382197));
#34791=CARTESIAN_POINT('Ctrl Pts',(82.4032294849873,135.954067390945,50.187667964563));
#34792=CARTESIAN_POINT('Ctrl Pts',(82.7458685871294,135.87660085275,51.0845570851549));
#34793=CARTESIAN_POINT('Ctrl Pts',(82.9095994626181,135.799134314556,52.0502633081634));
#34794=CARTESIAN_POINT('Ctrl Pts',(82.9035238655686,135.721667776361,53.0179225264982));
#34795=CARTESIAN_POINT('Origin',(74.9879498948689,255.,53.0228109606356));
#34796=CARTESIAN_POINT('',(82.9145063072273,130.278332223638,53.0234757497479));
#34797=CARTESIAN_POINT('',(82.9112639633797,131.721667776361,53.0239353364917));
#34798=CARTESIAN_POINT('',(82.9129498948689,255.,53.0228109606356));
#34799=CARTESIAN_POINT('Ctrl Pts',(82.9208881629639,130.278332223638,53.0262016265857));
#34800=CARTESIAN_POINT('Ctrl Pts',(82.9158838709538,130.358537216171,52.0302352857169));
#34801=CARTESIAN_POINT('Ctrl Pts',(82.716706393915,130.438742208703,51.0317289921228));
#34802=CARTESIAN_POINT('Ctrl Pts',(82.3471180811525,130.518947201235,50.1008836172503));
#34803=CARTESIAN_POINT('Ctrl Pts',(81.8583057320879,130.625025206011,48.8697605037879));
#34804=CARTESIAN_POINT('Ctrl Pts',(81.0714049762425,130.731103210788,47.7569921614725));
#34805=CARTESIAN_POINT('Ctrl Pts',(80.0578201388033,130.837181215564,46.9184657733554));
#34806=CARTESIAN_POINT('Ctrl Pts',(78.0306504639246,131.049337225116,45.2414129971209));
#34807=CARTESIAN_POINT('Ctrl Pts',(75.0967444626701,131.261493234668,44.6613280376804));
#34808=CARTESIAN_POINT('Ctrl Pts',(72.5919475119749,131.473649244221,45.4540782931361));
#34809=CARTESIAN_POINT('Ctrl Pts',(70.0871505612799,131.685805253773,46.2468285485919));
#34810=CARTESIAN_POINT('Ctrl Pts',(68.0114626611442,131.897961263325,48.4124140189437));
#34811=CARTESIAN_POINT('Ctrl Pts',(67.324404396993,132.110117272878,50.9504988196226));
#34812=CARTESIAN_POINT('Ctrl Pts',(66.6373461328418,132.32227328243,53.4885836203017));
#34813=CARTESIAN_POINT('Ctrl Pts',(67.3389175046757,132.534429291982,56.3991677513083));
#34814=CARTESIAN_POINT('Ctrl Pts',(69.1028352259173,132.746585301535,58.348406619716));
#34815=CARTESIAN_POINT('Ctrl Pts',(70.8667529471589,132.958741311087,60.2976454881235));
#34816=CARTESIAN_POINT('Ctrl Pts',(73.6930170178079,133.170897320639,61.2855390939326));
#34817=CARTESIAN_POINT('Ctrl Pts',(76.2868996221862,133.383053330192,60.8546138701645));
#34818=CARTESIAN_POINT('Ctrl Pts',(78.8807822265645,133.595209339744,60.4236886463964));
#34819=CARTESIAN_POINT('Ctrl Pts',(81.2422833646718,133.807365349296,58.5739445930511));
#34820=CARTESIAN_POINT('Ctrl Pts',(82.2804982552316,134.019521358848,56.1605298809147));
#34821=CARTESIAN_POINT('Ctrl Pts',(82.702673889459,134.105791647112,55.1791483807895));
#34822=CARTESIAN_POINT('Ctrl Pts',(82.9060403020962,134.192061935375,54.1045623012985));
#34823=CARTESIAN_POINT('Ctrl Pts',(82.9001107603132,134.278332223638,53.027992387025));
#34824=CARTESIAN_POINT('Ctrl Pts',(82.9129498948689,135.721667776361,53.022810960641));
#34825=CARTESIAN_POINT('Ctrl Pts',(82.9129498948674,135.544571204363,55.2274084205507));
#34826=CARTESIAN_POINT('Ctrl Pts',(81.9432795991078,135.367474632364,57.4147653849862));
#34827=CARTESIAN_POINT('Ctrl Pts',(80.3096882702505,135.190378060365,58.895180641096));
#34828=CARTESIAN_POINT('Ctrl Pts',(78.6760969413933,135.013281488366,60.3755958972058));
#34829=CARTESIAN_POINT('Ctrl Pts',(76.4041347530397,134.836184916368,61.1259150206688));
#34830=CARTESIAN_POINT('Ctrl Pts',(74.2101800112174,134.659088344369,60.9095529374017));
#34831=CARTESIAN_POINT('Ctrl Pts',(72.0162252693952,134.48199177237,60.6931908541345));
#34832=CARTESIAN_POINT('Ctrl Pts',(69.9345925076945,134.304895200372,59.513531573767));
#34833=CARTESIAN_POINT('Ctrl Pts',(68.6216467656583,134.127798628373,57.7425365317894));
#34834=CARTESIAN_POINT('Ctrl Pts',(67.3087010236222,133.950702056374,55.9715414898118));
#34835=CARTESIAN_POINT('Ctrl Pts',(66.7849774198237,133.773605484375,53.6369099216266));
#34836=CARTESIAN_POINT('Ctrl Pts',(67.2156126057613,133.596508912377,51.4747805783927));
#34837=CARTESIAN_POINT('Ctrl Pts',(67.6462477916989,133.419412340378,49.3126512351589));
#34838=CARTESIAN_POINT('Ctrl Pts',(69.024506420799,133.242315768379,47.3568408855458));
#34839=CARTESIAN_POINT('Ctrl Pts',(70.9158061804491,133.06521919638,46.2240411771298));
#34840=CARTESIAN_POINT('Ctrl Pts',(72.8071059400993,132.888122624382,45.0912414687137));
#34841=CARTESIAN_POINT('Ctrl Pts',(75.1818659698129,132.711026052383,44.7991699473059));
#34842=CARTESIAN_POINT('Ctrl Pts',(77.2912945088691,132.533929480384,45.4399204438764));
#34843=CARTESIAN_POINT('Ctrl Pts',(79.4007230479253,132.356832908386,46.0806709404469));
#34844=CARTESIAN_POINT('Ctrl Pts',(81.2118275942091,132.179736336387,47.6442218013954));
#34845=CARTESIAN_POINT('Ctrl Pts',(82.1535440633108,132.002639764388,49.6375657386182));
#34846=CARTESIAN_POINT('Ctrl Pts',(82.6515697929921,131.908982435046,50.6917435101806));
#34847=CARTESIAN_POINT('Ctrl Pts',(82.9129498948697,131.815325105704,51.8569119935426));
#34848=CARTESIAN_POINT('Ctrl Pts',(82.9129498948689,131.721667776361,53.0228109606409));
#34849=CARTESIAN_POINT('Origin',(74.9879498948689,255.,53.0228109606356));
#34850=CARTESIAN_POINT('',(82.9138193369606,126.278332223638,53.0221792875591));
#34851=CARTESIAN_POINT('',(82.9235377668022,127.721667776361,53.0258702510677));
#34852=CARTESIAN_POINT('',(82.9129498948689,255.,53.0228109606356));
#34853=CARTESIAN_POINT('Ctrl Pts',(82.9129498948689,126.278332223638,53.0228109606273));
#34854=CARTESIAN_POINT('Ctrl Pts',(82.9129498948666,126.455428795637,50.8182135007172));
#34855=CARTESIAN_POINT('Ctrl Pts',(81.9432795991058,126.632525367636,48.6308565362817));
#34856=CARTESIAN_POINT('Ctrl Pts',(80.3096882702475,126.809621939635,47.1504412801724));
#34857=CARTESIAN_POINT('Ctrl Pts',(78.6760969413891,126.986718511633,45.6700260240632));
#34858=CARTESIAN_POINT('Ctrl Pts',(76.4041347530346,127.163815083632,44.9197069006013));
#34859=CARTESIAN_POINT('Ctrl Pts',(74.210180011212,127.340911655631,45.13606898387));
#34860=CARTESIAN_POINT('Ctrl Pts',(72.0162252693894,127.51800822763,45.3524310671387));
#34861=CARTESIAN_POINT('Ctrl Pts',(69.9345925076892,127.695104799628,46.5320903475081));
#34862=CARTESIAN_POINT('Ctrl Pts',(68.6216467656543,127.872201371627,48.3030853894872));
#34863=CARTESIAN_POINT('Ctrl Pts',(67.3087010236194,128.049297943626,50.0740804314663));
#34864=CARTESIAN_POINT('Ctrl Pts',(66.784977419823,128.226394515625,52.4087119996526));
#34865=CARTESIAN_POINT('Ctrl Pts',(67.2156126057629,128.403491087624,54.5708413428864));
#34866=CARTESIAN_POINT('Ctrl Pts',(67.6462477917028,128.580587659622,56.7329706861202));
#34867=CARTESIAN_POINT('Ctrl Pts',(69.0245064208054,128.757684231621,58.6887810357323));
#34868=CARTESIAN_POINT('Ctrl Pts',(70.9158061804573,128.93478080362,59.8215807441463));
#34869=CARTESIAN_POINT('Ctrl Pts',(72.8071059401092,129.111877375619,60.9543804525602));
#34870=CARTESIAN_POINT('Ctrl Pts',(75.1818659698237,129.288973947617,61.2464519739651));
#34871=CARTESIAN_POINT('Ctrl Pts',(77.2912945088795,129.466070519616,60.6057014773916));
#34872=CARTESIAN_POINT('Ctrl Pts',(79.4007230479353,129.643167091615,59.964950980818));
#34873=CARTESIAN_POINT('Ctrl Pts',(81.2118275942172,129.820263663614,58.4014001198665));
#34874=CARTESIAN_POINT('Ctrl Pts',(82.153544063316,129.997360235612,56.4080561826419));
#34875=CARTESIAN_POINT('Ctrl Pts',(82.6515697929944,130.091017564954,55.3538784110816));
#34876=CARTESIAN_POINT('Ctrl Pts',(82.9129498948701,130.184674894296,54.1887099277226));
#34877=CARTESIAN_POINT('Ctrl Pts',(82.9129498948689,130.278332223638,53.0228109606275));
#34878=CARTESIAN_POINT('Ctrl Pts',(82.9051652400584,131.721667776361,53.0280026768235));
#34879=CARTESIAN_POINT('Ctrl Pts',(82.9116631823551,131.647375581023,53.9548329532724));
#34880=CARTESIAN_POINT('Ctrl Pts',(82.7614734299345,131.573083385685,54.8798174951143));
#34881=CARTESIAN_POINT('Ctrl Pts',(82.4455487077382,131.498791190346,55.7446903029458));
#34882=CARTESIAN_POINT('Ctrl Pts',(81.5433633829565,131.286635180794,58.2145051044087));
#34883=CARTESIAN_POINT('Ctrl Pts',(79.2896083620333,131.074479171242,60.1941083459282));
#34884=CARTESIAN_POINT('Ctrl Pts',(76.7260550880175,130.862323161689,60.7691347305574));
#34885=CARTESIAN_POINT('Ctrl Pts',(74.1625018140018,130.650167152137,61.3441611151866));
#34886=CARTESIAN_POINT('Ctrl Pts',(71.2891502868935,130.438011142585,60.5146106429257));
#34887=CARTESIAN_POINT('Ctrl Pts',(69.4132672444211,130.225855133032,58.6698923132104));
#34888=CARTESIAN_POINT('Ctrl Pts',(68.4753257231848,130.119777128256,57.7475331483527));
#34889=CARTESIAN_POINT('Ctrl Pts',(67.7867513231075,130.01369912348,56.5713820191313));
#34890=CARTESIAN_POINT('Ctrl Pts',(67.4053169315246,129.907621118704,55.3028752442113));
#34891=CARTESIAN_POINT('Ctrl Pts',(67.0238825399419,129.801543113928,54.0343684692913));
#34892=CARTESIAN_POINT('Ctrl Pts',(66.9495881568535,129.695465109152,52.6735060486728));
#34893=CARTESIAN_POINT('Ctrl Pts',(67.2232779325066,129.589387104375,51.3868146975871));
#34894=CARTESIAN_POINT('Ctrl Pts',(67.7706574838129,129.377231094823,48.8134319954155));
#34895=CARTESIAN_POINT('Ctrl Pts',(69.7099736700853,129.165075085271,46.5367335713753));
#34896=CARTESIAN_POINT('Ctrl Pts',(72.1655260602513,128.952919075718,45.6025370230583));
#34897=CARTESIAN_POINT('Ctrl Pts',(74.6210784504169,128.740763066166,44.6683404747414));
#34898=CARTESIAN_POINT('Ctrl Pts',(77.5928670444764,128.528607056614,45.0766458021476));
#34899=CARTESIAN_POINT('Ctrl Pts',(79.7075944750379,128.316451047062,46.6392882462806));
#34900=CARTESIAN_POINT('Ctrl Pts',(81.6838202101202,128.118189956828,48.0995871804121));
#34901=CARTESIAN_POINT('Ctrl Pts',(82.9115729772427,127.919928866595,50.5679706767429));
#34902=CARTESIAN_POINT('Ctrl Pts',(82.9235377668022,127.721667776361,53.0258702510677));
#34903=CARTESIAN_POINT('Origin',(74.9879498948689,255.,53.0228109606356));
#34904=CARTESIAN_POINT('',(82.9069886672033,122.278332223639,53.0212720983085));
#34905=CARTESIAN_POINT('',(82.9132333187719,123.721667776361,53.0218936349848));
#34906=CARTESIAN_POINT('',(82.9129498948689,255.,53.0228109606356));
#34907=CARTESIAN_POINT('Ctrl Pts',(82.8984425219126,122.278332223638,53.0190659519314));
#34908=CARTESIAN_POINT('Ctrl Pts',(82.9027496025291,122.373253763433,51.8339480579543));
#34909=CARTESIAN_POINT('Ctrl Pts',(82.65469030603,122.468175303228,50.6504444566772));
#34910=CARTESIAN_POINT('Ctrl Pts',(82.146555570156,122.563096843023,49.5904784597474));
#34911=CARTESIAN_POINT('Ctrl Pts',(81.0108403456583,122.775252852576,47.2213833454514));
#34912=CARTESIAN_POINT('Ctrl Pts',(78.575911790868,122.987408862128,45.4694234083418));
#34913=CARTESIAN_POINT('Ctrl Pts',(75.9666213292996,123.19956487168,45.1445745189417));
#34914=CARTESIAN_POINT('Ctrl Pts',(73.3573308677313,123.411720881233,44.8197256295416));
#34915=CARTESIAN_POINT('Ctrl Pts',(70.5736784993851,123.623876890785,45.9219877878507));
#34916=CARTESIAN_POINT('Ctrl Pts',(68.8906711024336,123.836032900337,47.9414986185291));
#34917=CARTESIAN_POINT('Ctrl Pts',(67.207663705482,124.04818890989,49.9610094492078));
#34918=CARTESIAN_POINT('Ctrl Pts',(66.6253012799254,124.260344919442,52.8977689522558));
#34919=CARTESIAN_POINT('Ctrl Pts',(67.4152328050517,124.472500928994,55.4057425763972));
#34920=CARTESIAN_POINT('Ctrl Pts',(68.205164330178,124.684656938547,57.9137162005383));
#34921=CARTESIAN_POINT('Ctrl Pts',(70.3673898059867,124.896812948099,59.9929039457728));
#34922=CARTESIAN_POINT('Ctrl Pts',(72.9024154550697,125.108968957651,60.6829080691138));
#34923=CARTESIAN_POINT('Ctrl Pts',(75.4374411041527,125.321124967204,61.3729121924548));
#34924=CARTESIAN_POINT('Ctrl Pts',(78.3452669265099,125.533280976756,60.6737326939024));
#34925=CARTESIAN_POINT('Ctrl Pts',(80.3024009664751,125.745436986308,58.9154524959155));
#34926=CARTESIAN_POINT('Ctrl Pts',(81.2809679864577,125.851514991084,58.0363123969221));
#34927=CARTESIAN_POINT('Ctrl Pts',(82.0218620608422,125.95759299586,56.89239712307));
#34928=CARTESIAN_POINT('Ctrl Pts',(82.4600916525821,126.063671000637,55.6423745400647));
#34929=CARTESIAN_POINT('Ctrl Pts',(82.7556945607658,126.135224741637,54.7991856778871));
#34930=CARTESIAN_POINT('Ctrl Pts',(82.9135843024676,126.206778482638,53.9077177001598));
#34931=CARTESIAN_POINT('Ctrl Pts',(82.9189338752071,126.278332223638,53.0184634379379));
#34932=CARTESIAN_POINT('Ctrl Pts',(82.9235377668022,127.721667776361,53.0258702510677));
#34933=CARTESIAN_POINT('Ctrl Pts',(82.9243763064541,127.707772857042,53.1981295493446));
#34934=CARTESIAN_POINT('Ctrl Pts',(82.9192431881647,127.693877937723,53.3703373531198));
#34935=CARTESIAN_POINT('Ctrl Pts',(82.9079775455321,127.679983018405,53.5421430349923));
#34936=CARTESIAN_POINT('Ctrl Pts',(82.7359669184006,127.467827008852,56.1653758187108));
#34937=CARTESIAN_POINT('Ctrl Pts',(81.1342793970736,127.2556709993,58.6948618252878));
#34938=CARTESIAN_POINT('Ctrl Pts',(78.8336056229594,127.043514989748,59.9679775697825));
#34939=CARTESIAN_POINT('Ctrl Pts',(76.5329318488456,126.831358980195,61.2410933142769));
#34940=CARTESIAN_POINT('Ctrl Pts',(73.5332718219452,126.619202970643,61.2578387966896));
#34941=CARTESIAN_POINT('Ctrl Pts',(71.2207350026679,126.407046961091,60.0109890899398));
#34942=CARTESIAN_POINT('Ctrl Pts',(68.9081981833903,126.194890951538,58.7641393831897));
#34943=CARTESIAN_POINT('Ctrl Pts',(67.2827845717363,125.982734941986,56.2536944872763));
#34944=CARTESIAN_POINT('Ctrl Pts',(67.0761308428276,125.770578932434,53.6308683128316));
#34945=CARTESIAN_POINT('Ctrl Pts',(66.9728039783733,125.664500927658,52.3194552256093));
#34946=CARTESIAN_POINT('Ctrl Pts',(67.2241670846051,125.558422922881,50.9799468187542));
#34947=CARTESIAN_POINT('Ctrl Pts',(67.7679802600526,125.452344918105,49.7721103797818));
#34948=CARTESIAN_POINT('Ctrl Pts',(68.3117934355002,125.346266913329,48.5642739408093));
#34949=CARTESIAN_POINT('Ctrl Pts',(69.1480566801635,125.240188908553,47.4881094697194));
#34950=CARTESIAN_POINT('Ctrl Pts',(70.1984110257089,125.134110903777,46.6961268467724));
#34951=CARTESIAN_POINT('Ctrl Pts',(72.2991197167995,124.921954894224,45.1121616008784));
#34952=CARTESIAN_POINT('Ctrl Pts',(75.2561928114182,124.709798884672,44.664923747555));
#34953=CARTESIAN_POINT('Ctrl Pts',(77.7227071033452,124.49764287512,45.5697817361127));
#34954=CARTESIAN_POINT('Ctrl Pts',(80.1892213952723,124.285486865568,46.4746397246703));
#34955=CARTESIAN_POINT('Ctrl Pts',(82.1651768845073,124.073330856015,48.7315935551091));
#34956=CARTESIAN_POINT('Ctrl Pts',(82.7371225012787,123.861174846463,51.2980700746261));
#34957=CARTESIAN_POINT('Ctrl Pts',(82.8624869401202,123.814672489762,51.8606146229795));
#34958=CARTESIAN_POINT('Ctrl Pts',(82.9203971144115,123.768170133062,52.4380298825457));
#34959=CARTESIAN_POINT('Ctrl Pts',(82.9149187311829,123.721667776361,53.016438653844));
#34960=CARTESIAN_POINT('Origin',(74.9879498948689,255.,53.0228109606356));
#34961=CARTESIAN_POINT('',(82.9120726157757,118.278332223638,53.026230598807));
#34962=CARTESIAN_POINT('',(82.9129498948689,119.721667776361,53.0228109606404));
#34963=CARTESIAN_POINT('',(82.9129498948689,255.,53.0228109606356));
#34964=CARTESIAN_POINT('Ctrl Pts',(82.9129498948689,118.278332223638,53.022810960627));
#34965=CARTESIAN_POINT('Ctrl Pts',(82.9129498948665,118.455428795637,50.8182135007173));
#34966=CARTESIAN_POINT('Ctrl Pts',(81.943279599106,118.632525367636,48.6308565362822));
#34967=CARTESIAN_POINT('Ctrl Pts',(80.3096882702482,118.809621939635,47.1504412801731));
#34968=CARTESIAN_POINT('Ctrl Pts',(78.6760969413904,118.986718511633,45.6700260240639));
#34969=CARTESIAN_POINT('Ctrl Pts',(76.4041347530365,119.163815083632,44.9197069006017));
#34970=CARTESIAN_POINT('Ctrl Pts',(74.2101800112143,119.340911655631,45.1360689838698));
#34971=CARTESIAN_POINT('Ctrl Pts',(72.0162252693922,119.518008227629,45.3524310671378));
#34972=CARTESIAN_POINT('Ctrl Pts',(69.9345925076919,119.695104799628,46.5320903475061));
#34973=CARTESIAN_POINT('Ctrl Pts',(68.6216467656565,119.872201371627,48.3030853894842));
#34974=CARTESIAN_POINT('Ctrl Pts',(67.308701023621,120.049297943626,50.0740804314624));
#34975=CARTESIAN_POINT('Ctrl Pts',(66.7849774198234,120.226394515624,52.4087119996478));
#34976=CARTESIAN_POINT('Ctrl Pts',(67.2156126057619,120.403491087623,54.5708413428815));
#34977=CARTESIAN_POINT('Ctrl Pts',(67.6462477917003,120.580587659622,56.7329706861151));
#34978=CARTESIAN_POINT('Ctrl Pts',(69.0245064208012,120.757684231621,58.6887810357277));
#34979=CARTESIAN_POINT('Ctrl Pts',(70.9158061804518,120.934780803619,59.821580744143));
#34980=CARTESIAN_POINT('Ctrl Pts',(72.8071059401024,121.111877375618,60.9543804525582));
#34981=CARTESIAN_POINT('Ctrl Pts',(75.1818659698161,121.288973947617,61.2464519739652));
#34982=CARTESIAN_POINT('Ctrl Pts',(77.2912945088721,121.466070519615,60.6057014773938));
#34983=CARTESIAN_POINT('Ctrl Pts',(79.400723047928,121.643167091614,59.9649509808225));
#34984=CARTESIAN_POINT('Ctrl Pts',(81.2118275942112,121.820263663613,58.4014001198733));
#34985=CARTESIAN_POINT('Ctrl Pts',(82.1535440633121,121.997360235612,56.4080561826501));
#34986=CARTESIAN_POINT('Ctrl Pts',(82.651569792993,122.091017564954,55.3538784110875));
#34987=CARTESIAN_POINT('Ctrl Pts',(82.9129498948701,122.184674894296,54.1887099277254));
#34988=CARTESIAN_POINT('Ctrl Pts',(82.9129498948689,122.278332223638,53.0228109606271));
#34989=CARTESIAN_POINT('Ctrl Pts',(82.9129498948689,123.721667776361,53.0228109606405));
#34990=CARTESIAN_POINT('Ctrl Pts',(82.9129498948675,123.544571204363,55.2274084205502));
#34991=CARTESIAN_POINT('Ctrl Pts',(81.9432795991081,123.367474632364,57.4147653849857));
#34992=CARTESIAN_POINT('Ctrl Pts',(80.3096882702509,123.190378060365,58.8951806410956));
#34993=CARTESIAN_POINT('Ctrl Pts',(78.6760969413938,123.013281488366,60.3755958972055));
#34994=CARTESIAN_POINT('Ctrl Pts',(76.4041347530403,122.836184916368,61.1259150206688));
#34995=CARTESIAN_POINT('Ctrl Pts',(74.210180011218,122.659088344369,60.9095529374017));
#34996=CARTESIAN_POINT('Ctrl Pts',(72.0162252693957,122.48199177237,60.6931908541347));
#34997=CARTESIAN_POINT('Ctrl Pts',(69.9345925076949,122.304895200372,59.5135315737674));
#34998=CARTESIAN_POINT('Ctrl Pts',(68.6216467656586,122.127798628373,57.7425365317898));
#34999=CARTESIAN_POINT('Ctrl Pts',(67.3087010236223,121.950702056374,55.9715414898123));
#35000=CARTESIAN_POINT('Ctrl Pts',(66.7849774198237,121.773605484375,53.6369099216271));
#35001=CARTESIAN_POINT('Ctrl Pts',(67.2156126057612,121.596508912377,51.4747805783933));
#35002=CARTESIAN_POINT('Ctrl Pts',(67.6462477916986,121.419412340378,49.3126512351594));
#35003=CARTESIAN_POINT('Ctrl Pts',(69.0245064207986,121.242315768379,47.3568408855462));
#35004=CARTESIAN_POINT('Ctrl Pts',(70.9158061804487,121.065219196381,46.22404117713));
#35005=CARTESIAN_POINT('Ctrl Pts',(72.8071059400988,120.888122624382,45.0912414687139));
#35006=CARTESIAN_POINT('Ctrl Pts',(75.1818659698123,120.711026052383,44.7991699473058));
#35007=CARTESIAN_POINT('Ctrl Pts',(77.2912945088686,120.533929480384,45.4399204438762));
#35008=CARTESIAN_POINT('Ctrl Pts',(79.4007230479249,120.356832908386,46.0806709404466));
#35009=CARTESIAN_POINT('Ctrl Pts',(81.2118275942088,120.179736336387,47.644221801395));
#35010=CARTESIAN_POINT('Ctrl Pts',(82.1535440633106,120.002639764388,49.6375657386177));
#35011=CARTESIAN_POINT('Ctrl Pts',(82.651569792992,119.908982435046,50.6917435101801));
#35012=CARTESIAN_POINT('Ctrl Pts',(82.9129498948696,119.815325105704,51.8569119935421));
#35013=CARTESIAN_POINT('Ctrl Pts',(82.9129498948689,119.721667776361,53.0228109606404));
#35014=CARTESIAN_POINT('Origin',(74.9879498948689,255.,53.0228109606356));
#35015=CARTESIAN_POINT('',(82.9265976773671,114.278332223639,53.0209215921915));
#35016=CARTESIAN_POINT('',(82.9129498948689,115.721667776361,53.0228109606402));
#35017=CARTESIAN_POINT('',(82.9129498948689,255.,53.0228109606356));
#35018=CARTESIAN_POINT('Ctrl Pts',(82.9265976773671,114.278332223639,53.0209215921915));
#35019=CARTESIAN_POINT('Ctrl Pts',(82.926669806443,114.28189230592,52.9767949794036));
#35020=CARTESIAN_POINT('Ctrl Pts',(82.9263402120587,114.285452388202,52.9326702304328));
#35021=CARTESIAN_POINT('Ctrl Pts',(82.9256058490196,114.289012470483,52.8885531439508));
#35022=CARTESIAN_POINT('Ctrl Pts',(82.881842947036,114.501168480036,50.259483285201));
#35023=CARTESIAN_POINT('Ctrl Pts',(81.4006143848999,114.713324489588,47.6576254258715));
#35024=CARTESIAN_POINT('Ctrl Pts',(79.1653127964464,114.92548049914,46.274019737072));
#35025=CARTESIAN_POINT('Ctrl Pts',(76.930011207993,115.137636508692,44.8904140482725));
#35026=CARTESIAN_POINT('Ctrl Pts',(73.9406365932216,115.349792518245,44.7250605300029));
#35027=CARTESIAN_POINT('Ctrl Pts',(71.5680013688734,115.561948527797,45.8584296693205));
#35028=CARTESIAN_POINT('Ctrl Pts',(69.1953661445251,115.774104537349,46.9917988086382));
#35029=CARTESIAN_POINT('Ctrl Pts',(67.4394703105995,115.986260546902,49.4238906055428));
#35030=CARTESIAN_POINT('Ctrl Pts',(67.1112761817494,116.198416556454,52.030564606166));
#35031=CARTESIAN_POINT('Ctrl Pts',(66.7830820528992,116.410572566006,54.6372386067891));
#35032=CARTESIAN_POINT('Ctrl Pts',(67.8825896291245,116.622728575559,57.4184948111306));
#35033=CARTESIAN_POINT('Ctrl Pts',(69.8976241478683,116.834884585111,59.1101090677785));
#35034=CARTESIAN_POINT('Ctrl Pts',(70.9051414072403,116.940962589887,59.9559161961026));
#35035=CARTESIAN_POINT('Ctrl Pts',(72.1415404022421,117.047040594663,60.5293128375032));
#35036=CARTESIAN_POINT('Ctrl Pts',(73.440615299286,117.153118599439,60.7881680962311));
#35037=CARTESIAN_POINT('Ctrl Pts',(74.7396901963296,117.259196604216,61.0470233549589));
#35038=CARTESIAN_POINT('Ctrl Pts',(76.1014409954152,117.365274608992,60.9913372310143));
#35039=CARTESIAN_POINT('Ctrl Pts',(77.3562073346029,117.471352613768,60.5963155097164));
#35040=CARTESIAN_POINT('Ctrl Pts',(79.8657400129785,117.68350862332,59.8062720671206));
#35041=CARTESIAN_POINT('Ctrl Pts',(81.9473348517627,117.895664632872,57.6588862351121));
#35042=CARTESIAN_POINT('Ctrl Pts',(82.643354326633,118.107820642425,55.125505564479));
#35043=CARTESIAN_POINT('Ctrl Pts',(82.8298199083623,118.164657836163,54.4468057327257));
#35044=CARTESIAN_POINT('Ctrl Pts',(82.9168400828375,118.221495029901,53.7404023094359));
#35045=CARTESIAN_POINT('Ctrl Pts',(82.9105319413203,118.278332223638,53.0322361553416));
#35046=CARTESIAN_POINT('Ctrl Pts',(82.9129498948689,119.721667776361,53.0228109606404));
#35047=CARTESIAN_POINT('Ctrl Pts',(82.9129498948676,119.544571204363,55.2274084205503));
#35048=CARTESIAN_POINT('Ctrl Pts',(81.9432795991079,119.367474632364,57.4147653849862));
#35049=CARTESIAN_POINT('Ctrl Pts',(80.3096882702504,119.190378060365,58.8951806410961));
#35050=CARTESIAN_POINT('Ctrl Pts',(78.6760969413929,119.013281488366,60.3755958972061));
#35051=CARTESIAN_POINT('Ctrl Pts',(76.4041347530389,118.836184916368,61.1259150206691));
#35052=CARTESIAN_POINT('Ctrl Pts',(74.2101800112163,118.659088344369,60.9095529374016));
#35053=CARTESIAN_POINT('Ctrl Pts',(72.0162252693938,118.48199177237,60.6931908541341));
#35054=CARTESIAN_POINT('Ctrl Pts',(69.934592507693,118.304895200371,59.513531573766));
#35055=CARTESIAN_POINT('Ctrl Pts',(68.6216467656571,118.127798628373,57.7425365317878));
#35056=CARTESIAN_POINT('Ctrl Pts',(67.3087010236212,117.950702056374,55.9715414898096));
#35057=CARTESIAN_POINT('Ctrl Pts',(66.7849774198234,117.773605484375,53.6369099216238));
#35058=CARTESIAN_POINT('Ctrl Pts',(67.2156126057618,117.596508912376,51.4747805783899));
#35059=CARTESIAN_POINT('Ctrl Pts',(67.6462477917003,117.419412340378,49.3126512351559));
#35060=CARTESIAN_POINT('Ctrl Pts',(69.0245064208014,117.242315768379,47.3568408855431));
#35061=CARTESIAN_POINT('Ctrl Pts',(70.9158061804524,117.06521919638,46.2240411771278));
#35062=CARTESIAN_POINT('Ctrl Pts',(72.8071059401034,116.888122624381,45.0912414687125));
#35063=CARTESIAN_POINT('Ctrl Pts',(75.1818659698175,116.711026052383,44.7991699473059));
#35064=CARTESIAN_POINT('Ctrl Pts',(77.2912945088736,116.533929480384,45.4399204438778));
#35065=CARTESIAN_POINT('Ctrl Pts',(79.4007230479297,116.356832908385,46.0806709404496));
#35066=CARTESIAN_POINT('Ctrl Pts',(81.2118275942128,116.179736336386,47.6442218013996));
#35067=CARTESIAN_POINT('Ctrl Pts',(82.1535440633132,116.002639764388,49.6375657386233));
#35068=CARTESIAN_POINT('Ctrl Pts',(82.6515697929929,115.908982435046,50.6917435101841));
#35069=CARTESIAN_POINT('Ctrl Pts',(82.9129498948696,115.815325105703,51.856911993544));
#35070=CARTESIAN_POINT('Ctrl Pts',(82.9129498948689,115.721667776361,53.0228109606402));
#35071=CARTESIAN_POINT('Origin',(74.9879498948689,255.,53.0228109606356));
#35072=CARTESIAN_POINT('',(82.9072283316561,110.278332223639,53.0161030812075));
#35073=CARTESIAN_POINT('',(82.914162998225,111.721667776361,53.022195355026));
#35074=CARTESIAN_POINT('',(82.9129498948689,255.,53.0228109606356));
#35075=CARTESIAN_POINT('Ctrl Pts',(82.9072283316561,110.278332223639,53.0161030812075));
#35076=CARTESIAN_POINT('Ctrl Pts',(82.91339009057,110.34228958194,52.2189267668967));
#35077=CARTESIAN_POINT('Ctrl Pts',(82.8024737341836,110.406246940241,51.4234892477125));
#35078=CARTESIAN_POINT('Ctrl Pts',(82.5672179608654,110.470204298542,50.666704134855));
#35079=CARTESIAN_POINT('Ctrl Pts',(81.7868397930174,110.682360308094,48.1563360724852));
#35080=CARTESIAN_POINT('Ctrl Pts',(79.6382966506498,110.894516317646,46.0712785819531));
#35081=CARTESIAN_POINT('Ctrl Pts',(77.1037815994124,111.106672327198,45.3711664703411));
#35082=CARTESIAN_POINT('Ctrl Pts',(74.5692665481747,111.318828336751,44.671054358729));
#35083=CARTESIAN_POINT('Ctrl Pts',(71.6487795880667,111.530984346303,45.3558876260377));
#35084=CARTESIAN_POINT('Ctrl Pts',(69.6917252898121,111.743140355855,47.1087136885494));
#35085=CARTESIAN_POINT('Ctrl Pts',(67.7346709915576,111.955296365408,48.8615397510611));
#35086=CARTESIAN_POINT('Ctrl Pts',(66.741049355156,112.16745237496,51.682358608776));
#35087=CARTESIAN_POINT('Ctrl Pts',(67.1531566815994,112.379608384512,54.2808370975297));
#35088=CARTESIAN_POINT('Ctrl Pts',(67.3592103448211,112.485686389289,55.5800763419067));
#35089=CARTESIAN_POINT('Ctrl Pts',(67.9166962487536,112.591764394065,56.8237304940425));
#35090=CARTESIAN_POINT('Ctrl Pts',(68.7277558216382,112.697842398841,57.8710050532353));
#35091=CARTESIAN_POINT('Ctrl Pts',(69.5388153945226,112.803920403617,58.918279612428));
#35092=CARTESIAN_POINT('Ctrl Pts',(70.6034486363594,112.909998408393,59.7691745786775));
#35093=CARTESIAN_POINT('Ctrl Pts',(71.8098206718925,113.016076413169,60.2937193700344));
#35094=CARTESIAN_POINT('Ctrl Pts',(74.2225647429588,113.228232422722,61.3428089527482));
#35095=CARTESIAN_POINT('Ctrl Pts',(77.2022639888126,113.440388432274,61.0864978358941));
#35096=CARTESIAN_POINT('Ctrl Pts',(79.3889649908238,113.652544441826,59.6302013483819));
#35097=CARTESIAN_POINT('Ctrl Pts',(81.5389720735405,113.861140369097,58.1983422328436));
#35098=CARTESIAN_POINT('Ctrl Pts',(82.9223714178924,114.069736296368,55.6064325393708));
#35099=CARTESIAN_POINT('Ctrl Pts',(82.9265976773671,114.278332223639,53.0209215921915));
#35100=CARTESIAN_POINT('Ctrl Pts',(82.9129498948689,115.721667776361,53.0228109606402));
#35101=CARTESIAN_POINT('Ctrl Pts',(82.9129498948676,115.544571204363,55.2274084205502));
#35102=CARTESIAN_POINT('Ctrl Pts',(81.943279599108,115.367474632364,57.414765384986));
#35103=CARTESIAN_POINT('Ctrl Pts',(80.3096882702505,115.190378060365,58.895180641096));
#35104=CARTESIAN_POINT('Ctrl Pts',(78.676096941393,115.013281488366,60.375595897206));
#35105=CARTESIAN_POINT('Ctrl Pts',(76.4041347530391,114.836184916368,61.125915020669));
#35106=CARTESIAN_POINT('Ctrl Pts',(74.2101800112165,114.659088344369,60.9095529374016));
#35107=CARTESIAN_POINT('Ctrl Pts',(72.0162252693939,114.48199177237,60.6931908541341));
#35108=CARTESIAN_POINT('Ctrl Pts',(69.9345925076931,114.304895200371,59.5135315737661));
#35109=CARTESIAN_POINT('Ctrl Pts',(68.6216467656572,114.127798628373,57.7425365317879));
#35110=CARTESIAN_POINT('Ctrl Pts',(67.3087010236213,113.950702056374,55.9715414898098));
#35111=CARTESIAN_POINT('Ctrl Pts',(66.7849774198234,113.773605484375,53.636909921624));
#35112=CARTESIAN_POINT('Ctrl Pts',(67.2156126057618,113.596508912376,51.47478057839));
#35113=CARTESIAN_POINT('Ctrl Pts',(67.6462477917002,113.419412340378,49.3126512351561));
#35114=CARTESIAN_POINT('Ctrl Pts',(69.0245064208013,113.242315768379,47.3568408855432));
#35115=CARTESIAN_POINT('Ctrl Pts',(70.9158061804523,113.06521919638,46.2240411771279));
#35116=CARTESIAN_POINT('Ctrl Pts',(72.8071059401032,112.888122624381,45.0912414687126));
#35117=CARTESIAN_POINT('Ctrl Pts',(75.1818659698173,112.711026052383,44.7991699473059));
#35118=CARTESIAN_POINT('Ctrl Pts',(77.2912945088734,112.533929480384,45.4399204438777));
#35119=CARTESIAN_POINT('Ctrl Pts',(79.4007230479296,112.356832908385,46.0806709404495));
#35120=CARTESIAN_POINT('Ctrl Pts',(81.2118275942127,112.179736336386,47.6442218013994));
#35121=CARTESIAN_POINT('Ctrl Pts',(82.1535440633131,112.002639764388,49.6375657386231));
#35122=CARTESIAN_POINT('Ctrl Pts',(82.6515697929928,111.908982435046,50.691743510184));
#35123=CARTESIAN_POINT('Ctrl Pts',(82.9129498948696,111.815325105703,51.8569119935438));
#35124=CARTESIAN_POINT('Ctrl Pts',(82.9129498948689,111.721667776361,53.02281096064));
#35125=CARTESIAN_POINT('Origin',(74.9879498948689,255.,53.0228109606356));
#35126=CARTESIAN_POINT('',(82.9013905598197,106.278332223639,53.0264432070762));
#35127=CARTESIAN_POINT('',(82.9112471737191,107.721667776361,53.0211761040089));
#35128=CARTESIAN_POINT('',(82.9129498948689,255.,53.0228109606356));
#35129=CARTESIAN_POINT('Ctrl Pts',(82.9013905598197,106.278332223639,53.0264432070762));
#35130=CARTESIAN_POINT('Ctrl Pts',(82.8957299962823,106.402686857959,51.473491209011));
#35131=CARTESIAN_POINT('Ctrl Pts',(82.4553262468078,106.527041492279,49.9172246269154));
#35132=CARTESIAN_POINT('Ctrl Pts',(81.602793261273,106.6513961266,48.633248972721));
#35133=CARTESIAN_POINT('Ctrl Pts',(80.148323975016,106.863552136152,46.4427141957518));
#35134=CARTESIAN_POINT('Ctrl Pts',(77.4942997286751,107.075708145705,45.0447170612752));
#35135=CARTESIAN_POINT('Ctrl Pts',(74.8673520726336,107.287864155257,45.0848012745632));
#35136=CARTESIAN_POINT('Ctrl Pts',(72.2404044165922,107.500020164809,45.1248854878513));
#35137=CARTESIAN_POINT('Ctrl Pts',(69.6405333508502,107.712176174362,46.6030510489039));
#35138=CARTESIAN_POINT('Ctrl Pts',(68.2477787460151,107.924332183914,48.8351257599594));
#35139=CARTESIAN_POINT('Ctrl Pts',(67.5514014435974,108.03041018869,49.9511631154873));
#35140=CARTESIAN_POINT('Ctrl Pts',(67.1568032564067,108.136488193466,51.2556777585156));
#35141=CARTESIAN_POINT('Ctrl Pts',(67.0824240849773,108.242566198242,52.5782016229346));
#35142=CARTESIAN_POINT('Ctrl Pts',(67.008044913548,108.348644203018,53.9007254873536));
#35143=CARTESIAN_POINT('Ctrl Pts',(67.2538847578803,108.454722207795,55.2412585731629));
#35144=CARTESIAN_POINT('Ctrl Pts',(67.8207339014658,108.560800212571,56.4283401940603));
#35145=CARTESIAN_POINT('Ctrl Pts',(68.9544321886369,108.772956222123,58.8025034358548));
#35146=CARTESIAN_POINT('Ctrl Pts',(71.3721676728211,108.985112231675,60.5628608180023));
#35147=CARTESIAN_POINT('Ctrl Pts',(73.9780553079737,109.197268241228,60.8972413866579));
#35148=CARTESIAN_POINT('Ctrl Pts',(76.5839429431266,109.40942425078,61.2316219553135));
#35149=CARTESIAN_POINT('Ctrl Pts',(79.3779827292481,109.621580260332,60.140025710477));
#35150=CARTESIAN_POINT('Ctrl Pts',(81.0688960256448,109.833736269885,58.1263882709549));
#35151=CARTESIAN_POINT('Ctrl Pts',(82.2500601625347,109.981934921136,56.7197896397118));
#35152=CARTESIAN_POINT('Ctrl Pts',(82.8929506256246,110.130133572387,54.8632784137831));
#35153=CARTESIAN_POINT('Ctrl Pts',(82.9072283316561,110.278332223639,53.0161030812075));
#35154=CARTESIAN_POINT('Ctrl Pts',(82.9203893972147,111.721667776361,53.0190356850543));
#35155=CARTESIAN_POINT('Ctrl Pts',(82.9044169888665,111.525049942016,55.4585889787224));
#35156=CARTESIAN_POINT('Ctrl Pts',(81.7038364465635,111.32843210767,57.9063818370155));
#35157=CARTESIAN_POINT('Ctrl Pts',(79.7574894659549,111.131814273324,59.369308726392));
#35158=CARTESIAN_POINT('Ctrl Pts',(77.6573279522039,110.919658263772,60.9478467677124));
#35159=CARTESIAN_POINT('Ctrl Pts',(74.6888706496056,110.707502254219,61.3797054608276));
#35160=CARTESIAN_POINT('Ctrl Pts',(72.2237319036017,110.495346244667,60.4648205081005));
#35161=CARTESIAN_POINT('Ctrl Pts',(69.7585931575979,110.283190235115,59.5499355553734));
#35162=CARTESIAN_POINT('Ctrl Pts',(67.7967729681888,110.071034225562,57.2883069568041));
#35163=CARTESIAN_POINT('Ctrl Pts',(67.2345508544968,109.85887821601,54.7202640856088));
#35164=CARTESIAN_POINT('Ctrl Pts',(66.6723287408047,109.646722206458,52.1522212144135));
#35165=CARTESIAN_POINT('Ctrl Pts',(67.5097047028302,109.434566196906,49.277764070592));
#35166=CARTESIAN_POINT('Ctrl Pts',(69.3670720102395,109.222410187353,47.4165520463605));
#35167=CARTESIAN_POINT('Ctrl Pts',(71.2244393176486,109.010254177801,45.5553400221291));
#35168=CARTESIAN_POINT('Ctrl Pts',(74.1017979704413,108.798098168248,44.7073731174872));
#35169=CARTESIAN_POINT('Ctrl Pts',(76.6694103498548,108.585942158696,45.2639945335493));
#35170=CARTESIAN_POINT('Ctrl Pts',(79.2370227292686,108.373786149144,45.8206159496114));
#35171=CARTESIAN_POINT('Ctrl Pts',(81.494888835303,108.161630139592,47.7818256863778));
#35172=CARTESIAN_POINT('Ctrl Pts',(82.4208099654913,107.949474130039,50.2444651170894));
#35173=CARTESIAN_POINT('Ctrl Pts',(82.7522181540638,107.873538678813,51.1258996650548));
#35174=CARTESIAN_POINT('Ctrl Pts',(82.9129926600863,107.797603227587,52.0715716978783));
#35175=CARTESIAN_POINT('Ctrl Pts',(82.9088160628959,107.721667776361,53.0188418887739));
#35176=CARTESIAN_POINT('Origin',(74.9879498948689,255.,53.0228109606356));
#35177=CARTESIAN_POINT('',(82.9152391029311,102.278332223638,53.0245422282611));
#35178=CARTESIAN_POINT('',(82.9071031787868,103.721667776361,53.0246287521325));
#35179=CARTESIAN_POINT('',(82.9129498948689,255.,53.0228109606356));
#35180=CARTESIAN_POINT('Ctrl Pts',(82.9213199937229,102.278332223639,53.0291410455188));
#35181=CARTESIAN_POINT('Ctrl Pts',(82.9025444830628,102.463084133978,50.7348024945283));
#35182=CARTESIAN_POINT('Ctrl Pts',(81.852113259209,102.647836044318,48.4242605728558));
#35183=CARTESIAN_POINT('Ctrl Pts',(80.1020724172332,102.832587954658,46.9505550011793));
#35184=CARTESIAN_POINT('Ctrl Pts',(78.092449453638,103.044743964211,45.258255891705));
#35185=CARTESIAN_POINT('Ctrl Pts',(75.1602793383455,103.256899973763,44.6694593229734));
#35186=CARTESIAN_POINT('Ctrl Pts',(72.6451198214141,103.469055983315,45.4414020082891));
#35187=CARTESIAN_POINT('Ctrl Pts',(71.3875400629484,103.575133988091,45.827373350947));
#35188=CARTESIAN_POINT('Ctrl Pts',(70.2342129540729,103.681211992867,46.5535295071167));
#35189=CARTESIAN_POINT('Ctrl Pts',(69.3108412201961,103.787289997644,47.5032590866166));
#35190=CARTESIAN_POINT('Ctrl Pts',(68.3874694863192,103.89336800242,48.4529886661165));
#35191=CARTESIAN_POINT('Ctrl Pts',(67.694053127441,103.999446007196,49.6262916689466));
#35192=CARTESIAN_POINT('Ctrl Pts',(67.3436203427675,104.105524011972,50.8942339348569));
#35193=CARTESIAN_POINT('Ctrl Pts',(66.6427547734206,104.317680021524,53.4301184666777));
#35194=CARTESIAN_POINT('Ctrl Pts',(67.313823500893,104.529836031077,56.3445600508194));
#35195=CARTESIAN_POINT('Ctrl Pts',(69.0619992390115,104.741992040629,58.3057694533032));
#35196=CARTESIAN_POINT('Ctrl Pts',(70.8101749771299,104.954148050181,60.2669788557869));
#35197=CARTESIAN_POINT('Ctrl Pts',(73.6354577258942,105.166304059734,61.2749560766129));
#35198=CARTESIAN_POINT('Ctrl Pts',(76.2324908878125,105.378460069286,60.8634439022218));
#35199=CARTESIAN_POINT('Ctrl Pts',(78.8295240497311,105.590616078838,60.4519317278306));
#35200=CARTESIAN_POINT('Ctrl Pts',(81.1983076248037,105.802772088391,58.6209301582221));
#35201=CARTESIAN_POINT('Ctrl Pts',(82.2552422492533,106.014928097943,56.2138931636867));
#35202=CARTESIAN_POINT('Ctrl Pts',(82.6926576859061,106.102729473175,55.2177339749835));
#35203=CARTESIAN_POINT('Ctrl Pts',(82.9053872364686,106.190530848407,54.1229147768275));
#35204=CARTESIAN_POINT('Ctrl Pts',(82.9013905598197,106.278332223639,53.0264432070762));
#35205=CARTESIAN_POINT('Ctrl Pts',(82.9129498948689,107.721667776361,53.0228109606394));
#35206=CARTESIAN_POINT('Ctrl Pts',(82.9129498948679,107.544571204363,55.2274084205489));
#35207=CARTESIAN_POINT('Ctrl Pts',(81.9432795991088,107.367474632364,57.4147653849844));
#35208=CARTESIAN_POINT('Ctrl Pts',(80.3096882702521,107.190378060365,58.8951806410946));
#35209=CARTESIAN_POINT('Ctrl Pts',(78.6760969413954,107.013281488367,60.3755958972047));
#35210=CARTESIAN_POINT('Ctrl Pts',(76.4041347530422,106.836184916368,61.1259150206684));
#35211=CARTESIAN_POINT('Ctrl Pts',(74.21018001122,106.659088344369,60.9095529374019));
#35212=CARTESIAN_POINT('Ctrl Pts',(72.0162252693978,106.48199177237,60.6931908541355));
#35213=CARTESIAN_POINT('Ctrl Pts',(69.9345925076968,106.304895200372,59.5135315737688));
#35214=CARTESIAN_POINT('Ctrl Pts',(68.6216467656601,106.127798628373,57.7425365317918));
#35215=CARTESIAN_POINT('Ctrl Pts',(67.3087010236234,105.950702056374,55.9715414898148));
#35216=CARTESIAN_POINT('Ctrl Pts',(66.784977419824,105.773605484376,53.63690992163));
#35217=CARTESIAN_POINT('Ctrl Pts',(67.2156126057606,105.596508912377,51.4747805783961));
#35218=CARTESIAN_POINT('Ctrl Pts',(67.6462477916972,105.419412340378,49.3126512351623));
#35219=CARTESIAN_POINT('Ctrl Pts',(69.0245064207963,105.242315768379,47.3568408855486));
#35220=CARTESIAN_POINT('Ctrl Pts',(70.9158061804458,105.065219196381,46.2240411771318));
#35221=CARTESIAN_POINT('Ctrl Pts',(72.8071059400953,104.888122624382,45.0912414687149));
#35222=CARTESIAN_POINT('Ctrl Pts',(75.1818659698085,104.711026052383,44.7991699473058));
#35223=CARTESIAN_POINT('Ctrl Pts',(77.2912945088649,104.533929480385,45.4399204438751));
#35224=CARTESIAN_POINT('Ctrl Pts',(79.4007230479214,104.356832908386,46.0806709404444));
#35225=CARTESIAN_POINT('Ctrl Pts',(81.2118275942059,104.179736336387,47.6442218013918));
#35226=CARTESIAN_POINT('Ctrl Pts',(82.1535440633088,104.002639764389,49.6375657386139));
#35227=CARTESIAN_POINT('Ctrl Pts',(82.6515697929912,103.908982435046,50.691743510177));
#35228=CARTESIAN_POINT('Ctrl Pts',(82.9129498948695,103.815325105704,51.8569119935402));
#35229=CARTESIAN_POINT('Ctrl Pts',(82.9129498948689,103.721667776361,53.0228109606397));
#35230=CARTESIAN_POINT('Origin',(74.9879498948689,255.,53.0228109606356));
#35231=CARTESIAN_POINT('',(82.9148571242665,98.2783322236385,53.0204066145287));
#35232=CARTESIAN_POINT('',(82.9174705652005,99.7216677763613,53.0248696685428));
#35233=CARTESIAN_POINT('',(82.9129498948689,255.,53.0228109606356));
#35234=CARTESIAN_POINT('Ctrl Pts',(82.9129498948689,98.2783322236385,53.0228109606261));
#35235=CARTESIAN_POINT('Ctrl Pts',(82.9129498948663,98.4554287956372,50.8182135007165));
#35236=CARTESIAN_POINT('Ctrl Pts',(81.9432795991056,98.632525367636,48.6308565362815));
#35237=CARTESIAN_POINT('Ctrl Pts',(80.3096882702476,98.8096219396347,47.1504412801725));
#35238=CARTESIAN_POINT('Ctrl Pts',(78.6760969413896,98.9867185116334,45.6700260240635));
#35239=CARTESIAN_POINT('Ctrl Pts',(76.4041347530357,99.1638150836321,44.9197069006016));
#35240=CARTESIAN_POINT('Ctrl Pts',(74.2101800112135,99.3409116556309,45.1360689838698));
#35241=CARTESIAN_POINT('Ctrl Pts',(72.0162252693913,99.5180082276296,45.3524310671381));
#35242=CARTESIAN_POINT('Ctrl Pts',(69.9345925076912,99.6951047996283,46.5320903475066));
#35243=CARTESIAN_POINT('Ctrl Pts',(68.621646765656,99.872201371627,48.3030853894849));
#35244=CARTESIAN_POINT('Ctrl Pts',(67.3087010236207,100.049297943626,50.0740804314632));
#35245=CARTESIAN_POINT('Ctrl Pts',(66.7849774198233,100.226394515624,52.4087119996487));
#35246=CARTESIAN_POINT('Ctrl Pts',(67.215612605762,100.403491087623,54.5708413428823));
#35247=CARTESIAN_POINT('Ctrl Pts',(67.6462477917007,100.580587659622,56.7329706861159));
#35248=CARTESIAN_POINT('Ctrl Pts',(69.0245064208018,100.757684231621,58.6887810357283));
#35249=CARTESIAN_POINT('Ctrl Pts',(70.9158061804525,100.934780803619,59.8215807441434));
#35250=CARTESIAN_POINT('Ctrl Pts',(72.8071059401033,101.111877375618,60.9543804525585));
#35251=CARTESIAN_POINT('Ctrl Pts',(75.181865969817,101.288973947617,61.2464519739652));
#35252=CARTESIAN_POINT('Ctrl Pts',(77.2912945088729,101.466070519615,60.6057014773936));
#35253=CARTESIAN_POINT('Ctrl Pts',(79.4007230479288,101.643167091614,59.964950980822));
#35254=CARTESIAN_POINT('Ctrl Pts',(81.2118275942118,101.820263663613,58.4014001198726));
#35255=CARTESIAN_POINT('Ctrl Pts',(82.1535440633125,101.997360235612,56.4080561826493));
#35256=CARTESIAN_POINT('Ctrl Pts',(82.6515697929932,102.091017564954,55.3538784110869));
#35257=CARTESIAN_POINT('Ctrl Pts',(82.9129498948702,102.184674894296,54.1887099277249));
#35258=CARTESIAN_POINT('Ctrl Pts',(82.9129498948689,102.278332223638,53.0228109606267));
#35259=CARTESIAN_POINT('Ctrl Pts',(82.9002911396369,103.721667776361,53.0267466703926));
#35260=CARTESIAN_POINT('Ctrl Pts',(82.9057021213605,103.645844494054,53.9729164059735));
#35261=CARTESIAN_POINT('Ctrl Pts',(82.7488630974118,103.570021211748,54.9176096992055));
#35262=CARTESIAN_POINT('Ctrl Pts',(82.4215784532667,103.494197929441,55.7991000146744));
#35263=CARTESIAN_POINT('Ctrl Pts',(81.9637019147087,103.388119924664,57.0323192983762));
#35264=CARTESIAN_POINT('Ctrl Pts',(81.1722212836696,103.282041919888,58.1418347754652));
#35265=CARTESIAN_POINT('Ctrl Pts',(80.1708053598078,103.175963915112,59.0088802071099));
#35266=CARTESIAN_POINT('Ctrl Pts',(79.169389435946,103.069885910336,59.8759256387545));
#35267=CARTESIAN_POINT('Ctrl Pts',(77.9580382192615,102.96380790556,60.5005010249548));
#35268=CARTESIAN_POINT('Ctrl Pts',(76.6719915821466,102.857729900784,60.7772044282973));
#35269=CARTESIAN_POINT('Ctrl Pts',(74.0998983079167,102.645573891231,61.3306112349823));
#35270=CARTESIAN_POINT('Ctrl Pts',(71.2290233519653,102.433417881679,60.4925301102361));
#35271=CARTESIAN_POINT('Ctrl Pts',(69.3719298576632,102.221261872127,58.6341263636949));
#35272=CARTESIAN_POINT('Ctrl Pts',(67.5148363633613,102.009105862574,56.7757226171537));
#35273=CARTESIAN_POINT('Ctrl Pts',(66.6715243307089,101.796949853022,53.8969962488175));
#35274=CARTESIAN_POINT('Ctrl Pts',(67.2321703217131,101.58479384347,51.328027664629));
#35275=CARTESIAN_POINT('Ctrl Pts',(67.7928163127172,101.372637833918,48.7590590804408));
#35276=CARTESIAN_POINT('Ctrl Pts',(69.7574203273777,101.160481824365,46.4998482804));
#35277=CARTESIAN_POINT('Ctrl Pts',(72.2214217592123,100.948325814813,45.5835323756284));
#35278=CARTESIAN_POINT('Ctrl Pts',(74.6854231910471,100.736169805261,44.6672164708568));
#35279=CARTESIAN_POINT('Ctrl Pts',(77.6488220400558,100.524013795708,45.0937954613543));
#35280=CARTESIAN_POINT('Ctrl Pts',(79.7518025028245,100.311857786156,46.6722113403257));
#35281=CARTESIAN_POINT('Ctrl Pts',(81.7018738403247,100.115127782891,48.1358595380769));
#35282=CARTESIAN_POINT('Ctrl Pts',(82.9121010957909,99.9183977796261,50.5899325326873));
#35283=CARTESIAN_POINT('Ctrl Pts',(82.9250431686022,99.7216677763613,53.0283182231438));
#35284=CARTESIAN_POINT('Origin',(74.9879498948689,255.,53.0228109606356));
#35285=CARTESIAN_POINT('',(82.9078887632605,94.2783322236386,53.0225290086082));
#35286=CARTESIAN_POINT('',(82.9129498948689,95.7216677763614,53.0228109606393));
#35287=CARTESIAN_POINT('',(82.9129498948689,255.,53.0228109606356));
#35288=CARTESIAN_POINT('Ctrl Pts',(82.8975201390833,94.2783322236385,53.0219513800174));
#35289=CARTESIAN_POINT('Ctrl Pts',(82.8998090143212,94.371722676465,51.8556225753435));
#35290=CARTESIAN_POINT('Ctrl Pts',(82.658061451432,94.4651131292914,50.6900196140694));
#35291=CARTESIAN_POINT('Ctrl Pts',(82.1665533003896,94.5585035821179,49.6413515712521));
#35292=CARTESIAN_POINT('Ctrl Pts',(81.608271351691,94.6645815868941,48.4502168215223));
#35293=CARTESIAN_POINT('Ctrl Pts',(80.7277566876189,94.7706595916702,47.409947572931));
#35294=CARTESIAN_POINT('Ctrl Pts',(79.6580752337028,94.8767375964464,46.6286773122345));
#35295=CARTESIAN_POINT('Ctrl Pts',(78.588393779787,94.9828156012226,45.8474070515383));
#35296=CARTESIAN_POINT('Ctrl Pts',(77.3295455360272,95.0888936059988,45.3251357787369));
#35297=CARTESIAN_POINT('Ctrl Pts',(76.025022796263,95.194971610775,45.1557216479993));
#35298=CARTESIAN_POINT('Ctrl Pts',(73.4159773167343,95.4071276203273,44.8168933865239));
#35299=CARTESIAN_POINT('Ctrl Pts',(70.6242338531869,95.6192836298796,45.8894936933033));
#35300=CARTESIAN_POINT('Ctrl Pts',(68.9271693444514,95.8314396394319,47.8950940485404));
#35301=CARTESIAN_POINT('Ctrl Pts',(67.2301048357161,96.0435956489842,49.9006944037773));
#35302=CARTESIAN_POINT('Ctrl Pts',(66.6277192817928,96.2557516585364,52.839294807472));
#35303=CARTESIAN_POINT('Ctrl Pts',(67.398870273312,96.4679076680887,55.353106586833));
#35304=CARTESIAN_POINT('Ctrl Pts',(68.1700212648314,96.6800636776411,57.8669183661945));
#35305=CARTESIAN_POINT('Ctrl Pts',(70.3147088017936,96.8922196871935,59.9559415212221));
#35306=CARTESIAN_POINT('Ctrl Pts',(72.8460411335263,97.1043756967458,60.6653740548343));
#35307=CARTESIAN_POINT('Ctrl Pts',(75.3773734652585,97.3165317062981,61.3748065884463));
#35308=CARTESIAN_POINT('Ctrl Pts',(78.2953505917612,97.5286877158503,60.7046485006431));
#35309=CARTESIAN_POINT('Ctrl Pts',(80.2606118745933,97.7408437254026,58.9577450677149));
#35310=CARTESIAN_POINT('Ctrl Pts',(81.9202480039677,97.9200065581479,57.4825091399822));
#35311=CARTESIAN_POINT('Ctrl Pts',(82.9004481365671,98.0991693908933,55.2393847052011));
#35312=CARTESIAN_POINT('Ctrl Pts',(82.9197187285079,98.2783322236386,53.0142778398783));
#35313=CARTESIAN_POINT('Ctrl Pts',(82.9129498948689,99.7216677763614,53.0228109606395));
#35314=CARTESIAN_POINT('Ctrl Pts',(82.9129498948678,99.5445712043626,55.2274084205496));
#35315=CARTESIAN_POINT('Ctrl Pts',(81.9432795991082,99.3674746323639,57.4147653849857));
#35316=CARTESIAN_POINT('Ctrl Pts',(80.3096882702507,99.1903780603651,58.8951806410958));
#35317=CARTESIAN_POINT('Ctrl Pts',(78.6760969413931,99.0132814883663,60.375595897206));
#35318=CARTESIAN_POINT('Ctrl Pts',(76.404134753039,98.8361849163676,61.1259150206691));
#35319=CARTESIAN_POINT('Ctrl Pts',(74.2101800112163,98.6590883443688,60.9095529374016));
#35320=CARTESIAN_POINT('Ctrl Pts',(72.0162252693936,98.4819917723701,60.693190854134));
#35321=CARTESIAN_POINT('Ctrl Pts',(69.9345925076927,98.3048952003713,59.5135315737658));
#35322=CARTESIAN_POINT('Ctrl Pts',(68.6216467656568,98.1277986283726,57.7425365317874));
#35323=CARTESIAN_POINT('Ctrl Pts',(67.308701023621,97.9507020563738,55.971541489809));
#35324=CARTESIAN_POINT('Ctrl Pts',(66.7849774198233,97.7736054843751,53.636909921623));
#35325=CARTESIAN_POINT('Ctrl Pts',(67.215612605762,97.5965089123763,51.474780578389));
#35326=CARTESIAN_POINT('Ctrl Pts',(67.6462477917008,97.4194123403775,49.3126512351549));
#35327=CARTESIAN_POINT('Ctrl Pts',(69.0245064208023,97.2423157683788,47.3568408855421));
#35328=CARTESIAN_POINT('Ctrl Pts',(70.9158061804536,97.06521919638,46.2240411771271));
#35329=CARTESIAN_POINT('Ctrl Pts',(72.8071059401049,96.8881226243813,45.0912414687121));
#35330=CARTESIAN_POINT('Ctrl Pts',(75.1818659698193,96.7110260523825,44.7991699473059));
#35331=CARTESIAN_POINT('Ctrl Pts',(77.2912945088754,96.5339294803838,45.4399204438783));
#35332=CARTESIAN_POINT('Ctrl Pts',(79.4007230479315,96.356832908385,46.0806709404507));
#35333=CARTESIAN_POINT('Ctrl Pts',(81.2118275942143,96.1797363363863,47.6442218014012));
#35334=CARTESIAN_POINT('Ctrl Pts',(82.1535440633142,96.0026397643875,49.6375657386254));
#35335=CARTESIAN_POINT('Ctrl Pts',(82.651569792993,95.9089824350455,50.6917435101853));
#35336=CARTESIAN_POINT('Ctrl Pts',(82.9129498948694,95.8153251057034,51.8569119935439));
#35337=CARTESIAN_POINT('Ctrl Pts',(82.9129498948689,95.7216677763614,53.0228109606389));
#35338=CARTESIAN_POINT('Origin',(74.9879498948689,255.,53.0228109606356));
#35339=CARTESIAN_POINT('',(82.9129498948689,90.2783322236385,53.0228109606262));
#35340=CARTESIAN_POINT('',(82.906851181591,91.7216677763616,53.0226606669491));
#35341=CARTESIAN_POINT('',(82.9129498948689,255.,53.0228109606356));
#35342=CARTESIAN_POINT('Ctrl Pts',(82.9129498948689,90.2783322236385,53.0228109606262));
#35343=CARTESIAN_POINT('Ctrl Pts',(82.9129498948663,90.4554287956373,50.8182135007164));
#35344=CARTESIAN_POINT('Ctrl Pts',(81.9432795991055,90.632525367636,48.6308565362813));
#35345=CARTESIAN_POINT('Ctrl Pts',(80.3096882702473,90.8096219396347,47.1504412801723));
#35346=CARTESIAN_POINT('Ctrl Pts',(78.6760969413892,90.9867185116335,45.6700260240633));
#35347=CARTESIAN_POINT('Ctrl Pts',(76.404134753035,91.1638150836322,44.9197069006014));
#35348=CARTESIAN_POINT('Ctrl Pts',(74.2101800112127,91.3409116556309,45.1360689838699));
#35349=CARTESIAN_POINT('Ctrl Pts',(72.0162252693904,91.5180082276297,45.3524310671384));
#35350=CARTESIAN_POINT('Ctrl Pts',(69.9345925076903,91.6951047996284,46.5320903475073));
#35351=CARTESIAN_POINT('Ctrl Pts',(68.6216467656552,91.8722013716271,48.3030853894859));
#35352=CARTESIAN_POINT('Ctrl Pts',(67.3087010236201,92.0492979436258,50.0740804314645));
#35353=CARTESIAN_POINT('Ctrl Pts',(66.7849774198232,92.2263945156246,52.4087119996503));
#35354=CARTESIAN_POINT('Ctrl Pts',(67.2156126057624,92.4034910876233,54.5708413428839));
#35355=CARTESIAN_POINT('Ctrl Pts',(67.6462477917016,92.580587659622,56.7329706861176));
#35356=CARTESIAN_POINT('Ctrl Pts',(69.0245064208032,92.7576842316208,58.6887810357299));
#35357=CARTESIAN_POINT('Ctrl Pts',(70.9158061804544,92.9347808036195,59.8215807441445));
#35358=CARTESIAN_POINT('Ctrl Pts',(72.8071059401056,93.1118773756182,60.9543804525592));
#35359=CARTESIAN_POINT('Ctrl Pts',(75.1818659698196,93.288973947617,61.2464519739652));
#35360=CARTESIAN_POINT('Ctrl Pts',(77.2912945088754,93.4660705196157,60.6057014773928));
#35361=CARTESIAN_POINT('Ctrl Pts',(79.4007230479312,93.6431670916144,59.9649509808205));
#35362=CARTESIAN_POINT('Ctrl Pts',(81.2118275942138,93.8202636636132,58.4014001198703));
#35363=CARTESIAN_POINT('Ctrl Pts',(82.1535440633138,93.9973602356119,56.4080561826466));
#35364=CARTESIAN_POINT('Ctrl Pts',(82.6515697929939,94.0910175649541,55.3538784110845));
#35365=CARTESIAN_POINT('Ctrl Pts',(82.9129498948704,94.1846748942963,54.188709927723));
#35366=CARTESIAN_POINT('Ctrl Pts',(82.9129498948689,94.2783322236386,53.0228109606255));
#35367=CARTESIAN_POINT('Ctrl Pts',(82.9129498948689,95.7216677763614,53.0228109606389));
#35368=CARTESIAN_POINT('Ctrl Pts',(82.912949894868,95.5445712043627,55.2274084205487));
#35369=CARTESIAN_POINT('Ctrl Pts',(81.9432795991088,95.367474632364,57.4147653849845));
#35370=CARTESIAN_POINT('Ctrl Pts',(80.3096882702518,95.1903780603652,58.8951806410948));
#35371=CARTESIAN_POINT('Ctrl Pts',(78.6760969413948,95.0132814883665,60.3755958972051));
#35372=CARTESIAN_POINT('Ctrl Pts',(76.4041347530412,94.8361849163678,61.1259150206686));
#35373=CARTESIAN_POINT('Ctrl Pts',(74.2101800112187,94.659088344369,60.9095529374018));
#35374=CARTESIAN_POINT('Ctrl Pts',(72.0162252693962,94.4819917723703,60.693190854135));
#35375=CARTESIAN_POINT('Ctrl Pts',(69.9345925076952,94.3048952003716,59.5135315737677));
#35376=CARTESIAN_POINT('Ctrl Pts',(68.6216467656588,94.1277986283728,57.7425365317901));
#35377=CARTESIAN_POINT('Ctrl Pts',(67.3087010236224,93.9507020563741,55.9715414898125));
#35378=CARTESIAN_POINT('Ctrl Pts',(66.7849774198237,93.7736054843754,53.6369099216271));
#35379=CARTESIAN_POINT('Ctrl Pts',(67.2156126057612,93.5965089123766,51.4747805783931));
#35380=CARTESIAN_POINT('Ctrl Pts',(67.6462477916987,93.4194123403779,49.3126512351591));
#35381=CARTESIAN_POINT('Ctrl Pts',(69.0245064207989,93.2423157683792,47.3568408855458));
#35382=CARTESIAN_POINT('Ctrl Pts',(70.9158061804492,93.0652191963804,46.2240411771297));
#35383=CARTESIAN_POINT('Ctrl Pts',(72.8071059400995,92.8881226243817,45.0912414687136));
#35384=CARTESIAN_POINT('Ctrl Pts',(75.1818659698133,92.711026052383,44.7991699473058));
#35385=CARTESIAN_POINT('Ctrl Pts',(77.2912945088696,92.5339294803842,45.4399204438765));
#35386=CARTESIAN_POINT('Ctrl Pts',(79.4007230479259,92.3568329083855,46.0806709404473));
#35387=CARTESIAN_POINT('Ctrl Pts',(81.2118275942097,92.1797363363868,47.6442218013961));
#35388=CARTESIAN_POINT('Ctrl Pts',(82.1535440633112,92.0026397643881,49.6375657386191));
#35389=CARTESIAN_POINT('Ctrl Pts',(82.6515697929919,91.9089824350458,50.6917435101805));
#35390=CARTESIAN_POINT('Ctrl Pts',(82.9129498948693,91.8153251057037,51.8569119935412));
#35391=CARTESIAN_POINT('Ctrl Pts',(82.9129498948689,91.7216677763615,53.0228109606383));
#35392=CARTESIAN_POINT('Origin',(74.9879498948689,255.,53.0228109606356));
#35393=CARTESIAN_POINT('',(82.923214744261,86.2783322236386,53.0234237509025));
#35394=CARTESIAN_POINT('',(82.9133860738174,87.7216677763614,53.0299211193051));
#35395=CARTESIAN_POINT('',(82.9129498948689,255.,53.0228109606356));
#35396=CARTESIAN_POINT('Ctrl Pts',(82.923214744261,86.2783322236386,53.0234237509025));
#35397=CARTESIAN_POINT('Ctrl Pts',(82.9231887310882,86.2803612189517,52.998261746315));
#35398=CARTESIAN_POINT('Ctrl Pts',(82.9230330643765,86.2823902142647,52.9731001886098));
#35399=CARTESIAN_POINT('Ctrl Pts',(82.9227472344118,86.2844192095777,52.947940164016));
#35400=CARTESIAN_POINT('Ctrl Pts',(82.8928602532351,86.4965752191301,50.3171551721588));
#35401=CARTESIAN_POINT('Ctrl Pts',(81.4398681471162,86.7087312286823,47.703132042207));
#35402=CARTESIAN_POINT('Ctrl Pts',(79.2163713661519,86.9208872382346,46.3036597142281));
#35403=CARTESIAN_POINT('Ctrl Pts',(76.9928745851877,87.1330432477869,44.9041873862493));
#35404=CARTESIAN_POINT('Ctrl Pts',(73.9988731293783,87.3451992573393,44.719265860243));
#35405=CARTESIAN_POINT('Ctrl Pts',(71.6178272157902,87.5573552668916,45.8348571255192));
#35406=CARTESIAN_POINT('Ctrl Pts',(69.236781302202,87.7695112764439,46.9504483907955));
#35407=CARTESIAN_POINT('Ctrl Pts',(67.4686909308351,87.9816672859962,49.3665524473543));
#35408=CARTESIAN_POINT('Ctrl Pts',(67.1207426280689,88.1938232955485,51.9722903221266));
#35409=CARTESIAN_POINT('Ctrl Pts',(66.7727943253027,88.4059793051008,54.5780281968992));
#35410=CARTESIAN_POINT('Ctrl Pts',(67.8449880911375,88.6181353146531,57.3733998898852));
#35411=CARTESIAN_POINT('Ctrl Pts',(69.8498961129948,88.8302913242055,59.0746545262256));
#35412=CARTESIAN_POINT('Ctrl Pts',(71.8548041348518,89.0424473337578,60.7759091625658));
#35413=CARTESIAN_POINT('Ctrl Pts',(74.7924264127309,89.2546033433102,61.3830467422606));
#35414=CARTESIAN_POINT('Ctrl Pts',(77.3052194191063,89.4667593528625,60.6160186861589));
#35415=CARTESIAN_POINT('Ctrl Pts',(79.8180124254817,89.6789153624148,59.8489906300571));
#35416=CARTESIAN_POINT('Ctrl Pts',(81.9059761603533,89.891071371967,57.7077969381589));
#35417=CARTESIAN_POINT('Ctrl Pts',(82.625093647743,90.1032273815193,55.1770276985099));
#35418=CARTESIAN_POINT('Ctrl Pts',(82.8229369775333,90.1615956622257,54.4807634272564));
#35419=CARTESIAN_POINT('Ctrl Pts',(82.9171712325869,90.2199639429321,53.7550118690877));
#35420=CARTESIAN_POINT('Ctrl Pts',(82.9127205943178,90.2783322236385,53.0279097020349));
#35421=CARTESIAN_POINT('Ctrl Pts',(82.9000974149753,91.7216677763615,53.0224942304407));
#35422=CARTESIAN_POINT('Ctrl Pts',(82.9004702208451,91.6148803125606,54.3566851265562));
#35423=CARTESIAN_POINT('Ctrl Pts',(82.5815271080044,91.5080928487596,55.6910138645003));
#35424=CARTESIAN_POINT('Ctrl Pts',(81.9431078719293,91.4013053849587,56.8503669330465));
#35425=CARTESIAN_POINT('Ctrl Pts',(80.6747522735636,91.1891493754064,59.1536683874527));
#35426=CARTESIAN_POINT('Ctrl Pts',(78.1454156900416,90.9769933658541,60.7663360951428));
#35427=CARTESIAN_POINT('Ctrl Pts',(75.524149721516,90.7648373563018,60.9436083546364));
#35428=CARTESIAN_POINT('Ctrl Pts',(72.9028837529902,90.5526813467495,61.1208806141299));
#35429=CARTESIAN_POINT('Ctrl Pts',(70.1896883994607,90.3405253371971,59.8627574254265));
#35430=CARTESIAN_POINT('Ctrl Pts',(68.6171357769601,90.1283693276448,57.7534918768312));
#35431=CARTESIAN_POINT('Ctrl Pts',(67.8308594657099,90.0222913228686,56.6988591025336));
#35432=CARTESIAN_POINT('Ctrl Pts',(67.3297438372168,89.9162133180924,55.4314407382631));
#35433=CARTESIAN_POINT('Ctrl Pts',(67.1462614461992,89.8101353133163,54.1195962942507));
#35434=CARTESIAN_POINT('Ctrl Pts',(66.9627790551816,89.7040573085401,52.8077518502383));
#35435=CARTESIAN_POINT('Ctrl Pts',(67.0969299016394,89.597979303764,51.4514813264839));
#35436=CARTESIAN_POINT('Ctrl Pts',(67.563679444442,89.4919012989879,50.2215928800997));
#35437=CARTESIAN_POINT('Ctrl Pts',(68.4971785300472,89.2797452894356,47.7618159873313));
#35438=CARTESIAN_POINT('Ctrl Pts',(70.7610724010317,89.0675892798832,45.8075674040433));
#35439=CARTESIAN_POINT('Ctrl Pts',(73.3303864196594,88.8554332703309,45.2588541771032));
#35440=CARTESIAN_POINT('Ctrl Pts',(75.8997004382875,88.6432772607786,44.7101409501631));
#35441=CARTESIAN_POINT('Ctrl Pts',(78.7744346045589,88.4311212512264,45.5669630795712));
#35442=CARTESIAN_POINT('Ctrl Pts',(80.6260625288807,88.2189652416741,47.4338850232124));
#35443=CARTESIAN_POINT('Ctrl Pts',(82.0728121408136,88.0531994199032,48.892584453046));
#35444=CARTESIAN_POINT('Ctrl Pts',(82.8949645428175,87.8874335981323,50.9679407850187));
#35445=CARTESIAN_POINT('Ctrl Pts',(82.9133860738174,87.7216677763614,53.0299211193051));
#35446=CARTESIAN_POINT('Origin',(74.9879498948689,255.,53.0228109606356));
#35447=CARTESIAN_POINT('',(82.9112619154184,82.2783322236386,53.0204263509097));
#35448=CARTESIAN_POINT('',(82.9253497859361,83.7216677763615,53.0207628815399));
#35449=CARTESIAN_POINT('',(82.9129498948689,255.,53.0228109606356));
#35450=CARTESIAN_POINT('Ctrl Pts',(82.9076441624805,82.2783322236387,53.0153155489345));
#35451=CARTESIAN_POINT('Ctrl Pts',(82.9148898770911,82.3407584949712,52.2380428063635));
#35452=CARTESIAN_POINT('Ctrl Pts',(82.8102713239623,82.4031847663036,51.4624782333206));
#35453=CARTESIAN_POINT('Ctrl Pts',(82.5863312910923,82.4656110376361,50.7225627634984));
#35454=CARTESIAN_POINT('Ctrl Pts',(81.8252699183938,82.6777670471884,48.2079561702668));
#35455=CARTESIAN_POINT('Ctrl Pts',(79.6860648096109,82.8899230567406,46.105090936656));
#35456=CARTESIAN_POINT('Ctrl Pts',(77.1568571560168,83.1020790662929,45.3860414538124));
#35457=CARTESIAN_POINT('Ctrl Pts',(74.6276495024229,83.3142350758453,44.6669919709688));
#35458=CARTESIAN_POINT('Ctrl Pts',(71.7084393040178,83.5263910853977,45.3317582388919));
#35459=CARTESIAN_POINT('Ctrl Pts',(69.7370844997,83.73854709495,47.0709241679838));
#35460=CARTESIAN_POINT('Ctrl Pts',(67.7657296953823,83.9507031045023,48.8100900970757));
#35461=CARTESIAN_POINT('Ctrl Pts',(66.7422302851519,84.1628591140545,51.6236556873363));
#35462=CARTESIAN_POINT('Ctrl Pts',(67.1403706679598,84.3750151236068,54.2227724121782));
#35463=CARTESIAN_POINT('Ctrl Pts',(67.5385110507677,84.5871711331591,56.8218891370208));
#35464=CARTESIAN_POINT('Ctrl Pts',(69.3582912266146,84.7993271427115,59.2065569964446));
#35465=CARTESIAN_POINT('Ctrl Pts',(71.7584050082544,85.0114831522639,60.2751610236323));
#35466=CARTESIAN_POINT('Ctrl Pts',(74.1585187898934,85.2236391618162,61.3437650508196));
#35467=CARTESIAN_POINT('Ctrl Pts',(77.1389661773251,85.4357951713685,61.0963052457719));
#35468=CARTESIAN_POINT('Ctrl Pts',(79.3413937306905,85.6479511809208,59.6571263905914));
#35469=CARTESIAN_POINT('Ctrl Pts',(80.4426075073733,85.7540291856969,58.9375369630011));
#35470=CARTESIAN_POINT('Ctrl Pts',(81.3493163255395,85.8601071904731,57.9200177728776));
#35471=CARTESIAN_POINT('Ctrl Pts',(81.9730871299462,85.9661851952492,56.7514666971134));
#35472=CARTESIAN_POINT('Ctrl Pts',(82.5849268272283,86.0702342047124,55.6052669529073));
#35473=CARTESIAN_POINT('Ctrl Pts',(82.9245487270679,86.1742832141755,54.3137577583859));
#35474=CARTESIAN_POINT('Ctrl Pts',(82.923214744261,86.2783322236386,53.0234237509025));
#35475=CARTESIAN_POINT('Ctrl Pts',(82.9133860738174,87.7216677763614,53.0299211193051));
#35476=CARTESIAN_POINT('Ctrl Pts',(82.9185414084526,87.6752775885799,53.6069740599373));
#35477=CARTESIAN_POINT('Ctrl Pts',(82.8607500486254,87.6288874007985,54.1829794175166));
#35478=CARTESIAN_POINT('Ctrl Pts',(82.7360858105918,87.5824972130171,54.7441283695434));
#35479=CARTESIAN_POINT('Ctrl Pts',(82.1659594856094,87.3703412034647,57.3104280143593));
#35480=CARTESIAN_POINT('Ctrl Pts',(80.1971851532724,87.1581851939125,59.5660055461174));
#35481=CARTESIAN_POINT('Ctrl Pts',(77.7292412067298,86.9460291843602,60.4732961227791));
#35482=CARTESIAN_POINT('Ctrl Pts',(75.2612972601866,86.7338731748078,61.380586699441));
#35483=CARTESIAN_POINT('Ctrl Pts',(72.2941836994374,86.5217171652554,60.9395903210058));
#35484=CARTESIAN_POINT('Ctrl Pts',(70.1988923804859,86.3095611557031,59.354593469127));
#35485=CARTESIAN_POINT('Ctrl Pts',(68.1036010615352,86.0974051461508,57.7695966172488));
#35486=CARTESIAN_POINT('Ctrl Pts',(66.8801319843817,85.8852491365986,55.0405992919284));
#35487=CARTESIAN_POINT('Ctrl Pts',(67.0759628953565,85.6730931270463,52.4169428435099));
#35488=CARTESIAN_POINT('Ctrl Pts',(67.173878350844,85.5670151222701,51.1051146193002));
#35489=CARTESIAN_POINT('Ctrl Pts',(67.6266188033639,85.4609371174939,49.819621614316));
#35490=CARTESIAN_POINT('Ctrl Pts',(68.3483029371681,85.3548591127177,48.7088679764125));
#35491=CARTESIAN_POINT('Ctrl Pts',(69.0699870709721,85.2487811079416,47.5981143385093));
#35492=CARTESIAN_POINT('Ctrl Pts',(70.0606148860604,85.1427031031655,46.6621000676865));
#35493=CARTESIAN_POINT('Ctrl Pts',(71.2194816091533,85.0366250983894,46.0395981445058));
#35494=CARTESIAN_POINT('Ctrl Pts',(73.5372150553394,84.8244690888371,44.7945942981443));
#35495=CARTESIAN_POINT('Ctrl Pts',(76.5279041335448,84.6123130792847,44.8036398423513));
#35496=CARTESIAN_POINT('Ctrl Pts',(78.827536031194,84.4001570697323,46.0741333948936));
#35497=CARTESIAN_POINT('Ctrl Pts',(81.127167928843,84.18800106018,47.3446269474357));
#35498=CARTESIAN_POINT('Ctrl Pts',(82.7357426459362,83.9758450506277,49.8765685083131));
#35499=CARTESIAN_POINT('Ctrl Pts',(82.9095242971506,83.7636890410754,52.5002535983109));
#35500=CARTESIAN_POINT('Ctrl Pts',(82.9209978110418,83.7496819528374,52.6734760709703));
#35501=CARTESIAN_POINT('Ctrl Pts',(82.9262170881152,83.7356748645995,52.8470984520006));
#35502=CARTESIAN_POINT('Ctrl Pts',(82.9253497859361,83.7216677763615,53.0207628815399));
#35503=CARTESIAN_POINT('Origin',(74.9879498948689,255.,53.0228109606356));
#35504=CARTESIAN_POINT('',(82.9085981452144,78.2783322236386,53.0246573544551));
#35505=CARTESIAN_POINT('',(82.911245752919,79.7216677763615,53.0212425220677));
#35506=CARTESIAN_POINT('',(82.9129498948689,255.,53.0228109606356));
#35507=CARTESIAN_POINT('Ctrl Pts',(82.9129498948689,78.2783322236386,53.0228109606257));
#35508=CARTESIAN_POINT('Ctrl Pts',(82.9129498948662,78.4554287956373,50.8182135007157));
#35509=CARTESIAN_POINT('Ctrl Pts',(81.9432795991051,78.6325253676361,48.6308565362806));
#35510=CARTESIAN_POINT('Ctrl Pts',(80.3096882702466,78.8096219396348,47.1504412801716));
#35511=CARTESIAN_POINT('Ctrl Pts',(78.6760969413882,78.9867185116336,45.6700260240627));
#35512=CARTESIAN_POINT('Ctrl Pts',(76.4041347530337,79.1638150836323,44.9197069006012));
#35513=CARTESIAN_POINT('Ctrl Pts',(74.2101800112113,79.340911655631,45.1360689838701));
#35514=CARTESIAN_POINT('Ctrl Pts',(72.0162252693889,79.5180082276298,45.352431067139));
#35515=CARTESIAN_POINT('Ctrl Pts',(69.9345925076889,79.6951047996286,46.5320903475084));
#35516=CARTESIAN_POINT('Ctrl Pts',(68.6216467656541,79.8722013716273,48.3030853894874));
#35517=CARTESIAN_POINT('Ctrl Pts',(67.3087010236194,80.049297943626,50.0740804314665));
#35518=CARTESIAN_POINT('Ctrl Pts',(66.784977419823,80.2263945156247,52.4087119996525));
#35519=CARTESIAN_POINT('Ctrl Pts',(67.2156126057628,80.4034910876235,54.5708413428862));
#35520=CARTESIAN_POINT('Ctrl Pts',(67.6462477917027,80.5805876596222,56.7329706861199));
#35521=CARTESIAN_POINT('Ctrl Pts',(69.0245064208051,80.757684231621,58.6887810357319));
#35522=CARTESIAN_POINT('Ctrl Pts',(70.9158061804568,80.9347808036198,59.8215807441459));
#35523=CARTESIAN_POINT('Ctrl Pts',(72.8071059401084,81.1118773756185,60.95438045256));
#35524=CARTESIAN_POINT('Ctrl Pts',(75.1818659698227,81.2889739476172,61.2464519739651));
#35525=CARTESIAN_POINT('Ctrl Pts',(77.2912945088785,81.466070519616,60.6057014773919));
#35526=CARTESIAN_POINT('Ctrl Pts',(79.4007230479342,81.6431670916147,59.9649509808187));
#35527=CARTESIAN_POINT('Ctrl Pts',(81.2118275942163,81.8202636636135,58.4014001198676));
#35528=CARTESIAN_POINT('Ctrl Pts',(82.1535440633154,81.9973602356122,56.4080561826433));
#35529=CARTESIAN_POINT('Ctrl Pts',(82.6515697929944,82.0910175649544,55.3538784110821));
#35530=CARTESIAN_POINT('Ctrl Pts',(82.9129498948703,82.1846748942964,54.1887099277221));
#35531=CARTESIAN_POINT('Ctrl Pts',(82.9129498948689,82.2783322236386,53.0228109606259));
#35532=CARTESIAN_POINT('Ctrl Pts',(82.9253497859361,83.7216677763615,53.0207628815399));
#35533=CARTESIAN_POINT('Ctrl Pts',(82.91308064132,83.5235188550472,55.4774775676541));
#35534=CARTESIAN_POINT('Ctrl Pts',(81.6827731049543,83.3253699337328,57.9426069471548));
#35535=CARTESIAN_POINT('Ctrl Pts',(79.7090566453533,83.1272210124185,59.4030691718097));
#35536=CARTESIAN_POINT('Ctrl Pts',(77.5958187570055,82.9150650028661,60.9667710361928));
#35537=CARTESIAN_POINT('Ctrl Pts',(74.6303543949743,82.7029089933138,61.3787461458397));
#35538=CARTESIAN_POINT('Ctrl Pts',(72.1721275036747,82.4907529837614,60.4454487309336));
#35539=CARTESIAN_POINT('Ctrl Pts',(69.713900612376,82.2785969742091,59.5121513160278));
#35540=CARTESIAN_POINT('Ctrl Pts',(67.7629111918085,82.0664409646569,57.23358137657));
#35541=CARTESIAN_POINT('Ctrl Pts',(67.2202981950566,81.8542849551046,54.6629721360415));
#35542=CARTESIAN_POINT('Ctrl Pts',(66.6776851983047,81.6421289455523,52.0923628955127));
#35543=CARTESIAN_POINT('Ctrl Pts',(67.5434486253686,81.429972936,49.2297143539131));
#35544=CARTESIAN_POINT('Ctrl Pts',(69.4117049022399,81.2178169264477,47.377272347006));
#35545=CARTESIAN_POINT('Ctrl Pts',(70.3458330406758,81.1117389216715,46.4510513435522));
#35546=CARTESIAN_POINT('Ctrl Pts',(71.5305843915636,81.0056609168953,45.7773819737716));
#35547=CARTESIAN_POINT('Ctrl Pts',(72.8038060612515,80.8995829121191,45.4119942168095));
#35548=CARTESIAN_POINT('Ctrl Pts',(74.0770277309391,80.7935049073429,45.0466064598474));
#35549=CARTESIAN_POINT('Ctrl Pts',(75.4387197194266,80.6874269025668,44.9895003157035));
#35550=CARTESIAN_POINT('Ctrl Pts',(76.7218528853392,80.5813488977906,45.2794141042527));
#35551=CARTESIAN_POINT('Ctrl Pts',(79.2881192171644,80.3691928882383,45.859241681351));
#35552=CARTESIAN_POINT('Ctrl Pts',(81.5401502586898,80.1570368786861,47.8271489892214));
#35553=CARTESIAN_POINT('Ctrl Pts',(82.4432684135962,79.9448808691338,50.2943008552432));
#35554=CARTESIAN_POINT('Ctrl Pts',(82.7599972788634,79.8704765048764,51.1595455707012));
#35555=CARTESIAN_POINT('Ctrl Pts',(82.9108171050971,79.796072140619,52.0861946849957));
#35556=CARTESIAN_POINT('Ctrl Pts',(82.9045916518496,79.7216677763616,53.0151182970485));
#35557=CARTESIAN_POINT('Origin',(74.9879498948689,255.,53.0228109606356));
#35558=CARTESIAN_POINT('',(82.9153733449052,74.2783322236386,53.0241785897874));
#35559=CARTESIAN_POINT('',(82.9105899036684,75.7216677763615,53.0242486736905));
#35560=CARTESIAN_POINT('',(82.9129498948689,255.,53.0228109606356));
#35561=CARTESIAN_POINT('Ctrl Pts',(82.9213292833048,74.2783322236386,53.0275397134229));
#35562=CARTESIAN_POINT('Ctrl Pts',(82.9025944532997,74.4615530470099,50.7531106339741));
#35563=CARTESIAN_POINT('Ctrl Pts',(81.8714282549828,74.6447738703813,48.4655481839494));
#35564=CARTESIAN_POINT('Ctrl Pts',(80.1458417428987,74.8279946937527,46.9901750960443));
#35565=CARTESIAN_POINT('Ctrl Pts',(78.1477416263029,75.040150703305,45.2818034100573));
#35566=CARTESIAN_POINT('Ctrl Pts',(75.2185691545151,75.2523067128573,44.6624077336402));
#35567=CARTESIAN_POINT('Ctrl Pts',(72.7008217304853,75.4644627224097,45.4206104918576));
#35568=CARTESIAN_POINT('Ctrl Pts',(70.1830743064558,75.676618731962,46.1788132500749));
#35569=CARTESIAN_POINT('Ctrl Pts',(68.0767519301841,75.8887747415143,48.3146144429265));
#35570=CARTESIAN_POINT('Ctrl Pts',(67.3547954479706,76.1009307510666,50.8407259942096));
#35571=CARTESIAN_POINT('Ctrl Pts',(66.632838965757,76.3130867606189,53.3668375454927));
#35572=CARTESIAN_POINT('Ctrl Pts',(67.2952483776016,76.5252427701712,56.2832594552074));
#35573=CARTESIAN_POINT('Ctrl Pts',(69.0286775479858,76.7373987797235,58.262437622095));
#35574=CARTESIAN_POINT('Ctrl Pts',(69.8953921331778,76.8434767844997,59.2520267055389));
#35575=CARTESIAN_POINT('Ctrl Pts',(71.0298616580048,76.9495547892759,60.0073048532759));
#35576=CARTESIAN_POINT('Ctrl Pts',(72.2742514908426,77.055632794052,60.4612823604607));
#35577=CARTESIAN_POINT('Ctrl Pts',(73.5186413236806,77.1617107988282,60.9152598676457));
#35578=CARTESIAN_POINT('Ctrl Pts',(74.8729514645296,77.2677888036043,61.0679367342783));
#35579=CARTESIAN_POINT('Ctrl Pts',(76.1732887679165,77.3738668083805,60.8689301422339));
#35580=CARTESIAN_POINT('Ctrl Pts',(78.7739633746896,77.5860228179328,60.4709169581452));
#35581=CARTESIAN_POINT('Ctrl Pts',(81.1587466316146,77.7981788274851,58.6661699393487));
#35582=CARTESIAN_POINT('Ctrl Pts',(82.2330447085192,78.0103348370374,56.2685994244952));
#35583=CARTESIAN_POINT('Ctrl Pts',(82.6853990516724,78.0996672992378,55.2590551846553));
#35584=CARTESIAN_POINT('Ctrl Pts',(82.9054048022027,78.1889997614382,54.1444035333906));
#35585=CARTESIAN_POINT('Ctrl Pts',(82.9011716266685,78.2783322236386,53.0278083348896));
#35586=CARTESIAN_POINT('Ctrl Pts',(82.9129498948689,79.7216677763615,53.0228109606377));
#35587=CARTESIAN_POINT('Ctrl Pts',(82.9129498948683,79.5445712043628,55.2274084205477));
#35588=CARTESIAN_POINT('Ctrl Pts',(81.9432795991093,79.367474632364,57.4147653849839));
#35589=CARTESIAN_POINT('Ctrl Pts',(80.3096882702523,79.1903780603653,58.8951806410944));
#35590=CARTESIAN_POINT('Ctrl Pts',(78.6760969413953,79.0132814883665,60.3755958972049));
#35591=CARTESIAN_POINT('Ctrl Pts',(76.4041347530416,78.8361849163678,61.1259150206686));
#35592=CARTESIAN_POINT('Ctrl Pts',(74.2101800112189,78.6590883443691,60.9095529374018));
#35593=CARTESIAN_POINT('Ctrl Pts',(72.0162252693963,78.4819917723703,60.6931908541351));
#35594=CARTESIAN_POINT('Ctrl Pts',(69.9345925076951,78.3048952003716,59.5135315737677));
#35595=CARTESIAN_POINT('Ctrl Pts',(68.6216467656587,78.1277986283728,57.7425365317899));
#35596=CARTESIAN_POINT('Ctrl Pts',(67.3087010236222,77.9507020563741,55.9715414898121));
#35597=CARTESIAN_POINT('Ctrl Pts',(66.7849774198236,77.7736054843754,53.6369099216265));
#35598=CARTESIAN_POINT('Ctrl Pts',(67.2156126057613,77.5965089123766,51.4747805783924));
#35599=CARTESIAN_POINT('Ctrl Pts',(67.6462477916991,77.4194123403779,49.3126512351583));
#35600=CARTESIAN_POINT('Ctrl Pts',(69.0245064207996,77.2423157683791,47.356840885545));
#35601=CARTESIAN_POINT('Ctrl Pts',(70.9158061804502,77.0652191963804,46.2240411771291));
#35602=CARTESIAN_POINT('Ctrl Pts',(72.8071059401008,76.8881226243816,45.0912414687133));
#35603=CARTESIAN_POINT('Ctrl Pts',(75.1818659698148,76.7110260523829,44.7991699473058));
#35604=CARTESIAN_POINT('Ctrl Pts',(77.2912945088711,76.5339294803842,45.439920443877));
#35605=CARTESIAN_POINT('Ctrl Pts',(79.4007230479274,76.3568329083854,46.0806709404482));
#35606=CARTESIAN_POINT('Ctrl Pts',(81.211827594211,76.1797363363866,47.6442218013975));
#35607=CARTESIAN_POINT('Ctrl Pts',(82.1535440633121,76.0026397643879,49.6375657386209));
#35608=CARTESIAN_POINT('Ctrl Pts',(82.6515697929922,75.9089824350457,50.6917435101819));
#35609=CARTESIAN_POINT('Ctrl Pts',(82.9129498948693,75.8153251057036,51.856911993542));
#35610=CARTESIAN_POINT('Ctrl Pts',(82.9129498948689,75.7216677763615,53.0228109606385));
#35611=CARTESIAN_POINT('Origin',(74.9879498948689,255.,53.0228109606356));
#35612=CARTESIAN_POINT('',(82.9144228299092,70.2783322236386,53.0212847568831));
#35613=CARTESIAN_POINT('',(82.9149525301073,71.7216677763616,53.0232506905358));
#35614=CARTESIAN_POINT('',(82.9129498948689,255.,53.0228109606356));
#35615=CARTESIAN_POINT('Ctrl Pts',(82.9129498948689,70.2783322236386,53.0228109606254));
#35616=CARTESIAN_POINT('Ctrl Pts',(82.9129498948661,70.4554287956373,50.8182135007157));
#35617=CARTESIAN_POINT('Ctrl Pts',(81.9432795991052,70.6325253676361,48.6308565362808));
#35618=CARTESIAN_POINT('Ctrl Pts',(80.3096882702471,70.8096219396348,47.150441280172));
#35619=CARTESIAN_POINT('Ctrl Pts',(78.6760969413889,70.9867185116335,45.6700260240632));
#35620=CARTESIAN_POINT('Ctrl Pts',(76.4041347530349,71.1638150836322,44.9197069006015));
#35621=CARTESIAN_POINT('Ctrl Pts',(74.2101800112128,71.3409116556309,45.1360689838699));
#35622=CARTESIAN_POINT('Ctrl Pts',(72.0162252693906,71.5180082276296,45.3524310671384));
#35623=CARTESIAN_POINT('Ctrl Pts',(69.9345925076906,71.6951047996284,46.5320903475071));
#35624=CARTESIAN_POINT('Ctrl Pts',(68.6216467656555,71.8722013716271,48.3030853894855));
#35625=CARTESIAN_POINT('Ctrl Pts',(67.3087010236204,72.0492979436258,50.0740804314639));
#35626=CARTESIAN_POINT('Ctrl Pts',(66.7849774198233,72.2263945156245,52.4087119996495));
#35627=CARTESIAN_POINT('Ctrl Pts',(67.2156126057622,72.4034910876232,54.570841342883));
#35628=CARTESIAN_POINT('Ctrl Pts',(67.6462477917011,72.580587659622,56.7329706861166));
#35629=CARTESIAN_POINT('Ctrl Pts',(69.0245064208023,72.7576842316206,58.6887810357289));
#35630=CARTESIAN_POINT('Ctrl Pts',(70.9158061804532,72.9347808036194,59.8215807441438));
#35631=CARTESIAN_POINT('Ctrl Pts',(72.807105940104,73.1118773756181,60.9543804525587));
#35632=CARTESIAN_POINT('Ctrl Pts',(75.1818659698178,73.2889739476168,61.2464519739652));
#35633=CARTESIAN_POINT('Ctrl Pts',(77.2912945088736,73.4660705196156,60.6057014773934));
#35634=CARTESIAN_POINT('Ctrl Pts',(79.4007230479294,73.6431670916143,59.9649509808216));
#35635=CARTESIAN_POINT('Ctrl Pts',(81.2118275942123,73.820263663613,58.401400119872));
#35636=CARTESIAN_POINT('Ctrl Pts',(82.1535440633128,73.9973602356117,56.4080561826487));
#35637=CARTESIAN_POINT('Ctrl Pts',(82.6515697929935,74.091017564954,55.353878411086));
#35638=CARTESIAN_POINT('Ctrl Pts',(82.9129498948704,74.1846748942963,54.1887099277238));
#35639=CARTESIAN_POINT('Ctrl Pts',(82.9129498948689,74.2783322236386,53.0228109606255));
#35640=CARTESIAN_POINT('Ctrl Pts',(82.9024847110463,75.7216677763615,53.0291863790398));
#35641=CARTESIAN_POINT('Ctrl Pts',(82.9094436057292,75.644313407086,53.993811927591));
#35642=CARTESIAN_POINT('Ctrl Pts',(82.7471053581289,75.5669590378106,54.9563720673458));
#35643=CARTESIAN_POINT('Ctrl Pts',(82.4058558444903,75.4896046685351,55.8514524956269));
#35644=CARTESIAN_POINT('Ctrl Pts',(81.4699276512495,75.2774486589828,58.3063453952938));
#35645=CARTESIAN_POINT('Ctrl Pts',(79.1882052139606,75.0652926494305,60.2536469660177));
#35646=CARTESIAN_POINT('Ctrl Pts',(76.6147118588759,74.8531366398782,60.7931425314416));
#35647=CARTESIAN_POINT('Ctrl Pts',(74.0412185037915,74.6409806303259,61.3326380968654));
#35648=CARTESIAN_POINT('Ctrl Pts',(71.1759542309114,74.4288246207735,60.4643276569895));
#35649=CARTESIAN_POINT('Ctrl Pts',(69.3317194678335,74.2166686112212,58.5908987066219));
#35650=CARTESIAN_POINT('Ctrl Pts',(67.4874847047556,74.0045126016689,56.7174697562543));
#35651=CARTESIAN_POINT('Ctrl Pts',(66.6642794514797,73.7923565921166,53.8389222953949));
#35652=CARTESIAN_POINT('Ctrl Pts',(67.2441244107334,73.5802005825643,51.2742189330149));
#35653=CARTESIAN_POINT('Ctrl Pts',(67.8239693699872,73.368044573012,48.7095155706345));
#35654=CARTESIAN_POINT('Ctrl Pts',(69.8068645417708,73.1558885634596,46.4586563067335));
#35655=CARTESIAN_POINT('Ctrl Pts',(72.2761531551931,72.9437325539073,45.5613968819512));
#35656=CARTESIAN_POINT('Ctrl Pts',(74.7454417686152,72.731576544355,44.664137457169));
#35657=CARTESIAN_POINT('Ctrl Pts',(77.7011238236759,72.5194205348028,45.1204778715052));
#35658=CARTESIAN_POINT('Ctrl Pts',(79.7969456072804,72.3072645252504,46.7109035869639));
#35659=CARTESIAN_POINT('Ctrl Pts',(80.8448564990826,72.2011865204743,47.5061164446932));
#35660=CARTESIAN_POINT('Ctrl Pts',(81.6778023230208,72.095108515698,48.5848506277031));
#35661=CARTESIAN_POINT('Ctrl Pts',(82.2178940525135,71.9890305109219,49.794355715263));
#35662=CARTESIAN_POINT('Ctrl Pts',(82.6716494501422,71.8999095994018,50.8105154377147));
#35663=CARTESIAN_POINT('Ctrl Pts',(82.9186956245664,71.8107886878817,51.9189789817963));
#35664=CARTESIAN_POINT('Ctrl Pts',(82.922415508883,71.7216677763616,53.0248893788183));
#35665=CARTESIAN_POINT('Origin',(74.9879498948689,255.,53.0228109606356));
#35666=CARTESIAN_POINT('',(82.908625053032,66.2783322236386,53.0218734498001));
#35667=CARTESIAN_POINT('',(82.9131277587349,67.7216677763615,53.0225723293765));
#35668=CARTESIAN_POINT('',(82.9129498948689,255.,53.0228109606356));
#35669=CARTESIAN_POINT('Ctrl Pts',(82.9012831846627,66.2783322236387,53.0202819278075));
#35670=CARTESIAN_POINT('Ctrl Pts',(82.9054592133395,66.3701915894966,51.8729674294636));
#35671=CARTESIAN_POINT('Ctrl Pts',(82.6726571039608,66.4620509553545,50.7270111641337));
#35672=CARTESIAN_POINT('Ctrl Pts',(82.194940541544,66.5539103212124,49.6935928802838));
#35673=CARTESIAN_POINT('Ctrl Pts',(81.0916187557596,66.7660663307647,47.3068368075379));
#35674=CARTESIAN_POINT('Ctrl Pts',(78.6818908535276,66.978222340317,45.5203732267803));
#35675=CARTESIAN_POINT('Ctrl Pts',(76.0795684308802,67.1903783498693,45.159293262891));
#35676=CARTESIAN_POINT('Ctrl Pts',(73.4772460082324,67.4025343594217,44.7982132990016));
#35677=CARTESIAN_POINT('Ctrl Pts',(70.6823290651691,67.614690368974,45.8625169519807));
#35678=CARTESIAN_POINT('Ctrl Pts',(68.9654077236915,67.8268463785263,47.8560324428168));
#35679=CARTESIAN_POINT('Ctrl Pts',(68.1069470529528,67.9329243833025,48.8527901882348));
#35680=CARTESIAN_POINT('Ctrl Pts',(67.5179852826105,68.0390023880786,50.0818508931169));
#35681=CARTESIAN_POINT('Ctrl Pts',(67.2427484732325,68.1450803928548,51.3775539192241));
#35682=CARTESIAN_POINT('Ctrl Pts',(66.9675116638546,68.2511583976309,52.6732569453312));
#35683=CARTESIAN_POINT('Ctrl Pts',(67.0059998154409,68.3572364024071,54.0356022926634));
#35684=CARTESIAN_POINT('Ctrl Pts',(67.3851473064755,68.4633144071832,55.2952561761957));
#35685=CARTESIAN_POINT('Ctrl Pts',(68.1434422885447,68.6754704167355,57.8145639432602));
#35686=CARTESIAN_POINT('Ctrl Pts',(70.2643746284068,68.8876264262879,59.9231058551253));
#35687=CARTESIAN_POINT('Ctrl Pts',(72.7887653822357,69.0997824358402,60.6510564397939));
#35688=CARTESIAN_POINT('Ctrl Pts',(75.3131561360648,69.3119384453925,61.3790070244627));
#35689=CARTESIAN_POINT('Ctrl Pts',(78.241005303861,69.5240944549449,60.7263662819347));
#35690=CARTESIAN_POINT('Ctrl Pts',(80.2192776127132,69.7362504644972,58.9942109234851));
#35691=CARTESIAN_POINT('Ctrl Pts',(81.9041781653871,69.916944384211,57.5189289273164));
#35692=CARTESIAN_POINT('Ctrl Pts',(82.9002574879822,70.0976383039249,55.2605691016666));
#35693=CARTESIAN_POINT('Ctrl Pts',(82.9187125221374,70.2783322236387,53.0168399279172));
#35694=CARTESIAN_POINT('Ctrl Pts',(82.9129498948689,71.7216677763616,53.0228109606374));
#35695=CARTESIAN_POINT('Ctrl Pts',(82.9129498948684,71.5445712043629,55.2274084205471));
#35696=CARTESIAN_POINT('Ctrl Pts',(81.9432795991098,71.3674746323641,57.414765384983));
#35697=CARTESIAN_POINT('Ctrl Pts',(80.3096882702532,71.1903780603654,58.8951806410935));
#35698=CARTESIAN_POINT('Ctrl Pts',(78.6760969413967,71.0132814883667,60.3755958972041));
#35699=CARTESIAN_POINT('Ctrl Pts',(76.4041347530435,70.836184916368,61.1259150206682));
#35700=CARTESIAN_POINT('Ctrl Pts',(74.2101800112211,70.6590883443693,60.909552937402));
#35701=CARTESIAN_POINT('Ctrl Pts',(72.0162252693987,70.4819917723705,60.6931908541359));
#35702=CARTESIAN_POINT('Ctrl Pts',(69.9345925076975,70.3048952003718,59.5135315737694));
#35703=CARTESIAN_POINT('Ctrl Pts',(68.6216467656605,70.1277986283731,57.7425365317923));
#35704=CARTESIAN_POINT('Ctrl Pts',(67.3087010236235,69.9507020563743,55.9715414898153));
#35705=CARTESIAN_POINT('Ctrl Pts',(66.7849774198239,69.7736054843757,53.6369099216303));
#35706=CARTESIAN_POINT('Ctrl Pts',(67.2156126057606,69.5965089123769,51.4747805783963));
#35707=CARTESIAN_POINT('Ctrl Pts',(67.6462477916972,69.4194123403782,49.3126512351623));
#35708=CARTESIAN_POINT('Ctrl Pts',(69.0245064207964,69.2423157683795,47.3568408855485));
#35709=CARTESIAN_POINT('Ctrl Pts',(70.915806180446,69.0652191963807,46.2240411771316));
#35710=CARTESIAN_POINT('Ctrl Pts',(72.8071059400957,68.888122624382,45.0912414687147));
#35711=CARTESIAN_POINT('Ctrl Pts',(75.1818659698091,68.7110260523833,44.7991699473058));
#35712=CARTESIAN_POINT('Ctrl Pts',(77.2912945088656,68.5339294803846,45.4399204438753));
#35713=CARTESIAN_POINT('Ctrl Pts',(79.4007230479221,68.3568329083859,46.0806709404449));
#35714=CARTESIAN_POINT('Ctrl Pts',(81.2118275942067,68.1797363363871,47.6442218013926));
#35715=CARTESIAN_POINT('Ctrl Pts',(82.1535440633093,68.0026397643884,49.6375657386149));
#35716=CARTESIAN_POINT('Ctrl Pts',(82.6515697929912,67.9089824350461,50.6917435101773));
#35717=CARTESIAN_POINT('Ctrl Pts',(82.9129498948693,67.8153251057038,51.8569119935396));
#35718=CARTESIAN_POINT('Ctrl Pts',(82.9129498948689,67.7216677763615,53.0228109606381));
#35719=CARTESIAN_POINT('Origin',(74.9879498948689,255.,53.0228109606356));
#35720=CARTESIAN_POINT('',(82.9129498948689,62.2783322236386,53.022810960625));
#35721=CARTESIAN_POINT('',(82.9062487487382,63.7216677763616,53.0219139020423));
#35722=CARTESIAN_POINT('',(82.9129498948689,255.,53.0228109606356));
#35723=CARTESIAN_POINT('Ctrl Pts',(82.9129498948689,62.2783322236386,53.022810960625));
#35724=CARTESIAN_POINT('Ctrl Pts',(82.912949894866,62.4554287956374,50.8182135007154));
#35725=CARTESIAN_POINT('Ctrl Pts',(81.943279599105,62.6325253676361,48.6308565362805));
#35726=CARTESIAN_POINT('Ctrl Pts',(80.3096882702468,62.8096219396348,47.1504412801718));
#35727=CARTESIAN_POINT('Ctrl Pts',(78.6760969413886,62.9867185116335,45.670026024063));
#35728=CARTESIAN_POINT('Ctrl Pts',(76.4041347530346,63.1638150836322,44.9197069006014));
#35729=CARTESIAN_POINT('Ctrl Pts',(74.2101800112124,63.3409116556309,45.1360689838699));
#35730=CARTESIAN_POINT('Ctrl Pts',(72.0162252693903,63.5180082276297,45.3524310671385));
#35731=CARTESIAN_POINT('Ctrl Pts',(69.9345925076903,63.6951047996283,46.5320903475073));
#35732=CARTESIAN_POINT('Ctrl Pts',(68.6216467656553,63.8722013716271,48.3030853894858));
#35733=CARTESIAN_POINT('Ctrl Pts',(67.3087010236203,64.0492979436258,50.0740804314643));
#35734=CARTESIAN_POINT('Ctrl Pts',(66.7849774198233,64.2263945156245,52.4087119996498));
#35735=CARTESIAN_POINT('Ctrl Pts',(67.2156126057623,64.4034910876233,54.5708413428834));
#35736=CARTESIAN_POINT('Ctrl Pts',(67.6462477917012,64.580587659622,56.7329706861169));
#35737=CARTESIAN_POINT('Ctrl Pts',(69.0245064208026,64.7576842316207,58.6887810357291));
#35738=CARTESIAN_POINT('Ctrl Pts',(70.9158061804535,64.9347808036194,59.821580744144));
#35739=CARTESIAN_POINT('Ctrl Pts',(72.8071059401044,65.1118773756181,60.9543804525588));
#35740=CARTESIAN_POINT('Ctrl Pts',(75.1818659698181,65.2889739476169,61.2464519739652));
#35741=CARTESIAN_POINT('Ctrl Pts',(77.2912945088739,65.4660705196156,60.6057014773933));
#35742=CARTESIAN_POINT('Ctrl Pts',(79.4007230479297,65.6431670916143,59.9649509808214));
#35743=CARTESIAN_POINT('Ctrl Pts',(81.2118275942126,65.820263663613,58.4014001198717));
#35744=CARTESIAN_POINT('Ctrl Pts',(82.153544063313,65.9973602356117,56.4080561826484));
#35745=CARTESIAN_POINT('Ctrl Pts',(82.6515697929936,66.091017564954,55.3538784110857));
#35746=CARTESIAN_POINT('Ctrl Pts',(82.9129498948704,66.1846748942963,54.1887099277235));
#35747=CARTESIAN_POINT('Ctrl Pts',(82.9129498948689,66.2783322236386,53.0228109606252));
#35748=CARTESIAN_POINT('Ctrl Pts',(82.9166465239286,67.7216677763615,53.0178513738214));
#35749=CARTESIAN_POINT('Ctrl Pts',(82.9116093512061,67.6590299543487,53.7969963792745));
#35750=CARTESIAN_POINT('Ctrl Pts',(82.7910644468045,67.596392132336,54.5778695919009));
#35751=CARTESIAN_POINT('Ctrl Pts',(82.5635267122257,67.5337543103233,55.3262109863277));
#35752=CARTESIAN_POINT('Ctrl Pts',(82.1781884593963,67.4276763055471,56.593537331042));
#35753=CARTESIAN_POINT('Ctrl Pts',(81.4859960123467,67.321598300771,57.7675627990191));
#35754=CARTESIAN_POINT('Ctrl Pts',(80.5452190389621,67.2155202959948,58.6870297166436));
#35755=CARTESIAN_POINT('Ctrl Pts',(78.6636650921934,67.0033642864425,60.5259635518921));
#35756=CARTESIAN_POINT('Ctrl Pts',(75.7877730400849,66.7912082768902,61.3466631857312));
#35757=CARTESIAN_POINT('Ctrl Pts',(73.2260023948809,66.5790522673379,60.7637464737497));
#35758=CARTESIAN_POINT('Ctrl Pts',(70.6642317496769,66.3668962577856,60.1808297617682));
#35759=CARTESIAN_POINT('Ctrl Pts',(68.4165825113773,66.1547402482333,58.194296703966));
#35760=CARTESIAN_POINT('Ctrl Pts',(67.5220058998071,65.942584238681,55.7217158256514));
#35761=CARTESIAN_POINT('Ctrl Pts',(66.6274292882369,65.7304282291287,53.2491349473366));
#35762=CARTESIAN_POINT('Ctrl Pts',(67.0859253033961,65.5182722195764,50.2905062485098));
#35763=CARTESIAN_POINT('Ctrl Pts',(68.6826220783526,65.3061162100241,48.2020864386379));
#35764=CARTESIAN_POINT('Ctrl Pts',(70.279318853309,65.0939602004718,46.113666628766));
#35765=CARTESIAN_POINT('Ctrl Pts',(73.0142163880631,64.8818041909194,44.8954557078497));
#35766=CARTESIAN_POINT('Ctrl Pts',(75.634848720819,64.6696481813671,45.1104201009277));
#35767=CARTESIAN_POINT('Ctrl Pts',(78.2554810535745,64.4574921718148,45.3253844940057));
#35768=CARTESIAN_POINT('Ctrl Pts',(80.7618481843323,64.2453361622624,46.9735242010776));
#35769=CARTESIAN_POINT('Ctrl Pts',(81.9960700343584,64.0331801527101,49.2928252071254));
#35770=CARTESIAN_POINT('Ctrl Pts',(82.6001465380191,63.9293426939273,50.4279819397991));
#35771=CARTESIAN_POINT('Ctrl Pts',(82.8994797620802,63.8255052351444,51.723915824649));
#35772=CARTESIAN_POINT('Ctrl Pts',(82.8974486171957,63.7216677763616,53.0207358597371));
#35773=CARTESIAN_POINT('Origin',(74.9879498948689,255.,53.0228109606356));
#35774=CARTESIAN_POINT('',(82.9163763150487,58.2783322236387,53.0223520988813));
#35775=CARTESIAN_POINT('',(82.9129498948689,59.7216677763615,53.0228109606378));
#35776=CARTESIAN_POINT('',(82.9129498948689,255.,53.0228109606356));
#35777=CARTESIAN_POINT('Ctrl Pts',(82.9129498948689,58.2783322236386,53.0228109606249));
#35778=CARTESIAN_POINT('Ctrl Pts',(82.9129498948659,58.4554287956374,50.8182135007149));
#35779=CARTESIAN_POINT('Ctrl Pts',(81.9432795991046,58.6325253676362,48.6308565362798));
#35780=CARTESIAN_POINT('Ctrl Pts',(80.309688270246,58.8096219396349,47.1504412801711));
#35781=CARTESIAN_POINT('Ctrl Pts',(78.6760969413874,58.9867185116336,45.6700260240623));
#35782=CARTESIAN_POINT('Ctrl Pts',(76.4041347530328,59.1638150836324,44.919706900601));
#35783=CARTESIAN_POINT('Ctrl Pts',(74.2101800112104,59.3409116556311,45.1360689838701));
#35784=CARTESIAN_POINT('Ctrl Pts',(72.0162252693881,59.5180082276298,45.3524310671393));
#35785=CARTESIAN_POINT('Ctrl Pts',(69.9345925076882,59.6951047996286,46.5320903475089));
#35786=CARTESIAN_POINT('Ctrl Pts',(68.6216467656536,59.8722013716274,48.3030853894881));
#35787=CARTESIAN_POINT('Ctrl Pts',(67.308701023619,60.0492979436261,50.0740804314673));
#35788=CARTESIAN_POINT('Ctrl Pts',(66.7849774198229,60.2263945156248,52.4087119996534));
#35789=CARTESIAN_POINT('Ctrl Pts',(67.215612605763,60.4034910876236,54.5708413428871));
#35790=CARTESIAN_POINT('Ctrl Pts',(67.6462477917031,60.5805876596223,56.7329706861207));
#35791=CARTESIAN_POINT('Ctrl Pts',(69.0245064208057,60.7576842316211,58.6887810357325));
#35792=CARTESIAN_POINT('Ctrl Pts',(70.9158061804575,60.9347808036198,59.8215807441464));
#35793=CARTESIAN_POINT('Ctrl Pts',(72.8071059401093,61.1118773756186,60.9543804525602));
#35794=CARTESIAN_POINT('Ctrl Pts',(75.1818659698236,61.2889739476173,61.2464519739651));
#35795=CARTESIAN_POINT('Ctrl Pts',(77.2912945088793,61.466070519616,60.6057014773917));
#35796=CARTESIAN_POINT('Ctrl Pts',(79.4007230479349,61.6431670916148,59.9649509808182));
#35797=CARTESIAN_POINT('Ctrl Pts',(81.2118275942168,61.8202636636135,58.4014001198669));
#35798=CARTESIAN_POINT('Ctrl Pts',(82.1535440633157,61.9973602356122,56.4080561826425));
#35799=CARTESIAN_POINT('Ctrl Pts',(82.6515697929946,62.0910175649543,55.3538784110813));
#35800=CARTESIAN_POINT('Ctrl Pts',(82.9129498948705,62.1846748942965,54.1887099277212));
#35801=CARTESIAN_POINT('Ctrl Pts',(82.9129498948689,62.2783322236386,53.022810960625));
#35802=CARTESIAN_POINT('Ctrl Pts',(82.9129498948689,63.7216677763616,53.0228109606371));
#35803=CARTESIAN_POINT('Ctrl Pts',(82.9129498948685,63.5445712043629,55.2274084205467));
#35804=CARTESIAN_POINT('Ctrl Pts',(81.94327959911,63.3674746323641,57.4147653849827));
#35805=CARTESIAN_POINT('Ctrl Pts',(80.3096882702535,63.1903780603654,58.8951806410933));
#35806=CARTESIAN_POINT('Ctrl Pts',(78.676096941397,63.0132814883667,60.3755958972039));
#35807=CARTESIAN_POINT('Ctrl Pts',(76.4041347530438,62.836184916368,61.1259150206681));
#35808=CARTESIAN_POINT('Ctrl Pts',(74.2101800112214,62.6590883443693,60.9095529374021));
#35809=CARTESIAN_POINT('Ctrl Pts',(72.016225269399,62.4819917723706,60.693190854136));
#35810=CARTESIAN_POINT('Ctrl Pts',(69.9345925076977,62.3048952003718,59.5135315737696));
#35811=CARTESIAN_POINT('Ctrl Pts',(68.6216467656607,62.1277986283731,57.7425365317926));
#35812=CARTESIAN_POINT('Ctrl Pts',(67.3087010236236,61.9507020563744,55.9715414898156));
#35813=CARTESIAN_POINT('Ctrl Pts',(66.784977419824,61.7736054843757,53.6369099216307));
#35814=CARTESIAN_POINT('Ctrl Pts',(67.2156126057605,61.596508912377,51.4747805783966));
#35815=CARTESIAN_POINT('Ctrl Pts',(67.646247791697,61.4194123403782,49.3126512351626));
#35816=CARTESIAN_POINT('Ctrl Pts',(69.0245064207961,61.2423157683795,47.3568408855488));
#35817=CARTESIAN_POINT('Ctrl Pts',(70.9158061804457,61.0652191963808,46.2240411771318));
#35818=CARTESIAN_POINT('Ctrl Pts',(72.8071059400953,60.888122624382,45.0912414687148));
#35819=CARTESIAN_POINT('Ctrl Pts',(75.1818659698088,60.7110260523834,44.7991699473058));
#35820=CARTESIAN_POINT('Ctrl Pts',(77.2912945088653,60.5339294803846,45.4399204438752));
#35821=CARTESIAN_POINT('Ctrl Pts',(79.4007230479218,60.3568329083859,46.0806709404447));
#35822=CARTESIAN_POINT('Ctrl Pts',(81.2118275942064,60.1797363363872,47.6442218013923));
#35823=CARTESIAN_POINT('Ctrl Pts',(82.1535440633091,60.0026397643884,49.6375657386146));
#35824=CARTESIAN_POINT('Ctrl Pts',(82.651569792991,59.9089824350462,50.6917435101767));
#35825=CARTESIAN_POINT('Ctrl Pts',(82.9129498948691,59.8153251057039,51.8569119935386));
#35826=CARTESIAN_POINT('Ctrl Pts',(82.9129498948689,59.7216677763616,53.0228109606369));
#35827=CARTESIAN_POINT('Origin',(74.9879498948689,255.,53.0228109606356));
#35828=CARTESIAN_POINT('',(82.9104010142055,54.2783322236387,53.0210824732343));
#35829=CARTESIAN_POINT('',(82.9171842364519,55.7216677763613,53.0215139011292));
#35830=CARTESIAN_POINT('',(82.9129498948689,255.,53.0228109606356));
#35831=CARTESIAN_POINT('Ctrl Pts',(82.904538510375,54.2783322236387,53.0171068991978));
#35832=CARTESIAN_POINT('Ctrl Pts',(82.9106802894969,54.3392274080026,52.2581622407597));
#35833=CARTESIAN_POINT('Ctrl Pts',(82.8107733365512,54.4001225923666,51.5005576736762));
#35834=CARTESIAN_POINT('Ctrl Pts',(82.5983352092591,54.4610177767305,50.7758908858849));
#35835=CARTESIAN_POINT('Ctrl Pts',(82.2282728978152,54.5670957815067,49.5135380778694));
#35836=CARTESIAN_POINT('Ctrl Pts',(81.5167365904301,54.6731737862828,48.351134418858));
#35837=CARTESIAN_POINT('Ctrl Pts',(80.5787412531064,54.779251791059,47.4158449555051));
#35838=CARTESIAN_POINT('Ctrl Pts',(79.6407459157828,54.8853297958351,46.4805554921522));
#35839=CARTESIAN_POINT('Ctrl Pts',(78.4762915485206,54.9914078006112,45.7723802244579));
#35840=CARTESIAN_POINT('Ctrl Pts',(77.2128749343213,55.0974858053874,45.4059662710925));
#35841=CARTESIAN_POINT('Ctrl Pts',(74.6860417059226,55.3096418149397,44.6731383643616));
#35842=CARTESIAN_POINT('Ctrl Pts',(71.7633594897756,55.5217978244921,45.3073557149463));
#35843=CARTESIAN_POINT('Ctrl Pts',(69.780233864638,55.7339538340444,47.0306297751755));
#35844=CARTESIAN_POINT('Ctrl Pts',(67.7971082395001,55.9461098435967,48.7539038354048));
#35845=CARTESIAN_POINT('Ctrl Pts',(66.7535392053719,56.158265853149,51.5662346052788));
#35846=CARTESIAN_POINT('Ctrl Pts',(67.1322283071543,56.3704218627014,54.1682565263949));
#35847=CARTESIAN_POINT('Ctrl Pts',(67.5109174089366,56.5825778722537,56.7702784475106));
#35848=CARTESIAN_POINT('Ctrl Pts',(69.3118646466293,56.794733881806,59.1619915198684));
#35849=CARTESIAN_POINT('Ctrl Pts',(71.7053648627521,57.0068898913583,60.2492332633831));
#35850=CARTESIAN_POINT('Ctrl Pts',(74.0988650788749,57.2190459009106,61.3364750068978));
#35851=CARTESIAN_POINT('Ctrl Pts',(77.0849182734277,57.4312019104629,61.1192454215695));
#35852=CARTESIAN_POINT('Ctrl Pts',(79.2936426408122,57.6433579200152,59.6925498749662));
#35853=CARTESIAN_POINT('Ctrl Pts',(81.4971833591665,57.855016021223,58.2692026361445));
#35854=CARTESIAN_POINT('Ctrl Pts',(82.9270395905761,58.0666741224308,55.6420597589509));
#35855=CARTESIAN_POINT('Ctrl Pts',(82.9268744173332,58.2783322236386,53.0209462066481));
#35856=CARTESIAN_POINT('Ctrl Pts',(82.9129498948689,59.7216677763616,53.0228109606369));
#35857=CARTESIAN_POINT('Ctrl Pts',(82.9129498948685,59.5445712043628,55.2274084205472));
#35858=CARTESIAN_POINT('Ctrl Pts',(81.9432795991095,59.367474632364,57.4147653849837));
#35859=CARTESIAN_POINT('Ctrl Pts',(80.3096882702523,59.1903780603653,58.8951806410944));
#35860=CARTESIAN_POINT('Ctrl Pts',(78.676096941395,59.0132814883665,60.3755958972051));
#35861=CARTESIAN_POINT('Ctrl Pts',(76.4041347530409,58.8361849163678,61.1259150206688));
#35862=CARTESIAN_POINT('Ctrl Pts',(74.210180011218,58.659088344369,60.9095529374017));
#35863=CARTESIAN_POINT('Ctrl Pts',(72.0162252693951,58.4819917723702,60.6931908541347));
#35864=CARTESIAN_POINT('Ctrl Pts',(69.9345925076938,58.3048952003714,59.5135315737667));
#35865=CARTESIAN_POINT('Ctrl Pts',(68.6216467656576,58.1277986283727,57.7425365317884));
#35866=CARTESIAN_POINT('Ctrl Pts',(67.3087010236213,57.9507020563739,55.9715414898101));
#35867=CARTESIAN_POINT('Ctrl Pts',(66.7849774198233,57.7736054843752,53.636909921624));
#35868=CARTESIAN_POINT('Ctrl Pts',(67.2156126057619,57.5965089123764,51.4747805783897));
#35869=CARTESIAN_POINT('Ctrl Pts',(67.6462477917004,57.4194123403776,49.3126512351555));
#35870=CARTESIAN_POINT('Ctrl Pts',(69.0245064208019,57.2423157683788,47.3568408855424));
#35871=CARTESIAN_POINT('Ctrl Pts',(70.9158061804533,57.0652191963801,46.2240411771273));
#35872=CARTESIAN_POINT('Ctrl Pts',(72.8071059401047,56.8881226243813,45.0912414687121));
#35873=CARTESIAN_POINT('Ctrl Pts',(75.1818659698192,56.7110260523826,44.7991699473058));
#35874=CARTESIAN_POINT('Ctrl Pts',(77.2912945088755,56.5339294803838,45.4399204438783));
#35875=CARTESIAN_POINT('Ctrl Pts',(79.4007230479317,56.356832908385,46.0806709404508));
#35876=CARTESIAN_POINT('Ctrl Pts',(81.2118275942146,56.1797363363862,47.6442218014015));
#35877=CARTESIAN_POINT('Ctrl Pts',(82.1535440633144,56.0026397643875,49.6375657386259));
#35878=CARTESIAN_POINT('Ctrl Pts',(82.6515697929931,55.9089824350455,50.6917435101855));
#35879=CARTESIAN_POINT('Ctrl Pts',(82.9129498948693,55.8153251057034,51.8569119935439));
#35880=CARTESIAN_POINT('Ctrl Pts',(82.9129498948689,55.7216677763614,53.0228109606385));
#35881=CARTESIAN_POINT('Origin',(74.9879498948689,255.,53.0228109606356));
#35882=CARTESIAN_POINT('',(82.9117139092691,50.2783322236387,53.0232455636512));
#35883=CARTESIAN_POINT('',(82.9045864038165,51.7216677763616,53.0169664367311));
#35884=CARTESIAN_POINT('',(82.9129498948689,255.,53.0228109606356));
#35885=CARTESIAN_POINT('Ctrl Pts',(82.9129498948689,50.2783322236387,53.0228109606245));
#35886=CARTESIAN_POINT('Ctrl Pts',(82.9129498948658,50.4554287956374,50.8182135007149));
#35887=CARTESIAN_POINT('Ctrl Pts',(81.9432795991047,50.6325253676361,48.6308565362801));
#35888=CARTESIAN_POINT('Ctrl Pts',(80.3096882702464,50.8096219396349,47.1504412801714));
#35889=CARTESIAN_POINT('Ctrl Pts',(78.6760969413881,50.9867185116336,45.6700260240628));
#35890=CARTESIAN_POINT('Ctrl Pts',(76.404134753034,51.1638150836323,44.9197069006013));
#35891=CARTESIAN_POINT('Ctrl Pts',(74.2101800112119,51.340911655631,45.13606898387));
#35892=CARTESIAN_POINT('Ctrl Pts',(72.0162252693898,51.5180082276297,45.3524310671387));
#35893=CARTESIAN_POINT('Ctrl Pts',(69.9345925076899,51.6951047996284,46.5320903475076));
#35894=CARTESIAN_POINT('Ctrl Pts',(68.621646765655,51.8722013716271,48.3030853894862));
#35895=CARTESIAN_POINT('Ctrl Pts',(67.3087010236201,52.0492979436258,50.0740804314648));
#35896=CARTESIAN_POINT('Ctrl Pts',(66.7849774198232,52.2263945156246,52.4087119996504));
#35897=CARTESIAN_POINT('Ctrl Pts',(67.2156126057624,52.4034910876233,54.5708413428839));
#35898=CARTESIAN_POINT('Ctrl Pts',(67.6462477917015,52.580587659622,56.7329706861174));
#35899=CARTESIAN_POINT('Ctrl Pts',(69.024506420803,52.7576842316207,58.6887810357295));
#35900=CARTESIAN_POINT('Ctrl Pts',(70.9158061804539,52.9347808036194,59.8215807441442));
#35901=CARTESIAN_POINT('Ctrl Pts',(72.8071059401049,53.1118773756182,60.9543804525589));
#35902=CARTESIAN_POINT('Ctrl Pts',(75.1818659698187,53.2889739476169,61.2464519739651));
#35903=CARTESIAN_POINT('Ctrl Pts',(77.2912945088744,53.4660705196156,60.6057014773931));
#35904=CARTESIAN_POINT('Ctrl Pts',(79.4007230479302,53.6431670916144,59.9649509808211));
#35905=CARTESIAN_POINT('Ctrl Pts',(81.2118275942129,53.820263663613,58.4014001198713));
#35906=CARTESIAN_POINT('Ctrl Pts',(82.1535440633132,53.9973602356118,56.4080561826479));
#35907=CARTESIAN_POINT('Ctrl Pts',(82.6515697929938,54.091017564954,55.3538784110852));
#35908=CARTESIAN_POINT('Ctrl Pts',(82.9129498948705,54.1846748942964,54.188709927723));
#35909=CARTESIAN_POINT('Ctrl Pts',(82.9129498948689,54.2783322236387,53.0228109606247));
#35910=CARTESIAN_POINT('Ctrl Pts',(82.9253894869644,55.7216677763615,53.01900047654));
#35911=CARTESIAN_POINT('Ctrl Pts',(82.9135514667677,55.5219877680786,55.495166293122));
#35912=CARTESIAN_POINT('Ctrl Pts',(81.661333110683,55.3223077597958,57.983619928366));
#35913=CARTESIAN_POINT('Ctrl Pts',(79.6626107189349,55.1226277515129,59.4395147710704));
#35914=CARTESIAN_POINT('Ctrl Pts',(77.5390082086855,54.9104717419606,60.9863738823661));
#35915=CARTESIAN_POINT('Ctrl Pts',(74.5727043979174,54.6983157324083,61.3676148646698));
#35916=CARTESIAN_POINT('Ctrl Pts',(72.1180247786696,54.486159722856,60.420793407439));
#35917=CARTESIAN_POINT('Ctrl Pts',(70.8906849690454,54.3800817180798,59.9473826788236));
#35918=CARTESIAN_POINT('Ctrl Pts',(69.7912512073013,54.2740037133036,59.1419563403243));
#35919=CARTESIAN_POINT('Ctrl Pts',(68.9369188167712,54.1679257085274,58.1296728822003));
#35920=CARTESIAN_POINT('Ctrl Pts',(68.0825864262412,54.0618477037513,57.1173894240764));
#35921=CARTESIAN_POINT('Ctrl Pts',(67.473355406925,53.9557696989751,55.8982488463278));
#35922=CARTESIAN_POINT('Ctrl Pts',(67.2129117490884,53.849691694199,54.6088110512604));
#35923=CARTESIAN_POINT('Ctrl Pts',(66.6920244334152,53.6375356846467,52.0299354611254));
#35924=CARTESIAN_POINT('Ctrl Pts',(67.5662865636604,53.4253796750944,49.1698710017148));
#35925=CARTESIAN_POINT('Ctrl Pts',(69.4479899286966,53.2132236655421,47.3363898379861));
#35926=CARTESIAN_POINT('Ctrl Pts',(71.3296932937327,53.0010676559898,45.5029086742575));
#35927=CARTESIAN_POINT('Ctrl Pts',(74.2188378935599,52.7889116464374,44.6960108062107));
#35928=CARTESIAN_POINT('Ctrl Pts',(76.7805229565297,52.5767556368851,45.2890480326417));
#35929=CARTESIAN_POINT('Ctrl Pts',(79.3422080194998,52.3645996273328,45.8820852590727));
#35930=CARTESIAN_POINT('Ctrl Pts',(81.5764335456124,52.1524436177805,47.8750575799819));
#35931=CARTESIAN_POINT('Ctrl Pts',(82.4615658042492,51.9402876082282,50.3504320522876));
#35932=CARTESIAN_POINT('Ctrl Pts',(82.7655990892693,51.8674143309393,51.2006962078717));
#35933=CARTESIAN_POINT('Ctrl Pts',(82.9104599242351,51.7945410536505,52.1078764671829));
#35934=CARTESIAN_POINT('Ctrl Pts',(82.9045864038165,51.7216677763616,53.0169664367311));
#35935=CARTESIAN_POINT('Origin',(74.9879498948689,255.,53.0228109606356));
#35936=CARTESIAN_POINT('',(82.9132360241053,46.278332223639,53.0234054380586));
#35937=CARTESIAN_POINT('',(82.9030927965636,47.7216677763615,53.0278642989338));
#35938=CARTESIAN_POINT('',(82.9129498948689,255.,53.0228109606356));
#35939=CARTESIAN_POINT('Ctrl Pts',(82.9156681820723,46.2783322236388,53.0284586201259));
#35940=CARTESIAN_POINT('Ctrl Pts',(82.8956280895017,46.4600219600416,50.7712696112924));
#35941=CARTESIAN_POINT('Ctrl Pts',(81.8908844774418,46.6417116964444,48.5021875442689));
#35942=CARTESIAN_POINT('Ctrl Pts',(80.1917817852738,46.8234014328472,47.0272563351391));
#35943=CARTESIAN_POINT('Ctrl Pts',(78.2077685210858,47.0355574423995,45.3050042922422));
#35944=CARTESIAN_POINT('Ctrl Pts',(75.2770081084107,47.2477134519518,44.6655638402333));
#35945=CARTESIAN_POINT('Ctrl Pts',(72.7536601184849,47.4598694615041,45.4049138490338));
#35946=CARTESIAN_POINT('Ctrl Pts',(70.2303121285595,47.6720254710564,46.1442638578342));
#35947=CARTESIAN_POINT('Ctrl Pts',(68.1143765613833,47.8841814806087,48.2624043274435));
#35948=CARTESIAN_POINT('Ctrl Pts',(67.3730398495798,48.0963374901609,50.784577551699));
#35949=CARTESIAN_POINT('Ctrl Pts',(66.631703137776,48.3084934997133,53.3067507759554));
#35950=CARTESIAN_POINT('Ctrl Pts',(67.264965281346,48.5206495092656,56.2329567548582));
#35951=CARTESIAN_POINT('Ctrl Pts',(68.9869159785598,48.732805518818,58.2201178731734));
#35952=CARTESIAN_POINT('Ctrl Pts',(70.7088666757733,48.9449615283703,60.2072789914881));
#35953=CARTESIAN_POINT('Ctrl Pts',(73.5195059266301,49.1571175379227,61.2553952492156));
#35954=CARTESIAN_POINT('Ctrl Pts',(76.119892113975,49.369273547475,60.8806254419981));
#35955=CARTESIAN_POINT('Ctrl Pts',(78.72027830132,49.5814295570273,60.5058556347807));
#35956=CARTESIAN_POINT('Ctrl Pts',(81.1104114251532,49.7935855665796,58.7081997626184));
#35957=CARTESIAN_POINT('Ctrl Pts',(82.2071389034964,50.0057415761319,56.3167333206063));
#35958=CARTESIAN_POINT('Ctrl Pts',(82.6768524476174,50.0966051253008,55.2925005915961));
#35959=CARTESIAN_POINT('Ctrl Pts',(82.9093174951633,50.1874686744697,54.1593456034027));
#35960=CARTESIAN_POINT('Ctrl Pts',(82.9067025264445,50.2783322236387,53.0250076894748));
#35961=CARTESIAN_POINT('Ctrl Pts',(82.9045864038165,51.7216677763616,53.0169664367311));
#35962=CARTESIAN_POINT('Ctrl Pts',(82.8933603412276,51.5823850440982,54.7545105618576));
#35963=CARTESIAN_POINT('Ctrl Pts',(82.3314911796438,51.4431023118347,56.4990309914926));
#35964=CARTESIAN_POINT('Ctrl Pts',(81.2778946571288,51.3038195795713,57.8664668211942));
#35965=CARTESIAN_POINT('Ctrl Pts',(79.6730522602106,51.0916635700189,59.9493504940937));
#35966=CARTESIAN_POINT('Ctrl Pts',(76.9273284752132,50.8795075604666,61.1573412161903));
#35967=CARTESIAN_POINT('Ctrl Pts',(74.3096956074956,50.6673515509142,60.9327106270388));
#35968=CARTESIAN_POINT('Ctrl Pts',(71.6920627397786,50.4551955413619,60.7080800378874));
#35969=CARTESIAN_POINT('Ctrl Pts',(69.2025207893409,50.2430395318095,59.050828137488));
#35970=CARTESIAN_POINT('Ctrl Pts',(67.9701012205266,50.0308835222573,56.7263787593717));
#35971=CARTESIAN_POINT('Ctrl Pts',(67.3538914361195,49.9248055174811,55.5641540703134));
#35972=CARTESIAN_POINT('Ctrl Pts',(67.0519622471181,49.818727512705,54.2351300118258));
#35973=CARTESIAN_POINT('Ctrl Pts',(67.0707259166118,49.7126495079289,52.9106491483147));
#35974=CARTESIAN_POINT('Ctrl Pts',(67.0894895861055,49.6065715031527,51.5861682848033));
#35975=CARTESIAN_POINT('Ctrl Pts',(67.4289461140944,49.5004934983765,50.2662306162687));
#35976=CARTESIAN_POINT('Ctrl Pts',(68.0778320296788,49.3944154936003,49.1219282983418));
#35977=CARTESIAN_POINT('Ctrl Pts',(69.3756038608473,49.182259484048,46.8333236624885));
#35978=CARTESIAN_POINT('Ctrl Pts',(71.9110932423966,48.9701034744957,45.2472604290661));
#35979=CARTESIAN_POINT('Ctrl Pts',(74.5340389317533,48.7579474649434,45.0968721235974));
#35980=CARTESIAN_POINT('Ctrl Pts',(77.1569846211103,48.5457914553911,44.9464838181288));
#35981=CARTESIAN_POINT('Ctrl Pts',(79.8673866182743,48.3336354458388,46.2317704406142));
#35982=CARTESIAN_POINT('Ctrl Pts',(81.4125811705769,48.1214794362864,48.3592800902543));
#35983=CARTESIAN_POINT('Ctrl Pts',(82.3832297672811,47.9882088829781,49.6957229691272));
#35984=CARTESIAN_POINT('Ctrl Pts',(82.8940868239913,47.8549383296698,51.3645075476531));
#35985=CARTESIAN_POINT('Ctrl Pts',(82.9030927965636,47.7216677763615,53.0278642989338));
#35986=CARTESIAN_POINT('Origin',(74.9879498948689,255.,53.0228109606356));
#35987=CARTESIAN_POINT('',(82.9147244314983,42.2783322236387,53.0216046455403));
#35988=CARTESIAN_POINT('',(82.9169881471838,43.7216677763615,53.0246207943705));
#35989=CARTESIAN_POINT('',(82.9129498948689,255.,53.0228109606356));
#35990=CARTESIAN_POINT('Ctrl Pts',(82.9129498948689,42.2783322236387,53.0228109606242));
#35991=CARTESIAN_POINT('Ctrl Pts',(82.9129498948657,42.4554287956375,50.8182135007139));
#35992=CARTESIAN_POINT('Ctrl Pts',(81.9432795991039,42.6325253676363,48.6308565362786));
#35993=CARTESIAN_POINT('Ctrl Pts',(80.3096882702448,42.809621939635,47.15044128017));
#35994=CARTESIAN_POINT('Ctrl Pts',(78.6760969413857,42.9867185116338,45.6700260240614));
#35995=CARTESIAN_POINT('Ctrl Pts',(76.4041347530306,43.1638150836325,44.9197069006005));
#35996=CARTESIAN_POINT('Ctrl Pts',(74.210180011208,43.3409116556313,45.1360689838704));
#35997=CARTESIAN_POINT('Ctrl Pts',(72.0162252693853,43.5180082276301,45.3524310671402));
#35998=CARTESIAN_POINT('Ctrl Pts',(69.9345925076856,43.6951047996289,46.5320903475108));
#35999=CARTESIAN_POINT('Ctrl Pts',(68.6216467656516,43.8722013716276,48.3030853894908));
#36000=CARTESIAN_POINT('Ctrl Pts',(67.3087010236176,44.0492979436264,50.0740804314708));
#36001=CARTESIAN_POINT('Ctrl Pts',(66.7849774198225,44.2263945156251,52.4087119996576));
#36002=CARTESIAN_POINT('Ctrl Pts',(67.2156126057638,44.4034910876239,54.5708413428913));
#36003=CARTESIAN_POINT('Ctrl Pts',(67.6462477917051,44.5805876596227,56.732970686125));
#36004=CARTESIAN_POINT('Ctrl Pts',(69.0245064208091,44.7576842316215,58.6887810357363));
#36005=CARTESIAN_POINT('Ctrl Pts',(70.9158061804619,44.9347808036202,59.821580744149));
#36006=CARTESIAN_POINT('Ctrl Pts',(72.8071059401148,45.111877375619,60.9543804525618));
#36007=CARTESIAN_POINT('Ctrl Pts',(75.1818659698297,45.2889739476177,61.246451973965));
#36008=CARTESIAN_POINT('Ctrl Pts',(77.2912945088851,45.4660705196165,60.6057014773899));
#36009=CARTESIAN_POINT('Ctrl Pts',(79.4007230479405,45.6431670916153,59.9649509808147));
#36010=CARTESIAN_POINT('Ctrl Pts',(81.2118275942214,45.8202636636141,58.4014001198617));
#36011=CARTESIAN_POINT('Ctrl Pts',(82.1535440633187,45.9973602356128,56.4080561826362));
#36012=CARTESIAN_POINT('Ctrl Pts',(82.6515697929959,46.0910175649548,55.3538784110762));
#36013=CARTESIAN_POINT('Ctrl Pts',(82.9129498948707,46.1846748942968,54.1887099277178));
#36014=CARTESIAN_POINT('Ctrl Pts',(82.9129498948689,46.2783322236388,53.0228109606235));
#36015=CARTESIAN_POINT('Ctrl Pts',(82.9030927965636,47.7216677763615,53.0278642989338));
#36016=CARTESIAN_POINT('Ctrl Pts',(82.9084236084921,47.6427823201175,54.0124378072146));
#36017=CARTESIAN_POINT('Ctrl Pts',(82.7379214356189,47.5638968638735,54.9951095739316));
#36018=CARTESIAN_POINT('Ctrl Pts',(82.3828635408296,47.4850114076295,55.9058295106122));
#36019=CARTESIAN_POINT('Ctrl Pts',(81.4279642513385,47.2728553980772,58.3551366045373));
#36020=CARTESIAN_POINT('Ctrl Pts',(79.1381785649148,47.0606993885249,60.2840181155929));
#36021=CARTESIAN_POINT('Ctrl Pts',(76.5607220279737,46.8485433789726,60.8042500964981));
#36022=CARTESIAN_POINT('Ctrl Pts',(73.9832654910329,46.6363873694202,61.3244820774033));
#36023=CARTESIAN_POINT('Ctrl Pts',(71.1181381035746,46.424231359868,60.4360645281585));
#36024=CARTESIAN_POINT('Ctrl Pts',(69.2891286337702,46.2120753503157,58.550014398628));
#36025=CARTESIAN_POINT('Ctrl Pts',(67.4601191639658,45.9999193407634,56.6639642690976));
#36026=CARTESIAN_POINT('Ctrl Pts',(66.6672276118151,45.787763331211,53.7802815592815));
#36027=CARTESIAN_POINT('Ctrl Pts',(67.2609601088651,45.5756073216587,51.2171965768882));
#36028=CARTESIAN_POINT('Ctrl Pts',(67.5578263573901,45.4695293168826,49.9356540856916));
#36029=CARTESIAN_POINT('Ctrl Pts',(68.2013486182152,45.3634513121065,48.7342610263506));
#36030=CARTESIAN_POINT('Ctrl Pts',(69.0840140518336,45.2573733073303,47.7465852873577));
#36031=CARTESIAN_POINT('Ctrl Pts',(69.9666794854519,45.1512953025541,46.7589095483649));
#36032=CARTESIAN_POINT('Ctrl Pts',(71.0884880918636,45.045217297778,45.9849511297201));
#36033=CARTESIAN_POINT('Ctrl Pts',(72.3287460984796,44.9391392930018,45.5464983919242));
#36034=CARTESIAN_POINT('Ctrl Pts',(74.8092621117119,44.7269832834495,44.6695929163322));
#36035=CARTESIAN_POINT('Ctrl Pts',(77.763575725762,44.5148272738971,45.1347101641362));
#36036=CARTESIAN_POINT('Ctrl Pts',(79.8425066737505,44.3026712643448,46.7411057708388));
#36037=CARTESIAN_POINT('Ctrl Pts',(81.7402707053649,44.109003435017,48.2075132077443));
#36038=CARTESIAN_POINT('Ctrl Pts',(82.9085734707273,43.9153356056892,50.6249542772596));
#36039=CARTESIAN_POINT('Ctrl Pts',(82.9240047689655,43.7216677763615,53.0277654514659));
#36040=CARTESIAN_POINT('Origin',(74.9879498948689,255.,53.0228109606356));
#36041=CARTESIAN_POINT('',(82.9091845765454,38.2783322236387,53.0220737411109));
#36042=CARTESIAN_POINT('',(82.9140883333191,39.7216677763616,53.0196810260503));
#36043=CARTESIAN_POINT('',(82.9129498948689,255.,53.0228109606356));
#36044=CARTESIAN_POINT('Ctrl Pts',(82.9008833462252,38.2783322236387,53.0204484259995));
#36045=CARTESIAN_POINT('Ctrl Pts',(82.9050287911047,38.3686605025281,51.8911974838658));
#36046=CARTESIAN_POINT('Ctrl Pts',(82.6800224357425,38.4589887814175,50.763391042182));
#36047=CARTESIAN_POINT('Ctrl Pts',(82.2178821027084,38.5493170603068,49.7437123836101));
#36048=CARTESIAN_POINT('Ctrl Pts',(81.1324429676421,38.7614730698592,47.3487707563791));
#36049=CARTESIAN_POINT('Ctrl Pts',(78.7388555001831,38.9736290794115,45.5503154722348));
#36050=CARTESIAN_POINT('Ctrl Pts',(76.1377185459513,39.1857850889638,45.1694947286408));
#36051=CARTESIAN_POINT('Ctrl Pts',(73.5365815917197,39.3979410985161,44.7886739850468));
#36052=CARTESIAN_POINT('Ctrl Pts',(70.7278951507152,39.6100971080685,45.8254877820027));
#36053=CARTESIAN_POINT('Ctrl Pts',(69.0014620556514,39.8222531176208,47.8087558632373));
#36054=CARTESIAN_POINT('Ctrl Pts',(67.2750289605875,40.0344091271731,49.7920239444719));
#36055=CARTESIAN_POINT('Ctrl Pts',(66.6308492114644,40.2465651367254,52.7217463099852));
#36056=CARTESIAN_POINT('Ctrl Pts',(67.3660894765719,40.4587211462777,55.2440235517453));
#36057=CARTESIAN_POINT('Ctrl Pts',(68.1013297416796,40.67087715583,57.7663007935056));
#36058=CARTESIAN_POINT('Ctrl Pts',(70.2159900210182,40.8830331653824,59.8811329115127));
#36059=CARTESIAN_POINT('Ctrl Pts',(72.7374779153666,41.0951891749347,60.6321466954601));
#36060=CARTESIAN_POINT('Ctrl Pts',(73.9982218625407,41.2012671797108,61.0076535874338));
#36061=CARTESIAN_POINT('Ctrl Pts',(75.3606727134672,41.3073451844869,61.0422058958927));
#36062=CARTESIAN_POINT('Ctrl Pts',(76.6555752005181,41.4134231892631,60.7632270756768));
#36063=CARTESIAN_POINT('Ctrl Pts',(77.9504776875691,41.5195011940392,60.4842482554609));
#36064=CARTESIAN_POINT('Ctrl Pts',(79.1778318107445,41.6255791988154,59.8917383065703));
#36065=CARTESIAN_POINT('Ctrl Pts',(80.1721053878536,41.7316572035916,59.0304016824108));
#36066=CARTESIAN_POINT('Ctrl Pts',(81.880107999848,41.913882210274,57.5507634442628));
#36067=CARTESIAN_POINT('Ctrl Pts',(82.9002961680271,42.0961072169563,55.2778248931831));
#36068=CARTESIAN_POINT('Ctrl Pts',(82.9205917520382,42.2783322236387,53.017616090358));
#36069=CARTESIAN_POINT('Ctrl Pts',(82.9129498948689,43.7216677763615,53.0228109606371));
#36070=CARTESIAN_POINT('Ctrl Pts',(82.9129498948685,43.5445712043628,55.2274084205465));
#36071=CARTESIAN_POINT('Ctrl Pts',(81.9432795991102,43.3674746323642,57.4147653849821));
#36072=CARTESIAN_POINT('Ctrl Pts',(80.3096882702541,43.1903780603655,58.8951806410927));
#36073=CARTESIAN_POINT('Ctrl Pts',(78.676096941398,43.0132814883668,60.3755958972033));
#36074=CARTESIAN_POINT('Ctrl Pts',(76.4041347530453,42.8361849163681,61.1259150206678));
#36075=CARTESIAN_POINT('Ctrl Pts',(74.2101800112232,42.6590883443694,60.9095529374023));
#36076=CARTESIAN_POINT('Ctrl Pts',(72.016225269401,42.4819917723707,60.6931908541367));
#36077=CARTESIAN_POINT('Ctrl Pts',(69.9345925076997,42.304895200372,59.513531573771));
#36078=CARTESIAN_POINT('Ctrl Pts',(68.6216467656623,42.1277986283733,57.7425365317947));
#36079=CARTESIAN_POINT('Ctrl Pts',(67.3087010236248,41.9507020563746,55.9715414898185));
#36080=CARTESIAN_POINT('Ctrl Pts',(66.7849774198243,41.7736054843759,53.6369099216341));
#36081=CARTESIAN_POINT('Ctrl Pts',(67.2156126057598,41.5965089123772,51.4747805784001));
#36082=CARTESIAN_POINT('Ctrl Pts',(67.6462477916953,41.4194123403785,49.3126512351662));
#36083=CARTESIAN_POINT('Ctrl Pts',(69.0245064207932,41.2423157683798,47.356840885552));
#36084=CARTESIAN_POINT('Ctrl Pts',(70.9158061804419,41.0652191963811,46.2240411771341));
#36085=CARTESIAN_POINT('Ctrl Pts',(72.8071059400906,40.8881226243824,45.0912414687162));
#36086=CARTESIAN_POINT('Ctrl Pts',(75.1818659698035,40.7110260523838,44.7991699473057));
#36087=CARTESIAN_POINT('Ctrl Pts',(77.2912945088602,40.5339294803851,45.4399204438737));
#36088=CARTESIAN_POINT('Ctrl Pts',(79.4007230479168,40.3568329083864,46.0806709404416));
#36089=CARTESIAN_POINT('Ctrl Pts',(81.2118275942023,40.1797363363876,47.6442218013876));
#36090=CARTESIAN_POINT('Ctrl Pts',(82.1535440633064,40.0026397643889,49.6375657386089));
#36091=CARTESIAN_POINT('Ctrl Pts',(82.65156979299,39.9089824350465,50.6917435101726));
#36092=CARTESIAN_POINT('Ctrl Pts',(82.9129498948691,39.815325105704,51.8569119935366));
#36093=CARTESIAN_POINT('Ctrl Pts',(82.9129498948689,39.7216677763615,53.0228109606369));
#36094=CARTESIAN_POINT('Origin',(74.9879498948689,255.,53.0228109606356));
#36095=CARTESIAN_POINT('',(82.9122935305125,34.2783322236387,53.0239510175697));
#36096=CARTESIAN_POINT('',(82.9072011753408,35.7216677763615,53.0231373687424));
#36097=CARTESIAN_POINT('',(82.9129498948689,255.,53.0228109606356));
#36098=CARTESIAN_POINT('Ctrl Pts',(82.9129498948689,34.2783322236387,53.0228109606238));
#36099=CARTESIAN_POINT('Ctrl Pts',(82.9129498948656,34.4554287956374,50.8182135007142));
#36100=CARTESIAN_POINT('Ctrl Pts',(81.9432795991043,34.6325253676362,48.6308565362795));
#36101=CARTESIAN_POINT('Ctrl Pts',(80.3096882702459,34.8096219396349,47.150441280171));
#36102=CARTESIAN_POINT('Ctrl Pts',(78.6760969413875,34.9867185116336,45.6700260240625));
#36103=CARTESIAN_POINT('Ctrl Pts',(76.4041347530333,35.1638150836323,44.9197069006012));
#36104=CARTESIAN_POINT('Ctrl Pts',(74.2101800112112,35.340911655631,45.1360689838701));
#36105=CARTESIAN_POINT('Ctrl Pts',(72.0162252693891,35.5180082276298,45.352431067139));
#36106=CARTESIAN_POINT('Ctrl Pts',(69.9345925076894,35.6951047996285,46.5320903475081));
#36107=CARTESIAN_POINT('Ctrl Pts',(68.6216467656546,35.8722013716272,48.3030853894867));
#36108=CARTESIAN_POINT('Ctrl Pts',(67.3087010236198,36.0492979436259,50.0740804314654));
#36109=CARTESIAN_POINT('Ctrl Pts',(66.7849774198232,36.2263945156246,52.4087119996511));
#36110=CARTESIAN_POINT('Ctrl Pts',(67.2156126057625,36.4034910876234,54.5708413428845));
#36111=CARTESIAN_POINT('Ctrl Pts',(67.6462477917018,36.5805876596221,56.732970686118));
#36112=CARTESIAN_POINT('Ctrl Pts',(69.0245064208034,36.7576842316208,58.6887810357301));
#36113=CARTESIAN_POINT('Ctrl Pts',(70.9158061804545,36.9347808036195,59.8215807441446));
#36114=CARTESIAN_POINT('Ctrl Pts',(72.8071059401056,37.1118773756182,60.9543804525591));
#36115=CARTESIAN_POINT('Ctrl Pts',(75.1818659698194,37.288973947617,61.2464519739651));
#36116=CARTESIAN_POINT('Ctrl Pts',(77.2912945088751,37.4660705196157,60.6057014773929));
#36117=CARTESIAN_POINT('Ctrl Pts',(79.4007230479308,37.6431670916144,59.9649509808207));
#36118=CARTESIAN_POINT('Ctrl Pts',(81.2118275942134,37.8202636636131,58.4014001198708));
#36119=CARTESIAN_POINT('Ctrl Pts',(82.1535440633135,37.9973602356118,56.4080561826473));
#36120=CARTESIAN_POINT('Ctrl Pts',(82.651569792994,38.0910175649541,55.3538784110845));
#36121=CARTESIAN_POINT('Ctrl Pts',(82.9129498948706,38.1846748942964,54.1887099277223));
#36122=CARTESIAN_POINT('Ctrl Pts',(82.9129498948689,38.2783322236387,53.022810960624));
#36123=CARTESIAN_POINT('Ctrl Pts',(82.9163423979736,39.7216677763616,53.0134838750938));
#36124=CARTESIAN_POINT('Ctrl Pts',(82.8967122734635,39.5514208626041,55.1304071046395));
#36125=CARTESIAN_POINT('Ctrl Pts',(82.0220163137799,39.3811739488467,57.264215047829));
#36126=CARTESIAN_POINT('Ctrl Pts',(80.5052432378788,39.2109270350893,58.731040228542));
#36127=CARTESIAN_POINT('Ctrl Pts',(78.6150913633022,38.998771025537,60.5589487067788));
#36128=CARTESIAN_POINT('Ctrl Pts',(75.7278379817599,38.7866150159847,61.3510789260064));
#36129=CARTESIAN_POINT('Ctrl Pts',(73.1689413445864,38.5744590064323,60.7485958194524));
#36130=CARTESIAN_POINT('Ctrl Pts',(70.610044707413,38.36230299688,60.1461127128985));
#36131=CARTESIAN_POINT('Ctrl Pts',(68.3795048146082,38.1501469873277,58.1490162805631));
#36132=CARTESIAN_POINT('Ctrl Pts',(67.5034469430443,37.9379909777754,55.6698135620572));
#36133=CARTESIAN_POINT('Ctrl Pts',(66.6273890714801,37.725834968223,53.1906108435509));
#36134=CARTESIAN_POINT('Ctrl Pts',(67.1058132211573,37.5136789586706,50.2293018388738));
#36135=CARTESIAN_POINT('Ctrl Pts',(68.7171389828885,37.3015229491183,48.1541897885691));
#36136=CARTESIAN_POINT('Ctrl Pts',(70.3284647446191,37.089366939566,46.079077738265));
#36137=CARTESIAN_POINT('Ctrl Pts',(73.0726921184028,36.8772109300138,44.8901626423325));
#36138=CARTESIAN_POINT('Ctrl Pts',(75.6936668597371,36.6650549204615,45.1191043604828));
#36139=CARTESIAN_POINT('Ctrl Pts',(77.0041542304044,36.5589769156853,45.2335752195579));
#36140=CARTESIAN_POINT('Ctrl Pts',(78.2838284429594,36.4528989109092,45.7025102821538));
#36141=CARTESIAN_POINT('Ctrl Pts',(79.3853815208773,36.346820906133,46.4381613200989));
#36142=CARTESIAN_POINT('Ctrl Pts',(80.4869345987952,36.2407429013569,47.1738123580439));
#36143=CARTESIAN_POINT('Ctrl Pts',(81.410366542076,36.1346648965807,48.1761793713381));
#36144=CARTESIAN_POINT('Ctrl Pts',(82.0181869354863,36.0285868918046,49.3428134594782));
#36145=CARTESIAN_POINT('Ctrl Pts',(82.6043961057642,35.9262805199903,50.4679675481548));
#36146=CARTESIAN_POINT('Ctrl Pts',(82.8970380499207,35.8239741481759,51.7459152514041));
#36147=CARTESIAN_POINT('Ctrl Pts',(82.8972143917247,35.7216677763616,53.0237044110371));
#36148=CARTESIAN_POINT('Origin',(74.9879498948689,255.,53.0228109606356));
#36149=CARTESIAN_POINT('',(82.9249771640168,30.2783322236387,53.0230473193048));
#36150=CARTESIAN_POINT('',(82.9129498948689,31.7216677763616,53.0228109606366));
#36151=CARTESIAN_POINT('',(82.9129498948689,255.,53.0228109606356));
#36152=CARTESIAN_POINT('Ctrl Pts',(82.9249771640168,30.2783322236387,53.0230473193048));
#36153=CARTESIAN_POINT('Ctrl Pts',(82.9238427714935,30.489455054567,50.4069753398425));
#36154=CARTESIAN_POINT('Ctrl Pts',(81.5070197109814,30.7005778854952,47.7898361564491));
#36155=CARTESIAN_POINT('Ctrl Pts',(79.3122628451038,30.9117007164234,46.3651293279602));
#36156=CARTESIAN_POINT('Ctrl Pts',(77.1067654265869,31.1238567259758,44.9334503655986));
#36157=CARTESIAN_POINT('Ctrl Pts',(74.115701572633,31.3360127355282,44.7059032047884));
#36158=CARTESIAN_POINT('Ctrl Pts',(71.7212446046575,31.5481687450805,45.7871231457241));
#36159=CARTESIAN_POINT('Ctrl Pts',(69.3267876366829,31.7603247546328,46.8683430866595));
#36160=CARTESIAN_POINT('Ctrl Pts',(67.5289375546867,31.972480764185,49.2583301293398));
#36161=CARTESIAN_POINT('Ctrl Pts',(67.1384391261447,32.1846367737373,51.8601437049917));
#36162=CARTESIAN_POINT('Ctrl Pts',(66.9431899118737,32.2907147785135,53.1610504928182));
#36163=CARTESIAN_POINT('Ctrl Pts',(67.0997786109667,32.3967927832898,54.5149139138883));
#36164=CARTESIAN_POINT('Ctrl Pts',(67.5573491443184,32.5028707880659,55.7579870574282));
#36165=CARTESIAN_POINT('Ctrl Pts',(68.01491967767,32.6089487928421,57.0010602009678));
#36166=CARTESIAN_POINT('Ctrl Pts',(68.7734720452802,32.7150267976183,58.1333430669779));
#36167=CARTESIAN_POINT('Ctrl Pts',(69.7655608529922,32.8211048023944,58.9971952093159));
#36168=CARTESIAN_POINT('Ctrl Pts',(71.7497384684161,33.0332608119467,60.7248994939919));
#36169=CARTESIAN_POINT('Ctrl Pts',(74.6680618442466,33.245416821499,61.3788808839789));
#36170=CARTESIAN_POINT('Ctrl Pts',(77.1920771926515,33.4575728310514,60.6496297251194));
#36171=CARTESIAN_POINT('Ctrl Pts',(79.7160925410564,33.6697288406037,59.9203785662599));
#36172=CARTESIAN_POINT('Ctrl Pts',(81.8457998620355,33.881884850156,57.8078948585541));
#36173=CARTESIAN_POINT('Ctrl Pts',(82.5967259301963,34.0940408597083,55.2879675671467));
#36174=CARTESIAN_POINT('Ctrl Pts',(82.8141589874456,34.1554713143518,54.5583145184003));
#36175=CARTESIAN_POINT('Ctrl Pts',(82.9159935570133,34.2169017689953,53.7945009659517));
#36176=CARTESIAN_POINT('Ctrl Pts',(82.9093304898678,34.2783322236387,53.0290976027477));
#36177=CARTESIAN_POINT('Ctrl Pts',(82.9129498948689,35.7216677763615,53.0228109606377));
#36178=CARTESIAN_POINT('Ctrl Pts',(82.9129498948683,35.5445712043628,55.2274084205473));
#36179=CARTESIAN_POINT('Ctrl Pts',(81.9432795991096,35.3674746323641,57.4147653849832));
#36180=CARTESIAN_POINT('Ctrl Pts',(80.309688270253,35.1903780603654,58.8951806410937));
#36181=CARTESIAN_POINT('Ctrl Pts',(78.6760969413964,35.0132814883666,60.3755958972042));
#36182=CARTESIAN_POINT('Ctrl Pts',(76.4041347530432,34.836184916368,61.1259150206682));
#36183=CARTESIAN_POINT('Ctrl Pts',(74.2101800112208,34.6590883443692,60.909552937402));
#36184=CARTESIAN_POINT('Ctrl Pts',(72.0162252693984,34.4819917723705,60.6931908541358));
#36185=CARTESIAN_POINT('Ctrl Pts',(69.9345925076972,34.3048952003718,59.5135315737692));
#36186=CARTESIAN_POINT('Ctrl Pts',(68.6216467656603,34.127798628373,57.7425365317921));
#36187=CARTESIAN_POINT('Ctrl Pts',(67.3087010236234,33.9507020563743,55.9715414898151));
#36188=CARTESIAN_POINT('Ctrl Pts',(66.7849774198239,33.7736054843756,53.63690992163));
#36189=CARTESIAN_POINT('Ctrl Pts',(67.2156126057606,33.5965089123769,51.4747805783961));
#36190=CARTESIAN_POINT('Ctrl Pts',(67.6462477916973,33.4194123403782,49.3126512351621));
#36191=CARTESIAN_POINT('Ctrl Pts',(69.0245064207966,33.2423157683794,47.3568408855483));
#36192=CARTESIAN_POINT('Ctrl Pts',(70.9158061804463,33.0652191963807,46.2240411771315));
#36193=CARTESIAN_POINT('Ctrl Pts',(72.8071059400959,32.888122624382,45.0912414687147));
#36194=CARTESIAN_POINT('Ctrl Pts',(75.1818659698094,32.7110260523833,44.7991699473058));
#36195=CARTESIAN_POINT('Ctrl Pts',(77.2912945088659,32.5339294803846,45.4399204438754));
#36196=CARTESIAN_POINT('Ctrl Pts',(79.4007230479224,32.3568329083859,46.080670940445));
#36197=CARTESIAN_POINT('Ctrl Pts',(81.2118275942068,32.1797363363871,47.6442218013928));
#36198=CARTESIAN_POINT('Ctrl Pts',(82.1535440633094,32.0026397643884,49.6375657386152));
#36199=CARTESIAN_POINT('Ctrl Pts',(82.651569792991,31.9089824350461,50.691743510177));
#36200=CARTESIAN_POINT('Ctrl Pts',(82.9129498948691,31.8153251057038,51.8569119935386));
#36201=CARTESIAN_POINT('Ctrl Pts',(82.9129498948689,31.7216677763616,53.0228109606366));
#36202=CARTESIAN_POINT('Origin',(74.9879498948689,255.,53.0228109606356));
#36203=CARTESIAN_POINT('',(82.911855653882,26.278332223639,53.0203857348343));
#36204=CARTESIAN_POINT('',(82.9155439867214,27.7216677763616,53.0225420064449));
#36205=CARTESIAN_POINT('',(82.9129498948689,255.,53.0228109606356));
#36206=CARTESIAN_POINT('Ctrl Pts',(82.9100720036525,26.2783322236389,53.0164325339422));
#36207=CARTESIAN_POINT('Ctrl Pts',(82.9166505231298,26.3376963210343,52.2769432483488));
#36208=CARTESIAN_POINT('Ctrl Pts',(82.8216651276326,26.3970604184296,51.5389728574951));
#36209=CARTESIAN_POINT('Ctrl Pts',(82.6184217847882,26.456424515825,50.8318508162249));
#36210=CARTESIAN_POINT('Ctrl Pts',(81.892068677812,26.6685805253773,48.3047309386457));
#36211=CARTESIAN_POINT('Ctrl Pts',(79.7830322414838,26.8807365349295,46.1716098366969));
#36212=CARTESIAN_POINT('Ctrl Pts',(77.2662375055457,27.0928925444818,45.4178161108577));
#36213=CARTESIAN_POINT('Ctrl Pts',(74.7494427696069,27.3050485540342,44.6640223850185));
#36214=CARTESIAN_POINT('Ctrl Pts',(71.8248897340578,27.5172045635866,45.2895560352895));
#36215=CARTESIAN_POINT('Ctrl Pts',(69.8239829670763,27.7293605731389,46.9978578318098));
#36216=CARTESIAN_POINT('Ctrl Pts',(68.8235295835859,27.8354385779151,47.8520087300698));
#36217=CARTESIAN_POINT('Ctrl Pts',(68.0539877672371,27.9415165826912,48.9768516648921));
#36218=CARTESIAN_POINT('Ctrl Pts',(67.5843347182215,28.0475945874674,50.2154103675274));
#36219=CARTESIAN_POINT('Ctrl Pts',(67.114681669206,28.1536725922435,51.4539690701625));
#36220=CARTESIAN_POINT('Ctrl Pts',(66.9449173875235,28.2597505970196,52.80624354061));
#36221=CARTESIAN_POINT('Ctrl Pts',(67.1274899938208,28.3658286017957,54.108989854011));
#36222=CARTESIAN_POINT('Ctrl Pts',(67.4926352064155,28.577984611348,56.714482480814));
#36223=CARTESIAN_POINT('Ctrl Pts',(69.2671279709314,28.7901406209003,59.1218624794284));
#36224=CARTESIAN_POINT('Ctrl Pts',(71.6509432294986,29.0022966304527,60.2263467700827));
#36225=CARTESIAN_POINT('Ctrl Pts',(74.0347584880657,29.214452640005,61.3308310607369));
#36226=CARTESIAN_POINT('Ctrl Pts',(77.0278962406845,29.4266086495573,61.1324196434312));
#36227=CARTESIAN_POINT('Ctrl Pts',(79.2472298230731,29.6387646591097,59.7222842001146));
#36228=CARTESIAN_POINT('Ctrl Pts',(81.4665634054615,29.850920668662,58.3121487567983));
#36229=CARTESIAN_POINT('Ctrl Pts',(82.9120928176202,30.0630766782143,55.6902892874712));
#36230=CARTESIAN_POINT('Ctrl Pts',(82.9248920321598,30.2752326877666,53.0614541708519));
#36231=CARTESIAN_POINT('Ctrl Pts',(82.9249543630591,30.2762658663907,53.0486520058115));
#36232=CARTESIAN_POINT('Ctrl Pts',(82.9249827154302,30.2772990450147,53.0358496753372));
#36233=CARTESIAN_POINT('Ctrl Pts',(82.9249771640168,30.2783322236387,53.0230473193048));
#36234=CARTESIAN_POINT('Ctrl Pts',(82.9129498948689,31.7216677763616,53.0228109606366));
#36235=CARTESIAN_POINT('Ctrl Pts',(82.9129498948686,31.5445712043628,55.2274084205469));
#36236=CARTESIAN_POINT('Ctrl Pts',(81.9432795991097,31.3674746323641,57.4147653849834));
#36237=CARTESIAN_POINT('Ctrl Pts',(80.3096882702525,31.1903780603653,58.8951806410942));
#36238=CARTESIAN_POINT('Ctrl Pts',(78.6760969413953,31.0132814883665,60.3755958972049));
#36239=CARTESIAN_POINT('Ctrl Pts',(76.4041347530412,30.8361849163677,61.1259150206688));
#36240=CARTESIAN_POINT('Ctrl Pts',(74.2101800112183,30.659088344369,60.9095529374018));
#36241=CARTESIAN_POINT('Ctrl Pts',(72.0162252693954,30.4819917723702,60.6931908541348));
#36242=CARTESIAN_POINT('Ctrl Pts',(69.934592507694,30.3048952003715,59.5135315737669));
#36243=CARTESIAN_POINT('Ctrl Pts',(68.6216467656577,30.1277986283727,57.7425365317886));
#36244=CARTESIAN_POINT('Ctrl Pts',(67.3087010236215,29.9507020563739,55.9715414898104));
#36245=CARTESIAN_POINT('Ctrl Pts',(66.7849774198233,29.7736054843751,53.6369099216243));
#36246=CARTESIAN_POINT('Ctrl Pts',(67.2156126057618,29.5965089123764,51.47478057839));
#36247=CARTESIAN_POINT('Ctrl Pts',(67.6462477917003,29.4194123403776,49.3126512351558));
#36248=CARTESIAN_POINT('Ctrl Pts',(69.0245064208017,29.2423157683789,47.3568408855427));
#36249=CARTESIAN_POINT('Ctrl Pts',(70.915806180453,29.0652191963801,46.2240411771274));
#36250=CARTESIAN_POINT('Ctrl Pts',(72.8071059401044,28.8881226243813,45.0912414687122));
#36251=CARTESIAN_POINT('Ctrl Pts',(75.1818659698189,28.7110260523825,44.7991699473058));
#36252=CARTESIAN_POINT('Ctrl Pts',(77.2912945088752,28.5339294803838,45.4399204438782));
#36253=CARTESIAN_POINT('Ctrl Pts',(79.4007230479315,28.356832908385,46.0806709404506));
#36254=CARTESIAN_POINT('Ctrl Pts',(81.2118275942144,28.1797363363863,47.6442218014013));
#36255=CARTESIAN_POINT('Ctrl Pts',(82.1535440633143,28.0026397643875,49.6375657386256));
#36256=CARTESIAN_POINT('Ctrl Pts',(82.6515697929927,27.9089824350455,50.6917435101847));
#36257=CARTESIAN_POINT('Ctrl Pts',(82.912949894869,27.8153251057035,51.8569119935424));
#36258=CARTESIAN_POINT('Ctrl Pts',(82.9129498948689,27.7216677763616,53.0228109606364));
#36259=CARTESIAN_POINT('Origin',(74.9879498948689,255.,53.0228109606356));
#36260=CARTESIAN_POINT('',(82.9129498948689,22.2783322236388,53.0228109606233));
#36261=CARTESIAN_POINT('',(82.9107744051909,23.7216677763616,53.0210350023561));
#36262=CARTESIAN_POINT('',(82.9129498948689,255.,53.0228109606356));
#36263=CARTESIAN_POINT('Ctrl Pts',(82.9129498948689,22.2783322236388,53.0228109606233));
#36264=CARTESIAN_POINT('Ctrl Pts',(82.9129498948655,22.4554287956375,50.8182135007137));
#36265=CARTESIAN_POINT('Ctrl Pts',(81.943279599104,22.6325253676362,48.630856536279));
#36266=CARTESIAN_POINT('Ctrl Pts',(80.3096882702455,22.8096219396349,47.1504412801706));
#36267=CARTESIAN_POINT('Ctrl Pts',(78.676096941387,22.9867185116336,45.6700260240622));
#36268=CARTESIAN_POINT('Ctrl Pts',(76.4041347530328,23.1638150836324,44.9197069006011));
#36269=CARTESIAN_POINT('Ctrl Pts',(74.2101800112107,23.3409116556311,45.1360689838701));
#36270=CARTESIAN_POINT('Ctrl Pts',(72.0162252693886,23.5180082276298,45.3524310671391));
#36271=CARTESIAN_POINT('Ctrl Pts',(69.9345925076889,23.6951047996285,46.5320903475084));
#36272=CARTESIAN_POINT('Ctrl Pts',(68.6216467656543,23.8722013716272,48.3030853894872));
#36273=CARTESIAN_POINT('Ctrl Pts',(67.3087010236196,24.0492979436259,50.0740804314659));
#36274=CARTESIAN_POINT('Ctrl Pts',(66.7849774198231,24.2263945156247,52.4087119996516));
#36275=CARTESIAN_POINT('Ctrl Pts',(67.2156126057626,24.4034910876234,54.570841342885));
#36276=CARTESIAN_POINT('Ctrl Pts',(67.6462477917021,24.5805876596221,56.7329706861185));
#36277=CARTESIAN_POINT('Ctrl Pts',(69.0245064208038,24.7576842316208,58.6887810357304));
#36278=CARTESIAN_POINT('Ctrl Pts',(70.915806180455,24.9347808036195,59.8215807441448));
#36279=CARTESIAN_POINT('Ctrl Pts',(72.8071059401061,25.1118773756182,60.9543804525592));
#36280=CARTESIAN_POINT('Ctrl Pts',(75.1818659698199,25.288973947617,61.2464519739651));
#36281=CARTESIAN_POINT('Ctrl Pts',(77.2912945088756,25.4660705196157,60.6057014773928));
#36282=CARTESIAN_POINT('Ctrl Pts',(79.4007230479312,25.6431670916144,59.9649509808204));
#36283=CARTESIAN_POINT('Ctrl Pts',(81.2118275942137,25.8202636636131,58.4014001198704));
#36284=CARTESIAN_POINT('Ctrl Pts',(82.1535440633137,25.9973602356119,56.4080561826468));
#36285=CARTESIAN_POINT('Ctrl Pts',(82.6515697929942,26.0910175649542,55.3538784110837));
#36286=CARTESIAN_POINT('Ctrl Pts',(82.9129498948708,26.1846748942965,54.1887099277212));
#36287=CARTESIAN_POINT('Ctrl Pts',(82.9129498948689,26.2783322236388,53.0228109606226));
#36288=CARTESIAN_POINT('Ctrl Pts',(82.9230491389377,27.7216677763615,53.0217638758786));
#36289=CARTESIAN_POINT('Ctrl Pts',(82.9208703146659,27.6265346858863,54.2018633476581));
#36290=CARTESIAN_POINT('Ctrl Pts',(82.6384364768388,27.531401595411,55.3842255652826));
#36291=CARTESIAN_POINT('Ctrl Pts',(82.123537086314,27.4362685049358,56.4547799592356));
#36292=CARTESIAN_POINT('Ctrl Pts',(81.5493993206381,27.3301905001596,57.6484999734551));
#36293=CARTESIAN_POINT('Ctrl Pts',(80.6862294529177,27.2241124953835,58.703205626511));
#36294=CARTESIAN_POINT('Ctrl Pts',(79.6162123658362,27.1180344906073,59.4684142012732));
#36295=CARTESIAN_POINT('Ctrl Pts',(77.4761781916732,26.905878481055,60.9988313507976));
#36296=CARTESIAN_POINT('Ctrl Pts',(74.5087551400656,26.6937224715027,61.3712601871467));
#36297=CARTESIAN_POINT('Ctrl Pts',(72.0658749947129,26.4815664619504,60.4044110161784));
#36298=CARTESIAN_POINT('Ctrl Pts',(69.6229948493599,26.2694104523981,59.4375618452099));
#36299=CARTESIAN_POINT('Ctrl Pts',(67.7046576102617,26.0572544428458,57.1314346669236));
#36300=CARTESIAN_POINT('Ctrl Pts',(67.197698117,25.8450984332934,54.5513347107468));
#36301=CARTESIAN_POINT('Ctrl Pts',(66.6907386237383,25.6329424237411,51.9712347545703));
#36302=CARTESIAN_POINT('Ctrl Pts',(67.5951568763126,25.4207864141888,49.1171620205034));
#36303=CARTESIAN_POINT('Ctrl Pts',(69.4917218674496,25.2086304046365,47.2967283534847));
#36304=CARTESIAN_POINT('Ctrl Pts',(71.3882868585865,24.9964743950842,45.4762946864661));
#36305=CARTESIAN_POINT('Ctrl Pts',(74.276998588286,24.7843183855319,44.6895000864957));
#36306=CARTESIAN_POINT('Ctrl Pts',(76.8341764136125,24.5721623759795,45.3016807310096));
#36307=CARTESIAN_POINT('Ctrl Pts',(79.3913542389393,24.3600063664272,45.9138613755236));
#36308=CARTESIAN_POINT('Ctrl Pts',(81.6169981598929,24.1478503568749,47.9250172645221));
#36309=CARTESIAN_POINT('Ctrl Pts',(82.4830085759959,23.9356943473226,50.4054382966083));
#36310=CARTESIAN_POINT('Ctrl Pts',(82.7742238946445,23.8643521570022,51.2395351940708));
#36311=CARTESIAN_POINT('Ctrl Pts',(82.9116931305271,23.7930099666819,52.1266961542172));
#36312=CARTESIAN_POINT('Ctrl Pts',(82.9044091330798,23.7216677763616,53.0158387204223));
#36313=CARTESIAN_POINT('Origin',(74.9879498948689,255.,53.0228109606356));
#36314=CARTESIAN_POINT('',(82.9129498948689,18.2783322236388,53.0228109606232));
#36315=CARTESIAN_POINT('',(82.9101799821405,19.7216677763616,53.0246693339172));
#36316=CARTESIAN_POINT('',(82.9129498948689,255.,53.0228109606356));
#36317=CARTESIAN_POINT('Ctrl Pts',(82.9129498948689,18.2783322236388,53.0228109606232));
#36318=CARTESIAN_POINT('Ctrl Pts',(82.9129498948655,18.4554287956375,50.8182135007132));
#36319=CARTESIAN_POINT('Ctrl Pts',(81.9432795991037,18.6325253676362,48.6308565362783));
#36320=CARTESIAN_POINT('Ctrl Pts',(80.3096882702447,18.809621939635,47.1504412801699));
#36321=CARTESIAN_POINT('Ctrl Pts',(78.6760969413858,18.9867185116337,45.6700260240615));
#36322=CARTESIAN_POINT('Ctrl Pts',(76.4041347530311,19.1638150836325,44.9197069006007));
#36323=CARTESIAN_POINT('Ctrl Pts',(74.2101800112087,19.3409116556312,45.1360689838703));
#36324=CARTESIAN_POINT('Ctrl Pts',(72.0162252693864,19.51800822763,45.3524310671399));
#36325=CARTESIAN_POINT('Ctrl Pts',(69.9345925076868,19.6951047996287,46.53209034751));
#36326=CARTESIAN_POINT('Ctrl Pts',(68.6216467656526,19.8722013716274,48.3030853894895));
#36327=CARTESIAN_POINT('Ctrl Pts',(67.3087010236184,20.0492979436262,50.0740804314689));
#36328=CARTESIAN_POINT('Ctrl Pts',(66.7849774198228,20.226394515625,52.4087119996552));
#36329=CARTESIAN_POINT('Ctrl Pts',(67.2156126057633,20.4034910876237,54.5708413428887));
#36330=CARTESIAN_POINT('Ctrl Pts',(67.6462477917039,20.5805876596225,56.7329706861223));
#36331=CARTESIAN_POINT('Ctrl Pts',(69.0245064208069,20.7576842316212,58.6887810357338));
#36332=CARTESIAN_POINT('Ctrl Pts',(70.915806180459,20.9347808036199,59.8215807441473));
#36333=CARTESIAN_POINT('Ctrl Pts',(72.807105940111,21.1118773756186,60.9543804525607));
#36334=CARTESIAN_POINT('Ctrl Pts',(75.1818659698254,21.2889739476174,61.2464519739651));
#36335=CARTESIAN_POINT('Ctrl Pts',(77.2912945088809,21.4660705196162,60.6057014773912));
#36336=CARTESIAN_POINT('Ctrl Pts',(79.4007230479364,21.6431670916149,59.9649509808173));
#36337=CARTESIAN_POINT('Ctrl Pts',(81.211827594218,21.8202636636136,58.4014001198656));
#36338=CARTESIAN_POINT('Ctrl Pts',(82.1535440633165,21.9973602356124,56.408056182641));
#36339=CARTESIAN_POINT('Ctrl Pts',(82.6515697929951,22.0910175649545,55.3538784110796));
#36340=CARTESIAN_POINT('Ctrl Pts',(82.9129498948707,22.1846748942966,54.1887099277195));
#36341=CARTESIAN_POINT('Ctrl Pts',(82.9129498948689,22.2783322236388,53.0228109606233));
#36342=CARTESIAN_POINT('Ctrl Pts',(82.9129498948689,23.7216677763616,53.0228109606362));
#36343=CARTESIAN_POINT('Ctrl Pts',(82.9129498948687,23.5445712043629,55.2274084205459));
#36344=CARTESIAN_POINT('Ctrl Pts',(81.9432795991104,23.3674746323642,57.414765384982));
#36345=CARTESIAN_POINT('Ctrl Pts',(80.3096882702541,23.1903780603655,58.8951806410928));
#36346=CARTESIAN_POINT('Ctrl Pts',(78.6760969413977,23.0132814883668,60.3755958972035));
#36347=CARTESIAN_POINT('Ctrl Pts',(76.4041347530446,22.8361849163681,61.125915020668));
#36348=CARTESIAN_POINT('Ctrl Pts',(74.2101800112222,22.6590883443694,60.9095529374022));
#36349=CARTESIAN_POINT('Ctrl Pts',(72.0162252693998,22.4819917723706,60.6931908541363));
#36350=CARTESIAN_POINT('Ctrl Pts',(69.9345925076984,22.3048952003719,59.5135315737701));
#36351=CARTESIAN_POINT('Ctrl Pts',(68.6216467656612,22.1277986283732,57.7425365317933));
#36352=CARTESIAN_POINT('Ctrl Pts',(67.308701023624,21.9507020563744,55.9715414898164));
#36353=CARTESIAN_POINT('Ctrl Pts',(66.784977419824,21.7736054843758,53.6369099216315));
#36354=CARTESIAN_POINT('Ctrl Pts',(67.2156126057603,21.596508912377,51.4747805783974));
#36355=CARTESIAN_POINT('Ctrl Pts',(67.6462477916966,21.4194123403783,49.3126512351634));
#36356=CARTESIAN_POINT('Ctrl Pts',(69.0245064207955,21.2423157683796,47.3568408855494));
#36357=CARTESIAN_POINT('Ctrl Pts',(70.915806180445,21.0652191963808,46.2240411771322));
#36358=CARTESIAN_POINT('Ctrl Pts',(72.8071059400945,20.8881226243821,45.0912414687151));
#36359=CARTESIAN_POINT('Ctrl Pts',(75.1818659698079,20.7110260523834,44.7991699473057));
#36360=CARTESIAN_POINT('Ctrl Pts',(77.2912945088645,20.5339294803847,45.439920443875));
#36361=CARTESIAN_POINT('Ctrl Pts',(79.4007230479211,20.356832908386,46.0806709404443));
#36362=CARTESIAN_POINT('Ctrl Pts',(81.2118275942059,20.1797363363872,47.6442218013917));
#36363=CARTESIAN_POINT('Ctrl Pts',(82.1535440633088,20.0026397643885,49.6375657386139));
#36364=CARTESIAN_POINT('Ctrl Pts',(82.6515697929907,19.9089824350462,50.6917435101759));
#36365=CARTESIAN_POINT('Ctrl Pts',(82.912949894869,19.8153251057039,51.8569119935378));
#36366=CARTESIAN_POINT('Ctrl Pts',(82.9129498948689,19.7216677763616,53.0228109606361));
#36367=CARTESIAN_POINT('Origin',(74.9879498948689,255.,53.0228109606356));
#36368=CARTESIAN_POINT('',(82.9129498948689,15.,53.0228109606356));
#36369=CARTESIAN_POINT('',(82.922834243019,15.7216677763616,53.0299163294501));
#36370=CARTESIAN_POINT('',(82.9129498948689,255.,53.0228109606356));
#36371=CARTESIAN_POINT('',(78.3434537325876,15.,45.8432414056375));
#36372=CARTESIAN_POINT('Origin',(74.9879498948689,15.,53.0228109606356));
#36373=CARTESIAN_POINT('Ctrl Pts',(78.3434537325868,15.0000000000001,45.8432414056371));
#36374=CARTESIAN_POINT('Ctrl Pts',(76.3462220853698,15.1770965719988,44.9097984734794));
#36375=CARTESIAN_POINT('Ctrl Pts',(73.9540436795002,15.3541931439975,44.8621177977932));
#36376=CARTESIAN_POINT('Ctrl Pts',(71.9212025091824,15.5312897159962,45.7152336964265));
#36377=CARTESIAN_POINT('Ctrl Pts',(69.8883613388645,15.7083862879949,46.5683495950599));
#36378=CARTESIAN_POINT('Ctrl Pts',(68.2466520420155,15.8854828599937,48.3089189148464));
#36379=CARTESIAN_POINT('Ctrl Pts',(67.51372624642,16.0625794319924,50.3881182170757));
#36380=CARTESIAN_POINT('Ctrl Pts',(66.7808004508245,16.2396760039911,52.4673175193051));
#36381=CARTESIAN_POINT('Ctrl Pts',(66.968121477194,16.4167725759898,54.8526271020265));
#36382=CARTESIAN_POINT('Ctrl Pts',(68.0166246455609,16.5938691479885,56.7919287975254));
#36383=CARTESIAN_POINT('Ctrl Pts',(69.0651278139278,16.7709657199872,58.7312304930242));
#36384=CARTESIAN_POINT('Ctrl Pts',(70.9584140179181,16.948062291986,60.1941926668765));
#36385=CARTESIAN_POINT('Ctrl Pts',(73.0995062609109,17.1251588639847,60.7195249114956));
#36386=CARTESIAN_POINT('Ctrl Pts',(75.2405985039036,17.3022554359834,61.2448571561147));
#36387=CARTESIAN_POINT('Ctrl Pts',(77.5960090478467,17.4793520079821,60.8243430162519));
#36388=CARTESIAN_POINT('Ctrl Pts',(79.4230472686975,17.6564485799808,59.5905758989277));
#36389=CARTESIAN_POINT('Ctrl Pts',(81.2500854895483,17.8335451519795,58.3568087816034));
#36390=CARTESIAN_POINT('Ctrl Pts',(82.5201756089623,18.0106417239783,56.3290854126722));
#36391=CARTESIAN_POINT('Ctrl Pts',(82.832842208417,18.187738295977,54.1467725208472));
#36392=CARTESIAN_POINT('Ctrl Pts',(82.8861571784615,18.2179362718643,53.7746510769253));
#36393=CARTESIAN_POINT('Ctrl Pts',(82.9129498948695,18.2481342477515,53.3987323022059));
#36394=CARTESIAN_POINT('Ctrl Pts',(82.9129498948689,18.2783322236388,53.0228109606232));
#36395=CARTESIAN_POINT('Ctrl Pts',(82.9030122912126,19.7216677763617,53.0294782382423));
#36396=CARTESIAN_POINT('Ctrl Pts',(82.9086579729621,19.6412512331491,54.0339957391183));
#36397=CARTESIAN_POINT('Ctrl Pts',(82.7316773075948,19.5608346899366,55.0362729807911));
#36398=CARTESIAN_POINT('Ctrl Pts',(82.3629950679762,19.480418146724,55.9613819431945));
#36399=CARTESIAN_POINT('Ctrl Pts',(81.390332607921,19.2682621371717,58.4020168924711));
#36400=CARTESIAN_POINT('Ctrl Pts',(79.0833945161164,19.0561061276194,60.3055474649299));
#36401=CARTESIAN_POINT('Ctrl Pts',(76.501790689728,18.8439501180671,60.8122568728204));
#36402=CARTESIAN_POINT('Ctrl Pts',(75.2109887765338,18.7378721132909,61.0656115767657));
#36403=CARTESIAN_POINT('Ctrl Pts',(73.8515204296936,18.6317941085148,60.9697609895688));
#36404=CARTESIAN_POINT('Ctrl Pts',(72.5891317440186,18.5257161037386,60.5685453417559));
#36405=CARTESIAN_POINT('Ctrl Pts',(71.3267430583433,18.4196380989624,60.1673296939429));
#36406=CARTESIAN_POINT('Ctrl Pts',(70.1614340338332,18.3135600941862,59.4607489855137));
#36407=CARTESIAN_POINT('Ctrl Pts',(69.253909830781,18.2074820894101,58.5084666850121));
#36408=CARTESIAN_POINT('Ctrl Pts',(67.4388614246767,17.9953260798577,56.6039020840091));
#36409=CARTESIAN_POINT('Ctrl Pts',(66.6549523044037,17.7831700703054,53.7165311147166));
#36410=CARTESIAN_POINT('Ctrl Pts',(67.2700601338688,17.5710140607531,51.1626732511785));
#36411=CARTESIAN_POINT('Ctrl Pts',(67.8851679633337,17.3588580512008,48.608815387641));
#36412=CARTESIAN_POINT('Ctrl Pts',(69.8992927425361,17.1467020416485,46.3884706298577));
#36413=CARTESIAN_POINT('Ctrl Pts',(72.3832175225222,16.9345460320962,45.5243909463029));
#36414=CARTESIAN_POINT('Ctrl Pts',(74.8671423025088,16.7223900225439,44.6603112627479));
#36415=CARTESIAN_POINT('Ctrl Pts',(77.8208670832794,16.5102340129916,45.152496653422));
#36416=CARTESIAN_POINT('Ctrl Pts',(79.8884469946644,16.2980780034393,46.7770485682758));
#36417=CARTESIAN_POINT('Ctrl Pts',(81.7609278618296,16.1059412610801,48.2483060328749));
#36418=CARTESIAN_POINT('Ctrl Pts',(82.9066087649531,15.9138045187209,50.648310000996));
#36419=CARTESIAN_POINT('Ctrl Pts',(82.922834243019,15.7216677763616,53.0299163294501));
#36420=CARTESIAN_POINT('Origin',(74.9879498948689,416.,53.0228109606356));
#36421=CARTESIAN_POINT('',(70.1710194129307,439.948460488314,53.0227057148971));
#36422=CARTESIAN_POINT('',(70.1715766354573,438.426539511686,53.0228415555562));
#36423=CARTESIAN_POINT('',(70.1711998948689,416.,53.0228109606356));
#36424=CARTESIAN_POINT('',(70.1716517717484,438.198460488314,53.0228096900326));
#36425=CARTESIAN_POINT('Ctrl Pts',(70.1716517717486,438.198460488314,53.0228096900326));
#36426=CARTESIAN_POINT('Ctrl Pts',(70.171762094604,438.224019932922,53.464926508948));
#36427=CARTESIAN_POINT('Ctrl Pts',(70.3403863287184,438.295435847886,54.7004002781471));
#36428=CARTESIAN_POINT('Ctrl Pts',(71.3835049550069,438.412708233207,56.5125746552081));
#36429=CARTESIAN_POINT('Ctrl Pts',(73.4687602399829,438.550277644276,57.8043411146894));
#36430=CARTESIAN_POINT('Ctrl Pts',(75.9171988302832,438.687847055345,57.9530481846181));
#36431=CARTESIAN_POINT('Ctrl Pts',(78.1434978095446,438.825416466414,56.9232374758342));
#36432=CARTESIAN_POINT('Ctrl Pts',(79.6154836096685,438.962985877483,54.9610361557711));
#36433=CARTESIAN_POINT('Ctrl Pts',(79.9812781097431,439.100555288552,52.5355178274692));
#36434=CARTESIAN_POINT('Ctrl Pts',(79.1534426071904,439.238124699621,50.2264819254732));
#36435=CARTESIAN_POINT('Ctrl Pts',(77.3298657797079,439.37569411069,48.5858962981143));
#36436=CARTESIAN_POINT('Ctrl Pts',(74.946465455023,439.513263521759,48.0059331744372));
#36437=CARTESIAN_POINT('Ctrl Pts',(72.5729817051559,439.650832932828,48.6252307671089));
#36438=CARTESIAN_POINT('Ctrl Pts',(70.7767845007438,439.788402343897,50.2957485891607));
#36439=CARTESIAN_POINT('Ctrl Pts',(70.2074030943593,439.887611529059,51.9705707881673));
#36440=CARTESIAN_POINT('Ctrl Pts',(70.170895409116,439.940964243864,52.8930801168023));
#36441=CARTESIAN_POINT('Ctrl Pts',(70.1710194129309,439.948460488314,53.0227057148971));
#36442=CARTESIAN_POINT('',(70.1711998948689,416.,53.0228109606356));
#36443=CARTESIAN_POINT('',(70.1711998948689,416.,53.0228109606356));
#36444=CARTESIAN_POINT('Origin',(74.9879498948689,416.,53.0228109606356));
#36445=CARTESIAN_POINT('',(71.3431312258735,438.,49.8737829466856));
#36446=CARTESIAN_POINT('Ctrl Pts',(71.3431312258736,438.,49.8737829466856));
#36447=CARTESIAN_POINT('Ctrl Pts',(70.8246667948602,438.045856470356,50.4738756829193));
#36448=CARTESIAN_POINT('Ctrl Pts',(70.2950910214935,438.112009966461,51.5275346151049));
#36449=CARTESIAN_POINT('Ctrl Pts',(70.1715641632004,438.178163462565,52.6717200402042));
#36450=CARTESIAN_POINT('Ctrl Pts',(70.1716517717486,438.198460488314,53.0228096900326));
#36451=CARTESIAN_POINT('',(74.7983630544234,438.,48.2104548970639));
#36452=CARTESIAN_POINT('Origin',(74.9879498948689,438.,53.0228109606356));
#36453=CARTESIAN_POINT('Ctrl Pts',(70.1715766354573,438.426539511686,53.0228415555562));
#36454=CARTESIAN_POINT('Ctrl Pts',(70.1716376521608,438.402395353675,52.6052026582204));
#36455=CARTESIAN_POINT('Ctrl Pts',(70.2254319475252,438.378251195664,52.1875501723899));
#36456=CARTESIAN_POINT('Ctrl Pts',(70.3327672197935,438.354107037653,51.7841487615086));
#36457=CARTESIAN_POINT('Ctrl Pts',(70.5366266801429,438.308250583211,51.0179775655125));
#36458=CARTESIAN_POINT('Ctrl Pts',(70.9336220846199,438.262394128769,50.3032136275511));
#36459=CARTESIAN_POINT('Ctrl Pts',(71.4763794327931,438.216537674328,49.7252773752126));
#36460=CARTESIAN_POINT('Ctrl Pts',(72.0191367809662,438.170681219886,49.1473411228741));
#36461=CARTESIAN_POINT('Ctrl Pts',(72.7076560728355,438.124824765444,48.7062325561585));
#36462=CARTESIAN_POINT('Ctrl Pts',(73.4594632851625,438.078968311002,48.4547383628616));
#36463=CARTESIAN_POINT('Ctrl Pts',(73.8910197329203,438.052645540668,48.3103743039495));
#36464=CARTESIAN_POINT('Ctrl Pts',(74.3434298781826,438.026322770334,48.2284891629282));
#36465=CARTESIAN_POINT('Ctrl Pts',(74.7983630544234,438.,48.2104548970639));
#36466=CARTESIAN_POINT('Origin',(74.9879498948689,416.,53.0228109606356));
#36467=CARTESIAN_POINT('',(70.1709154736136,441.698460488314,53.0228942458375));
#36468=CARTESIAN_POINT('',(70.1712218667098,440.176539511686,53.0226919906017));
#36469=CARTESIAN_POINT('',(70.1711998948689,416.,53.0228109606356));
#36470=CARTESIAN_POINT('Ctrl Pts',(70.1710194129309,439.948460488314,53.0227057148971));
#36471=CARTESIAN_POINT('Ctrl Pts',(70.1716539725937,439.986820714221,53.6860334998797));
#36472=CARTESIAN_POINT('Ctrl Pts',(70.4750683395013,440.071037410484,55.1428772890645));
#36473=CARTESIAN_POINT('Ctrl Pts',(71.8973337884151,440.201110577104,56.9748832301599));
#36474=CARTESIAN_POINT('Ctrl Pts',(74.1403626764107,440.338679988173,57.967745644851));
#36475=CARTESIAN_POINT('Ctrl Pts',(76.5860032023106,440.476249399242,57.7785452633612));
#36476=CARTESIAN_POINT('Ctrl Pts',(78.6496367890598,440.613818810311,56.4525095214311));
#36477=CARTESIAN_POINT('Ctrl Pts',(79.8379617752664,440.75138822138,54.3066208723653));
#36478=CARTESIAN_POINT('Ctrl Pts',(79.8669148016947,440.888957632449,51.8538436524662));
#36479=CARTESIAN_POINT('Ctrl Pts',(78.729574786843,441.026527043518,49.6805024325154));
#36480=CARTESIAN_POINT('Ctrl Pts',(76.6978173786037,441.164096454587,48.3061239541028));
#36481=CARTESIAN_POINT('Ctrl Pts',(74.257324391025,441.301665865656,48.0592467671762));
#36482=CARTESIAN_POINT('Ctrl Pts',(71.9914839080614,441.439235276725,48.9988856731345));
#36483=CARTESIAN_POINT('Ctrl Pts',(70.5016832392066,441.571500150944,50.8271031133775));
#36484=CARTESIAN_POINT('Ctrl Pts',(70.1714871278914,441.657908554807,52.3217110697681));
#36485=CARTESIAN_POINT('Ctrl Pts',(70.1709154736138,441.698460488314,53.0228942458375));
#36486=CARTESIAN_POINT('Ctrl Pts',(70.1712218667098,440.176539511686,53.0226919906017));
#36487=CARTESIAN_POINT('Ctrl Pts',(70.1710294008066,440.165195928084,52.8265141535113));
#36488=CARTESIAN_POINT('Ctrl Pts',(70.1827930416903,440.153852344482,52.6303592478741));
#36489=CARTESIAN_POINT('Ctrl Pts',(70.2066969022817,440.14250876088,52.4356951053063));
#36490=CARTESIAN_POINT('Ctrl Pts',(70.3033282960843,440.096652306438,51.6487650047139));
#36491=CARTESIAN_POINT('Ctrl Pts',(70.5983529615977,440.050795851997,50.886196684207));
#36492=CARTESIAN_POINT('Ctrl Pts',(71.056508807961,440.004939397555,50.2391342229322));
#36493=CARTESIAN_POINT('Ctrl Pts',(71.5146646543244,439.959082943113,49.5920717616573));
#36494=CARTESIAN_POINT('Ctrl Pts',(72.1359516815378,439.913226488672,49.0605151596145));
#36495=CARTESIAN_POINT('Ctrl Pts',(72.8461121117878,439.86737003423,48.7079973939007));
#36496=CARTESIAN_POINT('Ctrl Pts',(73.5562725420377,439.821513579788,48.3554796281869));
#36497=CARTESIAN_POINT('Ctrl Pts',(74.3553063753243,439.775657125346,48.1820006988021));
#36498=CARTESIAN_POINT('Ctrl Pts',(75.1477110700954,439.729800670905,48.2082952456863));
#36499=CARTESIAN_POINT('Ctrl Pts',(75.9401157648664,439.683944216463,48.2345897925705));
#36500=CARTESIAN_POINT('Ctrl Pts',(76.7258913211219,439.638087762021,48.4606578157238));
#36501=CARTESIAN_POINT('Ctrl Pts',(77.4111199028447,439.592231307579,48.8594790915802));
#36502=CARTESIAN_POINT('Ctrl Pts',(78.0963484845675,439.546374853138,49.2583003674367));
#36503=CARTESIAN_POINT('Ctrl Pts',(78.6810300917576,439.500518398696,49.8298748959963));
#36504=CARTESIAN_POINT('Ctrl Pts',(79.0952820469545,439.454661944254,50.5058866713264));
#36505=CARTESIAN_POINT('Ctrl Pts',(79.5095340021513,439.408805489813,51.1818984466564));
#36506=CARTESIAN_POINT('Ctrl Pts',(79.7533563053549,439.362949035371,51.9623474687568));
#36507=CARTESIAN_POINT('Ctrl Pts',(79.7976068454851,439.317092580929,52.7539524829401));
#36508=CARTESIAN_POINT('Ctrl Pts',(79.8418573856152,439.271236126487,53.5455574971234));
#36509=CARTESIAN_POINT('Ctrl Pts',(79.6865361626719,439.225379672046,54.3483185033896));
#36510=CARTESIAN_POINT('Ctrl Pts',(79.3502072440678,439.179523217604,55.0662875695242));
#36511=CARTESIAN_POINT('Ctrl Pts',(79.0138783254638,439.133666763162,55.7842566356588));
#36512=CARTESIAN_POINT('Ctrl Pts',(78.496541711199,439.08781030872,56.4174337616619));
#36513=CARTESIAN_POINT('Ctrl Pts',(77.8600314557391,439.041953854279,56.8901398913939));
#36514=CARTESIAN_POINT('Ctrl Pts',(77.2235212002792,438.996097399837,57.3628460211258));
#36515=CARTESIAN_POINT('Ctrl Pts',(76.4678373036241,438.950240945395,57.6750811545867));
#36516=CARTESIAN_POINT('Ctrl Pts',(75.6832994784698,438.904384490954,57.7895265539831));
#36517=CARTESIAN_POINT('Ctrl Pts',(74.8987616533154,438.858528036512,57.9039719533795));
#36518=CARTESIAN_POINT('Ctrl Pts',(74.0853698996618,438.81267158207,57.8206276187115));
#36519=CARTESIAN_POINT('Ctrl Pts',(73.3403461325011,438.766815127628,57.5494544577645));
#36520=CARTESIAN_POINT('Ctrl Pts',(72.5953223653404,438.720958673187,57.2782812968174));
#36521=CARTESIAN_POINT('Ctrl Pts',(71.9186665846726,438.675102218745,56.8192793095913));
#36522=CARTESIAN_POINT('Ctrl Pts',(71.391247014838,438.629245764303,56.2273115731785));
#36523=CARTESIAN_POINT('Ctrl Pts',(70.8638274450034,438.583389309861,55.6353438367656));
#36524=CARTESIAN_POINT('Ctrl Pts',(70.485644086002,438.53753285542,54.9104103511661));
#36525=CARTESIAN_POINT('Ctrl Pts',(70.3019141646122,438.491676400978,54.1391543813509));
#36526=CARTESIAN_POINT('Ctrl Pts',(70.2149209906975,438.469964104547,53.7739770373049));
#36527=CARTESIAN_POINT('Ctrl Pts',(70.1715217645128,438.448251808117,53.3984147909377));
#36528=CARTESIAN_POINT('Ctrl Pts',(70.1715766354573,438.426539511686,53.0228415555562));
#36529=CARTESIAN_POINT('Origin',(74.9879498948689,416.,53.0228109606356));
#36530=CARTESIAN_POINT('',(70.1715080739194,443.448460488314,53.0228810481615));
#36531=CARTESIAN_POINT('',(70.170796016094,441.926539511687,53.0228364485998));
#36532=CARTESIAN_POINT('',(70.1711998948689,416.,53.0228109606356));
#36533=CARTESIAN_POINT('Ctrl Pts',(70.1709154736138,441.698460488314,53.0228942458375));
#36534=CARTESIAN_POINT('Ctrl Pts',(70.1708406963857,441.703765025163,53.1146149524511));
#36535=CARTESIAN_POINT('Ctrl Pts',(70.1955986940716,441.754926032369,53.9991991984498));
#36536=CARTESIAN_POINT('Ctrl Pts',(70.713585383041,441.851943509931,55.6497085889238));
#36537=CARTESIAN_POINT('Ctrl Pts',(72.4698494135181,441.989512921,57.3621603468108));
#36538=CARTESIAN_POINT('Ctrl Pts',(74.828053225208,442.127082332069,58.0373115523705));
#36539=CARTESIAN_POINT('Ctrl Pts',(77.2244795649762,442.264651743138,57.5137705645742));
#36540=CARTESIAN_POINT('Ctrl Pts',(79.0862742686079,442.402221154207,55.9166873327523));
#36541=CARTESIAN_POINT('Ctrl Pts',(79.9683842872405,442.539790565276,53.6278369045098));
#36542=CARTESIAN_POINT('Ctrl Pts',(79.6599454732541,442.677359976345,51.194357940996));
#36543=CARTESIAN_POINT('Ctrl Pts',(78.2346886382596,442.814929387414,49.1979618575147));
#36544=CARTESIAN_POINT('Ctrl Pts',(76.0333145580138,442.952498798483,48.1158775139168));
#36545=CARTESIAN_POINT('Ctrl Pts',(73.5820510943691,443.090068209552,48.2067719562013));
#36546=CARTESIAN_POINT('Ctrl Pts',(71.466860961653,443.227637620621,49.4489173061093));
#36547=CARTESIAN_POINT('Ctrl Pts',(70.3609725105829,443.347101713542,51.2694715578199));
#36548=CARTESIAN_POINT('Ctrl Pts',(70.1717606038319,443.420709336106,52.542866079208));
#36549=CARTESIAN_POINT('Ctrl Pts',(70.1715080739196,443.448460488314,53.0228810481615));
#36550=CARTESIAN_POINT('Ctrl Pts',(70.170796016094,441.926539511687,53.0228364485998));
#36551=CARTESIAN_POINT('Ctrl Pts',(70.1710241501999,441.882140048052,52.2551809390674));
#36552=CARTESIAN_POINT('Ctrl Pts',(70.3579454689711,441.837740584417,51.4874182485368));
#36553=CARTESIAN_POINT('Ctrl Pts',(70.7112275018185,441.793341120782,50.805891752147));
#36554=CARTESIAN_POINT('Ctrl Pts',(71.0761026628707,441.747484666341,50.1020006198204));
#36555=CARTESIAN_POINT('Ctrl Pts',(71.6184361063414,441.701628211899,49.4900983141799));
#36556=CARTESIAN_POINT('Ctrl Pts',(72.2734067786708,441.655771757457,49.0433209336992));
#36557=CARTESIAN_POINT('Ctrl Pts',(72.9283774510002,441.609915303015,48.5965435532186));
#36558=CARTESIAN_POINT('Ctrl Pts',(73.6959853521882,441.564058848574,48.3148910978977));
#36559=CARTESIAN_POINT('Ctrl Pts',(74.4844840604079,441.518202394132,48.2320273756972));
#36560=CARTESIAN_POINT('Ctrl Pts',(75.2729827686276,441.47234593969,48.1491636534967));
#36561=CARTESIAN_POINT('Ctrl Pts',(76.082372283879,441.426489485249,48.2650886644164));
#36562=CARTESIAN_POINT('Ctrl Pts',(76.8159123410153,441.380633030807,48.5659467603638));
#36563=CARTESIAN_POINT('Ctrl Pts',(77.5494523981515,441.334776576365,48.8668048563111));
#36564=CARTESIAN_POINT('Ctrl Pts',(78.2071429971726,441.288920121923,49.3525960372861));
#36565=CARTESIAN_POINT('Ctrl Pts',(78.7103753079263,441.243063667482,49.9652573227733));
#36566=CARTESIAN_POINT('Ctrl Pts',(79.21360761868,441.19720721304,50.5779186082605));
#36567=CARTESIAN_POINT('Ctrl Pts',(79.5623816411664,441.151350758598,51.3174499982598));
#36568=CARTESIAN_POINT('Ctrl Pts',(79.7150110293437,441.105494304157,52.0954608459898));
#36569=CARTESIAN_POINT('Ctrl Pts',(79.8676404175208,441.059637849715,52.8734716937199));
#36570=CARTESIAN_POINT('Ctrl Pts',(79.8241251713888,441.013781395273,53.6899619991806));
#36571=CARTESIAN_POINT('Ctrl Pts',(79.5896663423308,440.967924940831,54.4473427929661));
#36572=CARTESIAN_POINT('Ctrl Pts',(79.3552075132728,440.92206848639,55.2047235867516));
#36573=CARTESIAN_POINT('Ctrl Pts',(78.9298051012887,440.876212031948,55.9029948688619));
#36574=CARTESIAN_POINT('Ctrl Pts',(78.3643042697189,440.830355577506,56.4586975041123));
#36575=CARTESIAN_POINT('Ctrl Pts',(77.7988034381491,440.784499123064,57.0144001393626));
#36576=CARTESIAN_POINT('Ctrl Pts',(77.0932041869936,440.738642668623,57.427534127753));
#36577=CARTESIAN_POINT('Ctrl Pts',(76.3318415087392,440.692786214181,57.6487206586682));
#36578=CARTESIAN_POINT('Ctrl Pts',(75.5704788304848,440.646929759739,57.8699071895835));
#36579=CARTESIAN_POINT('Ctrl Pts',(74.7533527251315,440.601073305297,57.8991462630236));
#36580=CARTESIAN_POINT('Ctrl Pts',(73.9781281543607,440.555216850856,57.7329431516146));
#36581=CARTESIAN_POINT('Ctrl Pts',(73.2029035835899,440.509360396414,57.5667400402056));
#36582=CARTESIAN_POINT('Ctrl Pts',(72.4695805474015,440.463503941972,57.2050947439475));
#36583=CARTESIAN_POINT('Ctrl Pts',(71.8658076548209,440.41764748753,56.691232015746));
#36584=CARTESIAN_POINT('Ctrl Pts',(71.2620347622404,440.371791033089,56.1773692875446));
#36585=CARTESIAN_POINT('Ctrl Pts',(70.7878120132677,440.325934578647,55.5112891273998));
#36586=CARTESIAN_POINT('Ctrl Pts',(70.4998196998274,440.280078124205,54.7726031069883));
#36587=CARTESIAN_POINT('Ctrl Pts',(70.2830685000765,440.245565253366,54.2166470147902));
#36588=CARTESIAN_POINT('Ctrl Pts',(70.1718074445211,440.211052382526,53.6195633665776));
#36589=CARTESIAN_POINT('Ctrl Pts',(70.1712218667098,440.176539511686,53.0226919906017));
#36590=CARTESIAN_POINT('Origin',(74.9879498948689,416.,53.0228109606356));
#36591=CARTESIAN_POINT('',(70.1713954601516,445.198460488314,53.0227079586499));
#36592=CARTESIAN_POINT('',(70.1713650637522,443.676539511686,53.0229190193667));
#36593=CARTESIAN_POINT('',(70.1711998948689,416.,53.0228109606356));
#36594=CARTESIAN_POINT('Ctrl Pts',(70.1715080739196,443.448460488314,53.0228810481615));
#36595=CARTESIAN_POINT('Ctrl Pts',(70.1713433191603,443.466565806462,53.3360508821162));
#36596=CARTESIAN_POINT('Ctrl Pts',(70.2776498508399,443.530527594967,54.4422951112801));
#36597=CARTESIAN_POINT('Ctrl Pts',(71.1151991800427,443.640345853828,56.2122599773613));
#36598=CARTESIAN_POINT('Ctrl Pts',(73.090160210338,443.777915264897,57.6670738130985));
#36599=CARTESIAN_POINT('Ctrl Pts',(75.5187787161611,443.915484675966,58.0116990022701));
#36600=CARTESIAN_POINT('Ctrl Pts',(77.8205051511885,444.053054087035,57.1637545547184));
#36601=CARTESIAN_POINT('Ctrl Pts',(79.4451229069195,444.190623498104,55.3259375029962));
#36602=CARTESIAN_POINT('Ctrl Pts',(80.004274940543,444.328192909173,52.9375691538648));
#36603=CARTESIAN_POINT('Ctrl Pts',(79.3642986538913,444.465762320242,50.569577447722));
#36604=CARTESIAN_POINT('Ctrl Pts',(77.6781772931937,444.603331731311,48.7880193866875));
#36605=CARTESIAN_POINT('Ctrl Pts',(75.3489700415422,444.74090114238,48.0187678370029));
#36606=CARTESIAN_POINT('Ctrl Pts',(72.9334626641764,444.878470553449,48.4457086733363));
#36607=CARTESIAN_POINT('Ctrl Pts',(71.0090705553659,445.016039964518,49.9667837468897));
#36608=CARTESIAN_POINT('Ctrl Pts',(70.2544612753753,445.12270327614,51.7125461193628));
#36609=CARTESIAN_POINT('Ctrl Pts',(70.1711887931693,445.183510117405,52.7641269590152));
#36610=CARTESIAN_POINT('Ctrl Pts',(70.1713954601518,445.198460488314,53.0227079586499));
#36611=CARTESIAN_POINT('Ctrl Pts',(70.1713650637522,443.676539511686,53.0229190193667));
#36612=CARTESIAN_POINT('Ctrl Pts',(70.1718277712569,443.644940622461,52.4763958288777));
#36613=CARTESIAN_POINT('Ctrl Pts',(70.2647396080943,443.613341733235,51.9297192730009));
#36614=CARTESIAN_POINT('Ctrl Pts',(70.447118527273,443.58174284401,51.4147264805034));
#36615=CARTESIAN_POINT('Ctrl Pts',(70.7117876597462,443.535886389568,50.6673665540712));
#36616=CARTESIAN_POINT('Ctrl Pts',(71.1648740101699,443.490029935126,49.9867324713112));
#36617=CARTESIAN_POINT('Ctrl Pts',(71.7522235614141,443.444173480685,49.454175325106));
#36618=CARTESIAN_POINT('Ctrl Pts',(72.3395731126582,443.398317026243,48.9216181789009));
#36619=CARTESIAN_POINT('Ctrl Pts',(73.0611858647228,443.352460571801,48.5371379692506));
#36620=CARTESIAN_POINT('Ctrl Pts',(73.8308128513784,443.306604117359,48.3466887352477));
#36621=CARTESIAN_POINT('Ctrl Pts',(74.600439838034,443.260747662918,48.1562395012448));
#36622=CARTESIAN_POINT('Ctrl Pts',(75.4180810592806,443.214891208476,48.1598212428892));
#36623=CARTESIAN_POINT('Ctrl Pts',(76.1860099853732,443.169034754034,48.3570058614351));
#36624=CARTESIAN_POINT('Ctrl Pts',(76.9539389114658,443.123178299593,48.554190479981));
#36625=CARTESIAN_POINT('Ctrl Pts',(77.6721555424045,443.077321845151,48.9449779754284));
#36626=CARTESIAN_POINT('Ctrl Pts',(78.2548168248756,443.031465390709,49.4826604460651));
#36627=CARTESIAN_POINT('Ctrl Pts',(78.8374781073467,442.985608936267,50.0203429167019));
#36628=CARTESIAN_POINT('Ctrl Pts',(79.2845840413502,442.939752481826,50.7049203625279));
#36629=CARTESIAN_POINT('Ctrl Pts',(79.5426954041279,442.893896027384,51.4545703700153));
#36630=CARTESIAN_POINT('Ctrl Pts',(79.8008067669057,442.848039572942,52.2042203775027));
#36631=CARTESIAN_POINT('Ctrl Pts',(79.8699235584575,442.8021831185,53.0189429466516));
#36632=CARTESIAN_POINT('Ctrl Pts',(79.7417847664839,442.756326664059,53.8013603923367));
#36633=CARTESIAN_POINT('Ctrl Pts',(79.6136459745102,442.710470209617,54.5837778380218));
#36634=CARTESIAN_POINT('Ctrl Pts',(79.2882515990109,442.664613755175,55.3338901602431));
#36635=CARTESIAN_POINT('Ctrl Pts',(78.8044935919692,442.618757300734,55.9620420526576));
#36636=CARTESIAN_POINT('Ctrl Pts',(78.3207355849274,442.572900846292,56.590193945072));
#36637=CARTESIAN_POINT('Ctrl Pts',(77.6786139463432,442.52704439185,57.0963854076795));
#36638=CARTESIAN_POINT('Ctrl Pts',(76.9548766651661,442.481187937408,57.4201151671322));
#36639=CARTESIAN_POINT('Ctrl Pts',(76.231139383989,442.435331482967,57.7438449265848));
#36640=CARTESIAN_POINT('Ctrl Pts',(75.4257864602191,442.389475028525,57.8851129828826));
#36641=CARTESIAN_POINT('Ctrl Pts',(74.6350756954628,442.343618574083,57.8270346235782));
#36642=CARTESIAN_POINT('Ctrl Pts',(73.8443649307066,442.297762119641,57.7689562642738));
#36643=CARTESIAN_POINT('Ctrl Pts',(73.0682963249641,442.2519056652,57.5115314893672));
#36644=CARTESIAN_POINT('Ctrl Pts',(72.3996275446939,442.206049210758,57.0855283536829));
#36645=CARTESIAN_POINT('Ctrl Pts',(71.7309587644238,442.160192756316,56.6595252179985));
#36646=CARTESIAN_POINT('Ctrl Pts',(71.169689809626,442.114336301875,56.0649437215364));
#36647=CARTESIAN_POINT('Ctrl Pts',(70.7829049536723,442.068479847433,55.3728497362095));
#36648=CARTESIAN_POINT('Ctrl Pts',(70.3961200977185,442.022623392991,54.6807557508826));
#36649=CARTESIAN_POINT('Ctrl Pts',(70.1838193406088,441.976766938549,53.8911492766908));
#36650=CARTESIAN_POINT('Ctrl Pts',(70.1713774013708,441.930910484108,53.0984060600886));
#36651=CARTESIAN_POINT('Ctrl Pts',(70.1709820853501,441.929453493301,53.0732183391237));
#36652=CARTESIAN_POINT('Ctrl Pts',(70.1707885297582,441.927996502494,53.0480274515711));
#36653=CARTESIAN_POINT('Ctrl Pts',(70.170796016094,441.926539511687,53.0228364485998));
#36654=CARTESIAN_POINT('Origin',(74.9879498948689,416.,53.0228109606356));
#36655=CARTESIAN_POINT('',(70.1708091458864,446.948460488314,53.022773765229));
#36656=CARTESIAN_POINT('',(70.1715262232373,445.426539511687,53.0227498862744));
#36657=CARTESIAN_POINT('',(70.1711998948689,416.,53.0228109606356));
#36658=CARTESIAN_POINT('Ctrl Pts',(70.1713954601518,445.198460488314,53.0227079586499));
#36659=CARTESIAN_POINT('Ctrl Pts',(70.1718226917137,445.229366587761,53.5572585820871));
#36660=CARTESIAN_POINT('Ctrl Pts',(70.3923929886614,445.306129157565,54.8852847418079));
#36661=CARTESIAN_POINT('Ctrl Pts',(71.5903202847087,445.428748197725,56.7142735653008));
#36662=CARTESIAN_POINT('Ctrl Pts',(73.7464922800195,445.566317608794,57.8838361734905));
#36663=CARTESIAN_POINT('Ctrl Pts',(76.1994287335407,445.703887019863,57.891394137796));
#36664=CARTESIAN_POINT('Ctrl Pts',(78.3627670107798,445.841456430932,56.7351407632842));
#36665=CARTESIAN_POINT('Ctrl Pts',(79.7193715252362,445.979025842001,54.691472845252));
#36666=CARTESIAN_POINT('Ctrl Pts',(79.9449525074299,446.11659525307,52.2489193477191));
#36667=CARTESIAN_POINT('Ctrl Pts',(78.9855859110121,446.254164664139,49.9913609096016));
#36668=CARTESIAN_POINT('Ctrl Pts',(77.0706036960962,446.391734075208,48.4584559926568));
#36669=CARTESIAN_POINT('Ctrl Pts',(74.6577731297195,446.529303486277,48.0166381276987));
#36670=CARTESIAN_POINT('Ctrl Pts',(72.3238697273887,446.666872897346,48.7715217455012));
#36671=CARTESIAN_POINT('Ctrl Pts',(70.6268018465247,446.804442308415,50.54265555625));
#36672=CARTESIAN_POINT('Ctrl Pts',(70.1802031047041,446.898304838737,52.155596267003));
#36673=CARTESIAN_POINT('Ctrl Pts',(70.1707936064121,446.946310898704,52.9856076092154));
#36674=CARTESIAN_POINT('Ctrl Pts',(70.1708091458866,446.948460488314,53.022773765229));
#36675=CARTESIAN_POINT('Ctrl Pts',(70.1715262232373,445.426539511687,53.0227498862744));
#36676=CARTESIAN_POINT('Ctrl Pts',(70.1713779019995,445.40774119687,52.6975896937802));
#36677=CARTESIAN_POINT('Ctrl Pts',(70.2038342589014,445.388942882054,52.3724587093238));
#36678=CARTESIAN_POINT('Ctrl Pts',(70.2691946807472,445.370144567237,52.0540827049399));
#36679=CARTESIAN_POINT('Ctrl Pts',(70.4286343558419,445.324288112796,51.2774389002736));
#36680=CARTESIAN_POINT('Ctrl Pts',(70.7838740194541,445.278431658354,50.5409914975681));
#36681=CARTESIAN_POINT('Ctrl Pts',(71.2924545359011,445.232575203912,49.9327625377089));
#36682=CARTESIAN_POINT('Ctrl Pts',(71.801035052348,445.18671874947,49.3245335778497));
#36683=CARTESIAN_POINT('Ctrl Pts',(72.4629564216298,445.140862295029,48.8445230608368));
#36684=CARTESIAN_POINT('Ctrl Pts',(73.1991041413178,445.095005840587,48.550103047728));
#36685=CARTESIAN_POINT('Ctrl Pts',(73.9352518610058,445.049149386145,48.2556830346191));
#36686=CARTESIAN_POINT('Ctrl Pts',(74.7456259311001,445.003292931703,48.1468535254144));
#36687=CARTESIAN_POINT('Ctrl Pts',(75.5333684099903,444.957436477262,48.2366220960433));
#36688=CARTESIAN_POINT('Ctrl Pts',(76.3211108888805,444.91158002282,48.3263906666722));
#36689=CARTESIAN_POINT('Ctrl Pts',(77.0862217765667,444.865723568378,48.6147573171347));
#36690=CARTESIAN_POINT('Ctrl Pts',(77.7372531005387,444.819867113937,49.0672557420249));
#36691=CARTESIAN_POINT('Ctrl Pts',(78.3882844245107,444.774010659495,49.5197541669151));
#36692=CARTESIAN_POINT('Ctrl Pts',(78.9252361847685,444.728154205053,50.1363843662331));
#36693=CARTESIAN_POINT('Ctrl Pts',(79.2839305600295,444.682297750611,50.8434451517932));
#36694=CARTESIAN_POINT('Ctrl Pts',(79.6426249352905,444.63644129617,51.5505059373534));
#36695=CARTESIAN_POINT('Ctrl Pts',(79.8230619255547,444.590584841728,52.3479973091559));
#36696=CARTESIAN_POINT('Ctrl Pts',(79.8036752491352,444.544728387286,53.1406010980052));
#36697=CARTESIAN_POINT('Ctrl Pts',(79.7842885727157,444.498871932844,53.9332048868545));
#36698=CARTESIAN_POINT('Ctrl Pts',(79.5650782296126,444.453015478403,54.7209210927507));
#36699=CARTESIAN_POINT('Ctrl Pts',(79.1722447899035,444.407159023961,55.4095998988477));
#36700=CARTESIAN_POINT('Ctrl Pts',(78.7794113501945,444.361302569519,56.0982787049447));
#36701=CARTESIAN_POINT('Ctrl Pts',(78.2129548138795,444.315446115077,56.6879201112425));
#36702=CARTESIAN_POINT('Ctrl Pts',(77.5405794870857,444.269589660636,57.1080486977965));
#36703=CARTESIAN_POINT('Ctrl Pts',(76.8682041602919,444.223733206194,57.5281772843504));
#36704=CARTESIAN_POINT('Ctrl Pts',(76.0899100430193,444.177876751752,57.7787930511605));
#36705=CARTESIAN_POINT('Ctrl Pts',(75.2987208004472,444.132020297311,57.8299417731297));
#36706=CARTESIAN_POINT('Ctrl Pts',(74.5075315578751,444.086163842869,57.8810904950989));
#36707=CARTESIAN_POINT('Ctrl Pts',(73.7034471900036,444.040307388427,57.7327721722273));
#36708=CARTESIAN_POINT('Ctrl Pts',(72.9825738774559,443.994450933985,57.4027141825081));
#36709=CARTESIAN_POINT('Ctrl Pts',(72.2617005649083,443.948594479544,57.0726561927889));
#36710=CARTESIAN_POINT('Ctrl Pts',(71.6240383076847,443.902738025102,56.560858536222));
#36711=CARTESIAN_POINT('Ctrl Pts',(71.1458020982885,443.85688157066,55.9284925525201));
#36712=CARTESIAN_POINT('Ctrl Pts',(70.6675658888923,443.811025116218,55.2961265688183));
#36713=CARTESIAN_POINT('Ctrl Pts',(70.3487557273236,443.765168661777,54.5431922579814));
#36714=CARTESIAN_POINT('Ctrl Pts',(70.2274766038005,443.719312207335,53.7596822175107));
#36715=CARTESIAN_POINT('Ctrl Pts',(70.1897688256036,443.705054642119,53.5160753875562));
#36716=CARTESIAN_POINT('Ctrl Pts',(70.1711562879823,443.690797076903,53.2695128149553));
#36717=CARTESIAN_POINT('Ctrl Pts',(70.1713650637522,443.676539511686,53.0229190193667));
#36718=CARTESIAN_POINT('Origin',(74.9879498948689,416.,53.0228109606356));
#36719=CARTESIAN_POINT('',(70.1711854681807,448.698460488313,53.022929878907));
#36720=CARTESIAN_POINT('',(70.1709464687216,447.176539511687,53.0227197042782));
#36721=CARTESIAN_POINT('',(70.1711998948689,416.,53.0228109606356));
#36722=CARTESIAN_POINT('Ctrl Pts',(70.1708091458866,446.948460488314,53.022773765229));
#36723=CARTESIAN_POINT('Ctrl Pts',(70.1711251047822,446.99216736906,53.7784606838785));
#36724=CARTESIAN_POINT('Ctrl Pts',(70.5418769104653,447.081730720163,55.3272999181237));
#36725=CARTESIAN_POINT('Ctrl Pts',(72.1299305918756,447.217150541622,57.1462208108926));
#36726=CARTESIAN_POINT('Ctrl Pts',(74.4263880163468,447.354719952691,58.0083331385092));
#36727=CARTESIAN_POINT('Ctrl Pts',(76.8570841007916,447.49228936376,57.6786804229088));
#36728=CARTESIAN_POINT('Ctrl Pts',(78.8409726637322,447.629858774829,56.236064556619));
#36729=CARTESIAN_POINT('Ctrl Pts',(79.9038147078087,447.767428185898,54.0253359081455));
#36730=CARTESIAN_POINT('Ctrl Pts',(79.7915429659626,447.904997596967,51.5749585037809));
#36731=CARTESIAN_POINT('Ctrl Pts',(78.5309954568607,448.042567008036,49.4706832496531));
#36732=CARTESIAN_POINT('Ctrl Pts',(76.423499985909,448.180136419105,48.2155270013095));
#36733=CARTESIAN_POINT('Ctrl Pts',(73.9728431859633,448.317705830174,48.1095288092612));
#36734=CARTESIAN_POINT('Ctrl Pts',(71.7648427513183,448.455275241243,49.1780270303383));
#36735=CARTESIAN_POINT('Ctrl Pts',(70.4386102196623,448.582193460623,51.0117160323741));
#36736=CARTESIAN_POINT('Ctrl Pts',(70.171791438985,448.663255209646,52.414097135008));
#36737=CARTESIAN_POINT('Ctrl Pts',(70.1711854681809,448.698460488314,53.022929878907));
#36738=CARTESIAN_POINT('Ctrl Pts',(70.1709464687216,447.176539511687,53.0227197042782));
#36739=CARTESIAN_POINT('Ctrl Pts',(70.1708561265147,447.170541771279,52.9190108868649));
#36740=CARTESIAN_POINT('Ctrl Pts',(70.1741384060741,447.164544030872,52.8153077803593));
#36741=CARTESIAN_POINT('Ctrl Pts',(70.1808329626729,447.158546290465,52.7118254233847));
#36742=CARTESIAN_POINT('Ctrl Pts',(70.2320170101361,447.112689836023,51.9206384653235));
#36743=CARTESIAN_POINT('Ctrl Pts',(70.4826675264911,447.066833381581,51.1423555384866));
#36744=CARTESIAN_POINT('Ctrl Pts',(70.9028261332883,447.020976927139,50.4699989705443));
#36745=CARTESIAN_POINT('Ctrl Pts',(71.3229847400855,446.975120472698,49.797642402602));
#36746=CARTESIAN_POINT('Ctrl Pts',(71.9126514373248,446.929264018256,49.2312121935544));
#36747=CARTESIAN_POINT('Ctrl Pts',(72.6013477822247,446.883407563814,48.8384095028275));
#36748=CARTESIAN_POINT('Ctrl Pts',(73.2900441271247,446.837551109372,48.4456068121006));
#36749=CARTESIAN_POINT('Ctrl Pts',(74.0777701196853,446.791694654931,48.2264316396944));
#36750=CARTESIAN_POINT('Ctrl Pts',(74.8703747733338,446.745838200489,48.2070803519968));
#36751=CARTESIAN_POINT('Ctrl Pts',(75.6629794269824,446.699981746047,48.1877290642992));
#36752=CARTESIAN_POINT('Ctrl Pts',(76.4604627417188,446.654125291606,48.3682016613101));
#36753=CARTESIAN_POINT('Ctrl Pts',(77.1675075113485,446.608268837164,48.726927605535));
#36754=CARTESIAN_POINT('Ctrl Pts',(77.8745522809783,446.562412382722,49.08565354976));
#36755=CARTESIAN_POINT('Ctrl Pts',(78.4911585055014,446.51655592828,49.6226328411989));
#36756=CARTESIAN_POINT('Ctrl Pts',(78.9436278622599,446.470699473839,50.2736843679735));
#36757=CARTESIAN_POINT('Ctrl Pts',(79.3960972190183,446.424843019397,50.924735894748));
#36758=CARTESIAN_POINT('Ctrl Pts',(79.6844297080122,446.378986564955,51.689859656858));
#36759=CARTESIAN_POINT('Ctrl Pts',(79.7741631069001,446.333130110513,52.4776061430101));
#36760=CARTESIAN_POINT('Ctrl Pts',(79.863896505788,446.287273656072,53.2653526291621));
#36761=CARTESIAN_POINT('Ctrl Pts',(79.7550308145699,446.24141720163,54.0757218393561));
#36762=CARTESIAN_POINT('Ctrl Pts',(79.4605779337402,446.195560747188,54.8118564128493));
#36763=CARTESIAN_POINT('Ctrl Pts',(79.1661250529105,446.149704292747,55.5479909863425));
#36764=CARTESIAN_POINT('Ctrl Pts',(78.6860849824693,446.103847838305,56.2098909231348));
#36765=CARTESIAN_POINT('Ctrl Pts',(78.0778333157743,446.057991383863,56.7184442824626));
#36766=CARTESIAN_POINT('Ctrl Pts',(77.4695816490793,446.012134929421,57.2269976417904));
#36767=CARTESIAN_POINT('Ctrl Pts',(76.7331183861305,445.96627847498,57.5822044236538));
#36768=CARTESIAN_POINT('Ctrl Pts',(75.9564674634694,445.920422020538,57.7416094224791));
#36769=CARTESIAN_POINT('Ctrl Pts',(75.1798165408083,445.874565566096,57.9010144213044));
#36770=CARTESIAN_POINT('Ctrl Pts',(74.3629779584348,445.828709111654,57.8646176370917));
#36771=CARTESIAN_POINT('Ctrl Pts',(73.6035823126826,445.782852657213,57.6367693047883));
#36772=CARTESIAN_POINT('Ctrl Pts',(72.8441866669304,445.736996202771,57.4089209724848));
#36773=CARTESIAN_POINT('Ctrl Pts',(72.1422339577995,445.691139748329,56.9896210920906));
#36774=CARTESIAN_POINT('Ctrl Pts',(71.5816233338722,445.645283293888,56.4289854370875));
#36775=CARTESIAN_POINT('Ctrl Pts',(71.0210127099449,445.599426839446,55.8683497820844));
#36776=CARTESIAN_POINT('Ctrl Pts',(70.6017441712213,445.553570385004,55.1663783524725));
#36777=CARTESIAN_POINT('Ctrl Pts',(70.3739297451482,445.507713930562,54.4069725343529));
#36778=CARTESIAN_POINT('Ctrl Pts',(70.2395051668771,445.480655790937,53.9588762105293));
#36779=CARTESIAN_POINT('Ctrl Pts',(70.1717397156061,445.453597651312,53.4907827910848));
#36780=CARTESIAN_POINT('Ctrl Pts',(70.1715262232373,445.426539511687,53.0227498862744));
#36781=CARTESIAN_POINT('Origin',(74.9879498948689,416.,53.0228109606356));
#36782=CARTESIAN_POINT('',(70.1715765014012,450.448460488314,53.022802847649));
#36783=CARTESIAN_POINT('',(70.1709848060094,448.926539511687,53.0229103046436));
#36784=CARTESIAN_POINT('',(70.1711998948689,416.,53.0228109606356));
#36785=CARTESIAN_POINT('Ctrl Pts',(70.1711854681809,448.698460488314,53.022929878907));
#36786=CARTESIAN_POINT('Ctrl Pts',(70.1710021345605,448.709111680003,53.2071293656684));
#36787=CARTESIAN_POINT('Ctrl Pts',(70.2260079845499,448.765619342048,54.1842522303751));
#36788=CARTESIAN_POINT('Ctrl Pts',(70.8718703381808,448.86798347445,55.8913771900424));
#36789=CARTESIAN_POINT('Ctrl Pts',(72.7237879497012,449.005552885519,57.4999030766785));
#36790=CARTESIAN_POINT('Ctrl Pts',(75.116942559506,449.143122296588,58.0382016754203));
#36791=CARTESIAN_POINT('Ctrl Pts',(77.4792620946565,449.280691707657,57.377595301182));
#36792=CARTESIAN_POINT('Ctrl Pts',(79.246045458165,449.418261118726,55.6759987231803));
#36793=CARTESIAN_POINT('Ctrl Pts',(79.9949516040101,449.555830529795,53.3401704006032));
#36794=CARTESIAN_POINT('Ctrl Pts',(79.5469581282337,449.693399940864,50.9284788337772));
#36795=CARTESIAN_POINT('Ctrl Pts',(78.0091557116053,449.830969351933,49.0174272658571));
#36796=CARTESIAN_POINT('Ctrl Pts',(75.7491486086294,449.968538763002,48.0638433616641));
#36797=CARTESIAN_POINT('Ctrl Pts',(73.3071806225934,450.10610817407,48.2956767566116));
#36798=CARTESIAN_POINT('Ctrl Pts',(71.2669924287125,450.24367758514,49.6575087952225));
#36799=CARTESIAN_POINT('Ctrl Pts',(70.3124472381403,450.35779502322,51.4545042986814));
#36800=CARTESIAN_POINT('Ctrl Pts',(70.1715533307098,450.426055990945,52.6352538315714));
#36801=CARTESIAN_POINT('Ctrl Pts',(70.1715765014014,450.448460488314,53.022802847649));
#36802=CARTESIAN_POINT('Ctrl Pts',(70.1709848060094,448.926539511687,53.0229103046436));
#36803=CARTESIAN_POINT('Ctrl Pts',(70.1716080264492,448.887485891247,52.3476063104968));
#36804=CARTESIAN_POINT('Ctrl Pts',(70.3150017485599,448.848432270807,51.672045946135));
#36805=CARTESIAN_POINT('Ctrl Pts',(70.5907335134134,448.809378650367,51.0556878585283));
#36806=CARTESIAN_POINT('Ctrl Pts',(70.9144955864482,448.763522195925,50.3319650321748));
#36807=CARTESIAN_POINT('Ctrl Pts',(71.4207157184263,448.717665741483,49.6898659950046));
#36808=CARTESIAN_POINT('Ctrl Pts',(72.0488892093647,448.671809287042,49.2061360345896));
#36809=CARTESIAN_POINT('Ctrl Pts',(72.6770627003032,448.6259528326,48.7224060741746));
#36810=CARTESIAN_POINT('Ctrl Pts',(73.4271895502019,448.580096378158,48.3970451905149));
#36811=CARTESIAN_POINT('Ctrl Pts',(74.2096127163334,448.534239923716,48.2689413325648));
#36812=CARTESIAN_POINT('Ctrl Pts',(74.9920358824648,448.488383469275,48.1408374746147));
#36813=CARTESIAN_POINT('Ctrl Pts',(75.806755364829,448.442527014833,48.2099906423743));
#36814=CARTESIAN_POINT('Ctrl Pts',(76.556393847241,448.396670560391,48.4681354757682));
#36815=CARTESIAN_POINT('Ctrl Pts',(77.306032329653,448.350814105949,48.7262803091621));
#36816=CARTESIAN_POINT('Ctrl Pts',(77.9905898121127,448.304957651508,49.1734168081904));
#36817=CARTESIAN_POINT('Ctrl Pts',(78.528246267164,448.259101197066,49.7561020968862));
#36818=CARTESIAN_POINT('Ctrl Pts',(79.0659027222152,448.213244742624,50.338787385582));
#36819=CARTESIAN_POINT('Ctrl Pts',(79.4566581498581,448.167388288183,51.0570214639455));
#36820=CARTESIAN_POINT('Ctrl Pts',(79.6538084812046,448.121531833741,51.824959193303));
#36821=CARTESIAN_POINT('Ctrl Pts',(79.8509588125512,448.075675379299,52.5928969226606));
#36822=CARTESIAN_POINT('Ctrl Pts',(79.8545040476015,448.029818924857,53.4105383030122));
#36823=CARTESIAN_POINT('Ctrl Pts',(79.6640204509694,447.983962470416,54.1801567855962));
#36824=CARTESIAN_POINT('Ctrl Pts',(79.4735368543374,447.938106015974,54.9497752681803));
#36825=CARTESIAN_POINT('Ctrl Pts',(79.089024426023,447.892249561532,55.6713708529968));
#36826=CARTESIAN_POINT('Ctrl Pts',(78.5564410559742,447.846393107091,56.2586966256889));
#36827=CARTESIAN_POINT('Ctrl Pts',(78.0238576859255,447.800536652649,56.846022398381));
#36828=CARTESIAN_POINT('Ctrl Pts',(77.3432033741424,447.754680198207,57.2990783589487));
#36829=CARTESIAN_POINT('Ctrl Pts',(76.5958316313312,447.708823743765,57.5637141225336));
#36830=CARTESIAN_POINT('Ctrl Pts',(75.8484598885199,447.662967289324,57.8283498861185));
#36831=CARTESIAN_POINT('Ctrl Pts',(75.0343707146806,447.617110834882,57.9045654527207));
#36832=CARTESIAN_POINT('Ctrl Pts',(74.2508660899421,447.57125438044,57.7832513466397));
#36833=CARTESIAN_POINT('Ctrl Pts',(73.4673614652036,447.525397925998,57.6619372405587));
#36834=CARTESIAN_POINT('Ctrl Pts',(72.7144413895659,447.479541471557,57.3430934617945));
#36835=CARTESIAN_POINT('Ctrl Pts',(72.0820967591035,447.433685017115,56.8648290185769));
#36836=CARTESIAN_POINT('Ctrl Pts',(71.4497521286412,447.387828562673,56.3865645753592));
#36837=CARTESIAN_POINT('Ctrl Pts',(70.9379829433542,447.341972108232,55.7488794676881));
#36838=CARTESIAN_POINT('Ctrl Pts',(70.6079571399963,447.29611565379,55.0279914192098));
#36839=CARTESIAN_POINT('Ctrl Pts',(70.3210966689862,447.256256939755,54.4013910654555));
#36840=CARTESIAN_POINT('Ctrl Pts',(70.1715468488558,447.216398225721,53.7119292757795));
#36841=CARTESIAN_POINT('Ctrl Pts',(70.1709464687216,447.176539511687,53.0227197042782));
#36842=CARTESIAN_POINT('Origin',(74.9879498948689,416.,53.0228109606356));
#36843=CARTESIAN_POINT('',(70.1711297808101,452.198460488313,53.0226941375257));
#36844=CARTESIAN_POINT('',(70.1715440079096,450.676539511686,53.0228609587722));
#36845=CARTESIAN_POINT('',(70.1711998948689,416.,53.0228109606356));
#36846=CARTESIAN_POINT('Ctrl Pts',(70.1715765014014,450.448460488314,53.022802847649));
#36847=CARTESIAN_POINT('Ctrl Pts',(70.1716007553904,450.471912461302,53.4284709109444));
#36848=CARTESIAN_POINT('Ctrl Pts',(70.3214916941221,450.541220904646,54.6273736565593));
#36849=CARTESIAN_POINT('Ctrl Pts',(71.3051976181603,450.656385818346,56.4298799059135));
#36850=CARTESIAN_POINT('Ctrl Pts',(73.3606205623162,450.793955229416,57.7686072450216));
#36851=CARTESIAN_POINT('Ctrl Pts',(75.8050487386511,450.931524640484,57.972874860119));
#36852=CARTESIAN_POINT('Ctrl Pts',(78.0541533753186,451.069094051554,56.9938535625169));
#36853=CARTESIAN_POINT('Ctrl Pts',(79.5702968510455,451.206663462622,55.065573673899));
#36854=CARTESIAN_POINT('Ctrl Pts',(79.9910523767396,451.344232873691,52.6489812060971));
#36855=CARTESIAN_POINT('Ctrl Pts',(79.2158403722948,451.48180228476,50.3217509390201));
#36856=CARTESIAN_POINT('Ctrl Pts',(77.4299715303552,451.619371695829,48.6401960492725));
#36857=CARTESIAN_POINT('Ctrl Pts',(75.0603491885598,451.756941106898,48.0062841270851));
#36858=CARTESIAN_POINT('Ctrl Pts',(72.6734201446142,451.894510517967,48.571548761583));
#36859=CARTESIAN_POINT('Ctrl Pts',(70.8397682799635,452.032079929036,50.2008661668549));
#36860=CARTESIAN_POINT('Ctrl Pts',(70.2196188326656,452.133396585818,51.8976271012186));
#36861=CARTESIAN_POINT('Ctrl Pts',(70.170963356447,452.188856772244,52.8566150075112));
#36862=CARTESIAN_POINT('Ctrl Pts',(70.1711297808103,452.198460488313,53.0226941375257));
#36863=CARTESIAN_POINT('Ctrl Pts',(70.1715440079096,450.676539511686,53.0228609587722));
#36864=CARTESIAN_POINT('Ctrl Pts',(70.1717127698825,450.650286465656,52.5687492006864));
#36865=CARTESIAN_POINT('Ctrl Pts',(70.2354503645211,450.624033419625,52.1145910364302));
#36866=CARTESIAN_POINT('Ctrl Pts',(70.3621002044194,450.597780373594,51.6787128073921));
#36867=CARTESIAN_POINT('Ctrl Pts',(70.5833207289459,450.551923919152,50.9173600055655));
#36868=CARTESIAN_POINT('Ctrl Pts',(70.9964862209847,450.50606746471,50.2117792010199));
#36869=CARTESIAN_POINT('Ctrl Pts',(71.5522141045377,450.460211010269,49.6463031814024));
#36870=CARTESIAN_POINT('Ctrl Pts',(72.1079419880908,450.414354555827,49.0808271617849));
#36871=CARTESIAN_POINT('Ctrl Pts',(72.8062322631582,450.368498101386,48.6554559270955));
#36872=CARTESIAN_POINT('Ctrl Pts',(73.5636235244637,450.322641646944,48.4210309143108));
#36873=CARTESIAN_POINT('Ctrl Pts',(74.3210147857691,450.276785192502,48.1866059015262));
#36874=CARTESIAN_POINT('Ctrl Pts',(75.1375070333125,450.23092873806,48.1431271106463));
#36875=CARTESIAN_POINT('Ctrl Pts',(75.915511065568,450.185072283619,48.29579123582));
#36876=CARTESIAN_POINT('Ctrl Pts',(76.6935150978235,450.139215829177,48.4484553609936));
#36877=CARTESIAN_POINT('Ctrl Pts',(77.4330309147911,450.093359374735,48.7972624022208));
#36878=CARTESIAN_POINT('Ctrl Pts',(78.045669731016,450.047502920294,49.3005220669819));
#36879=CARTESIAN_POINT('Ctrl Pts',(78.6583085472408,450.001646465852,49.8037817317431));
#36880=CARTESIAN_POINT('Ctrl Pts',(79.1440703627228,449.95579001141,50.4614940200382));
#36881=CARTESIAN_POINT('Ctrl Pts',(79.4448957067846,449.909933556968,51.1950475093565));
#36882=CARTESIAN_POINT('Ctrl Pts',(79.7457210508463,449.864077102526,51.9286009986747));
#36883=CARTESIAN_POINT('Ctrl Pts',(79.8616099234878,449.818220648085,52.7379956890161));
#36884=CARTESIAN_POINT('Ctrl Pts',(79.7787109959537,449.772364193643,53.526490696695));
#36885=CARTESIAN_POINT('Ctrl Pts',(79.6958120684197,449.726507739201,54.3149857043739));
#36886=CARTESIAN_POINT('Ctrl Pts',(79.4141253407101,449.68065128476,55.0825810293903));
#36887=CARTESIAN_POINT('Ctrl Pts',(78.9673187171074,449.634794830318,55.7375317530525));
#36888=CARTESIAN_POINT('Ctrl Pts',(78.5205120935046,449.588938375876,56.3924824767147));
#36889=CARTESIAN_POINT('Ctrl Pts',(77.9085855740088,449.543081921434,56.9347885990226));
#36890=CARTESIAN_POINT('Ctrl Pts',(77.2046781511943,449.497225466993,57.2996323319104));
#36891=CARTESIAN_POINT('Ctrl Pts',(76.5007707283798,449.451369012551,57.6644760647982));
#36892=CARTESIAN_POINT('Ctrl Pts',(75.7048824022466,449.405512558109,57.8518574082658));
#36893=CARTESIAN_POINT('Ctrl Pts',(74.9121397419505,449.359656103667,57.8393800741124));
#36894=CARTESIAN_POINT('Ctrl Pts',(74.1193970816544,449.313799649226,57.826902739959));
#36895=CARTESIAN_POINT('Ctrl Pts',(73.3298000871955,449.267943194784,57.6145667281844));
#36896=CARTESIAN_POINT('Ctrl Pts',(72.6377233719866,449.222086740342,57.2277509715424));
#36897=CARTESIAN_POINT('Ctrl Pts',(71.9456466567777,449.1762302859,56.8409352149004));
#36898=CARTESIAN_POINT('Ctrl Pts',(71.3510902208188,449.130373831459,56.2796397133909));
#36899=CARTESIAN_POINT('Ctrl Pts',(70.9251169407287,449.084517377017,55.6109519133151));
#36900=CARTESIAN_POINT('Ctrl Pts',(70.4991436606386,449.038660922575,54.9422641132394));
#36901=CARTESIAN_POINT('Ctrl Pts',(70.2417535364173,448.992804468134,54.1661840145974));
#36902=CARTESIAN_POINT('Ctrl Pts',(70.1837104813523,448.946948013692,53.375470657508));
#36903=CARTESIAN_POINT('Ctrl Pts',(70.1750997574451,448.94014517969,53.2581678311825));
#36904=CARTESIAN_POINT('Ctrl Pts',(70.1708762459027,448.933342345689,53.1405429574215));
#36905=CARTESIAN_POINT('Ctrl Pts',(70.1709848060094,448.926539511687,53.0229103046436));
#36906=CARTESIAN_POINT('Origin',(74.9879498948689,416.,53.0228109606356));
#36907=CARTESIAN_POINT('',(70.1708368207108,453.948460488313,53.0228652461544));
#36908=CARTESIAN_POINT('',(70.1713277050038,452.426539511687,53.0226981617181));
#36909=CARTESIAN_POINT('',(70.1711998948689,416.,53.0228109606356));
#36910=CARTESIAN_POINT('Ctrl Pts',(70.1711297808103,452.198460488313,53.0226941375257));
#36911=CARTESIAN_POINT('Ctrl Pts',(70.1717580107066,452.2347132426,53.6496208239294));
#36912=CARTESIAN_POINT('Ctrl Pts',(70.4504739081369,452.316822467244,55.0700956568864));
#36913=CARTESIAN_POINT('Ctrl Pts',(71.808425912791,452.444788162243,56.9037142545098));
#36914=CARTESIAN_POINT('Ctrl Pts',(74.0283409358903,452.582357573312,57.9472331376422));
#36915=CARTESIAN_POINT('Ctrl Pts',(76.4776458542147,452.719926984381,57.8135926372266));
#36916=CARTESIAN_POINT('Ctrl Pts',(78.5708461358004,452.85749639545,56.5347388738669));
#36917=CARTESIAN_POINT('Ctrl Pts',(79.8075723404659,452.995065806519,54.4163756677902));
#36918=CARTESIAN_POINT('Ctrl Pts',(79.8921910382349,453.132635217588,51.9648875470652));
#36919=CARTESIAN_POINT('Ctrl Pts',(78.8044745207126,453.270204628657,49.7662908954556));
#36920=CARTESIAN_POINT('Ctrl Pts',(76.8044362136501,453.407774039726,48.3461497189478));
#36921=CARTESIAN_POINT('Ctrl Pts',(74.3701755523407,453.545343450795,48.0439417574817));
#36922=CARTESIAN_POINT('Ctrl Pts',(72.0835909843443,453.682912861864,48.9319087309295));
#36923=CARTESIAN_POINT('Ctrl Pts',(70.5282839091672,453.817285207704,50.7544233060067));
#36924=CARTESIAN_POINT('Ctrl Pts',(70.1712626194858,453.905801083187,52.2852768041585));
#36925=CARTESIAN_POINT('Ctrl Pts',(70.170836820711,453.948460488313,53.0228652461544));
#36926=CARTESIAN_POINT('Ctrl Pts',(70.1713277050038,452.426539511687,53.0226981617181));
#36927=CARTESIAN_POINT('Ctrl Pts',(70.1711195125453,452.413087040065,52.7900341625413));
#36928=CARTESIAN_POINT('Ctrl Pts',(70.1876817062971,452.399634568443,52.5573995506344));
#36929=CARTESIAN_POINT('Ctrl Pts',(70.2212656740082,452.386182096821,52.327248783187));
#36930=CARTESIAN_POINT('Ctrl Pts',(70.3357458772472,452.34032564238,51.5427165069643));
#36931=CARTESIAN_POINT('Ctrl Pts',(70.648014834751,452.294469187938,50.7870458818604));
#36932=CARTESIAN_POINT('Ctrl Pts',(71.1207493774869,452.248612733496,50.1505565564186));
#36933=CARTESIAN_POINT('Ctrl Pts',(71.5934839202227,452.202756279055,49.5140672309767));
#36934=CARTESIAN_POINT('Ctrl Pts',(72.2266840481906,452.156899824613,48.996759205197));
#36935=CARTESIAN_POINT('Ctrl Pts',(72.944668093738,452.111043370171,48.6604624319896));
#36936=CARTESIAN_POINT('Ctrl Pts',(73.6626521392853,452.06518691573,48.3241656587821));
#36937=CARTESIAN_POINT('Ctrl Pts',(74.4654201024121,452.019330461288,48.1688801381469));
#36938=CARTESIAN_POINT('Ctrl Pts',(75.2570231425062,451.973474006846,48.213165985009));
#36939=CARTESIAN_POINT('Ctrl Pts',(76.0486261826002,451.927617552404,48.2574518318711));
#36940=CARTESIAN_POINT('Ctrl Pts',(76.8290642996615,451.881761097963,48.5013090462306));
#36941=CARTESIAN_POINT('Ctrl Pts',(77.5050575722715,451.835904643521,48.9155912021425));
#36942=CARTESIAN_POINT('Ctrl Pts',(78.1810508448815,451.790048189079,49.3298733580543));
#36943=CARTESIAN_POINT('Ctrl Pts',(78.7525992730403,451.744191734637,49.9145804555185));
#36944=CARTESIAN_POINT('Ctrl Pts',(79.1513899549379,451.698335280196,50.5998268355549));
#36945=CARTESIAN_POINT('Ctrl Pts',(79.5501806368354,451.652478825754,51.2850732155913));
#36946=CARTESIAN_POINT('Ctrl Pts',(79.7762135724718,451.606622371312,52.0708588781999));
#36947=CARTESIAN_POINT('Ctrl Pts',(79.8024727383945,451.560765916871,52.8632647499131));
#36948=CARTESIAN_POINT('Ctrl Pts',(79.8287319043172,451.514909462429,53.6556706216263));
#36949=CARTESIAN_POINT('Ctrl Pts',(79.6552173005262,451.469053007987,54.454696702444));
#36950=CARTESIAN_POINT('Ctrl Pts',(79.3026678277135,451.423196553545,55.1648413908988));
#36951=CARTESIAN_POINT('Ctrl Pts',(78.9501183549008,451.377340099104,55.8749860793536));
#36952=CARTESIAN_POINT('Ctrl Pts',(78.4185340130663,451.331483644662,56.4962493754455));
#36953=CARTESIAN_POINT('Ctrl Pts',(77.7714510961788,451.28562719022,56.9543763316412));
#36954=CARTESIAN_POINT('Ctrl Pts',(77.1243681792913,451.239770735778,57.4125032878369));
#36955=CARTESIAN_POINT('Ctrl Pts',(76.3617866873508,451.193914281337,57.7074939041364));
#36956=CARTESIAN_POINT('Ctrl Pts',(75.5748522731433,451.148057826895,57.8040901621213));
#36957=CARTESIAN_POINT('Ctrl Pts',(74.7879178589357,451.102201372453,57.9006864201062));
#36958=CARTESIAN_POINT('Ctrl Pts',(73.9766305224611,451.056344918012,57.7988883197764));
#36959=CARTESIAN_POINT('Ctrl Pts',(73.2379573612182,451.01048846357,57.5108630254351));
#36960=CARTESIAN_POINT('Ctrl Pts',(72.4992841999754,450.964632009128,57.2228377310937));
#36961=CARTESIAN_POINT('Ctrl Pts',(71.8332252139645,450.918775554686,56.7485852427409));
#36962=CARTESIAN_POINT('Ctrl Pts',(71.3193894439442,450.872919100245,56.1447894074054));
#36963=CARTESIAN_POINT('Ctrl Pts',(70.8055536739239,450.827062645803,55.5409935720698));
#36964=CARTESIAN_POINT('Ctrl Pts',(70.4439411198943,450.781206191361,54.8076543897516));
#36965=CARTESIAN_POINT('Ctrl Pts',(70.2777726213865,450.735349736919,54.0324223990388));
#36966=CARTESIAN_POINT('Ctrl Pts',(70.2067364067263,450.715746328508,53.7010145413626));
#36967=CARTESIAN_POINT('Ctrl Pts',(70.17141799168,450.696142920097,53.361950687542));
#36968=CARTESIAN_POINT('Ctrl Pts',(70.1715440079096,450.676539511686,53.0228609587722));
#36969=CARTESIAN_POINT('Origin',(74.9879498948689,416.,53.0228109606356));
#36970=CARTESIAN_POINT('',(70.1711998948689,455.,53.0228109606356));
#36971=CARTESIAN_POINT('',(70.170785177935,454.176539511687,53.0227998720929));
#36972=CARTESIAN_POINT('',(70.1711998948689,416.,53.0228109606356));
#36973=CARTESIAN_POINT('',(78.8686068361682,455.,50.1705810192547));
#36974=CARTESIAN_POINT('Origin',(74.9879498948689,455.,53.0228109606356));
#36975=CARTESIAN_POINT('Ctrl Pts',(70.170836820711,453.948460488313,53.0228652461544));
#36976=CARTESIAN_POINT('Ctrl Pts',(70.1708049096598,453.951657553543,53.0781430531125));
#36977=CARTESIAN_POINT('Ctrl Pts',(70.1851065053738,454.000711089129,53.9262705456493));
#36978=CARTESIAN_POINT('Ctrl Pts',(70.6550604420902,454.095621095071,55.5520112648156));
#36979=CARTESIAN_POINT('Ctrl Pts',(72.3720044217823,454.23319050614,57.3038901381464));
#36980=CARTESIAN_POINT('Ctrl Pts',(74.714270628573,454.370759917209,58.0323860252404));
#36981=CARTESIAN_POINT('Ctrl Pts',(77.1219697739619,454.508329328278,57.5633975942407));
#36982=CARTESIAN_POINT('Ctrl Pts',(79.0195060859316,454.645898739347,56.0089503824907));
#36983=CARTESIAN_POINT('Ctrl Pts',(79.9533662831374,454.783468150416,53.7408355040756));
#36984=CARTESIAN_POINT('Ctrl Pts',(79.7360467608705,454.901501903967,51.6473349742381));
#36985=CARTESIAN_POINT('Ctrl Pts',(79.1381333147689,454.973679187162,50.53747892867));
#36986=CARTESIAN_POINT('Ctrl Pts',(78.8686068361681,455.,50.1705810192548));
#36987=CARTESIAN_POINT('Ctrl Pts',(70.170785177935,454.176539511687,53.0227998720929));
#36988=CARTESIAN_POINT('Ctrl Pts',(70.1707835943913,454.175887614474,53.011528810388));
#36989=CARTESIAN_POINT('Ctrl Pts',(70.1708223389548,454.175235717261,53.0002577591952));
#36990=CARTESIAN_POINT('Ctrl Pts',(70.1709014783631,454.174583820049,52.9889869912234));
#36991=CARTESIAN_POINT('Ctrl Pts',(70.176468387687,454.128727365607,52.1961665157228));
#36992=CARTESIAN_POINT('Ctrl Pts',(70.3819149747748,454.082870911166,51.4047474592887));
#36993=CARTESIAN_POINT('Ctrl Pts',(70.7626840229485,454.037014456724,50.7093250836825));
#36994=CARTESIAN_POINT('Ctrl Pts',(71.1434530711222,453.991158002282,50.0139027080763));
#36995=CARTESIAN_POINT('Ctrl Pts',(71.6995445803816,453.94530154784,49.4144770132978));
#36996=CARTESIAN_POINT('Ctrl Pts',(72.3644939934935,453.899445093399,48.9826915707525));
#36997=CARTESIAN_POINT('Ctrl Pts',(73.0294434066053,453.853588638957,48.5509061282073));
#36998=CARTESIAN_POINT('Ctrl Pts',(73.8032507235696,453.807732184515,48.2867609378952));
#36999=CARTESIAN_POINT('Ctrl Pts',(74.593428185032,453.761875730073,48.221827889203));
#37000=CARTESIAN_POINT('Ctrl Pts',(75.3836056464944,453.716019275632,48.1568948405108));
#37001=CARTESIAN_POINT('Ctrl Pts',(76.1901532524549,453.67016282119,48.2911739334386));
#37002=CARTESIAN_POINT('Ctrl Pts',(76.9166705917121,453.624306366748,48.6086155257678));
#37003=CARTESIAN_POINT('Ctrl Pts',(77.6431879309693,453.578449912306,48.926057118097));
#37004=CARTESIAN_POINT('Ctrl Pts',(78.2896750035234,453.532593457865,49.4266612098278));
#37005=CARTESIAN_POINT('Ctrl Pts',(78.7788619752273,453.486737003423,50.0505944670632));
#37006=CARTESIAN_POINT('Ctrl Pts',(79.2680489469312,453.440880548981,50.6745277242986));
#37007=CARTESIAN_POINT('Ctrl Pts',(79.5999358177851,453.39502409454,51.4217901470387));
#37008=CARTESIAN_POINT('Ctrl Pts',(79.7348546736815,453.349167640098,52.2030670004071));
#37009=CARTESIAN_POINT('Ctrl Pts',(79.869773529578,453.303311185656,52.9843438537755));
#37010=CARTESIAN_POINT('Ctrl Pts',(79.8077243705171,453.257454731214,53.7996351377721));
#37011=CARTESIAN_POINT('Ctrl Pts',(79.5561234513778,453.211598276773,54.5514952184914));
#37012=CARTESIAN_POINT('Ctrl Pts',(79.3045225322384,453.165741822331,55.3033552992107));
#37013=CARTESIAN_POINT('Ctrl Pts',(78.8633698530205,453.119885367889,55.9917841766527));
#37014=CARTESIAN_POINT('Ctrl Pts',(78.2853930961865,453.074028913447,56.5344990929728));
#37015=CARTESIAN_POINT('Ctrl Pts',(77.7074163393524,453.028172459006,57.0772140092928));
#37016=CARTESIAN_POINT('Ctrl Pts',(76.9926155049022,452.982316004564,57.474214964491));
#37017=CARTESIAN_POINT('Ctrl Pts',(76.2264253781918,452.936459550122,57.6780514138309));
#37018=CARTESIAN_POINT('Ctrl Pts',(75.4602352514814,452.890603095681,57.8818878631709));
#37019=CARTESIAN_POINT('Ctrl Pts',(74.6426558325109,452.844746641239,57.8925598066526));
#37020=CARTESIAN_POINT('Ctrl Pts',(73.8714062658395,452.798890186797,57.7087917044262));
#37021=CARTESIAN_POINT('Ctrl Pts',(73.1001566991681,452.753033732355,57.5250236021999));
#37022=CARTESIAN_POINT('Ctrl Pts',(72.3752369847958,452.707177277914,57.1468154542655));
#37023=CARTESIAN_POINT('Ctrl Pts',(71.7832913446759,452.661320823472,56.6193716482587));
#37024=CARTESIAN_POINT('Ctrl Pts',(71.191345704556,452.61546436903,56.0919278422518));
#37025=CARTESIAN_POINT('Ctrl Pts',(70.7323741386884,452.569607914589,55.4152483781723));
#37026=CARTESIAN_POINT('Ctrl Pts',(70.4612340802417,452.523751460147,54.6702116824618));
#37027=CARTESIAN_POINT('Ctrl Pts',(70.2696358002897,452.491347477327,54.143739311625));
#37028=CARTESIAN_POINT('Ctrl Pts',(70.1718291938781,452.458943494507,53.583133481278));
#37029=CARTESIAN_POINT('Ctrl Pts',(70.1713277050038,452.426539511687,53.0226981617181));
#37030=CARTESIAN_POINT('Origin',(74.9879498948689,433.764859435991,53.0228109606356));
#37031=CARTESIAN_POINT('',(70.0693291699032,453.889859435991,53.0228663900751));
#37032=CARTESIAN_POINT('',(70.0692764388954,454.235140564009,53.0227996384331));
#37033=CARTESIAN_POINT('',(70.0696998948689,433.764859435991,53.0228109606359));
#37034=CARTESIAN_POINT('',(78.2551164949133,455.,49.3465621292785));
#37035=CARTESIAN_POINT('Ctrl Pts',(70.069329169903,453.88985943599,53.0228663900751));
#37036=CARTESIAN_POINT('Ctrl Pts',(70.0692965864127,453.89305650122,53.079309027553));
#37037=CARTESIAN_POINT('Ctrl Pts',(70.0838995496389,453.942110036806,53.9453085168704));
#37038=CARTESIAN_POINT('Ctrl Pts',(70.5637564965961,454.037020042748,55.6053073318474));
#37039=CARTESIAN_POINT('Ctrl Pts',(72.3168804345463,454.174589453817,57.394102321988));
#37040=CARTESIAN_POINT('Ctrl Pts',(74.708503577028,454.312158864886,58.1379492928087));
#37041=CARTESIAN_POINT('Ctrl Pts',(77.1669384806062,454.449728275955,57.6590781969942));
#37042=CARTESIAN_POINT('Ctrl Pts',(79.104460246599,454.587297687024,56.0718752075947));
#37043=CARTESIAN_POINT('Ctrl Pts',(80.0579990258397,454.724867098093,53.7559659325096));
#37044=CARTESIAN_POINT('Ctrl Pts',(79.7993775020766,454.862434535752,51.2645915204101));
#37045=CARTESIAN_POINT('Ctrl Pts',(78.8603576798458,454.954145503054,49.884454297563));
#37046=CARTESIAN_POINT('Ctrl Pts',(78.2551164948972,455.,49.3465621292932));
#37047=CARTESIAN_POINT('',(79.5259634688001,455.,54.9172708347097));
#37048=CARTESIAN_POINT('Origin',(74.9879498948689,455.,53.0228109606356));
#37049=CARTESIAN_POINT('Ctrl Pts',(70.0692764388952,454.23514056401,53.0227996384331));
#37050=CARTESIAN_POINT('Ctrl Pts',(70.0693885605861,454.280345121239,53.8208391932592));
#37051=CARTESIAN_POINT('Ctrl Pts',(70.4684746883736,454.37140613291,55.4285308409564));
#37052=CARTESIAN_POINT('Ctrl Pts',(72.1379853470107,454.508323599022,57.2796485035691));
#37053=CARTESIAN_POINT('Ctrl Pts',(74.4967427405941,454.645892962347,58.121944651965));
#37054=CARTESIAN_POINT('Ctrl Pts',(76.9728107558315,454.783462325672,57.745441606262));
#37055=CARTESIAN_POINT('Ctrl Pts',(78.6902915766538,454.90149800489,56.4535249040052));
#37056=CARTESIAN_POINT('Ctrl Pts',(79.3467648647433,454.973677229666,55.3462294167141));
#37057=CARTESIAN_POINT('Ctrl Pts',(79.5259634688003,455.,54.9172708347098));
#37058=CARTESIAN_POINT('Origin',(74.9879498948689,433.764859435991,53.0228109606356));
#37059=CARTESIAN_POINT('',(70.0696283033456,452.139859435991,53.0226916757941));
#37060=CARTESIAN_POINT('',(70.0698303982574,452.485140564009,53.0226957847854));
#37061=CARTESIAN_POINT('',(70.0696998948689,433.764859435991,53.0228109606359));
#37062=CARTESIAN_POINT('Ctrl Pts',(70.0696283033454,452.139859435991,53.0226916757941));
#37063=CARTESIAN_POINT('Ctrl Pts',(70.0702697714904,452.176112190277,53.6628291492784));
#37064=CARTESIAN_POINT('Ctrl Pts',(70.3548588538668,452.258221414921,55.1132366537557));
#37065=CARTESIAN_POINT('Ctrl Pts',(71.7414260302598,452.38618710992,56.9854938121638));
#37066=CARTESIAN_POINT('Ctrl Pts',(74.0081197682281,452.523756520989,58.0510020380353));
#37067=CARTESIAN_POINT('Ctrl Pts',(76.509037174062,452.661325932058,57.9145454249311));
#37068=CARTESIAN_POINT('Ctrl Pts',(78.646345999496,452.798895343127,56.6087432716859));
#37069=CARTESIAN_POINT('Ctrl Pts',(79.9091328695011,452.936464754196,54.4457412810724));
#37070=CARTESIAN_POINT('Ctrl Pts',(79.9955346778371,453.074034165265,51.9425946677425));
#37071=CARTESIAN_POINT('Ctrl Pts',(78.884897471774,453.211603576334,49.6976685283788));
#37072=CARTESIAN_POINT('Ctrl Pts',(76.842713757919,453.349172987403,48.2476017112594));
#37073=CARTESIAN_POINT('Ctrl Pts',(74.357157626194,453.486742398472,47.9390255330312));
#37074=CARTESIAN_POINT('Ctrl Pts',(72.0223894626918,453.624311809541,48.8457040127446));
#37075=CARTESIAN_POINT('Ctrl Pts',(70.4343084905653,453.75868415538,50.7066231613146));
#37076=CARTESIAN_POINT('Ctrl Pts',(70.0697639412373,453.847200030864,52.2697352633099));
#37077=CARTESIAN_POINT('Ctrl Pts',(70.069329169903,453.88985943599,53.0228663900751));
#37078=CARTESIAN_POINT('Ctrl Pts',(70.0698303982571,452.485140564009,53.0226957847854));
#37079=CARTESIAN_POINT('Ctrl Pts',(70.0703424546553,452.517544546829,53.5949407654106));
#37080=CARTESIAN_POINT('Ctrl Pts',(70.3115375997815,452.595804984091,54.9774179780456));
#37081=CARTESIAN_POINT('Ctrl Pts',(71.5799856751815,452.719921875795,56.8475398498696));
#37082=CARTESIAN_POINT('Ctrl Pts',(73.8005719949271,452.85749123912,58.0060734400985));
#37083=CARTESIAN_POINT('Ctrl Pts',(76.304995087688,452.995060602445,57.9733829624763));
#37084=CARTESIAN_POINT('Ctrl Pts',(78.4945850834537,453.13262996577,56.7572829274506));
#37085=CARTESIAN_POINT('Ctrl Pts',(79.8459314256328,453.270199329095,54.6484759560617));
#37086=CARTESIAN_POINT('Ctrl Pts',(80.0360014582592,453.407768692421,52.1510619170208));
#37087=CARTESIAN_POINT('Ctrl Pts',(79.0193599867834,453.545338055746,49.8620350354254));
#37088=CARTESIAN_POINT('Ctrl Pts',(77.0390298609172,453.682907419071,48.3285761217461));
#37089=CARTESIAN_POINT('Ctrl Pts',(74.5683996041992,453.820476782396,47.9172501350589));
#37090=CARTESIAN_POINT('Ctrl Pts',(72.1980599540245,453.958046145721,48.726384145908));
#37091=CARTESIAN_POINT('Ctrl Pts',(70.4946310452694,454.095615509047,50.562555064065));
#37092=CARTESIAN_POINT('Ctrl Pts',(70.0720972254101,454.187980315143,52.1902351426901));
#37093=CARTESIAN_POINT('Ctrl Pts',(70.0692748219826,454.234488666797,53.0112910695366));
#37094=CARTESIAN_POINT('Ctrl Pts',(70.0692764388952,454.23514056401,53.0227996384331));
#37095=CARTESIAN_POINT('Origin',(74.9879498948689,433.764859435991,53.0228109606356));
#37096=CARTESIAN_POINT('',(70.0700844373669,450.389859435991,53.0228026766897));
#37097=CARTESIAN_POINT('',(70.0700512591628,450.735140564009,53.0228620123491));
#37098=CARTESIAN_POINT('',(70.0696998948689,433.764859435991,53.0228109606359));
#37099=CARTESIAN_POINT('Ctrl Pts',(70.0700844373667,450.389859435991,53.0228026766897));
#37100=CARTESIAN_POINT('Ctrl Pts',(70.070109202443,450.413311408979,53.4370190990291));
#37101=CARTESIAN_POINT('Ctrl Pts',(70.2231586879711,450.482619852323,54.6611854827153));
#37102=CARTESIAN_POINT('Ctrl Pts',(71.2275935581432,450.597784766023,56.5016746841243));
#37103=CARTESIAN_POINT('Ctrl Pts',(73.326328990768,450.735354177093,57.8686120870556));
#37104=CARTESIAN_POINT('Ctrl Pts',(75.8222668904432,450.872923588161,58.0771840905751));
#37105=CARTESIAN_POINT('Ctrl Pts',(78.1187653342674,451.01049299923,57.0775325626919));
#37106=CARTESIAN_POINT('Ctrl Pts',(79.6668574398354,451.148062410299,55.1086193821872));
#37107=CARTESIAN_POINT('Ctrl Pts',(80.096479252104,451.285631821368,52.6411037534401));
#37108=CARTESIAN_POINT('Ctrl Pts',(79.304931747903,451.423201232437,50.2648333925011));
#37109=CARTESIAN_POINT('Ctrl Pts',(77.4814305423453,451.560770643506,48.547844274008));
#37110=CARTESIAN_POINT('Ctrl Pts',(75.0618748081809,451.698340054575,47.9005743697575));
#37111=CARTESIAN_POINT('Ctrl Pts',(72.6246476798502,451.835909465644,48.4777504300927));
#37112=CARTESIAN_POINT('Ctrl Pts',(70.7523565534021,451.973478876713,50.1414013001772));
#37113=CARTESIAN_POINT('Ctrl Pts',(70.1191391310378,452.074795533495,51.8739168896172));
#37114=CARTESIAN_POINT('Ctrl Pts',(70.069458372038,452.130255719921,52.8531128765635));
#37115=CARTESIAN_POINT('Ctrl Pts',(70.0696283033454,452.139859435991,53.0226916757941));
#37116=CARTESIAN_POINT('Ctrl Pts',(70.0700512591626,450.735140564009,53.0228620123491));
#37117=CARTESIAN_POINT('Ctrl Pts',(70.0699225874812,450.75474397242,53.3690971415379));
#37118=CARTESIAN_POINT('Ctrl Pts',(70.1903433030529,450.820203835273,54.5251601145759));
#37119=CARTESIAN_POINT('Ctrl Pts',(71.0866535291021,450.931520152567,56.3428497963907));
#37120=CARTESIAN_POINT('Ctrl Pts',(73.1269366710226,451.069089515892,57.7955880332776));
#37121=CARTESIAN_POINT('Ctrl Pts',(75.6120857503499,451.206658879218,58.1074176945308));
#37122=CARTESIAN_POINT('Ctrl Pts',(77.9480382636025,451.344228242543,57.2037974535288));
#37123=CARTESIAN_POINT('Ctrl Pts',(79.5763964029459,451.481797605868,55.300733225987));
#37124=CARTESIAN_POINT('Ctrl Pts',(80.1079092695645,451.619366969193,52.8531430321954));
#37125=CARTESIAN_POINT('Ctrl Pts',(79.4155213613108,451.756936332518,50.4461111112164));
#37126=CARTESIAN_POINT('Ctrl Pts',(77.6647445573712,451.894505695844,48.6550264490875));
#37127=CARTESIAN_POINT('Ctrl Pts',(75.2740933282832,452.032075059169,47.9080389090301));
#37128=CARTESIAN_POINT('Ctrl Pts',(72.8150409373668,452.169644422494,48.3837121400662));
#37129=CARTESIAN_POINT('Ctrl Pts',(70.8754116046977,452.307213785819,49.96833882681));
#37130=CARTESIAN_POINT('Ctrl Pts',(70.1441754893215,452.412379166324,51.7378828020483));
#37131=CARTESIAN_POINT('Ctrl Pts',(70.0696178187047,452.471688092388,52.7851290200683));
#37132=CARTESIAN_POINT('Ctrl Pts',(70.0698303982571,452.485140564009,53.0226957847854));
#37133=CARTESIAN_POINT('Origin',(74.9879498948689,433.764859435991,53.0228109606356));
#37134=CARTESIAN_POINT('',(70.0696851641772,448.639859435991,53.0229323847884));
#37135=CARTESIAN_POINT('',(70.0694802735924,448.985140564009,53.0229123980504));
#37136=CARTESIAN_POINT('',(70.0696998948689,433.764859435991,53.0228109606359));
#37137=CARTESIAN_POINT('Ctrl Pts',(70.0696851641769,448.639859435991,53.0229323847884));
#37138=CARTESIAN_POINT('Ctrl Pts',(70.0694979672956,448.65051062768,53.2110133783555));
#37139=CARTESIAN_POINT('Ctrl Pts',(70.125662917046,448.707018289725,54.2087264689964));
#37140=CARTESIAN_POINT('Ctrl Pts',(70.7851350758139,448.809382422127,55.9518244775881));
#37141=CARTESIAN_POINT('Ctrl Pts',(72.6760768504256,448.946951833196,57.594245703923));
#37142=CARTESIAN_POINT('Ctrl Pts',(75.1196607316056,449.084521244265,58.1438874921126));
#37143=CARTESIAN_POINT('Ctrl Pts',(77.5317597721941,449.222090655334,57.469360622315));
#37144=CARTESIAN_POINT('Ctrl Pts',(79.3357733243977,449.359660066403,55.7319074911046));
#37145=CARTESIAN_POINT('Ctrl Pts',(80.1004606450606,449.497229477472,53.3468578938625));
#37146=CARTESIAN_POINT('Ctrl Pts',(79.6430269164599,449.634798888541,50.8843464393459));
#37147=CARTESIAN_POINT('Ctrl Pts',(78.0728194662947,449.77236829961,48.9330246198776));
#37148=CARTESIAN_POINT('Ctrl Pts',(75.7651888161234,449.909937710679,47.9593465097831));
#37149=CARTESIAN_POINT('Ctrl Pts',(73.2717629486147,450.047507121747,48.1960651675296));
#37150=CARTESIAN_POINT('Ctrl Pts',(71.1885832974899,450.185076532817,49.586594139118));
#37151=CARTESIAN_POINT('Ctrl Pts',(70.2139236445014,450.299193970897,51.4214564705422));
#37152=CARTESIAN_POINT('Ctrl Pts',(70.0700607784154,450.367454938622,52.627087111563));
#37153=CARTESIAN_POINT('Ctrl Pts',(70.0700844373667,450.389859435991,53.0228026766897));
#37154=CARTESIAN_POINT('Ctrl Pts',(70.0694802735922,448.985140564009,53.0229123980504));
#37155=CARTESIAN_POINT('Ctrl Pts',(70.0693694258745,448.991943398011,53.1430238413523));
#37156=CARTESIAN_POINT('Ctrl Pts',(70.102751651847,449.044602686455,54.0727194457198));
#37157=CARTESIAN_POINT('Ctrl Pts',(70.6673681160653,449.14311842934,55.7751452966382));
#37158=CARTESIAN_POINT('Ctrl Pts',(72.4886234383188,449.280687792665,57.4945151623977));
#37159=CARTESIAN_POINT('Ctrl Pts',(74.9073302954306,449.41825715599,58.1449464220086));
#37160=CARTESIAN_POINT('Ctrl Pts',(77.3453088660466,449.555826519316,57.5709567240733));
#37161=CARTESIAN_POINT('Ctrl Pts',(79.2197725217338,449.693395882641,55.9097554455925));
#37162=CARTESIAN_POINT('Ctrl Pts',(80.0826400663797,449.830965245966,53.5584444741309));
#37163=CARTESIAN_POINT('Ctrl Pts',(79.7276473132564,449.968534609291,51.0790929804237));
#37164=CARTESIAN_POINT('Ctrl Pts',(78.2396535110072,450.106103972616,49.0643775840001));
#37165=CARTESIAN_POINT('Ctrl Pts',(75.9743561631267,450.243673335941,47.9959059606967));
#37166=CARTESIAN_POINT('Ctrl Pts',(73.4732633122539,450.381242699267,48.1290909276837));
#37167=CARTESIAN_POINT('Ctrl Pts',(71.3342487410075,450.518812062591,49.4320952822867));
#37168=CARTESIAN_POINT('Ctrl Pts',(70.2489813568954,450.636778017506,51.2854539213402));
#37169=CARTESIAN_POINT('Ctrl Pts',(70.0702235773382,450.708887517979,52.5591810751596));
#37170=CARTESIAN_POINT('Ctrl Pts',(70.0700512591626,450.735140564009,53.0228620123491));
#37171=CARTESIAN_POINT('Origin',(74.9879498948689,433.764859435991,53.0228109606356));
#37172=CARTESIAN_POINT('',(70.0693009119067,446.889859435991,53.0227729814362));
#37173=CARTESIAN_POINT('',(70.0694411284499,447.235140564009,53.0227177812969));
#37174=CARTESIAN_POINT('',(70.0696998948689,433.764859435991,53.0228109606359));
#37175=CARTESIAN_POINT('Ctrl Pts',(70.0693009119065,446.889859435991,53.0227729814362));
#37176=CARTESIAN_POINT('Ctrl Pts',(70.0696235287826,446.933566316737,53.7943839613808));
#37177=CARTESIAN_POINT('Ctrl Pts',(70.4481879276617,447.02312966784,55.3758608002924));
#37178=CARTESIAN_POINT('Ctrl Pts',(72.069705552325,447.158549489299,57.2331105394031));
#37179=CARTESIAN_POINT('Ctrl Pts',(74.4145546160935,447.296118900368,58.1133895564375));
#37180=CARTESIAN_POINT('Ctrl Pts',(76.8964710571215,447.433688311437,57.7767902999883));
#37181=CARTESIAN_POINT('Ctrl Pts',(78.9221647146049,447.571257722506,56.3037751996861));
#37182=CARTESIAN_POINT('Ctrl Pts',(80.0074032848607,447.708827133575,54.0464614143837));
#37183=CARTESIAN_POINT('Ctrl Pts',(79.8927657192128,447.846396544644,51.5444489227623));
#37184=CARTESIAN_POINT('Ctrl Pts',(78.605655575103,447.983965955713,49.3958317496446));
#37185=CARTESIAN_POINT('Ctrl Pts',(76.4537503277871,448.121535366782,48.1142264725559));
#37186=CARTESIAN_POINT('Ctrl Pts',(73.9514525530772,448.259104777851,48.0059946548279));
#37187=CARTESIAN_POINT('Ctrl Pts',(71.6969244713428,448.39667418892,49.0970085907417));
#37188=CARTESIAN_POINT('Ctrl Pts',(70.3427451701921,448.5235924083,50.969337637145));
#37189=CARTESIAN_POINT('Ctrl Pts',(70.0703039041795,448.604654157323,52.4012701347896));
#37190=CARTESIAN_POINT('Ctrl Pts',(70.0696851641769,448.639859435991,53.0229323847884));
#37191=CARTESIAN_POINT('Ctrl Pts',(70.0694411284497,447.235140564009,53.0227177812969));
#37192=CARTESIAN_POINT('Ctrl Pts',(70.0700541599741,447.274999278044,53.7264505835051));
#37193=CARTESIAN_POINT('Ctrl Pts',(70.3984342289788,447.36071444652,55.2403642068889));
#37194=CARTESIAN_POINT('Ctrl Pts',(71.8977475035859,447.492286069438,57.1085691993689));
#37195=CARTESIAN_POINT('Ctrl Pts',(74.204105003148,447.629855432763,58.0852568507357));
#37196=CARTESIAN_POINT('Ctrl Pts',(76.6978367180401,447.767424796088,57.8517920391255));
#37197=CARTESIAN_POINT('Ctrl Pts',(78.7828285085176,447.904994159413,56.463983364358));
#37198=CARTESIAN_POINT('Ctrl Pts',(79.9606734769448,448.042563522738,54.2535795744433));
#37199=CARTESIAN_POINT('Ctrl Pts',(79.9498136530265,448.180132886064,51.7489666805328));
#37200=CARTESIAN_POINT('Ctrl Pts',(78.7528450235537,448.317702249389,49.5488599139924));
#37201=CARTESIAN_POINT('Ctrl Pts',(76.6558969746985,448.455271612714,48.1791838338476));
#37202=CARTESIAN_POINT('Ctrl Pts',(74.1602344880813,448.592840976039,47.9673526817221));
#37203=CARTESIAN_POINT('Ctrl Pts',(71.8624332448065,448.730410339365,48.9640036389398));
#37204=CARTESIAN_POINT('Ctrl Pts',(70.3884517474718,448.861176868688,50.833629203903));
#37205=CARTESIAN_POINT('Ctrl Pts',(70.07011662672,448.946086943569,52.3333781956913));
#37206=CARTESIAN_POINT('Ctrl Pts',(70.0694802735922,448.985140564009,53.0229123980504));
#37207=CARTESIAN_POINT('Origin',(74.9879498948689,433.764859435991,53.0228109606356));
#37208=CARTESIAN_POINT('',(70.0698995811618,445.139859435991,53.0227057881612));
#37209=CARTESIAN_POINT('',(70.0700330997265,445.485140564009,53.0227485992971));
#37210=CARTESIAN_POINT('',(70.0696998948689,433.764859435991,53.0228109606359));
#37211=CARTESIAN_POINT('Ctrl Pts',(70.0698995811616,445.139859435991,53.0227057881612));
#37212=CARTESIAN_POINT('Ctrl Pts',(70.0703358154751,445.170765535438,53.5685206225869));
#37213=CARTESIAN_POINT('Ctrl Pts',(70.2955540358443,445.247528105242,54.9245313476707));
#37214=CARTESIAN_POINT('Ctrl Pts',(71.5187244149973,445.370147145402,56.7920611719599));
#37215=CARTESIAN_POINT('Ctrl Pts',(73.7203319129862,445.507716556471,57.9862691540494));
#37216=CARTESIAN_POINT('Ctrl Pts',(76.2249573788151,445.64528596754,57.9939863820444));
#37217=CARTESIAN_POINT('Ctrl Pts',(78.4338821687736,445.782855378609,56.813368089795));
#37218=CARTESIAN_POINT('Ctrl Pts',(79.8190734602514,445.920424789678,54.7266353887282));
#37219=CARTESIAN_POINT('Ctrl Pts',(80.0494079525281,446.057994200747,52.2326116716488));
#37220=CARTESIAN_POINT('Ctrl Pts',(79.0698252955847,446.195563611816,49.927481285336));
#37221=CARTESIAN_POINT('Ctrl Pts',(77.1144900013488,446.333133022885,48.3622745364359));
#37222=CARTESIAN_POINT('Ctrl Pts',(74.6508155459415,446.470702433954,47.9111465529761));
#37223=CARTESIAN_POINT('Ctrl Pts',(72.2677314314422,446.608271845023,48.6819373046774));
#37224=CARTESIAN_POINT('Ctrl Pts',(70.5349024274333,446.745841256092,50.4903929780497));
#37225=CARTESIAN_POINT('Ctrl Pts',(70.0788928230404,446.839703786414,52.1373220589989));
#37226=CARTESIAN_POINT('Ctrl Pts',(70.0692850449795,446.887709846381,52.9848236490411));
#37227=CARTESIAN_POINT('Ctrl Pts',(70.0693009119065,446.889859435991,53.0227729814362));
#37228=CARTESIAN_POINT('Ctrl Pts',(70.0700330997263,445.485140564009,53.0227485992971));
#37229=CARTESIAN_POINT('Ctrl Pts',(70.0702510908703,445.512198703635,53.500644033788));
#37230=CARTESIAN_POINT('Ctrl Pts',(70.2567092353932,445.585113297702,54.7886134756791));
#37231=CARTESIAN_POINT('Ctrl Pts',(71.3655237114099,445.70388434621,56.6450754112051));
#37232=CARTESIAN_POINT('Ctrl Pts',(73.5157571125727,445.841453709536,57.9294818907289));
#37233=CARTESIAN_POINT('Ctrl Pts',(76.0179108621497,445.979023072861,58.0409731352117));
#37234=CARTESIAN_POINT('Ctrl Pts',(78.2738575749735,446.116592436186,56.95289771824));
#37235=CARTESIAN_POINT('Ctrl Pts',(79.7443244311198,446.254161799511,54.9253546461714));
#37236=CARTESIAN_POINT('Ctrl Pts',(80.0778036562199,446.391731162836,52.4430179867826));
#37237=CARTESIAN_POINT('Ctrl Pts',(79.1945787032988,446.529300526162,50.0992779485839));
#37238=CARTESIAN_POINT('Ctrl Pts',(77.3057800960881,446.666869889487,48.4543939084407));
#37239=CARTESIAN_POINT('Ctrl Pts',(74.8629157294284,446.804439252812,47.9015671994052));
#37240=CARTESIAN_POINT('Ctrl Pts',(72.4499401569502,446.942008616137,48.5729482914402));
#37241=CARTESIAN_POINT('Ctrl Pts',(70.643663164976,447.079577979463,50.308046880104));
#37242=CARTESIAN_POINT('Ctrl Pts',(70.0983242060101,447.177288628753,52.0013527917544));
#37243=CARTESIAN_POINT('Ctrl Pts',(70.0693488825247,447.229142823602,52.9168235805925));
#37244=CARTESIAN_POINT('Ctrl Pts',(70.0694411284497,447.235140564009,53.0227177812969));
#37245=CARTESIAN_POINT('Origin',(74.9879498948689,433.764859435991,53.0228109606356));
#37246=CARTESIAN_POINT('',(70.0700145679607,443.389859435991,53.0228825250668));
#37247=CARTESIAN_POINT('',(70.0698685442404,443.735140564009,53.0229212964126));
#37248=CARTESIAN_POINT('',(70.0696998948689,433.764859435991,53.0228109606359));
#37249=CARTESIAN_POINT('Ctrl Pts',(70.0700145679605,443.389859435991,53.0228825250668));
#37250=CARTESIAN_POINT('Ctrl Pts',(70.0698463414395,443.407964754139,53.342651567647));
#37251=CARTESIAN_POINT('Ctrl Pts',(70.178392996224,443.471926542644,54.4722069068458));
#37252=CARTESIAN_POINT('Ctrl Pts',(71.0335914159785,443.581744801505,56.279469003198));
#37253=CARTESIAN_POINT('Ctrl Pts',(73.0501694171724,443.719314212574,57.7649391122166));
#37254=CARTESIAN_POINT('Ctrl Pts',(75.5299645002191,443.856883623643,58.1168263466887));
#37255=CARTESIAN_POINT('Ctrl Pts',(77.8801936047136,443.994453034712,57.2510137595351));
#37256=CARTESIAN_POINT('Ctrl Pts',(79.5390457928333,444.132022445781,55.3744696759449));
#37257=CARTESIAN_POINT('Ctrl Pts',(80.1099804457359,444.26959185685,52.9357729129582));
#37258=CARTESIAN_POINT('Ctrl Pts',(79.4565183869152,444.407161267919,50.5178821756897));
#37259=CARTESIAN_POINT('Ctrl Pts',(77.7348665714272,444.544730678988,48.6987825891046));
#37260=CARTESIAN_POINT('Ctrl Pts',(75.3565775663022,444.682300090057,47.9133211401532));
#37261=CARTESIAN_POINT('Ctrl Pts',(72.8901698933421,444.819869501126,48.3492586017812));
#37262=CARTESIAN_POINT('Ctrl Pts',(70.9252264171065,444.957438912195,49.9023862252835));
#37263=CARTESIAN_POINT('Ctrl Pts',(70.1547157841456,445.064102223817,51.6849358258267));
#37264=CARTESIAN_POINT('Ctrl Pts',(70.0696885592305,445.124909065082,52.7586758921829));
#37265=CARTESIAN_POINT('Ctrl Pts',(70.0698995811616,445.139859435991,53.0227057881612));
#37266=CARTESIAN_POINT('Ctrl Pts',(70.0698685442402,443.735140564009,53.0229212964126));
#37267=CARTESIAN_POINT('Ctrl Pts',(70.0696553690848,443.749398129226,53.2747113903876));
#37268=CARTESIAN_POINT('Ctrl Pts',(70.1497848787881,443.809512148883,54.336196850122));
#37269=CARTESIAN_POINT('Ctrl Pts',(70.9020536867909,443.915482622983,56.1128309251798));
#37270=CARTESIAN_POINT('Ctrl Pts',(72.8553514892035,444.053051986308,57.6805781558292));
#37271=CARTESIAN_POINT('Ctrl Pts',(75.3184363133803,444.190621349633,58.1349093489344));
#37272=CARTESIAN_POINT('Ctrl Pts',(77.7025200060835,444.328190712959,57.3672188967954));
#37273=CARTESIAN_POINT('Ctrl Pts',(79.4376992408775,444.465760076284,55.5610193764604));
#37274=CARTESIAN_POINT('Ctrl Pts',(80.1091880683859,444.603329439609,53.1480737826581));
#37275=CARTESIAN_POINT('Ctrl Pts',(79.5564704305387,444.740898802934,50.7051847354578));
#37276=CARTESIAN_POINT('Ctrl Pts',(77.9116707243749,444.878468166259,48.8163126882502));
#37277=CARTESIAN_POINT('Ctrl Pts',(75.567970123329,445.016037529584,47.9329830913412));
#37278=CARTESIAN_POINT('Ctrl Pts',(73.0856185770117,445.15360689291,48.2663514830863));
#37279=CARTESIAN_POINT('Ctrl Pts',(71.0580098525792,445.291176256235,49.7367278106718));
#37280=CARTESIAN_POINT('Ctrl Pts',(70.1838640833086,445.401687479935,51.5489195429218));
#37281=CARTESIAN_POINT('Ctrl Pts',(70.0698816530189,445.466342249193,52.6907365337478));
#37282=CARTESIAN_POINT('Ctrl Pts',(70.0700330997263,445.485140564009,53.0227485992971));
#37283=CARTESIAN_POINT('Origin',(74.9879498948689,433.764859435991,53.0228109606356));
#37284=CARTESIAN_POINT('',(70.0694094802036,441.639859435991,53.0228960008483));
#37285=CARTESIAN_POINT('',(70.0692875054394,441.985140564009,53.0228369856911));
#37286=CARTESIAN_POINT('',(70.0696998948689,433.764859435991,53.0228109606359));
#37287=CARTESIAN_POINT('Ctrl Pts',(70.0694094802034,441.639859435991,53.0228960008483));
#37288=CARTESIAN_POINT('Ctrl Pts',(70.0693331272471,441.64516397284,53.1165494736883));
#37289=CARTESIAN_POINT('Ctrl Pts',(70.0946128328825,441.696324980046,54.0197739441058));
#37290=CARTESIAN_POINT('Ctrl Pts',(70.6235146926476,441.793342457608,55.7050633632576));
#37291=CARTESIAN_POINT('Ctrl Pts',(72.4167872452805,441.930911868677,57.4536004179581));
#37292=CARTESIAN_POINT('Ctrl Pts',(74.8246838346499,442.068481279746,58.1429786121231));
#37293=CARTESIAN_POINT('Ctrl Pts',(77.2716083886679,442.206050690815,57.608405411681));
#37294=CARTESIAN_POINT('Ctrl Pts',(79.1726353884369,442.343620101884,55.9776679632129));
#37295=CARTESIAN_POINT('Ctrl Pts',(80.0733334938275,442.481189512953,53.6405861925782));
#37296=CARTESIAN_POINT('Ctrl Pts',(79.7583951646866,442.618758924023,51.1558282308192));
#37297=CARTESIAN_POINT('Ctrl Pts',(78.3031048903914,442.756328335091,49.1173634905726));
#37298=CARTESIAN_POINT('Ctrl Pts',(76.0553427955826,442.89389774616,48.0124771412913));
#37299=CARTESIAN_POINT('Ctrl Pts',(73.5524255733744,443.031467157229,48.1052869385125));
#37300=CARTESIAN_POINT('Ctrl Pts',(71.3926635200745,443.169036568298,49.3736071476132));
#37301=CARTESIAN_POINT('Ctrl Pts',(70.2634714560322,443.288500661219,51.232524664295));
#37302=CARTESIAN_POINT('Ctrl Pts',(70.0702724192588,443.362108283783,52.5327525367852));
#37303=CARTESIAN_POINT('Ctrl Pts',(70.0700145679605,443.389859435991,53.0228825250668));
#37304=CARTESIAN_POINT('Ctrl Pts',(70.0692875054392,441.985140564009,53.0228369856911));
#37305=CARTESIAN_POINT('Ctrl Pts',(70.0692798613491,441.986597554817,53.0485588210285));
#37306=CARTESIAN_POINT('Ctrl Pts',(70.0756977175085,442.033911000065,53.8838304412508));
#37307=CARTESIAN_POINT('Ctrl Pts',(70.5161341059696,442.127080899755,55.5219377590632));
#37308=CARTESIAN_POINT('Ctrl Pts',(72.2354226533932,442.264650263081,57.3432698470737));
#37309=CARTESIAN_POINT('Ctrl Pts',(74.6126891215678,442.402219626406,58.1318177678819));
#37310=CARTESIAN_POINT('Ctrl Pts',(77.0796598076102,442.539788989731,57.6990830704906));
#37311=CARTESIAN_POINT('Ctrl Pts',(79.0466176623673,442.677358353056,56.1485088279186));
#37312=CARTESIAN_POINT('Ctrl Pts',(80.0433712123539,442.814927716381,53.8507520860707));
#37313=CARTESIAN_POINT('Ctrl Pts',(79.8316514884425,442.952497079707,51.3550801439626));
#37314=CARTESIAN_POINT('Ctrl Pts',(78.4620690355979,443.090066443032,49.2580709429864));
#37315=CARTESIAN_POINT('Ctrl Pts',(76.2620157143041,443.227635806357,48.0610040828726));
#37316=CARTESIAN_POINT('Ctrl Pts',(73.7574033077667,443.365205169682,48.0500324313384));
#37317=CARTESIAN_POINT('Ctrl Pts',(71.5469469308476,443.502774533007,49.2277787070091));
#37318=CARTESIAN_POINT('Ctrl Pts',(70.3028860573773,443.626086331116,51.0966282777811));
#37319=CARTESIAN_POINT('Ctrl Pts',(70.0703410020562,443.703541674784,52.464881605413));
#37320=CARTESIAN_POINT('Ctrl Pts',(70.0698685442402,443.735140564009,53.0229212964126));
#37321=CARTESIAN_POINT('Origin',(74.9879498948689,433.764859435991,53.0228109606356));
#37322=CARTESIAN_POINT('',(70.0695156097612,439.889859435991,53.0227034971274));
#37323=CARTESIAN_POINT('',(70.069722329707,440.235140564009,53.0226894836296));
#37324=CARTESIAN_POINT('',(70.0696998948689,433.764859435991,53.0228109606359));
#37325=CARTESIAN_POINT('Ctrl Pts',(70.0695156097609,439.889859435991,53.0227034971274));
#37326=CARTESIAN_POINT('Ctrl Pts',(70.0701635410552,439.928219661898,53.7000091240524));
#37327=CARTESIAN_POINT('Ctrl Pts',(70.3799715464621,440.012436358161,55.1875519623061));
#37328=CARTESIAN_POINT('Ctrl Pts',(71.8322073992925,440.142509524781,57.0581624818043));
#37329=CARTESIAN_POINT('Ctrl Pts',(74.1225020644475,440.28007893585,58.0719467909454));
#37330=CARTESIAN_POINT('Ctrl Pts',(76.6196778606811,440.417648346919,57.8787595222969));
#37331=CARTESIAN_POINT('Ctrl Pts',(78.7267969530214,440.555217757988,56.5247811576843));
#37332=CARTESIAN_POINT('Ctrl Pts',(79.9401626795821,440.692787169057,54.3336736996951));
#37333=CARTESIAN_POINT('Ctrl Pts',(79.969725812863,440.830356580126,51.8292108229069));
#37334=CARTESIAN_POINT('Ctrl Pts',(78.8084194282583,440.967925991195,49.6100723052293));
#37335=CARTESIAN_POINT('Ctrl Pts',(76.7338482188175,441.105495402264,48.2067325114984));
#37336=CARTESIAN_POINT('Ctrl Pts',(74.2419284313758,441.243064813333,47.9546530544782));
#37337=CARTESIAN_POINT('Ctrl Pts',(71.928341478485,441.380634224401,48.9140923131546));
#37338=CARTESIAN_POINT('Ctrl Pts',(70.4071472833128,441.512899098621,50.7808344993748));
#37339=CARTESIAN_POINT('Ctrl Pts',(70.0699931805514,441.599307502484,52.3069372826869));
#37340=CARTESIAN_POINT('Ctrl Pts',(70.0694094802034,441.639859435991,53.0228960008483));
#37341=CARTESIAN_POINT('Ctrl Pts',(70.0697223297068,440.235140564009,53.0226894836296));
#37342=CARTESIAN_POINT('Ctrl Pts',(70.0703202469893,440.269653434849,53.6321383121744));
#37343=CARTESIAN_POINT('Ctrl Pts',(70.3348709418805,440.35002276013,55.051852454326));
#37344=CARTESIAN_POINT('Ctrl Pts',(71.6677368744888,440.476248539853,56.9239590872673));
#37345=CARTESIAN_POINT('Ctrl Pts',(73.9140643916323,440.613817903178,58.0317570703397));
#37346=CARTESIAN_POINT('Ctrl Pts',(76.4170988864601,440.751387266504,57.9421914464564));
#37347=CARTESIAN_POINT('Ctrl Pts',(78.5785024367767,440.888956629829,56.6766724315182));
#37348=CARTESIAN_POINT('Ctrl Pts',(79.8816022941954,441.026525993154,54.5377160398189));
#37349=CARTESIAN_POINT('Ctrl Pts',(80.014898931527,441.164095356479,52.0366291379667));
#37350=CARTESIAN_POINT('Ctrl Pts',(78.9465284517881,441.301664719805,49.7712840865122));
#37351=CARTESIAN_POINT('Ctrl Pts',(76.9318794943156,441.43923408313,48.2832003313887));
#37352=CARTESIAN_POINT('Ctrl Pts',(74.4525438530313,441.576803446455,47.9280968788807));
#37353=CARTESIAN_POINT('Ctrl Pts',(72.1011943580286,441.71437280978,48.7908594397661));
#37354=CARTESIAN_POINT('Ctrl Pts',(70.4575039816879,441.850485182298,50.6453973502539));
#37355=CARTESIAN_POINT('Ctrl Pts',(70.0695204468552,441.940741100375,52.239005209128));
#37356=CARTESIAN_POINT('Ctrl Pts',(70.0692875054392,441.985140564009,53.0228369856911));
#37357=CARTESIAN_POINT('Origin',(74.9879498948689,433.764859435991,53.0228109606356));
#37358=CARTESIAN_POINT('',(70.0701612938335,438.139859435991,53.0228096632581));
#37359=CARTESIAN_POINT('',(70.0700845742479,438.485140564009,53.0228422002615));
#37360=CARTESIAN_POINT('',(70.0696998948689,433.764859435991,53.0228109606359));
#37361=CARTESIAN_POINT('Ctrl Pts',(70.0701612938333,438.139859435991,53.0228096632581));
#37362=CARTESIAN_POINT('Ctrl Pts',(70.0702739414449,438.165418880599,53.4742429003227));
#37363=CARTESIAN_POINT('Ctrl Pts',(70.242451475972,438.236834795563,54.7357509431657));
#37364=CARTESIAN_POINT('Ctrl Pts',(71.3075510106673,438.354107180884,56.586112001967));
#37365=CARTESIAN_POINT('Ctrl Pts',(73.4367474201414,438.491676591953,57.9050989515375));
#37366=CARTESIAN_POINT('Ctrl Pts',(75.9367802424272,438.629246003022,58.0569396214243));
#37367=CARTESIAN_POINT('Ctrl Pts',(78.2099924611958,438.766815414091,57.0054284326608));
#37368=CARTESIAN_POINT('Ctrl Pts',(79.7129963873825,438.90438482516,55.0018790181383));
#37369=CARTESIAN_POINT('Ctrl Pts',(80.0864990188232,439.041954236229,52.5252494404828));
#37370=CARTESIAN_POINT('Ctrl Pts',(79.2412191183861,439.179523647298,50.1675568417403));
#37371=CARTESIAN_POINT('Ctrl Pts',(77.3792153333098,439.317093058367,48.492400302215));
#37372=CARTESIAN_POINT('Ctrl Pts',(74.9455912824701,439.454662469436,47.9002160217303));
#37373=CARTESIAN_POINT('Ctrl Pts',(72.5220927714855,439.592231880505,48.5325636389322));
#37374=CARTESIAN_POINT('Ctrl Pts',(70.6880455611049,439.729801291574,50.2382831133303));
#37375=CARTESIAN_POINT('Ctrl Pts',(70.1066659790318,439.829010476736,51.9483976678048));
#37376=CARTESIAN_POINT('Ctrl Pts',(70.0693889929006,439.882363191541,52.8903463895694));
#37377=CARTESIAN_POINT('Ctrl Pts',(70.0695156097609,439.889859435991,53.0227034971274));
#37378=CARTESIAN_POINT('Ctrl Pts',(70.0700845742477,438.485140564009,53.0228422002615));
#37379=CARTESIAN_POINT('Ctrl Pts',(70.0700285470462,438.50685286044,53.406329627451));
#37380=CARTESIAN_POINT('Ctrl Pts',(70.2079331020722,438.574421611312,54.5997090727309));
#37381=CARTESIAN_POINT('Ctrl Pts',(71.1630752524974,438.687846816626,56.4306054140694));
#37382=CARTESIAN_POINT('Ctrl Pts',(73.2358186748897,438.825416179951,57.836628058181));
#37383=CARTESIAN_POINT('Ctrl Pts',(75.7274140404831,438.962985543276,58.0919298326021));
#37384=CARTESIAN_POINT('Ctrl Pts',(78.0422377232922,439.100554906601,57.1354858952104));
#37385=CARTESIAN_POINT('Ctrl Pts',(79.6269519827668,439.238124269927,55.1959270225485));
#37386=CARTESIAN_POINT('Ctrl Pts',(80.1027345777162,439.375693633252,52.7368959420052));
#37387=CARTESIAN_POINT('Ctrl Pts',(79.3558539781017,439.513262996577,50.346211308417));
#37388=CARTESIAN_POINT('Ctrl Pts',(77.564847398211,439.650832359902,48.5953545532883));
#37389=CARTESIAN_POINT('Ctrl Pts',(75.1578464351838,439.788401723227,47.90285916436));
#37390=CARTESIAN_POINT('Ctrl Pts',(72.7102324938985,439.925971086553,48.4342627525347));
#37391=CARTESIAN_POINT('Ctrl Pts',(70.8070955727843,440.063540449878,50.0625359188796));
#37392=CARTESIAN_POINT('Ctrl Pts',(70.1300939560672,440.166596942364,51.8124234577472));
#37393=CARTESIAN_POINT('Ctrl Pts',(70.0695258081044,440.223796980407,52.8223777283444));
#37394=CARTESIAN_POINT('Ctrl Pts',(70.0697223297068,440.235140564009,53.0226894836296));
#37395=CARTESIAN_POINT('Origin',(74.9879498948689,423.667006141107,53.0228109606356));
#37396=CARTESIAN_POINT('',(80.6362536929626,17.6670061411077,53.0272245279143));
#37397=CARTESIAN_POINT('',(80.6384886732644,16.3329938588948,53.0278707901325));
#37398=CARTESIAN_POINT('',(80.6314498948689,423.667006141107,53.0228109606222));
#37399=CARTESIAN_POINT('',(72.1688064861925,15.,48.133892604668));
#37400=CARTESIAN_POINT('Ctrl Pts',(80.6362536929627,17.6670061411077,53.0272245279143));
#37401=CARTESIAN_POINT('Ctrl Pts',(80.6388674031541,17.6350087809895,53.3099173664622));
#37402=CARTESIAN_POINT('Ctrl Pts',(80.4919324779875,17.3908554113189,55.464601173614));
#37403=CARTESIAN_POINT('Ctrl Pts',(77.7100437690878,16.9345460320961,59.1173659193523));
#37404=CARTESIAN_POINT('Ctrl Pts',(71.3329561213306,16.2980780034392,58.6109033270751));
#37405=CARTESIAN_POINT('Ctrl Pts',(68.3132228555609,15.6616099747823,52.9593291895844));
#37406=CARTESIAN_POINT('Ctrl Pts',(70.4291852017175,15.2289173069691,49.1745538303573));
#37407=CARTESIAN_POINT('Ctrl Pts',(72.1003657071,15.0083806487084,48.1647847936954));
#37408=CARTESIAN_POINT('Ctrl Pts',(72.1646654645455,15.,48.1277497923176));
#37409=CARTESIAN_POINT('',(72.1688064861966,15.,57.9117293166054));
#37410=CARTESIAN_POINT('Origin',(74.9879498948689,15.,53.0228109606356));
#37411=CARTESIAN_POINT('Ctrl Pts',(80.6384886732644,16.3329938588948,53.0278707901325));
#37412=CARTESIAN_POINT('Ctrl Pts',(80.6396925569063,16.3129745917012,53.2045791057297));
#37413=CARTESIAN_POINT('Ctrl Pts',(80.5523891734711,16.0807993149553,55.252320400191));
#37414=CARTESIAN_POINT('Ctrl Pts',(78.6506201566575,15.7425460334332,58.0582788876747));
#37415=CARTESIAN_POINT('Ctrl Pts',(74.8443820757933,15.3182340143285,58.8942202496515));
#37416=CARTESIAN_POINT('Ctrl Pts',(72.983431993014,15.1060780047762,58.3814745569358));
#37417=CARTESIAN_POINT('Ctrl Pts',(72.1688064861966,15.,57.9117293166054));
#37418=CARTESIAN_POINT('Origin',(74.9879498948689,423.667006141107,53.0228109606356));
#37419=CARTESIAN_POINT('',(80.631428174539,21.6670061411077,53.0228143106163));
#37420=CARTESIAN_POINT('',(80.6243731925048,20.3329938588948,53.0275588194414));
#37421=CARTESIAN_POINT('',(80.6314498948689,423.667006141107,53.0228109606222));
#37422=CARTESIAN_POINT('Ctrl Pts',(80.6226532189624,21.6670061411077,53.0241676993539));
#37423=CARTESIAN_POINT('Ctrl Pts',(80.6252968410462,21.57461150497,53.8467888709005));
#37424=CARTESIAN_POINT('Ctrl Pts',(80.071690884932,21.2700608592801,56.5552810828106));
#37425=CARTESIAN_POINT('Ctrl Pts',(75.890175270785,20.7533542040378,59.633916297922));
#37426=CARTESIAN_POINT('Ctrl Pts',(69.9117395951546,20.1168861753808,57.3605004391449));
#37427=CARTESIAN_POINT('Ctrl Pts',(68.5965174256227,19.4804181467239,51.0887193976995));
#37428=CARTESIAN_POINT('Ctrl Pts',(72.3977774992468,18.9500281228431,47.3601749200438));
#37429=CARTESIAN_POINT('Ctrl Pts',(76.2793092635613,18.5257161037384,47.3001117920513));
#37430=CARTESIAN_POINT('Ctrl Pts',(79.4966060481514,18.1334014447521,48.8909550864173));
#37431=CARTESIAN_POINT('Ctrl Pts',(80.6215374008575,17.8471647905418,51.4355444702682));
#37432=CARTESIAN_POINT('Ctrl Pts',(80.6362536929627,17.6670061411077,53.0272245279143));
#37433=CARTESIAN_POINT('Ctrl Pts',(80.6243731925048,20.3329938588948,53.0275588194413));
#37434=CARTESIAN_POINT('Ctrl Pts',(80.6283935590626,20.2525773156817,53.7428893577669));
#37435=CARTESIAN_POINT('Ctrl Pts',(80.1698683025709,19.9600047629164,56.3396104649291));
#37436=CARTESIAN_POINT('Ctrl Pts',(77.0829706090005,19.5613542053749,58.8867113839554));
#37437=CARTESIAN_POINT('Ctrl Pts',(73.2105872069091,19.1370421862702,58.6136853706606));
#37438=CARTESIAN_POINT('Ctrl Pts',(69.8912577533702,18.7127301671655,56.6010225426405));
#37439=CARTESIAN_POINT('Ctrl Pts',(68.4956769583314,18.1823401432847,51.4606824589819));
#37440=CARTESIAN_POINT('Ctrl Pts',(72.7985336869453,17.5458721146278,46.717269598202));
#37441=CARTESIAN_POINT('Ctrl Pts',(78.9102182501813,16.9294233531645,47.7356724886824));
#37442=CARTESIAN_POINT('Ctrl Pts',(80.6269342902349,16.5251306012535,51.331896617944));
#37443=CARTESIAN_POINT('Ctrl Pts',(80.6384886732644,16.3329938588948,53.0278707901325));
#37444=CARTESIAN_POINT('Origin',(74.9879498948689,423.667006141107,53.0228109606356));
#37445=CARTESIAN_POINT('',(80.6314498948689,25.6670061411076,53.0228109606223));
#37446=CARTESIAN_POINT('',(80.6253679025463,24.3329938588948,53.0178459337856));
#37447=CARTESIAN_POINT('',(80.6314498948689,423.667006141107,53.0228109606222));
#37448=CARTESIAN_POINT('Ctrl Pts',(80.6314498948689,25.6670061411076,53.0228109606223));
#37449=CARTESIAN_POINT('Ctrl Pts',(80.6314498948729,25.4742213185053,54.7318077489414));
#37450=CARTESIAN_POINT('Ctrl Pts',(79.8060659192715,25.2814364959029,56.4221521097231));
#37451=CARTESIAN_POINT('Ctrl Pts',(78.4584055093469,25.0886516733005,57.473095229976));
#37452=CARTESIAN_POINT('Ctrl Pts',(77.1107450994222,24.8958668506981,58.5240383502288));
#37453=CARTESIAN_POINT('Ctrl Pts',(75.2702256751666,24.7030820280957,58.9126397065621));
#37454=CARTESIAN_POINT('Ctrl Pts',(73.6127451627081,24.5102972054933,58.4961923829962));
#37455=CARTESIAN_POINT('Ctrl Pts',(71.9552646502496,24.3175123828909,58.0797450594303));
#37456=CARTESIAN_POINT('Ctrl Pts',(70.5170033810758,24.1247275602885,56.8673394809208));
#37457=CARTESIAN_POINT('Ctrl Pts',(69.826137149614,23.9319427376861,55.3042099684649));
#37458=CARTESIAN_POINT('Ctrl Pts',(69.1352709181523,23.7391579150837,53.7410804560089));
#37459=CARTESIAN_POINT('Ctrl Pts',(69.2068803054892,23.5463730924813,51.8613477992592));
#37460=CARTESIAN_POINT('Ctrl Pts',(70.0146680415421,23.3535882698789,50.355310284465));
#37461=CARTESIAN_POINT('Ctrl Pts',(70.822455777595,23.1608034472765,48.8492727696708));
#37462=CARTESIAN_POINT('Ctrl Pts',(72.3487890589358,22.9680186246741,47.7498049531896));
#37463=CARTESIAN_POINT('Ctrl Pts',(74.0331492157569,22.7752338020717,47.4606667775738));
#37464=CARTESIAN_POINT('Ctrl Pts',(75.7175093725781,22.5824489794693,47.1715286019581));
#37465=CARTESIAN_POINT('Ctrl Pts',(77.5231293307811,22.389664156867,47.6990315230355));
#37466=CARTESIAN_POINT('Ctrl Pts',(78.7869273705855,22.1968793342646,48.8494595029941));
#37467=CARTESIAN_POINT('Ctrl Pts',(79.9447859852089,22.0202549365456,49.9034514424855));
#37468=CARTESIAN_POINT('Ctrl Pts',(80.6314498948652,21.8436305388266,51.4570729301807));
#37469=CARTESIAN_POINT('Ctrl Pts',(80.6314498948689,21.6670061411077,53.0228109606222));
#37470=CARTESIAN_POINT('Ctrl Pts',(80.6253679025463,24.3329938588948,53.0178459337856));
#37471=CARTESIAN_POINT('Ctrl Pts',(80.6151298375501,24.1921800396623,54.2675854419267));
#37472=CARTESIAN_POINT('Ctrl Pts',(79.8930755009726,23.9452882156536,56.4684188056548));
#37473=CARTESIAN_POINT('Ctrl Pts',(77.3122715737554,23.5923183868688,58.4096717625035));
#37474=CARTESIAN_POINT('Ctrl Pts',(73.4859668057208,23.1680063677642,59.0656658471794));
#37475=CARTESIAN_POINT('Ctrl Pts',(69.0626632683662,22.6376163438834,56.1021187103944));
#37476=CARTESIAN_POINT('Ctrl Pts',(69.1990635927837,22.0011483152264,49.695206442741));
#37477=CARTESIAN_POINT('Ctrl Pts',(74.6559956914946,21.3646802865695,46.3586883014623));
#37478=CARTESIAN_POINT('Ctrl Pts',(79.6894979343186,20.8086288011256,48.7854595298665));
#37479=CARTESIAN_POINT('Ctrl Pts',(80.6177869737537,20.464733325234,51.8556946779366));
#37480=CARTESIAN_POINT('Ctrl Pts',(80.6243731925048,20.3329938588948,53.0275588194413));
#37481=CARTESIAN_POINT('Origin',(74.9879498948689,423.667006141107,53.0228109606356));
#37482=CARTESIAN_POINT('',(80.6400146763751,29.6670061411077,53.0229792748411));
#37483=CARTESIAN_POINT('',(80.6386417035632,28.3329938588948,53.0220653173588));
#37484=CARTESIAN_POINT('',(80.6314498948689,423.667006141107,53.0228109606222));
#37485=CARTESIAN_POINT('Ctrl Pts',(80.6400146763751,29.6670061411077,53.0229792748411));
#37486=CARTESIAN_POINT('Ctrl Pts',(80.6400186296118,29.6659729624834,53.0320960062332));
#37487=CARTESIAN_POINT('Ctrl Pts',(80.6399984395038,29.6649397838592,53.041212719425));
#37488=CARTESIAN_POINT('Ctrl Pts',(80.6399540528249,29.663906605235,53.0503293148091));
#37489=CARTESIAN_POINT('Ctrl Pts',(80.6308395585354,29.4517505956827,54.9223584606314));
#37490=CARTESIAN_POINT('Ctrl Pts',(79.6014584560108,29.2395945861304,56.789420153395));
#37491=CARTESIAN_POINT('Ctrl Pts',(78.0210409074678,29.0274385765781,57.793596730602));
#37492=CARTESIAN_POINT('Ctrl Pts',(76.4406233589247,28.8152825670258,58.7977733078089));
#37493=CARTESIAN_POINT('Ctrl Pts',(74.3091693643633,28.6031265574734,58.939064769459));
#37494=CARTESIAN_POINT('Ctrl Pts',(72.6116221830727,28.3909705479211,58.152546524122));
#37495=CARTESIAN_POINT('Ctrl Pts',(70.9140750017821,28.1788145383688,57.3660282787849));
#37496=CARTESIAN_POINT('Ctrl Pts',(69.6504346337626,27.9666585288166,55.6517003264607));
#37497=CARTESIAN_POINT('Ctrl Pts',(69.3904097747983,27.7545025192642,53.7962936842702));
#37498=CARTESIAN_POINT('Ctrl Pts',(69.2603973453161,27.6484245144881,52.8685903631747));
#37499=CARTESIAN_POINT('Ctrl Pts',(69.381288793098,27.5423465097118,51.9056173696121));
#37500=CARTESIAN_POINT('Ctrl Pts',(69.7157350999898,27.4362685049356,51.0236229168265));
#37501=CARTESIAN_POINT('Ctrl Pts',(70.0501814068814,27.3301905001595,50.1416284640413));
#37502=CARTESIAN_POINT('Ctrl Pts',(70.5981825728826,27.2241124953834,49.3406125520325));
#37503=CARTESIAN_POINT('Ctrl Pts',(71.3106189980845,27.1180344906072,48.7323601111073));
#37504=CARTESIAN_POINT('Ctrl Pts',(72.7354918484887,26.9058784810549,47.5158552292564));
#37505=CARTESIAN_POINT('Ctrl Pts',(74.8181057356958,26.6937224715026,47.0704042317404));
#37506=CARTESIAN_POINT('Ctrl Pts',(76.6103494066449,26.4815664619503,47.6071909688715));
#37507=CARTESIAN_POINT('Ctrl Pts',(78.4025930775939,26.2694104523979,48.1439777060026));
#37508=CARTESIAN_POINT('Ctrl Pts',(79.9044665322848,26.0572544428457,49.6630021777805));
#37509=CARTESIAN_POINT('Ctrl Pts',(80.4217124325031,25.8450984332934,51.4625985221484));
#37510=CARTESIAN_POINT('Ctrl Pts',(80.5664447738713,25.7857343358981,51.9661497196119));
#37511=CARTESIAN_POINT('Ctrl Pts',(80.6340851624506,25.7263702385029,52.4916684452613));
#37512=CARTESIAN_POINT('Ctrl Pts',(80.6294005094961,25.6670061411077,53.0182687964583));
#37513=CARTESIAN_POINT('Ctrl Pts',(80.6386417035632,28.3329938588948,53.0220653173588));
#37514=CARTESIAN_POINT('Ctrl Pts',(80.637090133247,28.237860768419,53.8624301588762));
#37515=CARTESIAN_POINT('Ctrl Pts',(80.2117010840973,28.036649673167,55.6432505569544));
#37516=CARTESIAN_POINT('Ctrl Pts',(77.8164221205999,27.6232825683628,58.5700374594237));
#37517=CARTESIAN_POINT('Ctrl Pts',(72.5335666026989,27.092892544482,59.2330665250225));
#37518=CARTESIAN_POINT('Ctrl Pts',(68.4353446939828,26.4564245158251,54.3063931884985));
#37519=CARTESIAN_POINT('Ctrl Pts',(70.3674902113553,25.8199564871681,48.2091214630561));
#37520=CARTESIAN_POINT('Ctrl Pts',(76.5387626327649,25.1834884585111,46.5282601413106));
#37521=CARTESIAN_POINT('Ctrl Pts',(80.2415468362615,24.6878342490867,49.8742024937387));
#37522=CARTESIAN_POINT('Ctrl Pts',(80.6305549359316,24.4043360492146,52.3846754514713));
#37523=CARTESIAN_POINT('Ctrl Pts',(80.6253679025463,24.3329938588948,53.0178459337856));
#37524=CARTESIAN_POINT('Origin',(74.9879498948689,423.667006141107,53.0228109606356));
#37525=CARTESIAN_POINT('',(80.6314498948689,33.6670061411076,53.0228109606225));
#37526=CARTESIAN_POINT('',(80.6329429902157,32.3329938588949,53.0264768953321));
#37527=CARTESIAN_POINT('',(80.6314498948689,423.667006141107,53.0228109606222));
#37528=CARTESIAN_POINT('Ctrl Pts',(80.6288724674716,33.6670061411077,53.0272877637515));
#37529=CARTESIAN_POINT('Ctrl Pts',(80.633617327969,33.605575686464,53.5723418811337));
#37530=CARTESIAN_POINT('Ctrl Pts',(80.561099549628,33.5441452318203,54.1162638727118));
#37531=CARTESIAN_POINT('Ctrl Pts',(80.4062625201533,33.4827147771767,54.6358597062275));
#37532=CARTESIAN_POINT('Ctrl Pts',(79.8715178809539,33.2705587676244,56.4303341124181));
#37533=CARTESIAN_POINT('Ctrl Pts',(78.3549244089112,33.058402758072,57.9346624158183));
#37534=CARTESIAN_POINT('Ctrl Pts',(76.5575388418803,32.8462467485197,58.4539720580937));
#37535=CARTESIAN_POINT('Ctrl Pts',(74.7601532748492,32.6340907389674,58.9732817003692));
#37536=CARTESIAN_POINT('Ctrl Pts',(72.6819756128296,32.4219347294151,58.5075726815198));
#37537=CARTESIAN_POINT('Ctrl Pts',(71.2690158181734,32.2097787198628,57.2772510246664));
#37538=CARTESIAN_POINT('Ctrl Pts',(70.5625359208453,32.1037007150866,56.6620901962398));
#37539=CARTESIAN_POINT('Ctrl Pts',(70.022360490358,31.9976227103104,55.8557762083121));
#37540=CARTESIAN_POINT('Ctrl Pts',(69.6965183067651,31.8915447055342,54.9705669609224));
#37541=CARTESIAN_POINT('Ctrl Pts',(69.3706761231721,31.7854667007581,54.0853577135324));
#37542=CARTESIAN_POINT('Ctrl Pts',(69.2591671864736,31.679388695982,53.1212532066807));
#37543=CARTESIAN_POINT('Ctrl Pts',(69.3982068004462,31.5733106912058,52.1948598366998));
#37544=CARTESIAN_POINT('Ctrl Pts',(69.6762860283913,31.3611546816536,50.3420730967384));
#37545=CARTESIAN_POINT('Ctrl Pts',(70.9565594590206,31.1489986721012,48.6401309042619));
#37546=CARTESIAN_POINT('Ctrl Pts',(72.6616847459306,30.9368426625489,47.8701795179302));
#37547=CARTESIAN_POINT('Ctrl Pts',(74.3668100328406,30.7246866529966,47.1002281315985));
#37548=CARTESIAN_POINT('Ctrl Pts',(76.4967871760314,30.5125306434443,47.2622675514116));
#37549=CARTESIAN_POINT('Ctrl Pts',(78.0673518045997,30.300374633892,48.2817855607585));
#37550=CARTESIAN_POINT('Ctrl Pts',(79.6302679399409,30.0892518029639,49.2963386189995));
#37551=CARTESIAN_POINT('Ctrl Pts',(80.6392068600684,29.8781289720358,51.1600389321174));
#37552=CARTESIAN_POINT('Ctrl Pts',(80.6400146763751,29.6670061411077,53.0229792748411));
#37553=CARTESIAN_POINT('Ctrl Pts',(80.6329429902157,32.3329938588949,53.0264768953321));
#37554=CARTESIAN_POINT('Ctrl Pts',(80.635781829672,32.2835414971757,53.464786485973));
#37555=CARTESIAN_POINT('Ctrl Pts',(80.587714509014,32.2340891354566,53.9023462171139));
#37556=CARTESIAN_POINT('Ctrl Pts',(80.4860984518382,32.1846367737375,54.3270706628304));
#37557=CARTESIAN_POINT('Ctrl Pts',(80.0501545161511,31.9724807641851,56.1491847223035));
#37558=CARTESIAN_POINT('Ctrl Pts',(78.628644314649,31.7603247546329,57.7350649292334));
#37559=CARTESIAN_POINT('Ctrl Pts',(76.863771950532,31.5481687450806,58.3559537435553));
#37560=CARTESIAN_POINT('Ctrl Pts',(75.0988995864149,31.3360127355283,58.9768425578771));
#37561=CARTESIAN_POINT('Ctrl Pts',(72.990665059683,31.123856725976,58.6327399795908));
#37562=CARTESIAN_POINT('Ctrl Pts',(71.5133168751436,30.9117007164237,57.4822911256512));
#37563=CARTESIAN_POINT('Ctrl Pts',(70.035968690604,30.6995447068713,56.3318422717114));
#37564=CARTESIAN_POINT('Ctrl Pts',(69.1895068482571,30.487388697319,54.3750471421177));
#37565=CARTESIAN_POINT('Ctrl Pts',(69.3591270580384,30.2752326877666,52.5106959999642));
#37566=CARTESIAN_POINT('Ctrl Pts',(69.5287472678197,30.0630766782143,50.6463448578111));
#37567=CARTESIAN_POINT('Ctrl Pts',(70.7144495297283,29.8509206686621,48.874437703098));
#37568=CARTESIAN_POINT('Ctrl Pts',(72.3751599774456,29.6387646591098,48.0094920199503));
#37569=CARTESIAN_POINT('Ctrl Pts',(74.0358704251634,29.4266086495574,47.1445463368025));
#37570=CARTESIAN_POINT('Ctrl Pts',(76.1715890586898,29.2144526400051,47.1865621252207));
#37571=CARTESIAN_POINT('Ctrl Pts',(77.7954333266113,29.0022966304528,48.1157591853188));
#37572=CARTESIAN_POINT('Ctrl Pts',(79.4192775945326,28.7901406209005,49.0449562454168));
#37573=CARTESIAN_POINT('Ctrl Pts',(80.5312474968489,28.5779846113481,50.8613345771943));
#37574=CARTESIAN_POINT('Ctrl Pts',(80.631200650374,28.3658286017958,52.7322049902012));
#37575=CARTESIAN_POINT('Ctrl Pts',(80.636357132633,28.3548836874955,52.828721305627));
#37576=CARTESIAN_POINT('Ctrl Pts',(80.6388202093182,28.3439387731951,52.9253826475808));
#37577=CARTESIAN_POINT('Ctrl Pts',(80.6386417035632,28.3329938588948,53.0220653173588));
#37578=CARTESIAN_POINT('Origin',(74.9879498948689,423.667006141107,53.0228109606356));
#37579=CARTESIAN_POINT('',(80.6314498948689,37.6670061411077,53.0228109606227));
#37580=CARTESIAN_POINT('',(80.6202517864306,36.3329938588948,53.0234467810542));
#37581=CARTESIAN_POINT('',(80.6314498948689,423.667006141107,53.0228109606222));
#37582=CARTESIAN_POINT('Ctrl Pts',(80.6314498948689,37.6670061411077,53.022810960622));
#37583=CARTESIAN_POINT('Ctrl Pts',(80.631449894873,37.4742213185054,54.7318077489411));
#37584=CARTESIAN_POINT('Ctrl Pts',(79.8060659192717,37.2814364959029,56.4221521097229));
#37585=CARTESIAN_POINT('Ctrl Pts',(78.4584055093471,37.0886516733005,57.4730952299758));
#37586=CARTESIAN_POINT('Ctrl Pts',(77.1107450994225,36.8958668506981,58.5240383502287));
#37587=CARTESIAN_POINT('Ctrl Pts',(75.2702256751669,36.7030820280957,58.9126397065621));
#37588=CARTESIAN_POINT('Ctrl Pts',(73.6127451627084,36.5102972054933,58.4961923829963));
#37589=CARTESIAN_POINT('Ctrl Pts',(71.9552646502498,36.3175123828909,58.0797450594305));
#37590=CARTESIAN_POINT('Ctrl Pts',(70.517003381076,36.1247275602886,56.867339480921));
#37591=CARTESIAN_POINT('Ctrl Pts',(69.8261371496142,35.9319427376862,55.3042099684651));
#37592=CARTESIAN_POINT('Ctrl Pts',(69.1352709181523,35.7391579150838,53.7410804560092));
#37593=CARTESIAN_POINT('Ctrl Pts',(69.2068803054892,35.5463730924814,51.8613477992594));
#37594=CARTESIAN_POINT('Ctrl Pts',(70.014668041542,35.353588269879,50.3553102844652));
#37595=CARTESIAN_POINT('Ctrl Pts',(70.8224557775948,35.1608034472766,48.849272769671));
#37596=CARTESIAN_POINT('Ctrl Pts',(72.3487890589355,34.9680186246741,47.7498049531897));
#37597=CARTESIAN_POINT('Ctrl Pts',(74.0331492157566,34.7752338020717,47.4606667775739));
#37598=CARTESIAN_POINT('Ctrl Pts',(75.7175093725778,34.5824489794693,47.1715286019581));
#37599=CARTESIAN_POINT('Ctrl Pts',(77.5231293307808,34.389664156867,47.6990315230354));
#37600=CARTESIAN_POINT('Ctrl Pts',(78.7869273705853,34.1968793342646,48.8494595029939));
#37601=CARTESIAN_POINT('Ctrl Pts',(79.9447859852089,34.0202549365456,49.9034514424854));
#37602=CARTESIAN_POINT('Ctrl Pts',(80.6314498948653,33.8436305388266,51.4570729301809));
#37603=CARTESIAN_POINT('Ctrl Pts',(80.6314498948689,33.6670061411076,53.0228109606225));
#37604=CARTESIAN_POINT('Ctrl Pts',(80.620244429633,36.3329938588948,53.0234471987678));
#37605=CARTESIAN_POINT('Ctrl Pts',(80.6203792639667,36.2231442211563,54.0004693354651));
#37606=CARTESIAN_POINT('Ctrl Pts',(80.3804009483158,36.1132945834177,54.9773613084557));
#37607=CARTESIAN_POINT('Ctrl Pts',(79.9012805970799,36.0034449456792,55.81929120189));
#37608=CARTESIAN_POINT('Ctrl Pts',(78.9759406150268,35.7912889361269,57.4453364960856));
#37609=CARTESIAN_POINT('Ctrl Pts',(77.1585914201757,35.5791329265746,58.5679679172326));
#37610=CARTESIAN_POINT('Ctrl Pts',(75.2888161061955,35.3669769170222,58.6681202952851));
#37611=CARTESIAN_POINT('Ctrl Pts',(73.4190407922153,35.1548209074699,58.7682726733377));
#37612=CARTESIAN_POINT('Ctrl Pts',(71.4968393591057,34.9426648979176,57.8459460082958));
#37613=CARTESIAN_POINT('Ctrl Pts',(70.4023953172393,34.7305088883653,56.3271410709748));
#37614=CARTESIAN_POINT('Ctrl Pts',(69.3079512753728,34.518352878813,54.8083361336536));
#37615=CARTESIAN_POINT('Ctrl Pts',(69.0412646247494,34.3061968692607,52.6930529240536));
#37616=CARTESIAN_POINT('Ctrl Pts',(69.7279277601338,34.0940408597084,50.9510471944045));
#37617=CARTESIAN_POINT('Ctrl Pts',(70.4145908955182,33.8818848501561,49.2090414647555));
#37618=CARTESIAN_POINT('Ctrl Pts',(72.0546038169107,33.6697288406038,47.8403132150578));
#37619=CARTESIAN_POINT('Ctrl Pts',(73.8899023408418,33.4575728310515,47.4770547544705));
#37620=CARTESIAN_POINT('Ctrl Pts',(75.7252008647727,33.2454168214991,47.1137962938832));
#37621=CARTESIAN_POINT('Ctrl Pts',(77.7557849912424,33.0332608119468,47.756007622406));
#37622=CARTESIAN_POINT('Ctrl Pts',(79.0580310893936,32.8211048023945,49.1029678521407));
#37623=CARTESIAN_POINT('Ctrl Pts',(79.7091541384693,32.7150267976184,49.7764479670082));
#37624=CARTESIAN_POINT('Ctrl Pts',(80.1781926804654,32.6089487928422,50.6261153071788));
#37625=CARTESIAN_POINT('Ctrl Pts',(80.4269217507685,32.502870788066,51.5360067237003));
#37626=CARTESIAN_POINT('Ctrl Pts',(80.5596961518577,32.446245145009,52.021717090155));
#37627=CARTESIAN_POINT('Ctrl Pts',(80.6296923646812,32.3896195019519,52.5245885817045));
#37628=CARTESIAN_POINT('Ctrl Pts',(80.6329429902157,32.3329938588949,53.0264768953321));
#37629=CARTESIAN_POINT('Origin',(74.9879498948689,423.667006141107,53.0228109606356));
#37630=CARTESIAN_POINT('',(80.6368917650185,41.6670061411077,53.0191116230352));
#37631=CARTESIAN_POINT('',(80.633865742348,40.3329938588947,53.0161690164858));
#37632=CARTESIAN_POINT('',(80.6314498948689,423.667006141107,53.0228109606222));
#37633=CARTESIAN_POINT('Ctrl Pts',(80.6368917650185,41.6670061411077,53.0191116230352));
#37634=CARTESIAN_POINT('Ctrl Pts',(80.6224390043439,41.4847811344251,54.6286369705124));
#37635=CARTESIAN_POINT('Ctrl Pts',(79.473040189755,41.1964781229664,57.189451688561));
#37636=CARTESIAN_POINT('Ctrl Pts',(76.2235906019975,40.8020971067315,58.7581360420116));
#37637=CARTESIAN_POINT('Ctrl Pts',(72.3427116734402,40.3777850876269,58.6597153718375));
#37638=CARTESIAN_POINT('Ctrl Pts',(68.5780159994796,39.8473950637461,54.8947137762651));
#37639=CARTESIAN_POINT('Ctrl Pts',(69.9542034117819,39.2109270350892,48.6358286646777));
#37640=CARTESIAN_POINT('Ctrl Pts',(75.9545145524023,38.5744590064322,46.4208411581293));
#37641=CARTESIAN_POINT('Ctrl Pts',(80.0892431940405,38.0598187084384,49.5275271159818));
#37642=CARTESIAN_POINT('Ctrl Pts',(80.62580916943,37.7573344199969,52.2169736538586));
#37643=CARTESIAN_POINT('Ctrl Pts',(80.622857141901,37.6670061411077,53.0211285676652));
#37644=CARTESIAN_POINT('Ctrl Pts',(80.633865742348,40.3329938588947,53.0161690164858));
#37645=CARTESIAN_POINT('Ctrl Pts',(80.6198868644127,40.1627469451367,54.523658763612));
#37646=CARTESIAN_POINT('Ctrl Pts',(79.2207882231253,39.7803440218265,57.9367393444107));
#37647=CARTESIAN_POINT('Ctrl Pts',(73.4587819402533,39.185785088964,59.5175702230695));
#37648=CARTESIAN_POINT('Ctrl Pts',(68.6935887976469,38.5493170603069,55.2510918448196));
#37649=CARTESIAN_POINT('Ctrl Pts',(69.715665777593,37.91284903165,48.9247269106014));
#37650=CARTESIAN_POINT('Ctrl Pts',(74.601169621109,37.3824590077692,46.808120492965));
#37651=CARTESIAN_POINT('Ctrl Pts',(78.2462630815789,36.9581469886647,48.1438605690558));
#37652=CARTESIAN_POINT('Ctrl Pts',(80.1956475812481,36.6436846072985,50.2598786826923));
#37653=CARTESIAN_POINT('Ctrl Pts',(80.6201188542396,36.4353002307085,52.1135162054112));
#37654=CARTESIAN_POINT('Ctrl Pts',(80.620244429633,36.3329938588948,53.0234471987678));
#37655=CARTESIAN_POINT('Origin',(74.9879498948689,423.667006141107,53.0228109606356));
#37656=CARTESIAN_POINT('',(80.633385624059,45.6670061411077,53.0268327355589));
#37657=CARTESIAN_POINT('',(80.6393222206687,44.3329938588947,53.0263391207439));
#37658=CARTESIAN_POINT('',(80.6314498948689,423.667006141107,53.0228109606222));
#37659=CARTESIAN_POINT('Ctrl Pts',(80.6333856240591,45.6670061411077,53.0268327355589));
#37660=CARTESIAN_POINT('Ctrl Pts',(80.6357785977206,45.636539867958,53.2963621215798));
#37661=CARTESIAN_POINT('Ctrl Pts',(80.558137143727,45.4999955900322,54.5032763848713));
#37662=CARTESIAN_POINT('Ctrl Pts',(79.6816674585669,45.2573733073301,56.5427224905476));
#37663=CARTESIAN_POINT('Ctrl Pts',(76.6870768176045,44.8330612882254,59.0132153117264));
#37664=CARTESIAN_POINT('Ctrl Pts',(71.3759252168139,44.3026712643447,58.6392645053152));
#37665=CARTESIAN_POINT('Ctrl Pts',(68.3108182107715,43.6662032356877,53.011418232064));
#37666=CARTESIAN_POINT('Ctrl Pts',(71.38860861019,43.0297352070309,47.4045376647909));
#37667=CARTESIAN_POINT('Ctrl Pts',(77.7686820139573,42.3932671783739,46.9522470491929));
#37668=CARTESIAN_POINT('Ctrl Pts',(80.5030918708071,41.9390241563995,50.6184562946624));
#37669=CARTESIAN_POINT('Ctrl Pts',(80.6392656742262,41.6969371439774,52.7547422663191));
#37670=CARTESIAN_POINT('Ctrl Pts',(80.6368917650185,41.6670061411077,53.0191116230352));
#37671=CARTESIAN_POINT('Ctrl Pts',(80.6393222206687,44.3329938588947,53.0263391207439));
#37672=CARTESIAN_POINT('Ctrl Pts',(80.6403712518679,44.3145056786696,53.1896840219556));
#37673=CARTESIAN_POINT('Ctrl Pts',(80.5601215752485,44.0838614888923,55.226263817248));
#37674=CARTESIAN_POINT('Ctrl Pts',(78.0922262264452,43.6410612895625,58.9290551959863));
#37675=CARTESIAN_POINT('Ctrl Pts',(71.6968693820735,43.0045932609057,58.8325447221204));
#37676=CARTESIAN_POINT('Ctrl Pts',(68.3201615278016,42.3681252322486,53.3859514106338));
#37677=CARTESIAN_POINT('Ctrl Pts',(70.6207865388037,41.8377352083679,48.584358436323));
#37678=CARTESIAN_POINT('Ctrl Pts',(74.2487044880827,41.4134231892631,47.2026496248374));
#37679=CARTESIAN_POINT('Ctrl Pts',(78.1068463906541,40.9891111701586,47.6335196122566));
#37680=CARTESIAN_POINT('Ctrl Pts',(80.4344795314526,40.6289680600358,50.3998157139843));
#37681=CARTESIAN_POINT('Ctrl Pts',(80.637306874534,40.374902954689,52.6450754628535));
#37682=CARTESIAN_POINT('Ctrl Pts',(80.633865742348,40.3329938588947,53.0161690164858));
#37683=CARTESIAN_POINT('Origin',(74.9879498948689,423.667006141107,53.0228109606356));
#37684=CARTESIAN_POINT('',(80.6270010590704,49.6670061411077,53.0243752810309));
#37685=CARTESIAN_POINT('',(80.6244305214574,48.3329938588947,53.0264095113666));
#37686=CARTESIAN_POINT('',(80.6314498948689,423.667006141107,53.0228109606222));
#37687=CARTESIAN_POINT('Ctrl Pts',(80.6270010590704,49.6670061411077,53.0243752810309));
#37688=CARTESIAN_POINT('Ctrl Pts',(80.6288632137675,49.5761425919386,53.8321526964587));
#37689=CARTESIAN_POINT('Ctrl Pts',(80.4633217000993,49.4852790427694,54.6390877344253));
#37690=CARTESIAN_POINT('Ctrl Pts',(80.1288323138219,49.3944154936003,55.3684577541329));
#37691=CARTESIAN_POINT('Ctrl Pts',(79.3478377997498,49.1822594840479,57.0714534469405));
#37692=CARTESIAN_POINT('Ctrl Pts',(77.645791580905,48.9701034744957,58.3515885781149));
#37693=CARTESIAN_POINT('Ctrl Pts',(75.7940213035194,48.7579474649433,58.618467241464));
#37694=CARTESIAN_POINT('Ctrl Pts',(73.9422510261341,48.5457914553911,58.8853459048131));
#37695=CARTESIAN_POINT('Ctrl Pts',(71.9407566902084,48.3336354458388,58.138968100337));
#37696=CARTESIAN_POINT('Ctrl Pts',(70.7145322410308,48.1214794362864,56.7238837128038));
#37697=CARTESIAN_POINT('Ctrl Pts',(69.4883077918529,47.9093234267341,55.3087993252702));
#37698=CARTESIAN_POINT('Ctrl Pts',(69.0373532294238,47.6971674171817,53.2250083546785));
#37699=CARTESIAN_POINT('Ctrl Pts',(69.565269157885,47.4850114076293,51.4289345892408));
#37700=CARTESIAN_POINT('Ctrl Pts',(70.093185086346,47.272855398077,49.6328608238036));
#37701=CARTESIAN_POINT('Ctrl Pts',(71.5999715056962,47.0606993885248,48.1245042635199));
#37702=CARTESIAN_POINT('Ctrl Pts',(73.3968818377015,46.8485433789725,47.598003093214));
#37703=CARTESIAN_POINT('Ctrl Pts',(75.193792169707,46.6363873694202,47.071501922908));
#37704=CARTESIAN_POINT('Ctrl Pts',(77.2808264143674,46.4242313598679,47.52685614258));
#37705=CARTESIAN_POINT('Ctrl Pts',(78.6936691722792,46.2120753503156,48.7532951841045));
#37706=CARTESIAN_POINT('Ctrl Pts',(79.9036232471368,46.0303856139129,49.8036137050773));
#37707=CARTESIAN_POINT('Ctrl Pts',(80.6191148022999,45.8486958775103,51.4194578243488));
#37708=CARTESIAN_POINT('Ctrl Pts',(80.633385624059,45.6670061411077,53.0268327355589));
#37709=CARTESIAN_POINT('Ctrl Pts',(80.6244305214574,48.3329938588947,53.0264095113666));
#37710=CARTESIAN_POINT('Ctrl Pts',(80.6282266649446,48.2541084026502,53.7275376620316));
#37711=CARTESIAN_POINT('Ctrl Pts',(80.1802688641959,47.9630669368533,56.3092964517505));
#37712=CARTESIAN_POINT('Ctrl Pts',(76.3127965798036,47.4598694615042,59.5671977602111));
#37713=CARTESIAN_POINT('Ctrl Pts',(70.1919083484634,46.8234014328472,57.6692351964939));
#37714=CARTESIAN_POINT('Ctrl Pts',(68.7803362744653,46.2930114089665,52.535461261843));
#37715=CARTESIAN_POINT('Ctrl Pts',(70.6133799988629,45.8686993898619,49.113348085619));
#37716=CARTESIAN_POINT('Ctrl Pts',(73.808800501213,45.4443873707573,46.9087629319908));
#37717=CARTESIAN_POINT('Ctrl Pts',(78.8849827941382,44.9324855271014,47.707940083055));
#37718=CARTESIAN_POINT('Ctrl Pts',(80.6283333838672,44.5266616882219,51.3152646902586));
#37719=CARTESIAN_POINT('Ctrl Pts',(80.6393222206687,44.3329938588947,53.0263391207439));
#37720=CARTESIAN_POINT('Origin',(74.9879498948689,423.667006141107,53.0228109606356));
#37721=CARTESIAN_POINT('',(80.6254600338732,53.6670061411076,53.018749021103));
#37722=CARTESIAN_POINT('',(80.6254941394426,52.3329938588948,53.0186489958662));
#37723=CARTESIAN_POINT('',(80.6314498948689,423.667006141107,53.0228109606222));
#37724=CARTESIAN_POINT('Ctrl Pts',(80.6254600338732,53.6670061411076,53.018749021103));
#37725=CARTESIAN_POINT('Ctrl Pts',(80.6145961036434,53.5157453159191,54.3612137459823));
#37726=CARTESIAN_POINT('Ctrl Pts',(80.137779540393,53.3644844907305,55.7095665100964));
#37727=CARTESIAN_POINT('Ctrl Pts',(79.2657590440722,53.2132236655419,56.7189534378691));
#37728=CARTESIAN_POINT('Ctrl Pts',(78.0426770694989,53.0010676559896,58.1347033679884));
#37729=CARTESIAN_POINT('Ctrl Pts',(76.0421333948125,52.7889116464373,58.8836255331242));
#37730=CARTESIAN_POINT('Ctrl Pts',(74.1884269720648,52.576755636885,58.6193099606255));
#37731=CARTESIAN_POINT('Ctrl Pts',(72.3347205493172,52.3645996273327,58.3549943881269));
#37732=CARTESIAN_POINT('Ctrl Pts',(70.6278513785079,52.1524436177804,57.0774410779938));
#37733=CARTESIAN_POINT('Ctrl Pts',(69.8486910436903,51.9402876082281,55.3752409220011));
#37734=CARTESIAN_POINT('Ctrl Pts',(69.0695307088726,51.7281315986757,53.6730407660079));
#37735=CARTESIAN_POINT('Ctrl Pts',(69.2180792100468,51.5159755891234,51.5461937641553));
#37736=CARTESIAN_POINT('Ctrl Pts',(70.2295003756775,51.303819579571,49.9704027090604));
#37737=CARTESIAN_POINT('Ctrl Pts',(71.2409215413078,51.0916635700188,48.394611653966));
#37738=CARTESIAN_POINT('Ctrl Pts',(73.1152153713943,50.8795075604665,47.3698765456294));
#37739=CARTESIAN_POINT('Ctrl Pts',(74.9861181344609,50.6673515509142,47.3693945622379));
#37740=CARTESIAN_POINT('Ctrl Pts',(76.8570208975277,50.4551955413619,47.3689125788463));
#37741=CARTESIAN_POINT('Ctrl Pts',(78.7245325935749,50.2430395318096,48.3926837204001));
#37742=CARTESIAN_POINT('Ctrl Pts',(79.7408730892389,50.0308835222573,49.9665956485603));
#37743=CARTESIAN_POINT('Ctrl Pts',(80.2490433370711,49.9248055174811,50.7535516126407));
#37744=CARTESIAN_POINT('Ctrl Pts',(80.5444207848074,49.8187275127049,51.678042773373));
#37745=CARTESIAN_POINT('Ctrl Pts',(80.611992343254,49.7126495079288,52.6188948471453));
#37746=CARTESIAN_POINT('Ctrl Pts',(80.6216839327447,49.6974350523217,52.7538384873408));
#37747=CARTESIAN_POINT('Ctrl Pts',(80.6266892544993,49.6822205967147,52.8891186931059));
#37748=CARTESIAN_POINT('Ctrl Pts',(80.6270010590704,49.6670061411077,53.0243752810309));
#37749=CARTESIAN_POINT('Ctrl Pts',(80.6254941394426,52.3329938588948,53.0186489958662));
#37750=CARTESIAN_POINT('Ctrl Pts',(80.617499907999,52.1937111266308,54.255977736584));
#37751=CARTESIAN_POINT('Ctrl Pts',(80.2173852564667,52.0544283943668,55.4982743983749));
#37752=CARTESIAN_POINT('Ctrl Pts',(79.4671048810938,51.9151456621028,56.4720440015237));
#37753=CARTESIAN_POINT('Ctrl Pts',(78.3242748410938,51.7029896525505,57.9552937186233));
#37754=CARTESIAN_POINT('Ctrl Pts',(76.3690076889641,51.4908336429982,58.8155202978237));
#37755=CARTESIAN_POINT('Ctrl Pts',(74.5049558165395,51.2786776334458,58.6555578082506));
#37756=CARTESIAN_POINT('Ctrl Pts',(72.6409039441153,51.0665216238935,58.4955953186776));
#37757=CARTESIAN_POINT('Ctrl Pts',(70.8680673513958,50.8543656143412,57.3154437603313));
#37758=CARTESIAN_POINT('Ctrl Pts',(69.9904446590788,50.6422096047889,55.6601718277894));
#37759=CARTESIAN_POINT('Ctrl Pts',(69.5516333129203,50.5361316000128,54.8325358615184));
#37760=CARTESIAN_POINT('Ctrl Pts',(69.3366254418624,50.4300535952366,53.8861198016984));
#37761=CARTESIAN_POINT('Ctrl Pts',(69.3499873054311,50.3239755904605,52.9429390126479));
#37762=CARTESIAN_POINT('Ctrl Pts',(69.3633491689999,50.2178975856843,51.9997582235974));
#37763=CARTESIAN_POINT('Ctrl Pts',(69.6050807671954,50.1118195809082,51.0598127053167));
#37764=CARTESIAN_POINT('Ctrl Pts',(70.0671612296048,50.005741576132,50.2449395026388));
#37765=CARTESIAN_POINT('Ctrl Pts',(70.9913221544237,49.7935855665797,48.6151930972829));
#37766=CARTESIAN_POINT('Ctrl Pts',(72.7968785360981,49.5814295570274,47.485735954339));
#37767=CARTESIAN_POINT('Ctrl Pts',(74.6647137408786,49.369273547475,47.378642402046));
#37768=CARTESIAN_POINT('Ctrl Pts',(76.5325489456591,49.1571175379227,47.2715488497529));
#37769=CARTESIAN_POINT('Ctrl Pts',(78.4626629735455,48.9449615283704,48.1868188881107));
#37770=CARTESIAN_POINT('Ctrl Pts',(79.5630169742935,48.732805518818,49.7018473685824));
#37771=CARTESIAN_POINT('Ctrl Pts',(80.2542290065312,48.5995349655103,50.6535464710284));
#37772=CARTESIAN_POINT('Ctrl Pts',(80.6180172462219,48.4662644122025,51.8419106059009));
#37773=CARTESIAN_POINT('Ctrl Pts',(80.6244305214574,48.3329938588947,53.0264095113666));
#37774=CARTESIAN_POINT('Origin',(74.9879498948689,423.667006141107,53.0228109606356));
#37775=CARTESIAN_POINT('',(80.6413657361973,57.6670061411076,53.0214830440174));
#37776=CARTESIAN_POINT('',(80.6403082971391,56.3329938588947,53.0200974632052));
#37777=CARTESIAN_POINT('',(80.6314498948689,423.667006141107,53.0228109606222));
#37778=CARTESIAN_POINT('Ctrl Pts',(80.6413657361973,57.6670061411076,53.0214830440174));
#37779=CARTESIAN_POINT('Ctrl Pts',(80.6414833583072,57.4553480398996,54.888013559151));
#37780=CARTESIAN_POINT('Ctrl Pts',(78.6026480433023,57.0315339291392,58.6340626778927));
#37781=CARTESIAN_POINT('Ctrl Pts',(72.2284115525991,56.3955638088267,59.0977760344396));
#37782=CARTESIAN_POINT('Ctrl Pts',(68.3809746809543,55.7590957801697,53.9882620695771));
#37783=CARTESIAN_POINT('Ctrl Pts',(70.610393675563,55.1226277515128,47.9801654008882));
#37784=CARTESIAN_POINT('Ctrl Pts',(75.8135978038988,54.592237727632,46.8510784551353));
#37785=CARTESIAN_POINT('Ctrl Pts',(79.1304928053609,54.1679257085273,48.8682833122854));
#37786=CARTESIAN_POINT('Ctrl Pts',(80.4347554668827,53.8948745146113,50.9989963543705));
#37787=CARTESIAN_POINT('Ctrl Pts',(80.6298336780962,53.7279013254714,52.4782942349981));
#37788=CARTESIAN_POINT('Ctrl Pts',(80.6254600338732,53.6670061411077,53.018749021103));
#37789=CARTESIAN_POINT('Ctrl Pts',(80.6403082971391,56.3329938588947,53.0200974632052));
#37790=CARTESIAN_POINT('Ctrl Pts',(80.6318782823841,56.1333138506113,54.783408729567));
#37791=CARTESIAN_POINT('Ctrl Pts',(79.7401566050892,55.9336338423279,56.5554703182809));
#37792=CARTESIAN_POINT('Ctrl Pts',(78.3168392779151,55.7339538340445,57.5922327845057));
#37793=CARTESIAN_POINT('Ctrl Pts',(76.8045931244024,55.5217978244922,58.693772140292));
#37794=CARTESIAN_POINT('Ctrl Pts',(74.6922479438257,55.3096418149399,58.9652590151995));
#37795=CARTESIAN_POINT('Ctrl Pts',(72.9442372900428,55.0974858053875,58.2910146121869));
#37796=CARTESIAN_POINT('Ctrl Pts',(72.0702319631515,54.9914078006114,57.9538924106807));
#37797=CARTESIAN_POINT('Ctrl Pts',(71.2873102679585,54.8853297958352,57.3803373896945));
#37798=CARTESIAN_POINT('Ctrl Pts',(70.6789285839257,54.779251791059,56.6594766078752));
#37799=CARTESIAN_POINT('Ctrl Pts',(70.0705468998929,54.6731737862828,55.9386158260558));
#37800=CARTESIAN_POINT('Ctrl Pts',(69.6367052270203,54.5670957815067,55.0704492834031));
#37801=CARTESIAN_POINT('Ctrl Pts',(69.4512397654423,54.4610177767306,54.1522231387392));
#37802=CARTESIAN_POINT('Ctrl Pts',(69.0803088422862,54.2488617671783,52.315770849411));
#37803=CARTESIAN_POINT('Ctrl Pts',(69.7028827643085,54.036705757626,50.2790801520375));
#37804=CARTESIAN_POINT('Ctrl Pts',(71.0428692552329,53.8245497480737,48.9734333447806));
#37805=CARTESIAN_POINT('Ctrl Pts',(72.3828557461571,53.6123937385214,47.6677865375239));
#37806=CARTESIAN_POINT('Ctrl Pts',(74.4402548059832,53.400237728969,47.093183620384));
#37807=CARTESIAN_POINT('Ctrl Pts',(76.2644654877336,53.1880817194168,47.5154934736778));
#37808=CARTESIAN_POINT('Ctrl Pts',(78.0886761694843,52.9759257098644,47.9378033269716));
#37809=CARTESIAN_POINT('Ctrl Pts',(79.6796984731593,52.7637697003121,49.3570259506994));
#37810=CARTESIAN_POINT('Ctrl Pts',(80.3100131610616,52.5516136907598,51.1197736900626));
#37811=CARTESIAN_POINT('Ctrl Pts',(80.526519387434,52.4787404134715,51.7252583288011));
#37812=CARTESIAN_POINT('Ctrl Pts',(80.6296767530029,52.4058671361831,52.3712736970513));
#37813=CARTESIAN_POINT('Ctrl Pts',(80.6254941394426,52.3329938588948,53.0186489958662));
#37814=CARTESIAN_POINT('Origin',(74.9879498948689,423.667006141107,53.0228109606356));
#37815=CARTESIAN_POINT('',(80.6314498948689,61.6670061411077,53.0228109606227));
#37816=CARTESIAN_POINT('',(80.6321857743054,60.3329938588946,53.0296130592723));
#37817=CARTESIAN_POINT('',(80.6314498948689,423.667006141107,53.0228109606222));
#37818=CARTESIAN_POINT('Ctrl Pts',(80.6286885834456,61.6670061411076,53.0279061367502));
#37819=CARTESIAN_POINT('Ctrl Pts',(80.6333660002909,61.6071067734325,53.5597788572812));
#37820=CARTESIAN_POINT('Ctrl Pts',(80.3206569018713,61.335051396205,55.9699752993004));
#37821=CARTESIAN_POINT('Ctrl Pts',(76.8880290754071,60.8508400094253,59.418899735667));
#37822=CARTESIAN_POINT('Ctrl Pts',(70.6327739589726,60.2143719807683,58.0841012989217));
#37823=CARTESIAN_POINT('Ctrl Pts',(68.3763035247955,59.5779039521114,52.0861119846998));
#37824=CARTESIAN_POINT('Ctrl Pts',(71.5643353852583,59.0475139282306,47.82176873059));
#37825=CARTESIAN_POINT('Ctrl Pts',(75.3913197498731,58.623201909126,47.1697729028191));
#37826=CARTESIAN_POINT('Ctrl Pts',(79.0926822278916,58.1988898900212,48.3405947051246));
#37827=CARTESIAN_POINT('Ctrl Pts',(80.6388404574232,57.8801579673485,51.1417900962632));
#37828=CARTESIAN_POINT('Ctrl Pts',(80.6413654595009,57.6675040494519,53.0170921838845));
#37829=CARTESIAN_POINT('Ctrl Pts',(80.6413657361973,57.6670061411076,53.0214830440174));
#37830=CARTESIAN_POINT('Ctrl Pts',(80.6321857743054,60.3329938588946,53.0296130592723));
#37831=CARTESIAN_POINT('Ctrl Pts',(80.6361440296551,60.2850725841441,53.4542934594533));
#37832=CARTESIAN_POINT('Ctrl Pts',(80.3981394867326,60.0249952998413,55.753981612222));
#37833=CARTESIAN_POINT('Ctrl Pts',(77.9529272269266,59.6588400107624,58.4982913970464));
#37834=CARTESIAN_POINT('Ctrl Pts',(74.0841280030346,59.2345279916577,58.8196952732654));
#37835=CARTESIAN_POINT('Ctrl Pts',(70.4968069555375,58.8102159725532,57.3357695377179));
#37836=CARTESIAN_POINT('Ctrl Pts',(68.3331244406284,58.2798259486722,52.4709315643751));
#37837=CARTESIAN_POINT('Ctrl Pts',(71.8627679117568,57.6433579200153,47.1221792238239));
#37838=CARTESIAN_POINT('Ctrl Pts',(78.2582921364095,57.0068898913583,47.2068747390464));
#37839=CARTESIAN_POINT('Ctrl Pts',(80.5882341009387,56.5701018709849,50.9268863207001));
#37840=CARTESIAN_POINT('Ctrl Pts',(80.6408350042226,56.3454698601636,52.9099258251642));
#37841=CARTESIAN_POINT('Ctrl Pts',(80.6403082971391,56.3329938588947,53.0200974632052));
#37842=CARTESIAN_POINT('Origin',(74.9879498948689,423.667006141107,53.0228109606356));
#37843=CARTESIAN_POINT('',(80.6314498948689,65.6670061411076,53.0228109606235));
#37844=CARTESIAN_POINT('',(80.6204112247681,64.3329938588946,53.021333253121));
#37845=CARTESIAN_POINT('',(80.6314498948689,423.667006141107,53.0228109606222));
#37846=CARTESIAN_POINT('Ctrl Pts',(80.6314498948689,65.6670061411076,53.0228109606229));
#37847=CARTESIAN_POINT('Ctrl Pts',(80.6314498948728,65.4742213185052,54.7318077489422));
#37848=CARTESIAN_POINT('Ctrl Pts',(79.8060659192709,65.2814364959028,56.422152109724));
#37849=CARTESIAN_POINT('Ctrl Pts',(78.4584055093459,65.0886516733004,57.4730952299767));
#37850=CARTESIAN_POINT('Ctrl Pts',(77.1107450994209,64.8958668506979,58.5240383502293));
#37851=CARTESIAN_POINT('Ctrl Pts',(75.2702256751649,64.7030820280955,58.9126397065622));
#37852=CARTESIAN_POINT('Ctrl Pts',(73.6127451627063,64.5102972054931,58.4961923829958));
#37853=CARTESIAN_POINT('Ctrl Pts',(71.9552646502477,64.3175123828907,58.0797450594293));
#37854=CARTESIAN_POINT('Ctrl Pts',(70.5170033810742,64.1247275602883,56.867339480919));
#37855=CARTESIAN_POINT('Ctrl Pts',(69.826137149613,63.9319427376859,55.3042099684626));
#37856=CARTESIAN_POINT('Ctrl Pts',(69.1352709181519,63.7391579150834,53.7410804560061));
#37857=CARTESIAN_POINT('Ctrl Pts',(69.2068803054898,63.546373092481,51.8613477992561));
#37858=CARTESIAN_POINT('Ctrl Pts',(70.0146680415436,63.3535882698786,50.3553102844622));
#37859=CARTESIAN_POINT('Ctrl Pts',(70.8224557775975,63.1608034472762,48.8492727696683));
#37860=CARTESIAN_POINT('Ctrl Pts',(72.3487890589391,62.9680186246737,47.7498049531878));
#37861=CARTESIAN_POINT('Ctrl Pts',(74.0331492157606,62.7752338020713,47.4606667775732));
#37862=CARTESIAN_POINT('Ctrl Pts',(75.7175093725822,62.5824489794689,47.1715286019586));
#37863=CARTESIAN_POINT('Ctrl Pts',(77.5231293307851,62.3896641568665,47.6990315230374));
#37864=CARTESIAN_POINT('Ctrl Pts',(78.7869273705887,62.1968793342641,48.8494595029971));
#37865=CARTESIAN_POINT('Ctrl Pts',(79.9447859852104,62.0202549365453,49.9034514424885));
#37866=CARTESIAN_POINT('Ctrl Pts',(80.6314498948653,61.8436305388265,51.4570729301826));
#37867=CARTESIAN_POINT('Ctrl Pts',(80.6314498948689,61.6670061411077,53.0228109606227));
#37868=CARTESIAN_POINT('Ctrl Pts',(80.6204112247681,64.3329938588946,53.021333253121));
#37869=CARTESIAN_POINT('Ctrl Pts',(80.6189023994922,64.2246753081247,53.9846691853807));
#37870=CARTESIAN_POINT('Ctrl Pts',(80.1536906680074,64.0102787525785,55.8927738082689));
#37871=CARTESIAN_POINT('Ctrl Pts',(78.1067448734721,63.6898041922563,57.9921046355568));
#37872=CARTESIAN_POINT('Ctrl Pts',(74.4252754900851,63.2654921731517,59.2240506837341));
#37873=CARTESIAN_POINT('Ctrl Pts',(69.6016913704958,62.7351021492708,56.9698974561461));
#37874=CARTESIAN_POINT('Ctrl Pts',(68.7592374263501,62.0986341206141,50.6171180655309));
#37875=CARTESIAN_POINT('Ctrl Pts',(73.6433787437401,61.4621660919569,46.4873399806718));
#37876=CARTESIAN_POINT('Ctrl Pts',(79.3005017798363,60.8736193380506,48.2131327071158));
#37877=CARTESIAN_POINT('Ctrl Pts',(80.6186201289628,60.4972285936964,51.5741577680182));
#37878=CARTESIAN_POINT('Ctrl Pts',(80.6321857743054,60.3329938588946,53.0296130592723));
#37879=CARTESIAN_POINT('Origin',(74.9879498948689,423.667006141107,53.0228109606356));
#37880=CARTESIAN_POINT('',(80.635553539915,69.6670061411076,53.0185589072328));
#37881=CARTESIAN_POINT('',(80.634082314566,68.3329938588946,53.0192791715721));
#37882=CARTESIAN_POINT('',(80.6314498948689,423.667006141107,53.0228109606222));
#37883=CARTESIAN_POINT('Ctrl Pts',(80.635553539915,69.6670061411076,53.0185589072328));
#37884=CARTESIAN_POINT('Ctrl Pts',(80.6224114597592,69.4863122213936,54.6163488873045));
#37885=CARTESIAN_POINT('Ctrl Pts',(79.913089862654,69.3056183016796,56.2245575530554));
#37886=CARTESIAN_POINT('Ctrl Pts',(78.7132493239764,69.1249243819656,57.2751258742408));
#37887=CARTESIAN_POINT('Ctrl Pts',(77.304494778235,68.9127683724132,58.5086172011074));
#37888=CARTESIAN_POINT('Ctrl Pts',(75.2195336705436,68.7006123628609,58.9733715267185));
#37889=CARTESIAN_POINT('Ctrl Pts',(73.421880772217,68.4884563533086,58.4549880409685));
#37890=CARTESIAN_POINT('Ctrl Pts',(71.6242278738907,68.2763003437562,57.9366045552187));
#37891=CARTESIAN_POINT('Ctrl Pts',(70.1138831849293,68.064144334204,56.4350832581081));
#37892=CARTESIAN_POINT('Ctrl Pts',(69.5738910421763,67.8519883246516,54.6410500236063));
#37893=CARTESIAN_POINT('Ctrl Pts',(69.3038949707998,67.7459103198755,53.7440334063556));
#37894=CARTESIAN_POINT('Ctrl Pts',(69.2764870359754,67.6398323150993,52.7738888047566));
#37895=CARTESIAN_POINT('Ctrl Pts',(69.472486901429,67.5337543103232,51.8512011040834));
#37896=CARTESIAN_POINT('Ctrl Pts',(69.6684867668826,67.427676305547,50.92851340341));
#37897=CARTESIAN_POINT('Ctrl Pts',(70.0878944326141,67.3215983007709,50.0532826036618));
#37898=CARTESIAN_POINT('Ctrl Pts',(70.6992159209813,67.2155202959947,49.3434778924606));
#37899=CARTESIAN_POINT('Ctrl Pts',(71.9218588977159,67.0033642864424,47.923868470058));
#37900=CARTESIAN_POINT('Ctrl Pts',(73.9121571649931,66.7912082768901,47.1659634018436));
#37901=CARTESIAN_POINT('Ctrl Pts',(75.7653062618025,66.5790522673377,47.4230933420581));
#37902=CARTESIAN_POINT('Ctrl Pts',(77.6184553586117,66.3668962577854,47.6802232822726));
#37903=CARTESIAN_POINT('Ctrl Pts',(79.3344552849528,66.1547402482332,48.9523882309157));
#37904=CARTESIAN_POINT('Ctrl Pts',(80.1201456948056,65.9425842386809,50.6520296058731));
#37905=CARTESIAN_POINT('Ctrl Pts',(80.4603341389693,65.8507248728231,51.3879407837776));
#37906=CARTESIAN_POINT('Ctrl Pts',(80.626115678942,65.7588655069654,52.2039917848341));
#37907=CARTESIAN_POINT('Ctrl Pts',(80.6231418722761,65.6670061411076,53.0210100020442));
#37908=CARTESIAN_POINT('Ctrl Pts',(80.6340823145659,68.3329938588947,53.0192791715721));
#37909=CARTESIAN_POINT('Ctrl Pts',(80.6304952755444,68.2703560368814,53.5741188988039));
#37910=CARTESIAN_POINT('Ctrl Pts',(80.3992795908312,68.1016402100919,55.0719021143628));
#37911=CARTESIAN_POINT('Ctrl Pts',(78.6294574171612,67.7207683737503,58.0736920277588));
#37912=CARTESIAN_POINT('Ctrl Pts',(73.5095530650882,67.1903783498695,59.534770382201));
#37913=CARTESIAN_POINT('Ctrl Pts',(68.7078085314535,66.5539103212125,55.2908589708327));
#37914=CARTESIAN_POINT('Ctrl Pts',(69.6873122266739,65.9174422925556,48.9702200830722));
#37915=CARTESIAN_POINT('Ctrl Pts',(75.5299851241042,65.2809742638987,46.3677065188326));
#37916=CARTESIAN_POINT('Ctrl Pts',(79.9731810233658,64.7528247860117,49.2894682583619));
#37917=CARTESIAN_POINT('Ctrl Pts',(80.6218576305895,64.436831317677,52.0978501152049));
#37918=CARTESIAN_POINT('Ctrl Pts',(80.6204112247681,64.3329938588946,53.021333253121));
#37919=CARTESIAN_POINT('Origin',(74.9879498948689,423.667006141107,53.0228109606356));
#37920=CARTESIAN_POINT('',(80.6374169710376,73.6670061411077,53.0261783696298));
#37921=CARTESIAN_POINT('',(80.6381904870062,72.3329938588947,53.0242910303993));
#37922=CARTESIAN_POINT('',(80.6314498948689,423.667006141107,53.0228109606222));
#37923=CARTESIAN_POINT('Ctrl Pts',(80.6374169710376,73.6670061411077,53.0261783696298));
#37924=CARTESIAN_POINT('Ctrl Pts',(80.6395239027795,73.6380709549265,53.2819622128666));
#37925=CARTESIAN_POINT('Ctrl Pts',(80.623649672582,73.6091357687453,53.5375128025017));
#37926=CARTESIAN_POINT('Ctrl Pts',(80.588902319524,73.5802005825642,53.7905152642106));
#37927=CARTESIAN_POINT('Ctrl Pts',(80.3341308547354,73.3680445730119,55.6455575074846));
#37928=CARTESIAN_POINT('Ctrl Pts',(79.0647429823832,73.1558885634595,57.3636127549326));
#37929=CARTESIAN_POINT('Ctrl Pts',(77.367601272787,72.9437325539072,58.1510055404649));
#37930=CARTESIAN_POINT('Ctrl Pts',(75.6704595631907,72.7315765443549,58.9383983259973));
#37931=CARTESIAN_POINT('Ctrl Pts',(73.5455640163505,72.5194205348026,58.7951286496138));
#37932=CARTESIAN_POINT('Ctrl Pts',(71.9614739050273,72.3072645252503,57.7947260906705));
#37933=CARTESIAN_POINT('Ctrl Pts',(71.1694288493658,72.2011865204742,57.2945248111989));
#37934=CARTESIAN_POINT('Ctrl Pts',(70.5125851525835,72.095108515698,56.5800403110874));
#37935=CARTESIAN_POINT('Ctrl Pts',(70.0555325713626,71.9890305109218,55.7548909438627));
#37936=CARTESIAN_POINT('Ctrl Pts',(69.5984799901418,71.8829525061457,54.9297415766381));
#37937=CARTESIAN_POINT('Ctrl Pts',(69.3412185244824,71.7768745013695,53.9939273423004));
#37938=CARTESIAN_POINT('Ctrl Pts',(69.3373259782948,71.6707964965933,53.0571661463347));
#37939=CARTESIAN_POINT('Ctrl Pts',(69.3295408859195,71.458640487041,51.1836437544033));
#37940=CARTESIAN_POINT('Ctrl Pts',(70.3352314714312,71.2464844774887,49.30633351596));
#37941=CARTESIAN_POINT('Ctrl Pts',(71.9029614556376,71.0343284679364,48.2853045850381));
#37942=CARTESIAN_POINT('Ctrl Pts',(73.4706914398441,70.8221724583841,47.2642756541161));
#37943=CARTESIAN_POINT('Ctrl Pts',(75.6004608227454,70.6100164488317,47.0995280307156));
#37944=CARTESIAN_POINT('Ctrl Pts',(77.3081571194718,70.3978604392794,47.8675537996514));
#37945=CARTESIAN_POINT('Ctrl Pts',(79.0158534161979,70.1857044297271,48.6355795685871));
#37946=CARTESIAN_POINT('Ctrl Pts',(80.3014766267492,69.9735484201748,50.3363787298588));
#37947=CARTESIAN_POINT('Ctrl Pts',(80.5780142401291,69.7613924106225,52.1878924745556));
#37948=CARTESIAN_POINT('Ctrl Pts',(80.6190239256628,69.7299303207842,52.4624663218646));
#37949=CARTESIAN_POINT('Ctrl Pts',(80.6378418145131,69.6984682309459,52.7403546822356));
#37950=CARTESIAN_POINT('Ctrl Pts',(80.635553539915,69.6670061411076,53.0185589072328));
#37951=CARTESIAN_POINT('Ctrl Pts',(80.6381904870062,72.3329938588947,53.0242910303993));
#37952=CARTESIAN_POINT('Ctrl Pts',(80.6386945101535,72.3160367656382,53.1741355929961));
#37953=CARTESIAN_POINT('Ctrl Pts',(80.6329254382104,72.2990796723817,53.3239143339577));
#37954=CARTESIAN_POINT('Ctrl Pts',(80.6207036538708,72.2821225791251,53.4731619524118));
#37955=CARTESIAN_POINT('Ctrl Pts',(80.4677927182608,72.0699665695728,55.3404500947464));
#37956=CARTESIAN_POINT('Ctrl Pts',(79.3048148169729,71.8578105600204,57.1245996642243));
#37957=CARTESIAN_POINT('Ctrl Pts',(77.6552999893402,71.6456545504681,58.007423664));
#37958=CARTESIAN_POINT('Ctrl Pts',(76.0057851617079,71.4334985409158,58.8902476637755));
#37959=CARTESIAN_POINT('Ctrl Pts',(73.869733407731,71.2213425313635,58.8717460938492));
#37960=CARTESIAN_POINT('Ctrl Pts',(72.2341915565031,71.0091865218112,57.9601030296608));
#37961=CARTESIAN_POINT('Ctrl Pts',(70.5986497052751,70.7970305122589,57.0484599654722));
#37962=CARTESIAN_POINT('Ctrl Pts',(69.463617756796,70.5848745027065,55.2436754070206));
#37963=CARTESIAN_POINT('Ctrl Pts',(69.3468788376743,70.3727184931542,53.3752674689147));
#37964=CARTESIAN_POINT('Ctrl Pts',(69.2301399185525,70.1605624836019,51.5068595308084));
#37965=CARTESIAN_POINT('Ctrl Pts',(70.1316940287881,69.9484064740495,49.5748282130472));
#37966=CARTESIAN_POINT('Ctrl Pts',(71.6410391704125,69.7362504644972,48.4666912778906));
#37967=CARTESIAN_POINT('Ctrl Pts',(73.1503843120364,69.5240944549449,47.3585543427344));
#37968=CARTESIAN_POINT('Ctrl Pts',(75.2675204850484,69.3119384453926,47.0743117901824));
#37969=CARTESIAN_POINT('Ctrl Pts',(77.0140960782944,69.0997824358403,47.7449466224388));
#37970=CARTESIAN_POINT('Ctrl Pts',(78.7606716715407,68.887626426288,48.4155814546954));
#37971=CARTESIAN_POINT('Ctrl Pts',(80.1366866850208,68.6754704167358,50.0410936717606));
#37972=CARTESIAN_POINT('Ctrl Pts',(80.5208389391871,68.4633144071834,51.8748258785865));
#37973=CARTESIAN_POINT('Ctrl Pts',(80.5994963581544,68.4198742244205,52.2502932639831));
#37974=CARTESIAN_POINT('Ctrl Pts',(80.6365699749868,68.3764340416576,52.6344902632031));
#37975=CARTESIAN_POINT('Ctrl Pts',(80.634082314566,68.3329938588946,53.0192791715721));
#37976=CARTESIAN_POINT('Origin',(74.9879498948689,423.667006141107,53.0228109606356));
#37977=CARTESIAN_POINT('',(80.6230624303151,77.6670061411075,53.0263696586206));
#37978=CARTESIAN_POINT('',(80.623997495512,76.3329938588947,53.0273509825437));
#37979=CARTESIAN_POINT('',(80.6314498948689,423.667006141107,53.0228109606222));
#37980=CARTESIAN_POINT('Ctrl Pts',(80.6230624303151,77.6670061411075,53.0263696586206));
#37981=CARTESIAN_POINT('Ctrl Pts',(80.6260769320359,77.577673678907,53.8215122457189));
#37982=CARTESIAN_POINT('Ctrl Pts',(80.4694078527787,77.4883412167064,54.6152708064669));
#37983=CARTESIAN_POINT('Ctrl Pts',(80.1472801889822,77.3990087545058,55.3341809537919));
#37984=CARTESIAN_POINT('Ctrl Pts',(79.382257955922,77.1868527449535,57.0415234396697));
#37985=CARTESIAN_POINT('Ctrl Pts',(77.6840214498711,76.9746967354012,58.3267082725514));
#37986=CARTESIAN_POINT('Ctrl Pts',(75.8320457850984,76.7625407258489,58.6101388598591));
#37987=CARTESIAN_POINT('Ctrl Pts',(74.9060579527121,76.6564627210727,58.7518541535129));
#37988=CARTESIAN_POINT('Ctrl Pts',(73.9416353306453,76.5503847162965,58.6431308857733));
#37989=CARTESIAN_POINT('Ctrl Pts',(73.0554884509454,76.4443067115204,58.3198473448531));
#37990=CARTESIAN_POINT('Ctrl Pts',(72.1693415712455,76.3382287067442,57.9965638039329));
#37991=CARTESIAN_POINT('Ctrl Pts',(71.3614704339124,76.2321507019681,57.4587199898319));
#37992=CARTESIAN_POINT('Ctrl Pts',(70.7442712211004,76.1260726971919,56.7540201800639));
#37993=CARTESIAN_POINT('Ctrl Pts',(69.5098727954763,75.9139166876396,55.3446205605277));
#37994=CARTESIAN_POINT('Ctrl Pts',(69.0381620679362,75.7017606780873,53.2677969583232));
#37995=CARTESIAN_POINT('Ctrl Pts',(69.5522770720199,75.489604668535,51.4689186567875));
#37996=CARTESIAN_POINT('Ctrl Pts',(70.0663920761035,75.2774486589827,49.6700403552521));
#37997=CARTESIAN_POINT('Ctrl Pts',(71.5663328118108,75.0652926494304,48.1491073543856));
#37998=CARTESIAN_POINT('Ctrl Pts',(73.3592549048717,74.8531366398781,47.6091808854886));
#37999=CARTESIAN_POINT('Ctrl Pts',(75.1521769979327,74.6409806303257,47.0692544165915));
#38000=CARTESIAN_POINT('Ctrl Pts',(77.2380804483475,74.4288246207734,47.510334479664));
#38001=CARTESIAN_POINT('Ctrl Pts',(78.6609546449425,74.2166686112211,48.7268891307503));
#38002=CARTESIAN_POINT('Ctrl Pts',(79.8897682072063,74.03344778785,49.7775223195927));
#38003=CARTESIAN_POINT('Ctrl Pts',(80.6240756444564,73.8502269644788,51.4065265702791));
#38004=CARTESIAN_POINT('Ctrl Pts',(80.6374169710376,73.6670061411077,53.0261783696298));
#38005=CARTESIAN_POINT('Ctrl Pts',(80.623997495512,76.3329938588947,53.0273509825437));
#38006=CARTESIAN_POINT('Ctrl Pts',(80.628953018813,76.2556394896187,53.7142739204978));
#38007=CARTESIAN_POINT('Ctrl Pts',(80.5133497506328,76.1782851203428,54.3997260528318));
#38008=CARTESIAN_POINT('Ctrl Pts',(80.2703413430329,76.1009307510668,55.0371249672848));
#38009=CARTESIAN_POINT('Ctrl Pts',(79.6038541810714,75.8887747415144,56.7852875009471));
#38010=CARTESIAN_POINT('Ctrl Pts',(77.9790086826698,75.6766187319621,58.1719873639615));
#38011=CARTESIAN_POINT('Ctrl Pts',(76.1463891559292,75.4644627224097,58.5561694741797));
#38012=CARTESIAN_POINT('Ctrl Pts',(74.3137696291889,75.2523067128574,58.9403515843979));
#38013=CARTESIAN_POINT('Ctrl Pts',(72.2733760741098,75.0401507033052,58.3220159418202));
#38014=CARTESIAN_POINT('Ctrl Pts',(70.9600714828875,74.8279946937529,56.9879217738211));
#38015=CARTESIAN_POINT('Ctrl Pts',(69.6467668916651,74.6158386842005,55.6538276058221));
#38016=CARTESIAN_POINT('Ctrl Pts',(69.0605512642994,74.4036826746482,53.6039749124017));
#38017=CARTESIAN_POINT('Ctrl Pts',(69.4734667251875,74.1915266650959,51.7776148586989));
#38018=CARTESIAN_POINT('Ctrl Pts',(69.8863821860757,73.9793706555435,49.951254804996));
#38019=CARTESIAN_POINT('Ctrl Pts',(71.2984287352179,73.7672146459912,48.3483873910108));
#38020=CARTESIAN_POINT('Ctrl Pts',(73.0568426519176,73.5550586364389,47.7094367835952));
#38021=CARTESIAN_POINT('Ctrl Pts',(74.8152565686171,73.3429026268866,47.0704861761797));
#38022=CARTESIAN_POINT('Ctrl Pts',(76.9200378528742,73.1307466173343,47.3954523753337));
#38023=CARTESIAN_POINT('Ctrl Pts',(78.412500974108,72.918590607782,48.5280161009088));
#38024=CARTESIAN_POINT('Ctrl Pts',(79.1587325347249,72.8125126030058,49.0942979636963));
#38025=CARTESIAN_POINT('Ctrl Pts',(79.751884554586,72.7064345982297,49.8624792080891));
#38026=CARTESIAN_POINT('Ctrl Pts',(80.1364912013237,72.6003565934535,50.7237841874762));
#38027=CARTESIAN_POINT('Ctrl Pts',(80.4596165750155,72.5112356819339,51.4474053096998));
#38028=CARTESIAN_POINT('Ctrl Pts',(80.6355415069229,72.4221147704143,52.2367572353762));
#38029=CARTESIAN_POINT('Ctrl Pts',(80.6381904870062,72.3329938588947,53.0242910303993));
#38030=CARTESIAN_POINT('Origin',(74.9879498948689,423.667006141107,53.0228109606356));
#38031=CARTESIAN_POINT('',(80.6276716108647,81.6670061411075,53.0174733762821));
#38032=CARTESIAN_POINT('',(80.6254978766381,80.3329938588945,53.0173329105307));
#38033=CARTESIAN_POINT('',(80.6314498948689,423.667006141107,53.0228109606222));
#38034=CARTESIAN_POINT('Ctrl Pts',(80.6276716108647,81.6670061411075,53.0174733762821));
#38035=CARTESIAN_POINT('Ctrl Pts',(80.6152958715597,81.5172764028875,54.3450615231278));
#38036=CARTESIAN_POINT('Ctrl Pts',(79.8112139615196,81.2614686598914,56.6251524598295));
#38037=CARTESIAN_POINT('Ctrl Pts',(77.0839556680519,80.8995829121189,58.5025483215824));
#38038=CARTESIAN_POINT('Ctrl Pts',(73.2334767124565,80.4752708930145,58.9972398405646));
#38039=CARTESIAN_POINT('Ctrl Pts',(68.9385484018002,79.9448808691335,55.8505334134376));
#38040=CARTESIAN_POINT('Ctrl Pts',(69.3439483205791,79.3084128404767,49.4549735833925));
#38041=CARTESIAN_POINT('Ctrl Pts',(74.9361886871511,78.6719448118197,46.3506618849799));
#38042=CARTESIAN_POINT('Ctrl Pts',(79.7843452960189,78.1248092453634,48.9443577070945));
#38043=CARTESIAN_POINT('Ctrl Pts',(80.6189177802548,77.7898296884593,51.9331250441539));
#38044=CARTESIAN_POINT('Ctrl Pts',(80.6230624303151,77.6670061411075,53.0263696586206));
#38045=CARTESIAN_POINT('Ctrl Pts',(80.6254978766381,80.3329938588945,53.0173329105307));
#38046=CARTESIAN_POINT('Ctrl Pts',(80.6172902306014,80.1952422135991,54.2420270657874));
#38047=CARTESIAN_POINT('Ctrl Pts',(80.225754257094,80.0574905683037,55.4722729920021));
#38048=CARTESIAN_POINT('Ctrl Pts',(79.4909454765108,79.9197389230084,56.4408613921962));
#38049=CARTESIAN_POINT('Ctrl Pts',(78.3592413989422,79.7075829134561,57.932617439416));
#38050=CARTESIAN_POINT('Ctrl Pts',(76.4132897193138,79.4954269039038,58.8037184020166));
#38051=CARTESIAN_POINT('Ctrl Pts',(74.5469455541935,79.2832708943514,58.6576511033595));
#38052=CARTESIAN_POINT('Ctrl Pts',(72.6806013890734,79.0711148847992,58.5115838047024));
#38053=CARTESIAN_POINT('Ctrl Pts',(70.8938647384612,78.8589588752468,57.3483482447878));
#38054=CARTESIAN_POINT('Ctrl Pts',(70.0080197895437,78.6468028656945,55.6986910227933));
#38055=CARTESIAN_POINT('Ctrl Pts',(69.1221748406262,78.4346468561422,54.0490338007986));
#38056=CARTESIAN_POINT('Ctrl Pts',(69.1372215934034,78.2224908465899,51.9129549167242));
#38057=CARTESIAN_POINT('Ctrl Pts',(70.0458418447529,78.0103348370376,50.2775079992128));
#38058=CARTESIAN_POINT('Ctrl Pts',(70.9544620961024,77.7981788274852,48.6420610817015));
#38059=CARTESIAN_POINT('Ctrl Pts',(72.7566558460243,77.5860228179329,47.5072461307536));
#38060=CARTESIAN_POINT('Ctrl Pts',(74.6261151221574,77.3738668083806,47.3836792435535));
#38061=CARTESIAN_POINT('Ctrl Pts',(75.5608447602238,77.2677888036044,47.3218957999535));
#38062=CARTESIAN_POINT('Ctrl Pts',(76.5123907798431,77.1617107988283,47.5129243722904));
#38063=CARTESIAN_POINT('Ctrl Pts',(77.3675494076294,77.0556327940521,47.9110101187751));
#38064=CARTESIAN_POINT('Ctrl Pts',(78.2227080354158,76.949554789276,48.3090958652599));
#38065=CARTESIAN_POINT('Ctrl Pts',(78.9814792713693,76.8434767844998,48.9142387858926));
#38066=CARTESIAN_POINT('Ctrl Pts',(79.5359719577514,76.7373987797237,49.669271600366));
#38067=CARTESIAN_POINT('Ctrl Pts',(80.2406093027247,76.6025971394473,50.6287510142958));
#38068=CARTESIAN_POINT('Ctrl Pts',(80.6153617497143,76.467795499171,51.8302842926289));
#38069=CARTESIAN_POINT('Ctrl Pts',(80.623997495512,76.3329938588947,53.0273509825437));
#38070=CARTESIAN_POINT('Origin',(74.9879498948689,423.667006141107,53.0228109606356));
#38071=CARTESIAN_POINT('',(80.6387596333603,85.6670061411075,53.023247336888));
#38072=CARTESIAN_POINT('',(80.6402800254983,84.3329938588945,53.0213524957134));
#38073=CARTESIAN_POINT('',(80.6314498948689,423.667006141107,53.0228109606222));
#38074=CARTESIAN_POINT('Ctrl Pts',(80.6387596333603,85.6670061411075,53.023247336888));
#38075=CARTESIAN_POINT('Ctrl Pts',(80.6397095806137,85.5629571316442,53.942111686572));
#38076=CARTESIAN_POINT('Ctrl Pts',(80.151294702481,85.3528301174047,55.7994486431996));
#38077=CARTESIAN_POINT('Ctrl Pts',(77.580926274119,84.9305470936132,58.683946013413));
#38078=CARTESIAN_POINT('Ctrl Pts',(72.2748837406891,84.4001570697319,59.1244947231283));
#38079=CARTESIAN_POINT('Ctrl Pts',(68.3872132968793,83.7636890410755,54.030031733356));
#38080=CARTESIAN_POINT('Ctrl Pts',(70.5737567372417,83.1272210124182,48.0192970676245));
#38081=CARTESIAN_POINT('Ctrl Pts',(76.8101842784523,82.4907529837615,46.5991298374534));
#38082=CARTESIAN_POINT('Ctrl Pts',(80.3051414638775,82.0040146933244,50.034716227933));
#38083=CARTESIAN_POINT('Ctrl Pts',(80.6328313825237,81.7294324124398,52.4639669128515));
#38084=CARTESIAN_POINT('Ctrl Pts',(80.6276716108647,81.6670061411075,53.0174733762821));
#38085=CARTESIAN_POINT('Ctrl Pts',(80.6402800254983,84.3329938588945,53.0213524957134));
#38086=CARTESIAN_POINT('Ctrl Pts',(80.6315430011957,84.1348449375797,54.7708123482206));
#38087=CARTESIAN_POINT('Ctrl Pts',(78.8173730615227,83.7245400067127,58.4058088718737));
#38088=CARTESIAN_POINT('Ctrl Pts',(72.6215538909905,83.102079066293,59.2665588153995));
#38089=CARTESIAN_POINT('Ctrl Pts',(68.4535757982522,82.4656110376363,54.3987571295987));
#38090=CARTESIAN_POINT('Ctrl Pts',(69.9948804987645,81.9352210137553,49.3024299862164));
#38091=CARTESIAN_POINT('Ctrl Pts',(73.3695905296702,81.5109089946509,47.3835136009241));
#38092=CARTESIAN_POINT('Ctrl Pts',(77.2483078732814,81.0865969755459,47.2208493614383));
#38093=CARTESIAN_POINT('Ctrl Pts',(80.2162883538608,80.6939585969607,49.8143795435911));
#38094=CARTESIAN_POINT('Ctrl Pts',(80.62993110634,80.4073982231515,52.3558338058509));
#38095=CARTESIAN_POINT('Ctrl Pts',(80.6254978766381,80.3329938588945,53.0173329105307));
#38096=CARTESIAN_POINT('Origin',(74.9879498948689,423.667006141107,53.0228109606356));
#38097=CARTESIAN_POINT('',(80.631286606836,89.6670061411074,53.0264418435404));
#38098=CARTESIAN_POINT('',(80.6317605038146,88.3329938588946,53.0278742010531));
#38099=CARTESIAN_POINT('',(80.6314498948689,423.667006141107,53.0228109606222));
#38100=CARTESIAN_POINT('Ctrl Pts',(80.6312866068361,89.6670061411075,53.0264418435404));
#38101=CARTESIAN_POINT('Ctrl Pts',(80.6344559667197,89.6086378604009,53.5442211596003));
#38102=CARTESIAN_POINT('Ctrl Pts',(80.3234366051561,89.3381135701419,55.9395580373531));
#38103=CARTESIAN_POINT('Ctrl Pts',(76.9406356429825,88.8554332703309,59.4085991706795));
#38104=CARTESIAN_POINT('Ctrl Pts',(70.6648736271285,88.2189652416738,58.1115464523212));
#38105=CARTESIAN_POINT('Ctrl Pts',(68.3743024533118,87.5824972130169,52.1396801497238));
#38106=CARTESIAN_POINT('Ctrl Pts',(72.1515458643403,86.9460291843599,46.9780587327407));
#38107=CARTESIAN_POINT('Ctrl Pts',(78.5477530123006,86.3095611557031,47.3731141139413));
#38108=CARTESIAN_POINT('Ctrl Pts',(80.6270392993929,85.8832201412856,51.1138794115315));
#38109=CARTESIAN_POINT('Ctrl Pts',(80.6387411090271,85.6690351364204,53.0053291321087));
#38110=CARTESIAN_POINT('Ctrl Pts',(80.6387596333603,85.6670061411075,53.023247336888));
#38111=CARTESIAN_POINT('Ctrl Pts',(80.6317605038146,88.3329938588946,53.0278742010531));
#38112=CARTESIAN_POINT('Ctrl Pts',(80.6354316875401,88.2866036711127,53.438801427614));
#38113=CARTESIAN_POINT('Ctrl Pts',(80.4060682461895,88.0280574737784,55.7248623794342));
#38114=CARTESIAN_POINT('Ctrl Pts',(77.2955260761042,87.5573552668916,59.2885359377501));
#38115=CARTESIAN_POINT('Ctrl Pts',(70.9567606325384,86.9208872382348,58.3464174285945));
#38116=CARTESIAN_POINT('Ctrl Pts',(68.7786383180496,86.3904972143539,53.4880273953303));
#38117=CARTESIAN_POINT('Ctrl Pts',(70.0682487881018,85.9661851952494,49.8263593707863));
#38118=CARTESIAN_POINT('Ctrl Pts',(72.8900068067502,85.5418731761447,47.1601655348787));
#38119=CARTESIAN_POINT('Ctrl Pts',(78.2142824574917,85.0114831522641,47.1762691716988));
#38120=CARTESIAN_POINT('Ctrl Pts',(80.5808862801361,84.5731640449218,50.9013697299768));
#38121=CARTESIAN_POINT('Ctrl Pts',(80.6408976431443,84.347000947132,52.8976836997423));
#38122=CARTESIAN_POINT('Ctrl Pts',(80.6402800254983,84.3329938588945,53.0213524957134));
#38123=CARTESIAN_POINT('Origin',(74.9879498948689,423.667006141107,53.0228109606356));
#38124=CARTESIAN_POINT('',(80.6204621564745,93.6670061411077,53.0221988416072));
#38125=CARTESIAN_POINT('',(80.6222974695971,92.3329938588945,53.0225854127507));
#38126=CARTESIAN_POINT('',(80.6314498948689,423.667006141107,53.0228109606222));
#38127=CARTESIAN_POINT('Ctrl Pts',(80.6204621564745,93.6670061411077,53.0221988416072));
#38128=CARTESIAN_POINT('Ctrl Pts',(80.6183893468973,93.5482405843816,54.078428328712));
#38129=CARTESIAN_POINT('Ctrl Pts',(80.335268865848,93.4294750276555,55.1354937426111));
#38130=CARTESIAN_POINT('Ctrl Pts',(79.7794841936502,93.3107094709294,56.0231975011701));
#38131=CARTESIAN_POINT('Ctrl Pts',(78.7866621880601,93.0985534613771,57.6089408115375));
#38132=CARTESIAN_POINT('Ctrl Pts',(76.9237630301127,92.8863974518248,58.6542475278061));
#38133=CARTESIAN_POINT('Ctrl Pts',(75.0514311231125,92.6742414422725,58.6757755010019));
#38134=CARTESIAN_POINT('Ctrl Pts',(73.1790992161119,92.4620854327202,58.6973034741976));
#38135=CARTESIAN_POINT('Ctrl Pts',(71.2973345600582,92.2499294231679,57.6950527043195));
#38136=CARTESIAN_POINT('Ctrl Pts',(70.2676506174,92.0377734136155,56.1316182871956));
#38137=CARTESIAN_POINT('Ctrl Pts',(69.2379666747419,91.8256174040632,54.5681838700718));
#38138=CARTESIAN_POINT('Ctrl Pts',(69.0603634454785,91.6134613945108,52.4435658057023));
#38139=CARTESIAN_POINT('Ctrl Pts',(69.8195899162345,91.4013053849585,50.7319392723414));
#38140=CARTESIAN_POINT('Ctrl Pts',(70.5788163869904,91.1891493754062,49.0203127389806));
#38141=CARTESIAN_POINT('Ctrl Pts',(72.2748725577659,90.976993365854,47.7216777366283));
#38142=CARTESIAN_POINT('Ctrl Pts',(74.1238093241108,90.7648373563017,47.4358277493677));
#38143=CARTESIAN_POINT('Ctrl Pts',(75.9727460904561,90.5526813467493,47.1499777621071));
#38144=CARTESIAN_POINT('Ctrl Pts',(77.974563452371,90.3405253371969,47.8769127899383));
#38145=CARTESIAN_POINT('Ctrl Pts',(79.2190840426557,90.1283693276446,49.277382447264));
#38146=CARTESIAN_POINT('Ctrl Pts',(79.8413443377979,90.0222913228685,49.9776172759268));
#38147=CARTESIAN_POINT('Ctrl Pts',(80.2742804400326,89.9162133180923,50.8462357619631));
#38148=CARTESIAN_POINT('Ctrl Pts',(80.4845719094074,89.8101353133162,51.7657715351335));
#38149=CARTESIAN_POINT('Ctrl Pts',(80.5791527605388,89.7624255892466,52.179342643514));
#38150=CARTESIAN_POINT('Ctrl Pts',(80.6286959996827,89.714715865177,52.6032135421563));
#38151=CARTESIAN_POINT('Ctrl Pts',(80.631286606836,89.6670061411074,53.0264418435404));
#38152=CARTESIAN_POINT('Ctrl Pts',(80.6222974695971,92.3329938588945,53.0225854127507));
#38153=CARTESIAN_POINT('Ctrl Pts',(80.6225629497166,92.2262063950931,53.9726808477364));
#38154=CARTESIAN_POINT('Ctrl Pts',(79.9442096617391,91.9072629217394,56.8106361137177));
#38155=CARTESIAN_POINT('Ctrl Pts',(75.4352492268543,91.3761634388334,59.6854827972209));
#38156=CARTESIAN_POINT('Ctrl Pts',(70.6049911897418,90.8457734149526,57.4456663254745));
#38157=CARTESIAN_POINT('Ctrl Pts',(69.1775862436694,90.4214613958479,53.8354830882459));
#38158=CARTESIAN_POINT('Ctrl Pts',(69.5597087935644,89.9971493767433,49.9722085389421));
#38159=CARTESIAN_POINT('Ctrl Pts',(73.5900826298085,89.4667593528626,46.493091226704));
#38160=CARTESIAN_POINT('Ctrl Pts',(79.2838657016368,88.8766815119875,48.1901383461276));
#38161=CARTESIAN_POINT('Ctrl Pts',(80.618642281703,88.498759680665,51.5595100349322));
#38162=CARTESIAN_POINT('Ctrl Pts',(80.6317605038146,88.3329938588946,53.0278742010531));
#38163=CARTESIAN_POINT('Origin',(74.9879498948689,423.667006141107,53.0228109606356));
#38164=CARTESIAN_POINT('',(80.6362700731203,97.6670061411075,53.016734409587));
#38165=CARTESIAN_POINT('',(80.6327545556523,96.3329938588947,53.0173721012319));
#38166=CARTESIAN_POINT('',(80.6314498948689,423.667006141107,53.0228109606222));
#38167=CARTESIAN_POINT('Ctrl Pts',(80.6362700731203,97.6670061411075,53.016734409587));
#38168=CARTESIAN_POINT('Ctrl Pts',(80.6225472232024,97.487843308362,54.6012631912224));
#38169=CARTESIAN_POINT('Ctrl Pts',(79.924533412689,97.3086804756165,56.1986225284727));
#38170=CARTESIAN_POINT('Ctrl Pts',(78.7426840125468,97.1295176428711,57.2491580436995));
#38171=CARTESIAN_POINT('Ctrl Pts',(77.3431947949246,96.9173616333188,58.4931516744551));
#38172=CARTESIAN_POINT('Ctrl Pts',(75.2652637017498,96.7052056237665,58.9703803392536));
#38173=CARTESIAN_POINT('Ctrl Pts',(73.4626676116383,96.4930496142142,58.4651838088526));
#38174=CARTESIAN_POINT('Ctrl Pts',(71.6600715215263,96.2808936046619,57.9599872784515));
#38175=CARTESIAN_POINT('Ctrl Pts',(70.132810434478,96.0687375951095,56.47236555285));
#38176=CARTESIAN_POINT('Ctrl Pts',(69.5836633530081,95.8565815855572,54.6822460857428));
#38177=CARTESIAN_POINT('Ctrl Pts',(69.0345162715382,95.6444255760048,52.8921266186361));
#38178=CARTESIAN_POINT('Ctrl Pts',(69.4634831956461,95.4322695664525,50.7995094100236));
#38179=CARTESIAN_POINT('Ctrl Pts',(70.6719858524335,95.2201135569002,49.371294191754));
#38180=CARTESIAN_POINT('Ctrl Pts',(71.880488509221,95.0079575473479,47.9430789734843));
#38181=CARTESIAN_POINT('Ctrl Pts',(73.8685268986879,94.7958015377957,47.1792657455576));
#38182=CARTESIAN_POINT('Ctrl Pts',(75.7264635754982,94.5836455282434,47.4205499466461));
#38183=CARTESIAN_POINT('Ctrl Pts',(76.6554319139033,94.4775675234672,47.5411920471903));
#38184=CARTESIAN_POINT('Ctrl Pts',(77.5518748241443,94.371489518691,47.9131085049883));
#38185=CARTESIAN_POINT('Ctrl Pts',(78.3136094973527,94.2654115139148,48.4694616553019));
#38186=CARTESIAN_POINT('Ctrl Pts',(79.0753441705613,94.1593335091386,49.0258148056156));
#38187=CARTESIAN_POINT('Ctrl Pts',(79.7023706067374,94.0532555043625,49.7666046484449));
#38188=CARTESIAN_POINT('Ctrl Pts',(80.099930755316,93.9471774995863,50.6148278610756));
#38189=CARTESIAN_POINT('Ctrl Pts',(80.4499403768181,93.8537870467601,51.3615985991982));
#38190=CARTESIAN_POINT('Ctrl Pts',(80.6220920955778,93.7603965939339,52.1916402789372));
#38191=CARTESIAN_POINT('Ctrl Pts',(80.6204621564745,93.6670061411077,53.0221988416072));
#38192=CARTESIAN_POINT('Ctrl Pts',(80.6327545556523,96.3329938588947,53.0173721012319));
#38193=CARTESIAN_POINT('Ctrl Pts',(80.6186391321579,96.1658091190738,54.4991059289975));
#38194=CARTESIAN_POINT('Ctrl Pts',(80.0202136543595,95.9986243792528,55.9913418499903));
#38195=CARTESIAN_POINT('Ctrl Pts',(78.9748718282735,95.831439639432,57.0309993077515));
#38196=CARTESIAN_POINT('Ctrl Pts',(77.6483419627002,95.6192836298797,58.3503157583809));
#38197=CARTESIAN_POINT('Ctrl Pts',(75.6021251094401,95.4071276203275,58.9408272947501));
#38198=CARTESIAN_POINT('Ctrl Pts',(73.7717246599809,95.1949716107751,58.5411011943371));
#38199=CARTESIAN_POINT('Ctrl Pts',(72.8565244352513,95.088893605999,58.3412381441306));
#38200=CARTESIAN_POINT('Ctrl Pts',(71.995278311472,94.9828156012228,57.8938156847286));
#38201=CARTESIAN_POINT('Ctrl Pts',(71.2840608794616,94.8767375964466,57.2741881315675));
#38202=CARTESIAN_POINT('Ctrl Pts',(70.5728434474512,94.7706595916704,56.6545605784064));
#38203=CARTESIAN_POINT('Ctrl Pts',(70.0116547072098,94.6645815868943,55.8627279314863));
#38204=CARTESIAN_POINT('Ctrl Pts',(69.688300068699,94.5585035821182,54.983535991159));
#38205=CARTESIAN_POINT('Ctrl Pts',(69.0415907916772,94.3463475725659,53.2251521105042));
#38206=CARTESIAN_POINT('Ctrl Pts',(69.3462179215783,94.1341915630135,51.1173310562202));
#38207=CARTESIAN_POINT('Ctrl Pts',(70.4713707929385,93.9220355534611,49.6225707419123));
#38208=CARTESIAN_POINT('Ctrl Pts',(71.5965236642985,93.7098795439088,48.1278104276046));
#38209=CARTESIAN_POINT('Ctrl Pts',(73.5422022771169,93.4977235343564,47.2461108532722));
#38210=CARTESIAN_POINT('Ctrl Pts',(75.4094828660979,93.2855675248041,47.3852274432813));
#38211=CARTESIAN_POINT('Ctrl Pts',(77.2767634550792,93.0734115152518,47.5243440332904));
#38212=CARTESIAN_POINT('Ctrl Pts',(79.0656460202229,92.8612555056996,48.6842767876416));
#38213=CARTESIAN_POINT('Ctrl Pts',(79.9574615217452,92.6490994961473,50.3302540990467));
#38214=CARTESIAN_POINT('Ctrl Pts',(80.4003870022527,92.5437309503964,51.1477385342401));
#38215=CARTESIAN_POINT('Ctrl Pts',(80.6220355169939,92.4383624046455,52.0851141895814));
#38216=CARTESIAN_POINT('Ctrl Pts',(80.6222974695971,92.3329938588945,53.0225854127507));
#38217=CARTESIAN_POINT('Origin',(74.9879498948689,423.667006141107,53.0228109606356));
#38218=CARTESIAN_POINT('',(80.6374103558004,101.667006141107,53.0273186999381));
#38219=CARTESIAN_POINT('',(80.6400616791356,100.332993858895,53.0267327569543));
#38220=CARTESIAN_POINT('',(80.6314498948689,423.667006141107,53.0228109606222));
#38221=CARTESIAN_POINT('Ctrl Pts',(80.6374103558004,101.667006141107,53.0273186999381));
#38222=CARTESIAN_POINT('Ctrl Pts',(80.6393935608058,101.639602041895,53.2696633040341));
#38223=CARTESIAN_POINT('Ctrl Pts',(80.5154322052391,101.40004193313,55.3859628634931));
#38224=CARTESIAN_POINT('Ctrl Pts',(77.8414071731253,100.948325814813,59.0542315289232));
#38225=CARTESIAN_POINT('Ctrl Pts',(71.4557480292651,100.311857786156,58.689182577611));
#38226=CARTESIAN_POINT('Ctrl Pts',(68.3107929723319,99.6753897574989,53.1055643668355));
#38227=CARTESIAN_POINT('Ctrl Pts',(70.811068570169,99.144999733618,48.404841819497));
#38228=CARTESIAN_POINT('Ctrl Pts',(74.4938206403223,98.7206877145134,47.176735522705));
#38229=CARTESIAN_POINT('Ctrl Pts',(78.330459889719,98.2963756954088,47.7692784801554));
#38230=CARTESIAN_POINT('Ctrl Pts',(80.4851494606274,97.9451485042735,50.5600566397906));
#38231=CARTESIAN_POINT('Ctrl Pts',(80.6387971620634,97.6999993179143,52.7249404172344));
#38232=CARTESIAN_POINT('Ctrl Pts',(80.6362700731203,97.6670061411075,53.016734409587));
#38233=CARTESIAN_POINT('Ctrl Pts',(80.6400616791356,100.332993858895,53.0267327569543));
#38234=CARTESIAN_POINT('Ctrl Pts',(80.6407843424398,100.317567852607,53.1628880610317));
#38235=CARTESIAN_POINT('Ctrl Pts',(80.6362648167285,100.302141846319,53.2989746798747));
#38236=CARTESIAN_POINT('Ctrl Pts',(80.6263460537318,100.286715840031,53.4346471959759));
#38237=CARTESIAN_POINT('Ctrl Pts',(80.4899319269776,100.074559830478,55.3005701759463));
#38238=CARTESIAN_POINT('Ctrl Pts',(79.3322583638292,99.8624038209258,57.0881661052152));
#38239=CARTESIAN_POINT('Ctrl Pts',(77.6881992837944,99.6502478113736,57.9866183866898));
#38240=CARTESIAN_POINT('Ctrl Pts',(76.8661697437769,99.5441698065974,58.4358445274272));
#38241=CARTESIAN_POINT('Ctrl Pts',(75.9225438245377,99.4380918018213,58.6627847562159));
#38242=CARTESIAN_POINT('Ctrl Pts',(74.9792695105176,99.3320137970451,58.6613326054378));
#38243=CARTESIAN_POINT('Ctrl Pts',(74.0359951964976,99.225935792269,58.6598804546596));
#38244=CARTESIAN_POINT('Ctrl Pts',(73.0930724876966,99.1198577874928,58.4300359243145));
#38245=CARTESIAN_POINT('Ctrl Pts',(72.2724299890143,99.0137797827166,57.978280924852));
#38246=CARTESIAN_POINT('Ctrl Pts',(70.6311449916498,98.8016237731643,57.074770925927));
#38247=CARTESIAN_POINT('Ctrl Pts',(69.4789808347601,98.5894677636121,55.2836190505323));
#38248=CARTESIAN_POINT('Ctrl Pts',(69.3483124386082,98.3773117540598,53.417284902689));
#38249=CARTESIAN_POINT('Ctrl Pts',(69.2176440424562,98.1651557445075,51.5509507548455));
#38250=CARTESIAN_POINT('Ctrl Pts',(70.108471407042,97.9529997349551,49.6094343345535));
#38251=CARTESIAN_POINT('Ctrl Pts',(71.609485997445,97.7408437254028,48.4900392197709));
#38252=CARTESIAN_POINT('Ctrl Pts',(73.1105005878481,97.5286877158505,47.3706441049884));
#38253=CARTESIAN_POINT('Ctrl Pts',(75.2217024040683,97.3165317062982,47.0733702957154));
#38254=CARTESIAN_POINT('Ctrl Pts',(76.9743338504003,97.1043756967459,47.7312906645623));
#38255=CARTESIAN_POINT('Ctrl Pts',(78.7269652967321,96.8922196871936,48.3892110334092));
#38256=CARTESIAN_POINT('Ctrl Pts',(80.1210263731757,96.6800636776413,50.0023255803758));
#38257=CARTESIAN_POINT('Ctrl Pts',(80.5146354724544,96.4679076680889,51.832943536304));
#38258=CARTESIAN_POINT('Ctrl Pts',(80.5980698329034,96.4229363983575,52.2209844597968));
#38259=CARTESIAN_POINT('Ctrl Pts',(80.6365514842358,96.3779651286261,52.6187983336141));
#38260=CARTESIAN_POINT('Ctrl Pts',(80.6327545556523,96.3329938588947,53.0173721012319));
#38261=CARTESIAN_POINT('Origin',(74.9879498948689,423.667006141107,53.0228109606356));
#38262=CARTESIAN_POINT('',(80.6232183355818,105.667006141107,53.0253975325881));
#38263=CARTESIAN_POINT('',(80.6224354235563,104.332993858895,53.0256136329225));
#38264=CARTESIAN_POINT('',(80.6314498948689,423.667006141107,53.0228109606222));
#38265=CARTESIAN_POINT('Ctrl Pts',(80.6232183355818,105.667006141107,53.0253975325881));
#38266=CARTESIAN_POINT('Ctrl Pts',(80.6260644232382,105.579204765875,53.8062098106832));
#38267=CARTESIAN_POINT('Ctrl Pts',(80.1085346718932,105.279247381091,56.469692650254));
#38268=CARTESIAN_POINT('Ctrl Pts',(76.0367440446578,104.767133986754,59.6170696871648));
#38269=CARTESIAN_POINT('Ctrl Pts',(70.0009775363973,104.130665958098,57.4636869316869));
#38270=CARTESIAN_POINT('Ctrl Pts',(68.8062846772482,103.600275934217,52.2751534679328));
#38271=CARTESIAN_POINT('Ctrl Pts',(70.781449457728,103.175963915112,48.9330535328036));
#38272=CARTESIAN_POINT('Ctrl Pts',(74.0666489726483,102.751651896007,46.8646309372967));
#38273=CARTESIAN_POINT('Ctrl Pts',(79.0170332829222,102.248665971339,47.8586964864205));
#38274=CARTESIAN_POINT('Ctrl Pts',(80.6240400599734,101.851758051447,51.3934890958369));
#38275=CARTESIAN_POINT('Ctrl Pts',(80.6374103558004,101.667006141107,53.0273186999381));
#38276=CARTESIAN_POINT('Ctrl Pts',(80.6224354235563,104.332993858895,53.0256136329225));
#38277=CARTESIAN_POINT('Ctrl Pts',(80.626288657042,104.257170576587,53.6993939361133));
#38278=CARTESIAN_POINT('Ctrl Pts',(80.3583492568762,104.075269289503,55.3132815258189));
#38279=CARTESIAN_POINT('Ctrl Pts',(78.8282293448942,103.787289997644,57.4582382784806));
#38280=CARTESIAN_POINT('Ctrl Pts',(75.3777508129794,103.362977978539,59.2373126971688));
#38281=CARTESIAN_POINT('Ctrl Pts',(70.2667783164759,102.832587954658,57.7452903541108));
#38282=CARTESIAN_POINT('Ctrl Pts',(68.4651765033714,102.196119926002,51.5953500665264));
#38283=CARTESIAN_POINT('Ctrl Pts',(72.6622400074956,101.559651897344,46.7689060980581));
#38284=CARTESIAN_POINT('Ctrl Pts',(78.8396299348509,100.938609874976,47.6581366381825));
#38285=CARTESIAN_POINT('Ctrl Pts',(80.6308454535261,100.529723862159,51.2903252308906));
#38286=CARTESIAN_POINT('Ctrl Pts',(80.6400616791356,100.332993858895,53.0267327569543));
#38287=CARTESIAN_POINT('Origin',(74.9879498948689,423.667006141107,53.0228109606356));
#38288=CARTESIAN_POINT('',(80.627375492094,109.667006141107,53.018034188696));
#38289=CARTESIAN_POINT('',(80.6285061370469,108.332993858894,53.0199845307064));
#38290=CARTESIAN_POINT('',(80.6314498948689,423.667006141107,53.0228109606222));
#38291=CARTESIAN_POINT('Ctrl Pts',(80.627375492094,109.667006141107,53.018034188696));
#38292=CARTESIAN_POINT('Ctrl Pts',(80.6172081439586,109.518807489856,54.3334327993462));
#38293=CARTESIAN_POINT('Ctrl Pts',(79.5040108698863,109.158452829052,57.5480756578864));
#38294=CARTESIAN_POINT('Ctrl Pts',(74.1348045617336,108.585942158696,59.6457571128379));
#38295=CARTESIAN_POINT('Ctrl Pts',(69.8305489765598,108.055552134815,56.5118211866107));
#38296=CARTESIAN_POINT('Ctrl Pts',(69.1302854250172,107.631240115711,52.6933740094433));
#38297=CARTESIAN_POINT('Ctrl Pts',(70.2542803117838,107.206928096606,48.9775237190036));
#38298=CARTESIAN_POINT('Ctrl Pts',(74.8827889425443,106.676538072725,46.3459693518712));
#38299=CARTESIAN_POINT('Ctrl Pts',(79.7705207976768,106.1278714193,48.9205634374283));
#38300=CARTESIAN_POINT('Ctrl Pts',(80.6191873715017,105.791360775428,51.9195193494878));
#38301=CARTESIAN_POINT('Ctrl Pts',(80.6232183355818,105.667006141107,53.0253975325881));
#38302=CARTESIAN_POINT('Ctrl Pts',(80.6285061370469,108.332993858894,53.0199845307063));
#38303=CARTESIAN_POINT('Ctrl Pts',(80.6273255247201,108.302851305344,53.287752480045));
#38304=CARTESIAN_POINT('Ctrl Pts',(80.5383454663005,108.166630747017,54.498662736846));
#38305=CARTESIAN_POINT('Ctrl Pts',(79.3572700732904,107.818254179138,57.4591402729806));
#38306=CARTESIAN_POINT('Ctrl Pts',(74.52013864804,107.287864155257,59.6840740039152));
#38307=CARTESIAN_POINT('Ctrl Pts',(69.1272472113271,106.6513961266,56.2222455007014));
#38308=CARTESIAN_POINT('Ctrl Pts',(69.1311857674209,106.014928097943,49.8261617046435));
#38309=CARTESIAN_POINT('Ctrl Pts',(74.5085221507447,105.378460069286,46.362903576955));
#38310=CARTESIAN_POINT('Ctrl Pts',(79.6429858726333,104.817815322937,48.7087080503247));
#38311=CARTESIAN_POINT('Ctrl Pts',(80.6155071844479,104.469326586139,51.8141347374896));
#38312=CARTESIAN_POINT('Ctrl Pts',(80.6224354235563,104.332993858895,53.0256136329225));
#38313=CARTESIAN_POINT('Origin',(74.9879498948689,423.667006141107,53.0228109606356));
#38314=CARTESIAN_POINT('',(80.6411686659135,113.667006141107,53.0214655157299));
#38315=CARTESIAN_POINT('',(80.6367476654038,112.332993858895,53.0201225356658));
#38316=CARTESIAN_POINT('',(80.6314498948689,423.667006141107,53.0228109606222));
#38317=CARTESIAN_POINT('Ctrl Pts',(80.6411686659135,113.667006141107,53.0214655157299));
#38318=CARTESIAN_POINT('Ctrl Pts',(80.6381590892165,113.458410213836,54.8626429328173));
#38319=CARTESIAN_POINT('Ctrl Pts',(78.6510709869002,113.037658277013,58.5856119621277));
#38320=CARTESIAN_POINT('Ctrl Pts',(73.3819666201983,112.510828335414,59.0388557003805));
#38321=CARTESIAN_POINT('Ctrl Pts',(70.3494075285618,112.086516316309,56.6151203100856));
#38322=CARTESIAN_POINT('Ctrl Pts',(68.7614344313501,111.662204297205,53.0726283441146));
#38323=CARTESIAN_POINT('Ctrl Pts',(70.5303630449218,111.131814273324,48.0507699139827));
#38324=CARTESIAN_POINT('Ctrl Pts',(76.7695181841129,110.495346244667,46.587732736418));
#38325=CARTESIAN_POINT('Ctrl Pts',(80.290773265235,110.007076867261,50.0049409544789));
#38326=CARTESIAN_POINT('Ctrl Pts',(80.6317633641979,109.730963499408,52.4503541218443));
#38327=CARTESIAN_POINT('Ctrl Pts',(80.627375492094,109.667006141107,53.018034188696));
#38328=CARTESIAN_POINT('Ctrl Pts',(80.6367476654038,112.332993858895,53.0201225356658));
#38329=CARTESIAN_POINT('Ctrl Pts',(80.6253734967643,112.136376024548,54.7573615278239));
#38330=CARTESIAN_POINT('Ctrl Pts',(78.8479097578291,111.727602180649,58.3813275115759));
#38331=CARTESIAN_POINT('Ctrl Pts',(72.6610927960897,111.106672327199,59.2814013261173));
#38332=CARTESIAN_POINT('Ctrl Pts',(68.4699764911283,110.470204298542,54.4497921162674));
#38333=CARTESIAN_POINT('Ctrl Pts',(70.2588968349819,109.833736269885,48.3089723467443));
#38334=CARTESIAN_POINT('Ctrl Pts',(76.4059152161931,109.197268241228,46.4974261411829));
#38335=CARTESIAN_POINT('Ctrl Pts',(80.1971179225261,108.697020770898,49.7905105458927));
#38336=CARTESIAN_POINT('Ctrl Pts',(80.6314803485583,108.40892931012,52.3454205783677));
#38337=CARTESIAN_POINT('Ctrl Pts',(80.6285061370469,108.332993858894,53.0199845307063));
#38338=CARTESIAN_POINT('Origin',(74.9879498948689,423.667006141107,53.0228109606356));
#38339=CARTESIAN_POINT('',(80.6297280373482,117.667006141107,53.029522769627));
#38340=CARTESIAN_POINT('',(80.63273293575,116.332993858895,53.0278590605154));
#38341=CARTESIAN_POINT('',(80.6314498948689,423.667006141107,53.0228109606222));
#38342=CARTESIAN_POINT('Ctrl Pts',(80.6297280373482,117.667006141107,53.029522769627));
#38343=CARTESIAN_POINT('Ctrl Pts',(80.6342201504912,117.610168947369,53.5338174939984));
#38344=CARTESIAN_POINT('Ctrl Pts',(80.3409432296834,117.341175744079,55.9145507214586));
#38345=CARTESIAN_POINT('Ctrl Pts',(77.7203244431643,116.966104536013,58.6179969197401));
#38346=CARTESIAN_POINT('Ctrl Pts',(73.841439580255,116.541792516908,58.7766162966422));
#38347=CARTESIAN_POINT('Ctrl Pts',(70.3196135975197,116.117480497803,57.1433221915374));
#38348=CARTESIAN_POINT('Ctrl Pts',(68.3621779488011,115.587090473922,52.1918965167118));
#38349=CARTESIAN_POINT('Ctrl Pts',(72.1133696732489,114.950622445266,46.9961198394222));
#38350=CARTESIAN_POINT('Ctrl Pts',(78.4996923124141,114.314154416609,47.3493712893946));
#38351=CARTESIAN_POINT('Ctrl Pts',(80.6269983281491,113.886282315223,51.0860990420978));
#38352=CARTESIAN_POINT('Ctrl Pts',(80.6412200300068,113.670566223389,52.9900423562021));
#38353=CARTESIAN_POINT('Ctrl Pts',(80.6411686659135,113.667006141107,53.0214655157299));
#38354=CARTESIAN_POINT('Ctrl Pts',(80.63273293575,116.332993858895,53.0278590605154));
#38355=CARTESIAN_POINT('Ctrl Pts',(80.6367547024567,116.288134758081,53.4247644365811));
#38356=CARTESIAN_POINT('Ctrl Pts',(80.4185607171579,116.031119647715,55.695001895594));
#38357=CARTESIAN_POINT('Ctrl Pts',(77.3351104931415,115.561948527797,59.2738152357066));
#38358=CARTESIAN_POINT('Ctrl Pts',(71.002608172017,114.92548049914,58.3741943203373));
#38359=CARTESIAN_POINT('Ctrl Pts',(68.326532179209,114.289012470483,52.5648466186468));
#38360=CARTESIAN_POINT('Ctrl Pts',(71.7796338362221,113.652544441826,47.1663631667719));
#38361=CARTESIAN_POINT('Ctrl Pts',(77.1039338323076,113.122154417946,47.1666527860612));
#38362=CARTESIAN_POINT('Ctrl Pts',(79.9174693977396,112.697842398841,49.8415220367884));
#38363=CARTESIAN_POINT('Ctrl Pts',(80.6034465893773,112.470148214083,51.8085666155929));
#38364=CARTESIAN_POINT('Ctrl Pts',(80.6376465351616,112.348532034101,52.8828332408032));
#38365=CARTESIAN_POINT('Ctrl Pts',(80.6367476654038,112.332993858895,53.0201225356658));
#38366=CARTESIAN_POINT('Origin',(74.9879498948689,423.667006141107,53.0228109606356));
#38367=CARTESIAN_POINT('',(80.621118997799,121.667006141107,53.0201440891292));
#38368=CARTESIAN_POINT('',(80.6220356038237,120.332993858894,53.0220685349663));
#38369=CARTESIAN_POINT('',(80.6314498948689,423.667006141107,53.0228109606222));
#38370=CARTESIAN_POINT('Ctrl Pts',(80.621118997799,121.667006141107,53.0201440891292));
#38371=CARTESIAN_POINT('Ctrl Pts',(80.6173308858264,121.54977167135,54.0624647895258));
#38372=CARTESIAN_POINT('Ctrl Pts',(80.0879360230795,121.326459196816,56.0512552874316));
#38373=CARTESIAN_POINT('Ctrl Pts',(77.8952676648289,120.997068717506,58.1187176641229));
#38374=CARTESIAN_POINT('Ctrl Pts',(74.1653018934157,120.572756698402,59.1949440485428));
#38375=CARTESIAN_POINT('Ctrl Pts',(69.4406556577397,120.042366674521,56.7401755299422));
#38376=CARTESIAN_POINT('Ctrl Pts',(68.8657804610841,119.405898645864,50.3576170192741));
#38377=CARTESIAN_POINT('Ctrl Pts',(73.9190741955237,118.769430617207,46.4366317002641));
#38378=CARTESIAN_POINT('Ctrl Pts',(79.4141901927945,118.189799782288,48.3687963867855));
#38379=CARTESIAN_POINT('Ctrl Pts',(80.6174524542663,117.822324956922,51.6514382045845));
#38380=CARTESIAN_POINT('Ctrl Pts',(80.6297280373482,117.667006141107,53.029522769627));
#38381=CARTESIAN_POINT('Ctrl Pts',(80.6220356038237,120.332993858894,53.0220685349662));
#38382=CARTESIAN_POINT('Ctrl Pts',(80.6222590142985,120.227737482062,53.9594345098134));
#38383=CARTESIAN_POINT('Ctrl Pts',(79.9569189659327,119.910325095676,56.7865524380521));
#38384=CARTESIAN_POINT('Ctrl Pts',(75.4880780795087,119.380756699739,59.6763907722353));
#38385=CARTESIAN_POINT('Ctrl Pts',(69.6582969414783,118.744288671082,57.0451258062755));
#38386=CARTESIAN_POINT('Ctrl Pts',(68.7254440554294,118.107820642425,50.7049901510374));
#38387=CARTESIAN_POINT('Ctrl Pts',(72.7454665815478,117.577430618544,47.2139173328772));
#38388=CARTESIAN_POINT('Ctrl Pts',(76.6236647050234,117.153118599439,47.3885231790242));
#38389=CARTESIAN_POINT('Ctrl Pts',(79.6362958357505,116.773665681149,49.1138518710274));
#38390=CARTESIAN_POINT('Ctrl Pts',(80.6177342147434,116.500290767633,51.5476456528997));
#38391=CARTESIAN_POINT('Ctrl Pts',(80.63273293575,116.332993858895,53.0278590605154));
#38392=CARTESIAN_POINT('Origin',(74.9879498948689,423.667006141107,53.0228109606356));
#38393=CARTESIAN_POINT('',(80.6357111684385,125.667006141107,53.0197150307418));
#38394=CARTESIAN_POINT('',(80.6328519299148,124.332993858894,53.0182731545141));
#38395=CARTESIAN_POINT('',(80.6314498948689,423.667006141107,53.0228109606222));
#38396=CARTESIAN_POINT('Ctrl Pts',(80.6357111684385,125.667006141107,53.0197150307418));
#38397=CARTESIAN_POINT('Ctrl Pts',(80.6319016651264,125.595452400107,53.652965053311));
#38398=CARTESIAN_POINT('Ctrl Pts',(80.3527813722094,125.41782065433,55.2289179960977));
#38399=CARTESIAN_POINT('Ctrl Pts',(78.414091999895,125.028032899,58.2221885065829));
#38400=CARTESIAN_POINT('Ctrl Pts',(73.2373364704086,124.49764287512,59.4669265192302));
#38401=CARTESIAN_POINT('Ctrl Pts',(68.6180861968185,123.861174846463,55.0250731286094));
#38402=CARTESIAN_POINT('Ctrl Pts',(69.8622107451905,123.224706817806,48.7511542937376));
#38403=CARTESIAN_POINT('Ctrl Pts',(75.8090405776548,122.588238789149,46.3963467894746));
#38404=CARTESIAN_POINT('Ctrl Pts',(80.0527232061874,122.069005230249,49.4497267074848));
#38405=CARTESIAN_POINT('Ctrl Pts',(80.6241861283289,121.761927680902,52.1762055610979));
#38406=CARTESIAN_POINT('Ctrl Pts',(80.621118997799,121.667006141107,53.0201440891292));
#38407=CARTESIAN_POINT('Ctrl Pts',(80.6328519299148,124.332993858894,53.0182731545141));
#38408=CARTESIAN_POINT('Ctrl Pts',(80.6189547166767,124.167340206042,54.4855436430345));
#38409=CARTESIAN_POINT('Ctrl Pts',(79.2808346715744,123.789530543638,57.852453412815));
#38410=CARTESIAN_POINT('Ctrl Pts',(73.6016194435095,123.19956487168,59.5544497443309));
#38411=CARTESIAN_POINT('Ctrl Pts',(68.7399147931205,122.563096843024,55.3793614187719));
#38412=CARTESIAN_POINT('Ctrl Pts',(69.4858278482179,122.032706819143,50.107570048997));
#38413=CARTESIAN_POINT('Ctrl Pts',(72.5283512255512,121.608394800038,47.6963547154323));
#38414=CARTESIAN_POINT('Ctrl Pts',(76.33686993267,121.184082780934,46.9439630993421));
#38415=CARTESIAN_POINT('Ctrl Pts',(79.9412181579135,120.758949133886,49.2290963001954));
#38416=CARTESIAN_POINT('Ctrl Pts',(80.6218087054788,120.439893491614,52.0700684619069));
#38417=CARTESIAN_POINT('Ctrl Pts',(80.6220356038237,120.332993858894,53.0220685349662));
#38418=CARTESIAN_POINT('Origin',(74.9879498948689,423.667006141107,53.0228109606356));
#38419=CARTESIAN_POINT('',(80.6371028432593,129.667006141107,53.0252254998433));
#38420=CARTESIAN_POINT('',(80.6389896620935,128.332993858894,53.0249895228329));
#38421=CARTESIAN_POINT('',(80.6314498948689,423.667006141107,53.0228109606222));
#38422=CARTESIAN_POINT('Ctrl Pts',(80.6371028432593,129.667006141107,53.0252254998433));
#38423=CARTESIAN_POINT('Ctrl Pts',(80.6382524187439,129.641133128863,53.2540168026428));
#38424=CARTESIAN_POINT('Ctrl Pts',(80.5164513696564,129.403104107067,55.3571413879679));
#38425=CARTESIAN_POINT('Ctrl Pts',(77.8918269900061,128.952919075718,59.0360272806059));
#38426=CARTESIAN_POINT('Ctrl Pts',(71.4916583615966,128.316451047061,58.7114103344188));
#38427=CARTESIAN_POINT('Ctrl Pts',(68.3169862074485,127.679983018404,53.1588109294466));
#38428=CARTESIAN_POINT('Ctrl Pts',(71.2627145002853,127.043514989747,47.4814358085654));
#38429=CARTESIAN_POINT('Ctrl Pts',(77.644334875132,126.40704696109,46.8962383844676));
#38430=CARTESIAN_POINT('Ctrl Pts',(80.469995123209,125.94821067821,50.5336793739854));
#38431=CARTESIAN_POINT('Ctrl Pts',(80.6375492316251,125.701530404883,52.7141755787275));
#38432=CARTESIAN_POINT('Ctrl Pts',(80.6357111684385,125.667006141107,53.0197150307418));
#38433=CARTESIAN_POINT('Ctrl Pts',(80.6389896620935,128.332993858894,53.0249895228329));
#38434=CARTESIAN_POINT('Ctrl Pts',(80.6395867975546,128.319098939575,53.1476577057808));
#38435=CARTESIAN_POINT('Ctrl Pts',(80.5801191447157,128.093048010703,55.1427011305502));
#38436=CARTESIAN_POINT('Ctrl Pts',(78.2242510960193,127.654841072279,58.8632366177664));
#38437=CARTESIAN_POINT('Ctrl Pts',(71.8159553123667,127.018373043623,58.8990106732897));
#38438=CARTESIAN_POINT('Ctrl Pts',(68.9222576097237,126.487983019741,54.4297060139589));
#38439=CARTESIAN_POINT('Ctrl Pts',(69.6382539201413,126.063671000637,50.6141775879205));
#38440=CARTESIAN_POINT('Ctrl Pts',(72.0203115207733,125.639358981532,47.5487723172087));
#38441=CARTESIAN_POINT('Ctrl Pts',(77.2847411767612,125.108968957652,46.7525619622429));
#38442=CARTESIAN_POINT('Ctrl Pts',(80.4073730821569,124.638154581847,50.3192597336851));
#38443=CARTESIAN_POINT('Ctrl Pts',(80.636753160923,124.379496215594,52.6063804225535));
#38444=CARTESIAN_POINT('Ctrl Pts',(80.6328519299148,124.332993858894,53.0182731545141));
#38445=CARTESIAN_POINT('Origin',(74.9879498948689,423.667006141107,53.0228109606356));
#38446=CARTESIAN_POINT('',(80.6223069729932,133.667006141107,53.0265007246441));
#38447=CARTESIAN_POINT('',(80.6314498948689,132.332993858894,53.0228109606253));
#38448=CARTESIAN_POINT('',(80.6314498948689,423.667006141107,53.0228109606222));
#38449=CARTESIAN_POINT('Ctrl Pts',(80.6223069729932,133.667006141107,53.0265007246441));
#38450=CARTESIAN_POINT('Ctrl Pts',(80.6265294801301,133.580735852844,53.7931407639138));
#38451=CARTESIAN_POINT('Ctrl Pts',(80.1255680059032,133.282309555028,56.4402161564905));
#38452=CARTESIAN_POINT('Ctrl Pts',(76.0784316098281,132.77172724766,59.6103041826723));
#38453=CARTESIAN_POINT('Ctrl Pts',(70.0405686636907,132.135259219003,57.4998268712375));
#38454=CARTESIAN_POINT('Ctrl Pts',(68.5417731922881,131.498791190346,51.2818275488413));
#38455=CARTESIAN_POINT('Ctrl Pts',(72.9761497214014,130.862323161689,46.6553991821764));
#38456=CARTESIAN_POINT('Ctrl Pts',(78.1993353737933,130.331933137808,47.6881151028675));
#38457=CARTESIAN_POINT('Ctrl Pts',(80.30411061963,129.933494130948,50.6645098309892));
#38458=CARTESIAN_POINT('Ctrl Pts',(80.6335392190362,129.747211133639,52.3159843585587));
#38459=CARTESIAN_POINT('Ctrl Pts',(80.6371028432593,129.667006141107,53.0252254998433));
#38460=CARTESIAN_POINT('Ctrl Pts',(80.6259063365819,132.332993858894,53.0265080521389));
#38461=CARTESIAN_POINT('Ctrl Pts',(80.6305336094359,132.258701663556,53.6865164641486));
#38462=CARTESIAN_POINT('Ctrl Pts',(80.2181584724033,131.972253458664,56.2262411860581));
#38463=CARTESIAN_POINT('Ctrl Pts',(76.4462897180739,131.473649244221,59.5392914259234));
#38464=CARTESIAN_POINT('Ctrl Pts',(71.3309082217835,130.94325922034,58.0624560662408));
#38465=CARTESIAN_POINT('Ctrl Pts',(69.3695355394668,130.518947201236,54.7122433733663));
#38466=CARTESIAN_POINT('Ctrl Pts',(69.1579113875603,130.094635182131,50.8358890158844));
#38467=CARTESIAN_POINT('Ctrl Pts',(72.6104447936233,129.56424515825,46.7827194398347));
#38468=CARTESIAN_POINT('Ctrl Pts',(78.8205962231645,128.941672048912,47.6359557426244));
#38469=CARTESIAN_POINT('Ctrl Pts',(80.6304693731441,128.531254949127,51.2746858953672));
#38470=CARTESIAN_POINT('Ctrl Pts',(80.6389896620935,128.332993858894,53.0249895228329));
#38471=CARTESIAN_POINT('Origin',(74.9879498948689,423.667006141107,53.0228109606356));
#38472=CARTESIAN_POINT('',(80.6275033360921,137.667006141107,53.0165438204127));
#38473=CARTESIAN_POINT('',(80.6314498948689,136.332993858894,53.0228109606257));
#38474=CARTESIAN_POINT('',(80.6314498948689,423.667006141107,53.0228109606222));
#38475=CARTESIAN_POINT('Ctrl Pts',(80.6275033360921,137.667006141107,53.0165438204127));
#38476=CARTESIAN_POINT('Ctrl Pts',(80.6170493129659,137.520338576824,54.3192593131434));
#38477=CARTESIAN_POINT('Ctrl Pts',(79.5194214481417,137.161515002989,57.5247164620686));
#38478=CARTESIAN_POINT('Ctrl Pts',(74.1883937223739,136.590535419602,59.6470816704889));
#38479=CARTESIAN_POINT('Ctrl Pts',(68.9794920835046,135.954067390944,55.9353102396218));
#38480=CARTESIAN_POINT('Ctrl Pts',(69.2937571436266,135.317599362288,49.534624955543));
#38481=CARTESIAN_POINT('Ctrl Pts',(73.9144292228386,134.787209338407,46.8893347883613));
#38482=CARTESIAN_POINT('Ctrl Pts',(77.6851592684559,134.362897319302,47.8126455754286));
#38483=CARTESIAN_POINT('Ctrl Pts',(80.0200232668462,134.024855588461,49.8409324552161));
#38484=CARTESIAN_POINT('Ctrl Pts',(80.6161454848692,133.792891862396,51.9078185426905));
#38485=CARTESIAN_POINT('Ctrl Pts',(80.6223069729932,133.667006141107,53.0265007246441));
#38486=CARTESIAN_POINT('Ctrl Pts',(80.6314498948689,136.332993858894,53.0228109606257));
#38487=CARTESIAN_POINT('Ctrl Pts',(80.6314498948719,136.140209036292,54.7318077489449));
#38488=CARTESIAN_POINT('Ctrl Pts',(79.8060659192693,135.94742421369,56.4221521097263));
#38489=CARTESIAN_POINT('Ctrl Pts',(78.4584055093439,135.754639391087,57.4730952299782));
#38490=CARTESIAN_POINT('Ctrl Pts',(77.1107450994185,135.561854568485,58.5240383502302));
#38491=CARTESIAN_POINT('Ctrl Pts',(75.2702256751625,135.369069745882,58.9126397065623));
#38492=CARTESIAN_POINT('Ctrl Pts',(73.6127451627042,135.17628492328,58.4961923829952));
#38493=CARTESIAN_POINT('Ctrl Pts',(71.9552646502458,134.983500100678,58.0797450594281));
#38494=CARTESIAN_POINT('Ctrl Pts',(70.5170033810729,134.790715278075,56.8673394809174));
#38495=CARTESIAN_POINT('Ctrl Pts',(69.8261371496123,134.597930455473,55.3042099684609));
#38496=CARTESIAN_POINT('Ctrl Pts',(69.1352709181517,134.40514563287,53.7410804560043));
#38497=CARTESIAN_POINT('Ctrl Pts',(69.2068803054901,134.212360810268,51.8613477992545));
#38498=CARTESIAN_POINT('Ctrl Pts',(70.0146680415444,134.019575987666,50.3553102844608));
#38499=CARTESIAN_POINT('Ctrl Pts',(70.8224557775985,133.826791165063,48.8492727696672));
#38500=CARTESIAN_POINT('Ctrl Pts',(72.3487890589403,133.634006342461,47.7498049531873));
#38501=CARTESIAN_POINT('Ctrl Pts',(74.0331492157619,133.441221519858,47.460666777573));
#38502=CARTESIAN_POINT('Ctrl Pts',(75.7175093725834,133.248436697256,47.1715286019588));
#38503=CARTESIAN_POINT('Ctrl Pts',(77.523129330786,133.055651874653,47.6990315230379));
#38504=CARTESIAN_POINT('Ctrl Pts',(78.7869273705894,132.862867052051,48.8494595029977));
#38505=CARTESIAN_POINT('Ctrl Pts',(79.9447859852113,132.686242654332,49.9034514424897));
#38506=CARTESIAN_POINT('Ctrl Pts',(80.631449894866,132.509618256613,51.4570729301846));
#38507=CARTESIAN_POINT('Ctrl Pts',(80.6314498948689,132.332993858894,53.0228109606253));
#38508=CARTESIAN_POINT('Origin',(74.9879498948689,423.667006141107,53.0228109606356));
#38509=CARTESIAN_POINT('',(80.6411518234535,141.667006141107,53.0227491827673));
#38510=CARTESIAN_POINT('',(80.6397210784657,140.332993858894,53.0209782018833));
#38511=CARTESIAN_POINT('',(80.6314498948689,423.667006141107,53.0228109606222));
#38512=CARTESIAN_POINT('Ctrl Pts',(80.6411518234535,141.667006141107,53.0227491827673));
#38513=CARTESIAN_POINT('Ctrl Pts',(80.6375409305296,141.459941300805,54.8502991094422));
#38514=CARTESIAN_POINT('Ctrl Pts',(79.6692138860864,141.252876460503,56.679321513607));
#38515=CARTESIAN_POINT('Ctrl Pts',(78.1561081471227,141.0458116202,57.7034820184246));
#38516=CARTESIAN_POINT('Ctrl Pts',(76.6057991949101,140.833655610648,58.7528238841218));
#38517=CARTESIAN_POINT('Ctrl Pts',(74.4835929147854,140.621499601096,58.9572384899893));
#38518=CARTESIAN_POINT('Ctrl Pts',(72.7625167868681,140.409343591543,58.2196836204947));
#38519=CARTESIAN_POINT('Ctrl Pts',(71.0414406589509,140.197187581991,57.4821287510002));
#38520=CARTESIAN_POINT('Ctrl Pts',(69.7214946832408,139.985031572439,55.8026044061438));
#38521=CARTESIAN_POINT('Ctrl Pts',(69.4123227137353,139.772875562886,53.9574241779733));
#38522=CARTESIAN_POINT('Ctrl Pts',(69.1031507442298,139.560719553334,52.1122439498026));
#38523=CARTESIAN_POINT('Ctrl Pts',(69.8047527809292,139.348563543782,50.1014078383178));
#38524=CARTESIAN_POINT('Ctrl Pts',(71.1893974253191,139.136407534229,48.839304051185));
#38525=CARTESIAN_POINT('Ctrl Pts',(71.8817197475139,139.030329529453,48.2082521576187));
#38526=CARTESIAN_POINT('Ctrl Pts',(72.7448027216314,138.924251524677,47.7643833451403));
#38527=CARTESIAN_POINT('Ctrl Pts',(73.6616100464181,138.818173519901,47.5424985339224));
#38528=CARTESIAN_POINT('Ctrl Pts',(74.5784173712049,138.712095515125,47.3206137227045));
#38529=CARTESIAN_POINT('Ctrl Pts',(75.5489490466608,138.606017510349,47.3207129127471));
#38530=CARTESIAN_POINT('Ctrl Pts',(76.4532076287885,138.499939505572,47.5653618588544));
#38531=CARTESIAN_POINT('Ctrl Pts',(78.2617247930437,138.28778349602,48.0546597510688));
#38532=CARTESIAN_POINT('Ctrl Pts',(79.8051495839855,138.075627486468,49.522156667542));
#38533=CARTESIAN_POINT('Ctrl Pts',(80.3739101054989,137.863471476916,51.3045115284849));
#38534=CARTESIAN_POINT('Ctrl Pts',(80.5494754470752,137.797983031646,51.8546899043311));
#38535=CARTESIAN_POINT('Ctrl Pts',(80.6321711556246,137.732494586377,52.4348691150039));
#38536=CARTESIAN_POINT('Ctrl Pts',(80.6275033360921,137.667006141107,53.0165438204127));
#38537=CARTESIAN_POINT('Ctrl Pts',(80.6397210784657,140.332993858894,53.0209782018833));
#38538=CARTESIAN_POINT('Ctrl Pts',(80.6287643883681,140.137907111517,54.7421720158137));
#38539=CARTESIAN_POINT('Ctrl Pts',(79.321297971357,139.836742359363,57.4088279887623));
#38540=CARTESIAN_POINT('Ctrl Pts',(75.8739191842768,139.429499602433,58.8224506187867));
#38541=CARTESIAN_POINT('Ctrl Pts',(72.0061278849508,139.005187583328,58.4891364257266));
#38542=CARTESIAN_POINT('Ctrl Pts',(68.476400198112,138.474797559447,54.5030113663535));
#38543=CARTESIAN_POINT('Ctrl Pts',(70.2291765021866,137.83832953079,48.3389777955731));
#38544=CARTESIAN_POINT('Ctrl Pts',(76.3526370626844,137.201861502133,46.4915108263287));
#38545=CARTESIAN_POINT('Ctrl Pts',(80.1931527706955,136.700082944835,49.7591848231774));
#38546=CARTESIAN_POINT('Ctrl Pts',(80.6290640066136,136.410460397088,52.3302465850105));
#38547=CARTESIAN_POINT('Ctrl Pts',(80.6247374915432,136.332993858894,53.019329840359));
#38548=CARTESIAN_POINT('Origin',(74.9879498948689,423.667006141107,53.0228109606356));
#38549=CARTESIAN_POINT('',(80.629461543256,145.667006141107,53.0278924515447));
#38550=CARTESIAN_POINT('',(80.6299737020758,144.332993858894,53.0273121532265));
#38551=CARTESIAN_POINT('',(80.6314498948689,423.667006141107,53.0228109606222));
#38552=CARTESIAN_POINT('Ctrl Pts',(80.629461543256,145.667006141107,53.0278924515447));
#38553=CARTESIAN_POINT('Ctrl Pts',(80.633661519085,145.611700034338,53.5183154898172));
#38554=CARTESIAN_POINT('Ctrl Pts',(80.5749012622352,145.556393927568,54.0077190168699));
#38555=CARTESIAN_POINT('Ctrl Pts',(80.4491472122468,145.501087820799,54.4792559898802));
#38556=CARTESIAN_POINT('Ctrl Pts',(79.9667506200988,145.288931811246,56.288087028507));
#38557=CARTESIAN_POINT('Ctrl Pts',(78.4985307500936,145.076775801694,57.8340091610261));
#38558=CARTESIAN_POINT('Ctrl Pts',(76.7154875349777,144.864619792142,58.4057146067159));
#38559=CARTESIAN_POINT('Ctrl Pts',(74.9324443198619,144.65246378259,58.9774200524057));
#38560=CARTESIAN_POINT('Ctrl Pts',(72.8345777596355,144.440307773037,58.5749088112661));
#38561=CARTESIAN_POINT('Ctrl Pts',(71.3912177720621,144.228151763485,57.3845352029265));
#38562=CARTESIAN_POINT('Ctrl Pts',(69.9478577844887,144.015995753933,56.1941615945869));
#38563=CARTESIAN_POINT('Ctrl Pts',(69.1590043695682,143.80383974438,54.2159256190472));
#38564=CARTESIAN_POINT('Ctrl Pts',(69.3768109363074,143.591683734828,52.3550905752519));
#38565=CARTESIAN_POINT('Ctrl Pts',(69.485714219677,143.485605730052,51.4246730533542));
#38566=CARTESIAN_POINT('Ctrl Pts',(69.8462824984615,143.379527725276,50.5236057643925));
#38567=CARTESIAN_POINT('Ctrl Pts',(70.3929736009116,143.2734497205,49.7549072677544));
#38568=CARTESIAN_POINT('Ctrl Pts',(70.9396647033619,143.167371715723,48.9862087711162));
#38569=CARTESIAN_POINT('Ctrl Pts',(71.6724786294777,143.061293710947,48.3498790668017));
#38570=CARTESIAN_POINT('Ctrl Pts',(72.5156146144877,142.955215706171,47.9416408998399));
#38571=CARTESIAN_POINT('Ctrl Pts',(74.2018865845076,142.743059696619,47.1251645659165));
#38572=CARTESIAN_POINT('Ctrl Pts',(76.329446790104,142.530903687066,47.2210543814042));
#38573=CARTESIAN_POINT('Ctrl Pts',(77.9275991182749,142.318747677514,48.1937755732785));
#38574=CARTESIAN_POINT('Ctrl Pts',(79.5257514464457,142.106591667962,49.1664967651527));
#38575=CARTESIAN_POINT('Ctrl Pts',(80.5944958971913,141.894435658409,51.0160493334135));
#38576=CARTESIAN_POINT('Ctrl Pts',(80.6396623104136,141.682279648857,52.8879601803071));
#38577=CARTESIAN_POINT('Ctrl Pts',(80.6407461819222,141.677188479607,52.9328809674318));
#38578=CARTESIAN_POINT('Ctrl Pts',(80.6412406056292,141.672097310357,52.9778146300166));
#38579=CARTESIAN_POINT('Ctrl Pts',(80.6411518234535,141.667006141107,53.0227491827673));
#38580=CARTESIAN_POINT('Ctrl Pts',(80.6299737020758,144.332993858894,53.0273121532265));
#38581=CARTESIAN_POINT('Ctrl Pts',(80.6335616117796,144.28966584505,53.4111490723472));
#38582=CARTESIAN_POINT('Ctrl Pts',(80.5111600798701,144.140259826428,54.7328567481776));
#38583=CARTESIAN_POINT('Ctrl Pts',(79.4598393053229,143.884775803031,56.8205690949624));
#38584=CARTESIAN_POINT('Ctrl Pts',(76.3211035792066,143.460463783927,59.1051359965959));
#38585=CARTESIAN_POINT('Ctrl Pts',(71.0423553953876,142.930073760046,58.4101625121945));
#38586=CARTESIAN_POINT('Ctrl Pts',(68.3237688121462,142.293605731389,52.6069891024768));
#38587=CARTESIAN_POINT('Ctrl Pts',(71.7355301328902,141.657137702732,47.1968330854384));
#38588=CARTESIAN_POINT('Ctrl Pts',(78.131284816172,141.020669674075,47.1318294725001));
#38589=CARTESIAN_POINT('Ctrl Pts',(80.567608711688,140.579288392796,50.8486300315097));
#38590=CARTESIAN_POINT('Ctrl Pts',(80.6406797423337,140.350063121069,52.870381050318));
#38591=CARTESIAN_POINT('Ctrl Pts',(80.6397210784657,140.332993858894,53.0209782018833));
#38592=CARTESIAN_POINT('Origin',(74.9879498948689,423.667006141107,53.0228109606356));
#38593=CARTESIAN_POINT('',(80.6225096147018,149.667006141107,53.0213500647842));
#38594=CARTESIAN_POINT('',(80.6264905426344,148.332993858894,53.023059952509));
#38595=CARTESIAN_POINT('',(80.6314498948689,423.667006141107,53.0228109606222));
#38596=CARTESIAN_POINT('Ctrl Pts',(80.6225096147018,149.667006141107,53.0213500647842));
#38597=CARTESIAN_POINT('Ctrl Pts',(80.6207021386803,149.551302758318,54.0506438715325));
#38598=CARTESIAN_POINT('Ctrl Pts',(79.8583912421759,149.223443365977,56.970430727468));
#38599=CARTESIAN_POINT('Ctrl Pts',(75.1550028210449,148.683427964083,59.698390786709));
#38600=CARTESIAN_POINT('Ctrl Pts',(70.4230863720779,148.153037940203,57.2576660475808));
#38601=CARTESIAN_POINT('Ctrl Pts',(69.1485793584295,147.728725921098,53.5907136673885));
#38602=CARTESIAN_POINT('Ctrl Pts',(69.6926334846929,147.304413901994,49.7468987662606));
#38603=CARTESIAN_POINT('Ctrl Pts',(73.8655835469356,146.774023878113,46.4401392784498));
#38604=CARTESIAN_POINT('Ctrl Pts',(79.3981822703055,146.192861956225,48.3456113603836));
#38605=CARTESIAN_POINT('Ctrl Pts',(80.6175502763282,145.82385604389,51.6370368956453));
#38606=CARTESIAN_POINT('Ctrl Pts',(80.629461543256,145.667006141107,53.0278924515447));
#38607=CARTESIAN_POINT('Ctrl Pts',(80.6264905426344,148.332993858894,53.023059952509));
#38608=CARTESIAN_POINT('Ctrl Pts',(80.6268129881547,148.22926856903,53.9454088413081));
#38609=CARTESIAN_POINT('Ctrl Pts',(79.9631268520014,147.913387269614,56.7537913392259));
#38610=CARTESIAN_POINT('Ctrl Pts',(75.5416724725442,147.385349960645,59.6774833042897));
#38611=CARTESIAN_POINT('Ctrl Pts',(69.6838446044191,146.748881931988,57.0787552882691));
#38612=CARTESIAN_POINT('Ctrl Pts',(68.712125846895,146.112413903331,50.7569148841861));
#38613=CARTESIAN_POINT('Ctrl Pts',(73.4982792811873,145.475945874674,46.5139632297563));
#38614=CARTESIAN_POINT('Ctrl Pts',(79.2453262741431,144.882805859862,48.1381250442711));
#38615=CARTESIAN_POINT('Ctrl Pts',(80.6159933796395,144.501821854602,51.5316881450347));
#38616=CARTESIAN_POINT('Ctrl Pts',(80.6299737020758,144.332993858894,53.0273121532265));
#38617=CARTESIAN_POINT('Origin',(74.9879498948689,423.667006141107,53.0228109606356));
#38618=CARTESIAN_POINT('',(80.6352064155011,153.667006141107,53.0176672101712));
#38619=CARTESIAN_POINT('',(80.6287116038918,152.332993858894,53.0183048799968));
#38620=CARTESIAN_POINT('',(80.6314498948689,423.667006141107,53.0228109606222));
#38621=CARTESIAN_POINT('Ctrl Pts',(80.6352064155011,153.667006141107,53.0176672101712));
#38622=CARTESIAN_POINT('Ctrl Pts',(80.6209020684031,153.490905482299,54.5766293472566));
#38623=CARTESIAN_POINT('Ctrl Pts',(79.1397801677944,153.102648813938,58.0389759024666));
#38624=CARTESIAN_POINT('Ctrl Pts',(74.3184020126598,152.608314140801,59.2134233877355));
#38625=CARTESIAN_POINT('Ctrl Pts',(70.9516299530984,152.184002121697,57.2806135715887));
#38626=CARTESIAN_POINT('Ctrl Pts',(68.8418931422078,151.759690102592,54.0217919325278));
#38627=CARTESIAN_POINT('Ctrl Pts',(69.8241254614745,151.229300078712,48.7888778110099));
#38628=CARTESIAN_POINT('Ctrl Pts',(75.7671119106681,150.592832050054,46.3912859569748));
#38629=CARTESIAN_POINT('Ctrl Pts',(80.0346917712683,150.072067404186,49.4204165109013));
#38630=CARTESIAN_POINT('Ctrl Pts',(80.624016362438,149.763458767871,52.1633104035476));
#38631=CARTESIAN_POINT('Ctrl Pts',(80.6225096147018,149.667006141107,53.0213500647842));
#38632=CARTESIAN_POINT('Ctrl Pts',(80.6287116038918,152.332993858894,53.0183048799968));
#38633=CARTESIAN_POINT('Ctrl Pts',(80.615318583347,152.168871293011,54.4729876890807));
#38634=CARTESIAN_POINT('Ctrl Pts',(79.307288013441,151.792592717575,57.8257938433298));
#38635=CARTESIAN_POINT('Ctrl Pts',(73.642959648389,151.204158132586,59.5630876029432));
#38636=CARTESIAN_POINT('Ctrl Pts',(68.7639080710162,150.567690103929,55.4272975763874));
#38637=CARTESIAN_POINT('Ctrl Pts',(69.5952201151085,149.931222075272,49.0854663169038));
#38638=CARTESIAN_POINT('Ctrl Pts',(75.3939889653761,149.294754046615,46.3574973920444));
#38639=CARTESIAN_POINT('Ctrl Pts',(79.8991646679696,148.764364022735,49.1950249110227));
#38640=CARTESIAN_POINT('Ctrl Pts',(80.620971065803,148.443777293494,52.0379444949594));
#38641=CARTESIAN_POINT('Ctrl Pts',(80.6264832288695,148.335346573806,53.0021390759566));
#38642=CARTESIAN_POINT('Ctrl Pts',(80.6264905426344,148.332993858894,53.023059952509));
#38643=CARTESIAN_POINT('Origin',(74.9879498948689,423.667006141107,53.0228109606356));
#38644=CARTESIAN_POINT('',(80.6383546037414,157.667006141107,53.0279836470809));
#38645=CARTESIAN_POINT('',(80.6404628146951,156.332993858894,53.0238399447972));
#38646=CARTESIAN_POINT('',(80.6314498948689,423.667006141107,53.0228109606222));
#38647=CARTESIAN_POINT('Ctrl Pts',(80.6383546037414,157.667006141107,53.0279836470809));
#38648=CARTESIAN_POINT('Ctrl Pts',(80.639943014158,157.642664215832,53.24303366321));
#38649=CARTESIAN_POINT('Ctrl Pts',(80.5307282685173,157.406166281004,55.3303178933253));
#38650=CARTESIAN_POINT('Ctrl Pts',(78.5417996070232,157.0635903414,58.135748356356));
#38651=CARTESIAN_POINT('Ctrl Pts',(74.7324983674773,156.639278322295,58.8841679932114));
#38652=CARTESIAN_POINT('Ctrl Pts',(71.002752658437,156.214966303191,57.8071792131713));
#38653=CARTESIAN_POINT('Ctrl Pts',(68.3129682762291,155.68457627931,53.2122656656242));
#38654=CARTESIAN_POINT('Ctrl Pts',(71.2277399375131,155.048108250653,47.5051086854453));
#38655=CARTESIAN_POINT('Ctrl Pts',(77.5932150058283,154.411640221996,46.8801042110002));
#38656=CARTESIAN_POINT('Ctrl Pts',(80.4685585989152,153.951272852148,50.504449189847));
#38657=CARTESIAN_POINT('Ctrl Pts',(80.6381351282911,153.703061491851,52.6984808594245));
#38658=CARTESIAN_POINT('Ctrl Pts',(80.6352064155011,153.667006141107,53.0176672101712));
#38659=CARTESIAN_POINT('Ctrl Pts',(80.6404628146951,156.332993858894,53.0238399447972));
#38660=CARTESIAN_POINT('Ctrl Pts',(80.641007859621,156.320630026543,53.1328929203889));
#38661=CARTESIAN_POINT('Ctrl Pts',(80.5893550289291,156.09611018464,55.1129350212325));
#38662=CARTESIAN_POINT('Ctrl Pts',(78.2611269268695,155.659434333185,58.8426502572334));
#38663=CARTESIAN_POINT('Ctrl Pts',(71.8655032454052,155.022966304528,58.9194692881673));
#38664=CARTESIAN_POINT('Ctrl Pts',(68.33462666264,154.386498275871,53.5862888115946));
#38665=CARTESIAN_POINT('Ctrl Pts',(70.9238769856076,153.750030247214,47.7242654920534));
#38666=CARTESIAN_POINT('Ctrl Pts',(76.1859185490112,153.219640223333,46.9124224547526));
#38667=CARTESIAN_POINT('Ctrl Pts',(79.3745360971544,152.795328204228,49.1268356994087));
#38668=CARTESIAN_POINT('Ctrl Pts',(80.4920978723783,152.535138751008,51.2287370500932));
#38669=CARTESIAN_POINT('Ctrl Pts',(80.632631314106,152.381027302563,52.5925655894274));
#38670=CARTESIAN_POINT('Ctrl Pts',(80.6287116038918,152.332993858894,53.0183048799968));
#38671=CARTESIAN_POINT('Origin',(74.9879498948689,423.667006141107,53.0228109606356));
#38672=CARTESIAN_POINT('',(80.6211904296695,161.667006141107,53.0245698560322));
#38673=CARTESIAN_POINT('',(80.6314498948689,160.332993858894,53.0228109606264));
#38674=CARTESIAN_POINT('',(80.6314498948689,423.667006141107,53.0228109606222));
#38675=CARTESIAN_POINT('Ctrl Pts',(80.6211904296695,161.667006141107,53.0245698560322));
#38676=CARTESIAN_POINT('Ctrl Pts',(80.6241319221786,161.582266939812,53.7779642526502));
#38677=CARTESIAN_POINT('Ctrl Pts',(80.307523847763,161.391449733741,55.4724725522702));
#38678=CARTESIAN_POINT('Ctrl Pts',(78.6385393623837,161.094554522894,57.6156269035887));
#38679=CARTESIAN_POINT('Ctrl Pts',(75.1163796021698,160.670242503789,59.2482011009735));
#38680=CARTESIAN_POINT('Ctrl Pts',(70.0725868922178,160.139852479909,57.5428197268428));
#38681=CARTESIAN_POINT('Ctrl Pts',(68.530890451871,159.503384451252,51.3226343019818));
#38682=CARTESIAN_POINT('Ctrl Pts',(72.9269747274227,158.866916422595,46.6767386422982));
#38683=CARTESIAN_POINT('Ctrl Pts',(78.9734922431205,158.254790319213,47.8081729292422));
#38684=CARTESIAN_POINT('Ctrl Pts',(80.6260989647779,157.854820225384,51.3687302644544));
#38685=CARTESIAN_POINT('Ctrl Pts',(80.6383546037414,157.667006141107,53.0279836470809));
#38686=CARTESIAN_POINT('Ctrl Pts',(80.6256611505083,160.332993858894,53.0268354269295));
#38687=CARTESIAN_POINT('Ctrl Pts',(80.6302503427949,160.260232750524,53.6737963609542));
#38688=CARTESIAN_POINT('Ctrl Pts',(80.2289081100368,159.975315632601,56.2016586546249));
#38689=CARTESIAN_POINT('Ctrl Pts',(76.4971135606888,159.478242505127,59.5222476700871));
#38690=CARTESIAN_POINT('Ctrl Pts',(70.334196289122,158.841774476469,57.8110042209413));
#38691=CARTESIAN_POINT('Ctrl Pts',(68.4451819243434,158.205306447813,51.6873485020516));
#38692=CARTESIAN_POINT('Ctrl Pts',(71.8856615424623,157.674916423932,47.6239422302756));
#38693=CARTESIAN_POINT('Ctrl Pts',(75.7451117847744,157.250604404827,47.2049533120979));
#38694=CARTESIAN_POINT('Ctrl Pts',(79.2631705587981,156.838656218073,48.5572394850874));
#38695=CARTESIAN_POINT('Ctrl Pts',(80.6316552128679,156.532786036096,51.26160872025));
#38696=CARTESIAN_POINT('Ctrl Pts',(80.6404628146951,156.332993858894,53.0238399447972));
#38697=CARTESIAN_POINT('Origin',(74.9879498948689,423.667006141107,53.0228109606356));
#38698=CARTESIAN_POINT('',(80.6298086662852,165.667006141107,53.0194647221037));
#38699=CARTESIAN_POINT('',(80.6314498948689,164.332993858894,53.0228109606266));
#38700=CARTESIAN_POINT('',(80.6314498948689,423.667006141107,53.0228109606222));
#38701=CARTESIAN_POINT('Ctrl Pts',(80.6298086662852,165.667006141107,53.0194647221037));
#38702=CARTESIAN_POINT('Ctrl Pts',(80.6279297615169,165.627947668569,53.3662095389731));
#38703=CARTESIAN_POINT('Ctrl Pts',(80.504839828438,165.482811191255,54.6560627762247));
#38704=CARTESIAN_POINT('Ctrl Pts',(79.1670753196014,165.125518704388,57.6387493563994));
#38705=CARTESIAN_POINT('Ctrl Pts',(74.2407590117034,164.595128680508,59.6585459220802));
#38706=CARTESIAN_POINT('Ctrl Pts',(68.9980337649973,163.95866065185,55.9732553471886));
#38707=CARTESIAN_POINT('Ctrl Pts',(69.2706230284558,163.322192623193,49.5829816025151));
#38708=CARTESIAN_POINT('Ctrl Pts',(74.7886807951738,162.685724594536,46.3486436607436));
#38709=CARTESIAN_POINT('Ctrl Pts',(79.7400684039384,162.133995767174,48.8673383718253));
#38710=CARTESIAN_POINT('Ctrl Pts',(80.6167674992983,161.794422949365,51.8917398563494));
#38711=CARTESIAN_POINT('Ctrl Pts',(80.6211904296695,161.667006141107,53.0245698560322));
#38712=CARTESIAN_POINT('Ctrl Pts',(80.6314498948689,164.332993858894,53.0228109606266));
#38713=CARTESIAN_POINT('Ctrl Pts',(80.6314498948716,164.140209036292,54.7318077489456));
#38714=CARTESIAN_POINT('Ctrl Pts',(79.8060659192689,163.94742421369,56.4221521097268));
#38715=CARTESIAN_POINT('Ctrl Pts',(78.4584055093435,163.754639391087,57.4730952299786));
#38716=CARTESIAN_POINT('Ctrl Pts',(77.1107450994181,163.561854568485,58.5240383502304));
#38717=CARTESIAN_POINT('Ctrl Pts',(75.2702256751622,163.369069745882,58.9126397065623));
#38718=CARTESIAN_POINT('Ctrl Pts',(73.612745162704,163.17628492328,58.4961923829952));
#38719=CARTESIAN_POINT('Ctrl Pts',(71.9552646502458,162.983500100678,58.079745059428));
#38720=CARTESIAN_POINT('Ctrl Pts',(70.5170033810729,162.790715278075,56.8673394809174));
#38721=CARTESIAN_POINT('Ctrl Pts',(69.8261371496123,162.597930455473,55.304209968461));
#38722=CARTESIAN_POINT('Ctrl Pts',(69.1352709181517,162.40514563287,53.7410804560045));
#38723=CARTESIAN_POINT('Ctrl Pts',(69.2068803054901,162.212360810268,51.8613477992548));
#38724=CARTESIAN_POINT('Ctrl Pts',(70.0146680415442,162.019575987666,50.3553102844612));
#38725=CARTESIAN_POINT('Ctrl Pts',(70.8224557775982,161.826791165063,48.8492727696676));
#38726=CARTESIAN_POINT('Ctrl Pts',(72.3487890589397,161.634006342461,47.7498049531876));
#38727=CARTESIAN_POINT('Ctrl Pts',(74.0331492157611,161.441221519858,47.4606667775731));
#38728=CARTESIAN_POINT('Ctrl Pts',(75.7175093725825,161.248436697256,47.1715286019587));
#38729=CARTESIAN_POINT('Ctrl Pts',(77.5231293307851,161.055651874654,47.6990315230374));
#38730=CARTESIAN_POINT('Ctrl Pts',(78.7869273705886,160.862867052051,48.849459502997));
#38731=CARTESIAN_POINT('Ctrl Pts',(79.9447859852113,160.686242654332,49.9034514424893));
#38732=CARTESIAN_POINT('Ctrl Pts',(80.6314498948664,160.509618256613,51.457072930185));
#38733=CARTESIAN_POINT('Ctrl Pts',(80.6314498948689,160.332993858894,53.0228109606264));
#38734=CARTESIAN_POINT('Origin',(74.9879498948689,423.667006141107,53.0228109606356));
#38735=CARTESIAN_POINT('',(80.6381153479507,169.667006141107,53.0212138869262));
#38736=CARTESIAN_POINT('',(80.6382506461677,168.332993858894,53.0199786605548));
#38737=CARTESIAN_POINT('',(80.6314498948689,423.667006141107,53.0228109606222));
#38738=CARTESIAN_POINT('Ctrl Pts',(80.6381153479507,169.667006141107,53.0212138869262));
#38739=CARTESIAN_POINT('Ctrl Pts',(80.6306212693463,169.461472387773,54.8364412321562));
#38740=CARTESIAN_POINT('Ctrl Pts',(78.7087307956748,169.043782624887,58.5295467855593));
#38741=CARTESIAN_POINT('Ctrl Pts',(72.4002672174427,168.413936852449,59.1781432572696));
#38742=CARTESIAN_POINT('Ctrl Pts',(68.415791308239,167.777468823792,54.1747588859273));
#38743=CARTESIAN_POINT('Ctrl Pts',(70.4610652576824,167.141000795135,48.1144983378858));
#38744=CARTESIAN_POINT('Ctrl Pts',(76.6787490482889,166.504532766478,46.5627435525341));
#38745=CARTESIAN_POINT('Ctrl Pts',(80.263241046223,166.013201215135,49.950684280813));
#38746=CARTESIAN_POINT('Ctrl Pts',(80.6330326356445,165.734025673345,52.4244932876794));
#38747=CARTESIAN_POINT('Ctrl Pts',(80.6298086662852,165.667006141107,53.0194647221037));
#38748=CARTESIAN_POINT('Ctrl Pts',(80.6382506461677,168.332993858894,53.0199786605548));
#38749=CARTESIAN_POINT('Ctrl Pts',(80.6278923608474,168.139438198485,54.7293384245555));
#38750=CARTESIAN_POINT('Ctrl Pts',(78.8923093685276,167.733726528524,58.3308523866159));
#38751=CARTESIAN_POINT('Ctrl Pts',(72.7493845539464,167.11585884901,59.3140825259745));
#38752=CARTESIAN_POINT('Ctrl Pts',(69.207833010338,166.585468825129,55.3384589024206));
#38753=CARTESIAN_POINT('Ctrl Pts',(69.3334586153764,166.161156806024,51.4583653347606));
#38754=CARTESIAN_POINT('Ctrl Pts',(71.2200682242025,165.73684478692,48.0654886688141));
#38755=CARTESIAN_POINT('Ctrl Pts',(76.3014478199115,165.206454763039,46.4755981265107));
#38756=CARTESIAN_POINT('Ctrl Pts',(80.1821266586199,164.703145118772,49.7346730674102));
#38757=CARTESIAN_POINT('Ctrl Pts',(80.6293559903944,164.411991484057,52.3174616771233));
#38758=CARTESIAN_POINT('Ctrl Pts',(80.6249991981787,164.332993858894,53.0195421517516));
#38759=CARTESIAN_POINT('Origin',(74.9879498948689,423.667006141107,53.0228109606356));
#38760=CARTESIAN_POINT('',(80.6301199691199,173.667006141107,53.0281825627581));
#38761=CARTESIAN_POINT('',(80.6341311956073,172.332993858894,53.0271652027316));
#38762=CARTESIAN_POINT('',(80.6314498948689,423.667006141107,53.0228109606222));
#38763=CARTESIAN_POINT('Ctrl Pts',(80.6301199691199,173.667006141107,53.0281825627581));
#38764=CARTESIAN_POINT('Ctrl Pts',(80.634874351723,173.613231121306,53.504493868065));
#38765=CARTESIAN_POINT('Ctrl Pts',(80.3629297496774,173.347300091953,55.8552562258711));
#38766=CARTESIAN_POINT('Ctrl Pts',(77.0704786758444,172.869213053048,59.3668862437205));
#38767=CARTESIAN_POINT('Ctrl Pts',(70.781351567379,172.23274502439,58.2020756788708));
#38768=CARTESIAN_POINT('Ctrl Pts',(68.351646798808,171.596276995734,52.2854517956076));
#38769=CARTESIAN_POINT('Ctrl Pts',(72.0284531099989,170.959808967076,47.0367729157542));
#38770=CARTESIAN_POINT('Ctrl Pts',(77.3480421827307,170.429418943196,47.260698415578));
#38771=CARTESIAN_POINT('Ctrl Pts',(80.0467424555462,170.005106924091,50.0513837657998));
#38772=CARTESIAN_POINT('Ctrl Pts',(80.6258905036357,169.78632865832,51.9674207687533));
#38773=CARTESIAN_POINT('Ctrl Pts',(80.6383568056569,169.673628397326,52.9627276267381));
#38774=CARTESIAN_POINT('Ctrl Pts',(80.6381153479507,169.667006141107,53.0212138869262));
#38775=CARTESIAN_POINT('Ctrl Pts',(80.6341311956073,172.332993858894,53.0271652027315));
#38776=CARTESIAN_POINT('Ctrl Pts',(80.6376049499977,172.291196932018,53.3971740870304));
#38777=CARTESIAN_POINT('Ctrl Pts',(80.4355736701072,172.037243995589,55.6418677387875));
#38778=CARTESIAN_POINT('Ctrl Pts',(77.4232005111353,171.571135049609,59.2405940969629));
#38779=CARTESIAN_POINT('Ctrl Pts',(72.1424114296051,171.040745025728,58.5613024007155));
#38780=CARTESIAN_POINT('Ctrl Pts',(69.692973246283,170.616433006623,55.5494656733147));
#38781=CARTESIAN_POINT('Ctrl Pts',(68.8925550574566,170.192120987518,51.7507502839452));
#38782=CARTESIAN_POINT('Ctrl Pts',(71.6864479885501,169.661730963638,47.2183852476993));
#38783=CARTESIAN_POINT('Ctrl Pts',(78.0939616097122,169.025262934981,47.1120657835623));
#38784=CARTESIAN_POINT('Ctrl Pts',(80.5579189119324,168.582350566733,50.8188324455204));
#38785=CARTESIAN_POINT('Ctrl Pts',(80.639246058666,168.351594208037,52.8557122766402));
#38786=CARTESIAN_POINT('Ctrl Pts',(80.6382506461677,168.332993858894,53.0199786605548));
#38787=CARTESIAN_POINT('Origin',(74.9879498948689,423.667006141107,53.0228109606356));
#38788=CARTESIAN_POINT('',(80.6222904215375,177.667006141107,53.0205978427077));
#38789=CARTESIAN_POINT('',(80.622100390063,176.332993858894,53.0243351757114));
#38790=CARTESIAN_POINT('',(80.6314498948689,423.667006141107,53.0228109606222));
#38791=CARTESIAN_POINT('Ctrl Pts',(80.6222904215376,177.667006141107,53.0205978427077));
#38792=CARTESIAN_POINT('Ctrl Pts',(80.620411075197,177.552833845287,54.0372215553682));
#38793=CARTESIAN_POINT('Ctrl Pts',(79.8716611686231,177.226505539914,56.9464913633814));
#38794=CARTESIAN_POINT('Ctrl Pts',(75.208166943184,176.688021224989,59.6915257515102));
#38795=CARTESIAN_POINT('Ctrl Pts',(69.4940514634066,176.051553196332,56.8177150893079));
#38796=CARTESIAN_POINT('Ctrl Pts',(68.828326029216,175.415085167675,50.4439921364254));
#38797=CARTESIAN_POINT('Ctrl Pts',(72.9914360826229,174.884695143794,47.1248529083393));
#38798=CARTESIAN_POINT('Ctrl Pts',(76.8588776947801,174.46038312469,47.4622003004928));
#38799=CARTESIAN_POINT('Ctrl Pts',(79.7273594481839,174.089846125386,49.2690685230197));
#38800=CARTESIAN_POINT('Ctrl Pts',(80.6161171137957,173.825387130859,51.6253256927186));
#38801=CARTESIAN_POINT('Ctrl Pts',(80.6301199691199,173.667006141107,53.0281825627581));
#38802=CARTESIAN_POINT('Ctrl Pts',(80.622100390063,176.332993858894,53.0243351757114));
#38803=CARTESIAN_POINT('Ctrl Pts',(80.6228905078415,176.230799655998,53.9343920094406));
#38804=CARTESIAN_POINT('Ctrl Pts',(79.9847919659374,175.91644944355,56.7319395831436));
#38805=CARTESIAN_POINT('Ctrl Pts',(76.4713185355127,175.496021226327,59.0702562117385));
#38806=CARTESIAN_POINT('Ctrl Pts',(72.6470540467699,175.071709207221,58.4024920268817));
#38807=CARTESIAN_POINT('Ctrl Pts',(69.551817146766,174.647397188117,56.0593282640832));
#38808=CARTESIAN_POINT('Ctrl Pts',(68.6892013076634,174.117007164236,50.8053712366301));
#38809=CARTESIAN_POINT('Ctrl Pts',(73.4571407575176,173.480539135579,46.5235155598984));
#38810=CARTESIAN_POINT('Ctrl Pts',(79.2182824818878,172.885868033799,48.1117410261231));
#38811=CARTESIAN_POINT('Ctrl Pts',(80.6199726041598,172.50335294157,51.5190549462608));
#38812=CARTESIAN_POINT('Ctrl Pts',(80.6341311956073,172.332993858894,53.0271652027315));
#38813=CARTESIAN_POINT('Origin',(74.9879498948689,423.667006141107,53.0228109606356));
#38814=CARTESIAN_POINT('',(80.6352537257938,181.667006141107,53.0187032745236));
#38815=CARTESIAN_POINT('',(80.6313512644076,180.332993858894,53.0175461958891));
#38816=CARTESIAN_POINT('',(80.6314498948689,423.667006141107,53.0228109606222));
#38817=CARTESIAN_POINT('Ctrl Pts',(80.6352537257938,181.667006141107,53.0187032745236));
#38818=CARTESIAN_POINT('Ctrl Pts',(80.6210959151668,181.492436569267,54.5633324678709));
#38819=CARTESIAN_POINT('Ctrl Pts',(79.1610194561343,181.105710987875,58.0064109974519));
#38820=CARTESIAN_POINT('Ctrl Pts',(73.3284950085148,180.506829396931,59.4904555706305));
#38821=CARTESIAN_POINT('Ctrl Pts',(68.6464467632618,179.870361368274,55.1148460287544));
#38822=CARTESIAN_POINT('Ctrl Pts',(69.6131321617587,179.339971344393,49.8790376028731));
#38823=CARTESIAN_POINT('Ctrl Pts',(72.7542485557096,178.915659325288,47.5977450556339));
#38824=CARTESIAN_POINT('Ctrl Pts',(76.5910088428193,178.491347306184,47.0059863330989));
#38825=CARTESIAN_POINT('Ctrl Pts',(80.0226830505157,178.075129578123,49.3894393899014));
#38826=CARTESIAN_POINT('Ctrl Pts',(80.6239032938417,177.764989854839,52.148122027812));
#38827=CARTESIAN_POINT('Ctrl Pts',(80.6222904215376,177.667006141107,53.0205978427077));
#38828=CARTESIAN_POINT('Ctrl Pts',(80.6313512644076,180.332993858894,53.0175461958891));
#38829=CARTESIAN_POINT('Ctrl Pts',(80.6167777966843,180.170402379979,54.4569563804603));
#38830=CARTESIAN_POINT('Ctrl Pts',(79.6849478057585,179.901732896288,56.8499640912845));
#38831=CARTESIAN_POINT('Ctrl Pts',(76.7481860199208,179.52698540782,58.6194466045056));
#38832=CARTESIAN_POINT('Ctrl Pts',(72.8748126305075,179.102673388715,58.8799969309715));
#38833=CARTESIAN_POINT('Ctrl Pts',(68.7783742806616,178.572283364835,55.4789142536309));
#38834=CARTESIAN_POINT('Ctrl Pts',(69.5704243653522,177.935815336178,49.1196539745438));
#38835=CARTESIAN_POINT('Ctrl Pts',(75.340431971015,177.299347307521,46.3597779503322));
#38836=CARTESIAN_POINT('Ctrl Pts',(79.9125147985732,176.76507348176,49.1746134232404));
#38837=CARTESIAN_POINT('Ctrl Pts',(80.6212502168054,176.442955665551,52.0451065036207));
#38838=CARTESIAN_POINT('Ctrl Pts',(80.622100390063,176.332993858894,53.0243351757114));
#38839=CARTESIAN_POINT('Origin',(74.9879498948689,423.667006141107,53.0228109606356));
#38840=CARTESIAN_POINT('',(80.6374622679322,185.667006141107,53.0261725848653));
#38841=CARTESIAN_POINT('',(80.6375466782535,184.332993858894,53.0249433462478));
#38842=CARTESIAN_POINT('',(80.6314498948689,423.667006141107,53.0228109606222));
#38843=CARTESIAN_POINT('Ctrl Pts',(80.6374622679322,185.667006141107,53.0261725848653));
#38844=CARTESIAN_POINT('Ctrl Pts',(80.6388609160972,185.6441953028,53.2276980420194));
#38845=CARTESIAN_POINT('Ctrl Pts',(80.537213063289,185.409228454941,55.3020984961681));
#38846=CARTESIAN_POINT('Ctrl Pts',(77.9760801015144,184.962105597529,58.9940164661573));
#38847=CARTESIAN_POINT('Ctrl Pts',(71.5719371009017,184.325637568872,58.760591828347));
#38848=CARTESIAN_POINT('Ctrl Pts',(68.8685169582398,183.795247544992,54.1736876365801));
#38849=CARTESIAN_POINT('Ctrl Pts',(69.7441447209343,183.370935525887,50.3916003943771));
#38850=CARTESIAN_POINT('Ctrl Pts',(72.2528560934249,182.946623506783,47.4289537505847));
#38851=CARTESIAN_POINT('Ctrl Pts',(77.5460829854539,182.416233482901,46.8545674679323));
#38852=CARTESIAN_POINT('Ctrl Pts',(80.4599026306944,181.954335026085,50.4793096779496));
#38853=CARTESIAN_POINT('Ctrl Pts',(80.6383020329052,181.70459257882,52.6861303733431));
#38854=CARTESIAN_POINT('Ctrl Pts',(80.6352537257938,181.667006141107,53.0187032745236));
#38855=CARTESIAN_POINT('Ctrl Pts',(80.6375466782535,184.332993858894,53.0249433462478));
#38856=CARTESIAN_POINT('Ctrl Pts',(80.6380606391403,184.322161113512,53.1206316251517));
#38857=CARTESIAN_POINT('Ctrl Pts',(80.6157170314747,184.205250363353,54.1532044388168));
#38858=CARTESIAN_POINT('Ctrl Pts',(79.9867931126735,183.982261608419,56.094020531795));
#38859=CARTESIAN_POINT('Ctrl Pts',(77.2332563931867,183.557949589314,58.8306139288627));
#38860=CARTESIAN_POINT('Ctrl Pts',(71.9102716857639,183.027559565433,58.9489538491949));
#38861=CARTESIAN_POINT('Ctrl Pts',(68.3383237334809,182.391091536777,53.6283596662101));
#38862=CARTESIAN_POINT('Ctrl Pts',(70.8849370199572,181.754623508119,47.761106117269));
#38863=CARTESIAN_POINT('Ctrl Pts',(77.1959362348037,181.118155479463,46.7213021219764));
#38864=CARTESIAN_POINT('Ctrl Pts',(80.3896907770719,180.644278929721,50.2660677252129));
#38865=CARTESIAN_POINT('Ctrl Pts',(80.6357938532337,180.382558389531,52.5787551185917));
#38866=CARTESIAN_POINT('Ctrl Pts',(80.6313512644076,180.332993858894,53.0175461958891));
#38867=CARTESIAN_POINT('Origin',(74.9879498948689,423.667006141107,53.0228109606356));
#38868=CARTESIAN_POINT('',(80.6314498948689,189.667006141107,53.022810960627));
#38869=CARTESIAN_POINT('',(80.6291610643578,188.332993858894,53.0259379629415));
#38870=CARTESIAN_POINT('',(80.6314498948689,423.667006141107,53.0228109606222));
#38871=CARTESIAN_POINT('Ctrl Pts',(80.6242855516874,189.667006141107,53.0256421919302));
#38872=CARTESIAN_POINT('Ctrl Pts',(80.6282930065685,189.583798026781,53.7653643749688));
#38873=CARTESIAN_POINT('Ctrl Pts',(80.1488658331061,189.288433902902,56.3867402663278));
#38874=CARTESIAN_POINT('Ctrl Pts',(76.1712915211055,188.780913769471,59.5947950818913));
#38875=CARTESIAN_POINT('Ctrl Pts',(71.122455804744,188.25052374559,57.9044020975852));
#38876=CARTESIAN_POINT('Ctrl Pts',(69.3035327663159,187.826211726486,54.4747626315898));
#38877=CARTESIAN_POINT('Ctrl Pts',(69.2549135694621,187.40189970738,50.5929403713447));
#38878=CARTESIAN_POINT('Ctrl Pts',(72.8746450227851,186.871509683501,46.6883642435143));
#38879=CARTESIAN_POINT('Ctrl Pts',(78.9551331645321,186.25785249315,47.7857479804749));
#38880=CARTESIAN_POINT('Ctrl Pts',(80.6258525553586,185.856351312352,51.3533768865391));
#38881=CARTESIAN_POINT('Ctrl Pts',(80.6374622679322,185.667006141107,53.0261725848653));
#38882=CARTESIAN_POINT('Ctrl Pts',(80.6291610643578,188.332993858894,53.0259379629415));
#38883=CARTESIAN_POINT('Ctrl Pts',(80.6323067140524,188.261763837492,53.658494549645));
#38884=CARTESIAN_POINT('Ctrl Pts',(80.2325386454109,187.978377806538,56.1705775971628));
#38885=CARTESIAN_POINT('Ctrl Pts',(76.5502474625308,187.482835766032,59.515152526242));
#38886=CARTESIAN_POINT('Ctrl Pts',(70.3645745965685,186.846367737375,57.8403433343832));
#38887=CARTESIAN_POINT('Ctrl Pts',(68.4399397736334,186.209899708718,51.7406970957261));
#38888=CARTESIAN_POINT('Ctrl Pts',(72.5228993479575,185.573431680061,46.8173502104404));
#38889=CARTESIAN_POINT('Ctrl Pts',(78.7751754834161,184.947796396786,47.5858082695843));
#38890=CARTESIAN_POINT('Ctrl Pts',(80.6279948721579,184.534317123064,51.2466059099056));
#38891=CARTESIAN_POINT('Ctrl Pts',(80.6375466782535,184.332993858894,53.0249433462478));
#38892=CARTESIAN_POINT('Origin',(74.9879498948689,423.667006141107,53.0228109606356));
#38893=CARTESIAN_POINT('',(80.6314498948689,193.667006141107,53.0228109606274));
#38894=CARTESIAN_POINT('',(80.6217190853732,192.332993858894,53.0205375180906));
#38895=CARTESIAN_POINT('',(80.6314498948689,423.667006141107,53.0228109606222));
#38896=CARTESIAN_POINT('Ctrl Pts',(80.6314498948689,193.667006141107,53.0228109606274));
#38897=CARTESIAN_POINT('Ctrl Pts',(80.6314498948714,193.474221318505,54.7318077489466));
#38898=CARTESIAN_POINT('Ctrl Pts',(79.8060659192683,193.281436495902,56.4221521097277));
#38899=CARTESIAN_POINT('Ctrl Pts',(78.4584055093426,193.0886516733,57.4730952299793));
#38900=CARTESIAN_POINT('Ctrl Pts',(77.1107450994169,192.895866850697,58.5240383502309));
#38901=CARTESIAN_POINT('Ctrl Pts',(75.2702256751607,192.703082028095,58.9126397065624));
#38902=CARTESIAN_POINT('Ctrl Pts',(73.6127451627025,192.510297205493,58.4961923829948));
#38903=CARTESIAN_POINT('Ctrl Pts',(71.9552646502443,192.31751238289,58.0797450594272));
#38904=CARTESIAN_POINT('Ctrl Pts',(70.5170033810717,192.124727560288,56.8673394809161));
#38905=CARTESIAN_POINT('Ctrl Pts',(69.8261371496116,191.931942737685,55.3042099684593));
#38906=CARTESIAN_POINT('Ctrl Pts',(69.1352709181514,191.739157915083,53.7410804560025));
#38907=CARTESIAN_POINT('Ctrl Pts',(69.2068803054905,191.546373092481,51.8613477992527));
#38908=CARTESIAN_POINT('Ctrl Pts',(70.0146680415451,191.353588269878,50.3553102844593));
#38909=CARTESIAN_POINT('Ctrl Pts',(70.8224557775998,191.160803447276,48.849272769666));
#38910=CARTESIAN_POINT('Ctrl Pts',(72.3487890589419,190.968018624673,47.7498049531864));
#38911=CARTESIAN_POINT('Ctrl Pts',(74.0331492157635,190.775233802071,47.4606667775727));
#38912=CARTESIAN_POINT('Ctrl Pts',(75.7175093725851,190.582448979469,47.171528601959));
#38913=CARTESIAN_POINT('Ctrl Pts',(77.5231293307877,190.389664156866,47.6990315230386));
#38914=CARTESIAN_POINT('Ctrl Pts',(78.7869273705907,190.196879334264,48.8494595029988));
#38915=CARTESIAN_POINT('Ctrl Pts',(79.9447859852123,190.020254936545,49.9034514424912));
#38916=CARTESIAN_POINT('Ctrl Pts',(80.6314498948665,189.843630538826,51.4570729301863));
#38917=CARTESIAN_POINT('Ctrl Pts',(80.6314498948689,189.667006141107,53.022810960627));
#38918=CARTESIAN_POINT('Ctrl Pts',(80.6217190853732,192.332993858894,53.0205375180906));
#38919=CARTESIAN_POINT('Ctrl Pts',(80.6161145337634,192.201366561473,54.1905476069636));
#38920=CARTESIAN_POINT('Ctrl Pts',(79.6948479408142,191.8575832545,57.2532805854104));
#38921=CARTESIAN_POINT('Ctrl Pts',(74.65630346539,191.301643937974,59.6917110173807));
#38922=CARTESIAN_POINT('Ctrl Pts',(69.2035016326957,190.665175909317,56.3485305538422));
#38923=CARTESIAN_POINT('Ctrl Pts',(69.0577500836245,190.02870788066,49.9541064261852));
#38924=CARTESIAN_POINT('Ctrl Pts',(74.3725601345045,189.392239852003,46.3735577591653));
#38925=CARTESIAN_POINT('Ctrl Pts',(79.2578336803251,188.861849828122,48.4906956655628));
#38926=CARTESIAN_POINT('Ctrl Pts',(80.5210935629515,188.508767830419,51.4638814847399));
#38927=CARTESIAN_POINT('Ctrl Pts',(80.6276221128581,188.367841842269,52.7164712383355));
#38928=CARTESIAN_POINT('Ctrl Pts',(80.6291610643578,188.332993858894,53.0259379629415));
#38929=CARTESIAN_POINT('Origin',(74.9879498948689,423.667006141107,53.0228109606356));
#38930=CARTESIAN_POINT('',(80.640955218553,197.667006141107,53.0225373373321));
#38931=CARTESIAN_POINT('',(80.6392284044996,196.332993858894,53.0181925457554));
#38932=CARTESIAN_POINT('',(80.6314498948689,423.667006141107,53.0228109606222));
#38933=CARTESIAN_POINT('Ctrl Pts',(80.640955218553,197.667006141107,53.0225373373321));
#38934=CARTESIAN_POINT('Ctrl Pts',(80.6345183935671,197.463003474742,54.821619328168));
#38935=CARTESIAN_POINT('Ctrl Pts',(79.2099563276419,197.1529228036,57.5592190407096));
#38936=CARTESIAN_POINT('Ctrl Pts',(75.6295355167696,196.736764127683,58.8545456627842));
#38937=CARTESIAN_POINT('Ctrl Pts',(71.7791577583434,196.312452108578,58.3590671026649));
#38938=CARTESIAN_POINT('Ctrl Pts',(68.4199739824153,195.782062084697,54.2282009838377));
#38939=CARTESIAN_POINT('Ctrl Pts',(70.4301108370362,195.14559405604,48.1432289658392));
#38940=CARTESIAN_POINT('Ctrl Pts',(76.6257663738702,194.509126027384,46.5545956201064));
#38941=CARTESIAN_POINT('Ctrl Pts',(80.2598992249104,194.016263389073,49.9198215535398));
#38942=CARTESIAN_POINT('Ctrl Pts',(80.6312959048558,193.735556760314,52.4090928284891));
#38943=CARTESIAN_POINT('Ctrl Pts',(80.6265789855776,193.667006141107,53.018365003171));
#38944=CARTESIAN_POINT('Ctrl Pts',(80.6392284044996,196.332993858894,53.0181925457554));
#38945=CARTESIAN_POINT('Ctrl Pts',(80.6281979805195,196.140969285454,54.7138512508588));
#38946=CARTESIAN_POINT('Ctrl Pts',(78.9109854809454,195.73678870246,58.3085405343815));
#38947=CARTESIAN_POINT('Ctrl Pts',(72.8014733044529,195.120452109916,59.3267440686173));
#38948=CARTESIAN_POINT('Ctrl Pts',(68.498429651078,194.483984081258,54.5945438662197));
#38949=CARTESIAN_POINT('Ctrl Pts',(70.1632321105985,193.847516052601,48.4061702992275));
#38950=CARTESIAN_POINT('Ctrl Pts',(75.2398670646046,193.317126028721,46.8011942632874));
#38951=CARTESIAN_POINT('Ctrl Pts',(78.7289430044913,192.892814009616,48.5033273286335));
#38952=CARTESIAN_POINT('Ctrl Pts',(80.332017025861,192.600129287933,50.648315489177));
#38953=CARTESIAN_POINT('Ctrl Pts',(80.6251479130712,192.413522571025,52.3047330650381));
#38954=CARTESIAN_POINT('Ctrl Pts',(80.6217190853732,192.332993858894,53.0205375180906));
#38955=CARTESIAN_POINT('Origin',(74.9879498948689,423.667006141107,53.0228109606356));
#38956=CARTESIAN_POINT('',(80.6276048913152,201.667006141107,53.027244000928));
#38957=CARTESIAN_POINT('',(80.6340609079321,200.332993858894,53.0281408858031));
#38958=CARTESIAN_POINT('',(80.6314498948689,423.667006141107,53.0228109606222));
#38959=CARTESIAN_POINT('Ctrl Pts',(80.6276048913152,201.667006141107,53.027244000928));
#38960=CARTESIAN_POINT('Ctrl Pts',(80.6317528202149,201.614762208275,53.4905111224134));
#38961=CARTESIAN_POINT('Ctrl Pts',(80.4741758592005,201.456440270666,54.8920866086593));
#38962=CARTESIAN_POINT('Ctrl Pts',(79.2963758820999,201.192040328282,57.0050499361194));
#38963=CARTESIAN_POINT('Ctrl Pts',(76.064451658235,200.767728309176,59.1557646138185));
#38964=CARTESIAN_POINT('Ctrl Pts',(70.8195529427137,200.237338285297,58.2396816294403));
#38965=CARTESIAN_POINT('Ctrl Pts',(68.3471157639746,199.600870256639,52.3274410178494));
#38966=CARTESIAN_POINT('Ctrl Pts',(71.9831085027866,198.964402227983,47.0653634605732));
#38967=CARTESIAN_POINT('Ctrl Pts',(78.3759491980706,198.327934199325,47.2690575728888));
#38968=CARTESIAN_POINT('Ctrl Pts',(80.6079896926466,197.895468837034,51.0078303424387));
#38969=CARTESIAN_POINT('Ctrl Pts',(80.6412124781471,197.675159484294,52.9506337041384));
#38970=CARTESIAN_POINT('Ctrl Pts',(80.640955218553,197.667006141107,53.0225373373321));
#38971=CARTESIAN_POINT('Ctrl Pts',(80.6340609079321,200.332993858894,53.0281408858031));
#38972=CARTESIAN_POINT('Ctrl Pts',(80.6374212133726,200.292728018986,53.3847935610186));
#38973=CARTESIAN_POINT('Ctrl Pts',(80.444465303885,200.040306169526,55.6167934462686));
#38974=CARTESIAN_POINT('Ctrl Pts',(77.4708299078219,199.575728310514,59.2159974868797));
#38975=CARTESIAN_POINT('Ctrl Pts',(71.1190079787084,198.939260281857,58.4648239866103));
#38976=CARTESIAN_POINT('Ctrl Pts',(68.3180409606457,198.3027922532,52.7009608376928));
#38977=CARTESIAN_POINT('Ctrl Pts',(71.098459721967,197.77240222932,48.1603174867096));
#38978=CARTESIAN_POINT('Ctrl Pts',(74.8488389159196,197.348090210214,47.1575394509773));
#38979=CARTESIAN_POINT('Ctrl Pts',(78.6425415842146,196.92377819111,47.9813889218711));
#38980=CARTESIAN_POINT('Ctrl Pts',(80.5516622018494,196.58541274067,50.7907689994262));
#38981=CARTESIAN_POINT('Ctrl Pts',(80.6403848100141,196.353125295006,52.8404233973733));
#38982=CARTESIAN_POINT('Ctrl Pts',(80.6392284044996,196.332993858894,53.0181925457554));
#38983=CARTESIAN_POINT('Origin',(74.9879498948689,423.667006141107,53.0228109606356));
#38984=CARTESIAN_POINT('',(80.626574651087,205.667006141107,53.0221197938247));
#38985=CARTESIAN_POINT('',(80.6223425337288,204.332993858894,53.0236933593282));
#38986=CARTESIAN_POINT('',(80.6314498948689,423.667006141107,53.0228109606222));
#38987=CARTESIAN_POINT('Ctrl Pts',(80.626574651087,205.667006141107,53.0221197938247));
#38988=CARTESIAN_POINT('Ctrl Pts',(80.6265170704333,205.660442937031,53.0804789074155));
#38989=CARTESIAN_POINT('Ctrl Pts',(80.6105409825448,205.54780172818,54.0821013304582));
#38990=CARTESIAN_POINT('Ctrl Pts',(79.8222544701088,205.223004509775,56.947282442927));
#38991=CARTESIAN_POINT('Ctrl Pts',(75.2616679235261,204.692614485895,59.6948686777458));
#38992=CARTESIAN_POINT('Ctrl Pts',(69.5181641574838,204.056146457238,56.8523878495988));
#38993=CARTESIAN_POINT('Ctrl Pts',(68.8128385238247,203.419678428581,50.4953117049742));
#38994=CARTESIAN_POINT('Ctrl Pts',(73.7729845636653,202.783210399924,46.4571368186103));
#38995=CARTESIAN_POINT('Ctrl Pts',(79.361453787666,202.198986304099,48.2932371232192));
#38996=CARTESIAN_POINT('Ctrl Pts',(80.6149086050964,201.826918217827,51.6092418817071));
#38997=CARTESIAN_POINT('Ctrl Pts',(80.6276048913152,201.667006141107,53.027244000928));
#38998=CARTESIAN_POINT('Ctrl Pts',(80.6223425337288,204.332993858894,53.0236933593282));
#38999=CARTESIAN_POINT('Ctrl Pts',(80.6230594866242,204.232330742967,53.9192679121389));
#39000=CARTESIAN_POINT('Ctrl Pts',(79.9972097326935,203.919511617488,56.70082270821));
#39001=CARTESIAN_POINT('Ctrl Pts',(75.6353879853842,203.394536482455,59.668489377038));
#39002=CARTESIAN_POINT('Ctrl Pts',(69.7411399911392,202.758068453799,57.153459596108));
#39003=CARTESIAN_POINT('Ctrl Pts',(68.8629228367167,202.227678429917,51.902087877635));
#39004=CARTESIAN_POINT('Ctrl Pts',(71.0368999365241,201.803366410813,48.6857651951434));
#39005=CARTESIAN_POINT('Ctrl Pts',(74.4413565467986,201.379054391709,46.8201331300155));
#39006=CARTESIAN_POINT('Ctrl Pts',(79.1976249869001,200.888930207736,48.0791902280285));
#39007=CARTESIAN_POINT('Ctrl Pts',(80.6197161563126,200.504884028539,51.5056322534882));
#39008=CARTESIAN_POINT('Ctrl Pts',(80.6340609079321,200.332993858894,53.0281408858031));
#39009=CARTESIAN_POINT('Origin',(74.9879498948689,423.667006141107,53.0228109606356));
#39010=CARTESIAN_POINT('',(80.6311262248081,209.667006141107,53.0183737769086));
#39011=CARTESIAN_POINT('',(80.6305392456029,208.332993858894,53.0176923059613));
#39012=CARTESIAN_POINT('',(80.6314498948689,423.667006141107,53.0228109606222));
#39013=CARTESIAN_POINT('Ctrl Pts',(80.6311262248081,209.667006141107,53.0183737769086));
#39014=CARTESIAN_POINT('Ctrl Pts',(80.6168278466814,209.493967656236,54.5505890003982));
#39015=CARTESIAN_POINT('Ctrl Pts',(79.1885638263849,209.108773161812,57.9803147109756));
#39016=CARTESIAN_POINT('Ctrl Pts',(73.3694517075265,208.511422657837,59.5008055828234));
#39017=CARTESIAN_POINT('Ctrl Pts',(68.6683970655276,207.874954629179,55.1637564563535));
#39018=CARTESIAN_POINT('Ctrl Pts',(69.7653637905974,207.238486600523,48.8624258785963));
#39019=CARTESIAN_POINT('Ctrl Pts',(75.6735905312152,206.602018571865,46.3804373005538));
#39020=CARTESIAN_POINT('Ctrl Pts',(80.0013855133694,206.07819175206,49.3672640149237));
#39021=CARTESIAN_POINT('Ctrl Pts',(80.6274477196698,205.766520941808,52.1372477875521));
#39022=CARTESIAN_POINT('Ctrl Pts',(80.626574651087,205.667006141107,53.0221197938247));
#39023=CARTESIAN_POINT('Ctrl Pts',(80.6305392456029,208.332993858894,53.0176923059613));
#39024=CARTESIAN_POINT('Ctrl Pts',(80.6179689885373,208.171933466948,54.445179660362));
#39025=CARTESIAN_POINT('Ctrl Pts',(79.3448628719476,207.798717065448,57.7735864037716));
#39026=CARTESIAN_POINT('Ctrl Pts',(73.7352061577403,207.213344654398,59.5819163913665));
#39027=CARTESIAN_POINT('Ctrl Pts',(69.6286797739237,206.682954630516,56.1930196438724));
#39028=CARTESIAN_POINT('Ctrl Pts',(69.1609966055946,206.258642611412,52.3391654795781));
#39029=CARTESIAN_POINT('Ctrl Pts',(70.5080046768267,205.834330592307,48.6982221958113));
#39030=CARTESIAN_POINT('Ctrl Pts',(75.2874147618561,205.303940568427,46.3518592644304));
#39031=CARTESIAN_POINT('Ctrl Pts',(79.899510904419,204.768135655696,49.1506053771233));
#39032=CARTESIAN_POINT('Ctrl Pts',(80.6215484479093,204.444486752519,52.0317689843454));
#39033=CARTESIAN_POINT('Ctrl Pts',(80.6223425337288,204.332993858894,53.0236933593282));
#39034=CARTESIAN_POINT('Origin',(74.9879498948689,423.667006141107,53.0228109606356));
#39035=CARTESIAN_POINT('',(80.6382744059561,213.667006141107,53.0259194210108));
#39036=CARTESIAN_POINT('',(80.6406766150791,212.332993858894,53.0236886644395));
#39037=CARTESIAN_POINT('',(80.6314498948689,423.667006141107,53.0228109606222));
#39038=CARTESIAN_POINT('Ctrl Pts',(80.6382744059561,213.667006141107,53.0259194210108));
#39039=CARTESIAN_POINT('Ctrl Pts',(80.6395083226358,213.645726389769,53.2138936786102));
#39040=CARTESIAN_POINT('Ctrl Pts',(80.5450631830952,213.412290628878,55.2746757555776));
#39041=CARTESIAN_POINT('Ctrl Pts',(78.0159571360404,212.966698858435,58.9727077333983));
#39042=CARTESIAN_POINT('Ctrl Pts',(71.6194256917035,212.330230829778,58.7843319643082));
#39043=CARTESIAN_POINT('Ctrl Pts',(68.3174643030566,211.693762801121,53.3056650395866));
#39044=CARTESIAN_POINT('Ctrl Pts',(71.1496401123775,211.057294772464,47.5586365481913));
#39045=CARTESIAN_POINT('Ctrl Pts',(76.4416934236012,210.526904748583,46.9679457097492));
#39046=CARTESIAN_POINT('Ctrl Pts',(79.5342341192608,210.102592729479,49.3146003451081));
#39047=CARTESIAN_POINT('Ctrl Pts',(80.5273629254713,209.851319195245,51.3879369939694));
#39048=CARTESIAN_POINT('Ctrl Pts',(80.6343585529211,209.706123665788,52.6719972649662));
#39049=CARTESIAN_POINT('Ctrl Pts',(80.6311262248081,209.667006141107,53.0183737769086));
#39050=CARTESIAN_POINT('Ctrl Pts',(80.6406766150791,212.332993858894,53.0236886644395));
#39051=CARTESIAN_POINT('Ctrl Pts',(80.6409564956532,212.32369220048,53.1058016007408));
#39052=CARTESIAN_POINT('Ctrl Pts',(80.6016966775368,212.102234532514,55.0605671760039));
#39053=CARTESIAN_POINT('Ctrl Pts',(78.3435294198688,211.668620854996,58.7960171796599));
#39054=CARTESIAN_POINT('Ctrl Pts',(73.0203157428126,211.138230831115,58.9307022339566));
#39055=CARTESIAN_POINT('Ctrl Pts',(70.1404093382657,210.713918812011,56.3274859477036));
#39056=CARTESIAN_POINT('Ctrl Pts',(68.7697904747173,210.289606792905,52.6954344925807));
#39057=CARTESIAN_POINT('Ctrl Pts',(70.8397506710645,209.759216769025,47.7898625183533));
#39058=CARTESIAN_POINT('Ctrl Pts',(77.1560180005676,209.122748740368,46.7074779213906));
#39059=CARTESIAN_POINT('Ctrl Pts',(80.3767059902175,208.647341103658,50.2362176050114));
#39060=CARTESIAN_POINT('Ctrl Pts',(80.6345270978642,208.3840894765,52.5648289600087));
#39061=CARTESIAN_POINT('Ctrl Pts',(80.6305392456029,208.332993858894,53.0176923059613));
#39062=CARTESIAN_POINT('Origin',(74.9879498948689,423.667006141107,53.0228109606356));
#39063=CARTESIAN_POINT('',(80.6314498948689,217.667006141107,53.0228109606278));
#39064=CARTESIAN_POINT('',(80.6293939811109,216.332993858894,53.0260232150293));
#39065=CARTESIAN_POINT('',(80.6314498948689,423.667006141107,53.0228109606222));
#39066=CARTESIAN_POINT('Ctrl Pts',(80.6245279079042,217.667006141107,53.0258075780124));
#39067=CARTESIAN_POINT('Ctrl Pts',(80.628672686297,217.585329113749,53.7518430852284));
#39068=CARTESIAN_POINT('Ctrl Pts',(80.1610640643919,217.291496076839,56.3591821658415));
#39069=CARTESIAN_POINT('Ctrl Pts',(76.2187228071657,216.785507030377,59.5860802860795));
#39070=CARTESIAN_POINT('Ctrl Pts',(71.1576983282718,216.255117006495,57.9321749584298));
#39071=CARTESIAN_POINT('Ctrl Pts',(69.31426183066,215.830804987392,54.5157242093268));
#39072=CARTESIAN_POINT('Ctrl Pts',(69.2372749896401,215.406492968286,50.6344011155516));
#39073=CARTESIAN_POINT('Ctrl Pts',(72.829541004845,214.876102944406,46.7037054021372));
#39074=CARTESIAN_POINT('Ctrl Pts',(78.9315707928124,214.260914667087,47.7600025531877));
#39075=CARTESIAN_POINT('Ctrl Pts',(80.6272063537493,213.857882399321,51.3398178138765));
#39076=CARTESIAN_POINT('Ctrl Pts',(80.6382744059561,213.667006141107,53.0259194210108));
#39077=CARTESIAN_POINT('Ctrl Pts',(80.6293939811109,216.332993858894,53.0260232150293));
#39078=CARTESIAN_POINT('Ctrl Pts',(80.6326101171936,216.263294924461,53.6449102643575));
#39079=CARTESIAN_POINT('Ctrl Pts',(80.2440137931953,215.981439980475,56.1430625001089));
#39080=CARTESIAN_POINT('Ctrl Pts',(76.5965009308421,215.487429026938,59.503735860729));
#39081=CARTESIAN_POINT('Ctrl Pts',(70.4003730145984,214.85096099828,57.873534909508));
#39082=CARTESIAN_POINT('Ctrl Pts',(68.429181621647,214.214492969624,51.7880485052417));
#39083=CARTESIAN_POINT('Ctrl Pts',(72.4813418470979,213.578024940966,46.8351607156745));
#39084=CARTESIAN_POINT('Ctrl Pts',(78.7452529776764,212.950858570724,47.5606292096147));
#39085=CARTESIAN_POINT('Ctrl Pts',(80.6345728656489,212.535848210033,51.2329363413034));
#39086=CARTESIAN_POINT('Ctrl Pts',(80.6406766150791,212.332993858894,53.0236886644395));
#39087=CARTESIAN_POINT('Origin',(74.9879498948689,423.667006141107,53.0228109606356));
#39088=CARTESIAN_POINT('',(80.6314498948689,221.667006141107,53.0228109606282));
#39089=CARTESIAN_POINT('',(80.6215141333136,220.332993858894,53.0207205529598));
#39090=CARTESIAN_POINT('',(80.6314498948689,423.667006141107,53.0228109606222));
#39091=CARTESIAN_POINT('Ctrl Pts',(80.6314498948689,221.667006141107,53.0228109606279));
#39092=CARTESIAN_POINT('Ctrl Pts',(80.6314498948712,221.474221318505,54.7318077489469));
#39093=CARTESIAN_POINT('Ctrl Pts',(79.8060659192682,221.281436495902,56.4221521097277));
#39094=CARTESIAN_POINT('Ctrl Pts',(78.4584055093427,221.0886516733,57.4730952299792));
#39095=CARTESIAN_POINT('Ctrl Pts',(77.1107450994171,220.895866850698,58.5240383502307));
#39096=CARTESIAN_POINT('Ctrl Pts',(75.2702256751613,220.703082028095,58.9126397065623));
#39097=CARTESIAN_POINT('Ctrl Pts',(73.6127451627033,220.510297205493,58.496192382995));
#39098=CARTESIAN_POINT('Ctrl Pts',(71.9552646502452,220.31751238289,58.0797450594277));
#39099=CARTESIAN_POINT('Ctrl Pts',(70.5170033810726,220.124727560288,56.867339480917));
#39100=CARTESIAN_POINT('Ctrl Pts',(69.8261371496122,219.931942737686,55.3042099684606));
#39101=CARTESIAN_POINT('Ctrl Pts',(69.1352709181517,219.739157915083,53.7410804560042));
#39102=CARTESIAN_POINT('Ctrl Pts',(69.2068803054902,219.546373092481,51.8613477992546));
#39103=CARTESIAN_POINT('Ctrl Pts',(70.0146680415442,219.353588269878,50.3553102844611));
#39104=CARTESIAN_POINT('Ctrl Pts',(70.8224557775982,219.160803447276,48.8492727696676));
#39105=CARTESIAN_POINT('Ctrl Pts',(72.3487890589396,218.968018624674,47.7498049531877));
#39106=CARTESIAN_POINT('Ctrl Pts',(74.0331492157609,218.775233802071,47.4606667775732));
#39107=CARTESIAN_POINT('Ctrl Pts',(75.7175093725821,218.582448979469,47.1715286019587));
#39108=CARTESIAN_POINT('Ctrl Pts',(77.5231293307847,218.389664156867,47.6990315230373));
#39109=CARTESIAN_POINT('Ctrl Pts',(78.7869273705882,218.196879334264,48.8494595029966));
#39110=CARTESIAN_POINT('Ctrl Pts',(79.9447859852115,218.020254936545,49.9034514424892));
#39111=CARTESIAN_POINT('Ctrl Pts',(80.6314498948667,217.843630538826,51.4570729301857));
#39112=CARTESIAN_POINT('Ctrl Pts',(80.6314498948689,217.667006141107,53.0228109606278));
#39113=CARTESIAN_POINT('Ctrl Pts',(80.6215141333136,220.332993858894,53.0207205529598));
#39114=CARTESIAN_POINT('Ctrl Pts',(80.6163399326053,220.202897648442,54.1772185397082));
#39115=CARTESIAN_POINT('Ctrl Pts',(79.7114181348351,219.860645428437,57.2260257613491));
#39116=CARTESIAN_POINT('Ctrl Pts',(74.7044349299368,219.306237198879,59.6939299756169));
#39117=CARTESIAN_POINT('Ctrl Pts',(69.2276352050903,218.669769170223,56.3901794069435));
#39118=CARTESIAN_POINT('Ctrl Pts',(69.0357866029293,218.033301141565,49.9969717623945));
#39119=CARTESIAN_POINT('Ctrl Pts',(74.3245562273971,217.396833112908,46.3781728935986));
#39120=CARTESIAN_POINT('Ctrl Pts',(79.2251026994422,216.866443089028,48.4600028300045));
#39121=CARTESIAN_POINT('Ctrl Pts',(80.5151970792007,216.511830004356,51.4368566165362));
#39122=CARTESIAN_POINT('Ctrl Pts',(80.6277153321941,216.369372929237,52.702997681211));
#39123=CARTESIAN_POINT('Ctrl Pts',(80.6293939811109,216.332993858894,53.0260232150293));
#39124=CARTESIAN_POINT('Origin',(74.9879498948689,423.667006141107,53.0228109606356));
#39125=CARTESIAN_POINT('',(80.6407963231499,225.667006141107,53.0222595369741));
#39126=CARTESIAN_POINT('',(80.6389234508925,224.332993858894,53.0179829901466));
#39127=CARTESIAN_POINT('',(80.6314498948689,423.667006141107,53.0228109606222));
#39128=CARTESIAN_POINT('Ctrl Pts',(80.6407963231499,225.667006141107,53.0222595369741));
#39129=CARTESIAN_POINT('Ctrl Pts',(80.6334465165095,225.46453456171,54.8079251578411));
#39130=CARTESIAN_POINT('Ctrl Pts',(79.2294387037549,225.155984977538,57.533499672276));
#39131=CARTESIAN_POINT('Ctrl Pts',(75.6715948746436,224.741357388588,58.8497648206672));
#39132=CARTESIAN_POINT('Ctrl Pts',(71.8177424321106,224.317045369484,58.3820796919963));
#39133=CARTESIAN_POINT('Ctrl Pts',(68.4288418723472,223.786655345603,54.2755576487171));
#39134=CARTESIAN_POINT('Ctrl Pts',(70.395023167623,223.150187316946,48.1762408565892));
#39135=CARTESIAN_POINT('Ctrl Pts',(76.5790555611666,222.513719288289,46.5429470970313));
#39136=CARTESIAN_POINT('Ctrl Pts',(80.2487384158096,222.01932556301,49.8922375528076));
#39137=CARTESIAN_POINT('Ctrl Pts',(80.6309179385296,221.737087847282,52.3955344152688));
#39138=CARTESIAN_POINT('Ctrl Pts',(80.626235952703,221.667006141107,53.0185107809476));
#39139=CARTESIAN_POINT('Ctrl Pts',(80.6389234508925,224.332993858894,53.0179829901465));
#39140=CARTESIAN_POINT('Ctrl Pts',(80.6274057020489,224.142500372422,54.7003984290927));
#39141=CARTESIAN_POINT('Ctrl Pts',(78.9338615869445,223.739850876398,58.2827370241048));
#39142=CARTESIAN_POINT('Ctrl Pts',(72.8470130986032,223.125045370821,59.3423554510688));
#39143=CARTESIAN_POINT('Ctrl Pts',(68.5099388049065,222.488577342164,54.6413249332986));
#39144=CARTESIAN_POINT('Ctrl Pts',(70.1300482334095,221.852109313507,48.4411008882662));
#39145=CARTESIAN_POINT('Ctrl Pts',(75.1949720228243,221.321719289626,46.7995385915325));
#39146=CARTESIAN_POINT('Ctrl Pts',(78.6962367276934,220.897407270522,48.4764536776389));
#39147=CARTESIAN_POINT('Ctrl Pts',(80.3232136734672,220.60319146187,50.620979749766));
#39148=CARTESIAN_POINT('Ctrl Pts',(80.6247778246167,220.415053657994,52.2912450968989));
#39149=CARTESIAN_POINT('Ctrl Pts',(80.6215141333136,220.332993858894,53.0207205529598));
#39150=CARTESIAN_POINT('Origin',(74.9879498948689,423.667006141107,53.0228109606356));
#39151=CARTESIAN_POINT('',(80.6280038580037,229.667006141107,53.0272789318033));
#39152=CARTESIAN_POINT('',(80.6344810375604,228.332993858894,53.0280828052492));
#39153=CARTESIAN_POINT('',(80.6314498948689,423.667006141107,53.0228109606222));
#39154=CARTESIAN_POINT('Ctrl Pts',(80.6280038580037,229.667006141107,53.0272789318033));
#39155=CARTESIAN_POINT('Ctrl Pts',(80.6320769718372,229.616293295243,53.4768962186168));
#39156=CARTESIAN_POINT('Ctrl Pts',(80.4807879632803,229.459502444603,54.8647393944588));
#39157=CARTESIAN_POINT('Ctrl Pts',(79.3249956567615,229.196633589187,56.973860923079));
#39158=CARTESIAN_POINT('Ctrl Pts',(76.1086729866622,228.772321570083,59.1478380087876));
#39159=CARTESIAN_POINT('Ctrl Pts',(70.8573012407579,228.241931546201,58.2696208856052));
#39160=CARTESIAN_POINT('Ctrl Pts',(68.3422715097577,227.605463517545,52.3753728345039));
#39161=CARTESIAN_POINT('Ctrl Pts',(71.9402036438859,226.968995488888,47.087198498792));
#39162=CARTESIAN_POINT('Ctrl Pts',(78.3343475963114,226.332527460231,47.2447628702198));
#39163=CARTESIAN_POINT('Ctrl Pts',(80.6013028412971,225.89853101097,50.9805133951161));
#39164=CARTESIAN_POINT('Ctrl Pts',(80.6411478721884,225.676690571263,52.9368492584648));
#39165=CARTESIAN_POINT('Ctrl Pts',(80.6407963231499,225.667006141107,53.0222595369741));
#39166=CARTESIAN_POINT('Ctrl Pts',(80.6344810375604,228.332993858894,53.0280828052492));
#39167=CARTESIAN_POINT('Ctrl Pts',(80.6376880979176,228.294259105955,53.3711062959646));
#39168=CARTESIAN_POINT('Ctrl Pts',(80.4533246712096,228.043368343463,55.5892892119953));
#39169=CARTESIAN_POINT('Ctrl Pts',(77.5154492131354,227.58032157142,59.1979222716756));
#39170=CARTESIAN_POINT('Ctrl Pts',(71.1583728874286,226.943853542763,58.492596811605));
#39171=CARTESIAN_POINT('Ctrl Pts',(68.3158924128625,226.307385514106,52.7490927066299));
#39172=CARTESIAN_POINT('Ctrl Pts',(71.0634780017905,225.776995490225,48.1885067791575));
#39173=CARTESIAN_POINT('Ctrl Pts',(74.8065245107504,225.35268347112,47.1586958035716));
#39174=CARTESIAN_POINT('Ctrl Pts',(78.6060725394363,224.928371452016,47.955152209226));
#39175=CARTESIAN_POINT('Ctrl Pts',(80.5441433285849,224.588474914607,50.7633344776202));
#39176=CARTESIAN_POINT('Ctrl Pts',(80.6402332253356,224.354656381974,52.8266622056322));
#39177=CARTESIAN_POINT('Ctrl Pts',(80.6389234508925,224.332993858894,53.0179829901465));
#39178=CARTESIAN_POINT('Origin',(74.9879498948689,423.667006141107,53.0228109606356));
#39179=CARTESIAN_POINT('',(80.6265348678285,233.667006141107,53.0222797174675));
#39180=CARTESIAN_POINT('',(80.6223895405763,232.332993858894,53.0239051904298));
#39181=CARTESIAN_POINT('',(80.6314498948689,423.667006141107,53.0228109606222));
#39182=CARTESIAN_POINT('Ctrl Pts',(80.6265348678285,233.667006141107,53.0222797174675));
#39183=CARTESIAN_POINT('Ctrl Pts',(80.6265011449881,233.661974024,53.0670254804188));
#39184=CARTESIAN_POINT('Ctrl Pts',(80.6144193150399,233.550863902116,54.0550392157484));
#39185=CARTESIAN_POINT('Ctrl Pts',(79.8504433688653,233.227597770682,56.9123011334566));
#39186=CARTESIAN_POINT('Ctrl Pts',(75.3098000176901,232.697207746799,59.6927198950109));
#39187=CARTESIAN_POINT('Ctrl Pts',(69.5459368691264,232.060739718144,56.8917528765499));
#39188=CARTESIAN_POINT('Ctrl Pts',(68.7947633682085,231.424271689486,50.5399309481628));
#39189=CARTESIAN_POINT('Ctrl Pts',(73.7256447190361,230.78780366083,46.4660737412472));
#39190=CARTESIAN_POINT('Ctrl Pts',(79.3418961640255,230.202048478036,48.2665114230645));
#39191=CARTESIAN_POINT('Ctrl Pts',(80.6150371949788,229.828449304795,51.5959327709697));
#39192=CARTESIAN_POINT('Ctrl Pts',(80.6280038580037,229.667006141107,53.0272789318033));
#39193=CARTESIAN_POINT('Ctrl Pts',(80.6223895405763,232.332993858894,53.0239051904298));
#39194=CARTESIAN_POINT('Ctrl Pts',(80.6234035207467,232.233861829935,53.9058352652539));
#39195=CARTESIAN_POINT('Ctrl Pts',(80.0109577612122,231.922573791425,56.6733318748735));
#39196=CARTESIAN_POINT('Ctrl Pts',(75.683319836815,231.399129743361,59.6636450923455));
#39197=CARTESIAN_POINT('Ctrl Pts',(69.7710792277636,230.762661714704,57.1912079111794));
#39198=CARTESIAN_POINT('Ctrl Pts',(68.8549962387284,230.232271690823,51.9463092001141));
#39199=CARTESIAN_POINT('Ctrl Pts',(71.0057109233227,229.807959671719,48.71438496963));
#39200=CARTESIAN_POINT('Ctrl Pts',(74.3966183648981,229.383647652614,46.8242382530895));
#39201=CARTESIAN_POINT('Ctrl Pts',(79.1767330987352,228.891992381673,48.052771871417));
#39202=CARTESIAN_POINT('Ctrl Pts',(80.6201225508014,228.506415115507,51.4923155602383));
#39203=CARTESIAN_POINT('Ctrl Pts',(80.6344810375604,228.332993858894,53.0280828052492));
#39204=CARTESIAN_POINT('Origin',(74.9879498948689,423.667006141107,53.0228109606356));
#39205=CARTESIAN_POINT('',(80.6306964515364,237.667006141107,53.0183537100148));
#39206=CARTESIAN_POINT('',(80.6301424893571,236.332993858894,53.0176985262882));
#39207=CARTESIAN_POINT('',(80.6314498948689,423.667006141107,53.0228109606222));
#39208=CARTESIAN_POINT('Ctrl Pts',(80.6306964515364,237.667006141107,53.0183537100148));
#39209=CARTESIAN_POINT('Ctrl Pts',(80.6164849814828,237.495498743204,54.5372715917522));
#39210=CARTESIAN_POINT('Ctrl Pts',(79.2093644293768,237.111835335749,57.9538528736901));
#39211=CARTESIAN_POINT('Ctrl Pts',(73.4162169892982,236.516015918742,59.5123312044275));
#39212=CARTESIAN_POINT('Ctrl Pts',(68.6840167868883,235.879547890085,55.2092875510666));
#39213=CARTESIAN_POINT('Ctrl Pts',(69.735477959311,235.243079861428,48.9002200414177));
#39214=CARTESIAN_POINT('Ctrl Pts',(75.6256505593195,234.60661183277,46.3756604014124));
#39215=CARTESIAN_POINT('Ctrl Pts',(79.987591280419,234.081253925998,49.3398271333882));
#39216=CARTESIAN_POINT('Ctrl Pts',(80.6272120290057,233.768052028776,52.1237761173741));
#39217=CARTESIAN_POINT('Ctrl Pts',(80.6265348678285,233.667006141107,53.0222797174675));
#39218=CARTESIAN_POINT('Ctrl Pts',(80.6301424893571,236.332993858894,53.0176985262882));
#39219=CARTESIAN_POINT('Ctrl Pts',(80.6177952448289,236.173464553916,54.431871326041));
#39220=CARTESIAN_POINT('Ctrl Pts',(79.3643926740058,235.801779239385,57.7468592758642));
#39221=CARTESIAN_POINT('Ctrl Pts',(73.7825598716915,235.217937915303,59.5907868730799));
#39222=CARTESIAN_POINT('Ctrl Pts',(69.6516937528243,234.687547891422,56.2316030971915));
#39223=CARTESIAN_POINT('Ctrl Pts',(69.1562151927476,234.263235872318,52.3812253387187));
#39224=CARTESIAN_POINT('Ctrl Pts',(70.4769197368907,233.838923853213,48.7306572468295));
#39225=CARTESIAN_POINT('Ctrl Pts',(75.2392757088466,233.308533829332,46.3498724752568));
#39226=CARTESIAN_POINT('Ctrl Pts',(79.8846817431793,232.771197829634,49.1231713686024));
#39227=CARTESIAN_POINT('Ctrl Pts',(80.6212334654278,232.446017839488,52.018385090529));
#39228=CARTESIAN_POINT('Ctrl Pts',(80.6223895405763,232.332993858894,53.0239051904298));
#39229=CARTESIAN_POINT('Origin',(74.9879498948689,423.667006141107,53.0228109606356));
#39230=CARTESIAN_POINT('',(80.639219222663,241.667006141107,53.0250766137249));
#39231=CARTESIAN_POINT('',(80.6409723448486,240.332993858894,53.0233040863504));
#39232=CARTESIAN_POINT('',(80.6314498948689,423.667006141107,53.0228109606222));
#39233=CARTESIAN_POINT('Ctrl Pts',(80.6392192226631,241.667006141107,53.0250766137249));
#39234=CARTESIAN_POINT('Ctrl Pts',(80.6404467163709,241.647257476737,53.1993468669158));
#39235=CARTESIAN_POINT('Ctrl Pts',(80.554786019131,241.415352802815,55.2448933528202));
#39236=CARTESIAN_POINT('Ctrl Pts',(78.0566544293302,240.97129211934,58.9530107718744));
#39237=CARTESIAN_POINT('Ctrl Pts',(71.6622303016729,240.334824090684,58.8072592228149));
#39238=CARTESIAN_POINT('Ctrl Pts',(68.3190498381245,239.698356062027,53.3544573901267));
#39239=CARTESIAN_POINT('Ctrl Pts',(71.1106908750382,239.06188803337,47.586071571299));
#39240=CARTESIAN_POINT('Ctrl Pts',(76.3977930505111,238.531498009489,46.9578032223369));
#39241=CARTESIAN_POINT('Ctrl Pts',(79.507433526864,238.107185990384,49.2818178510052));
#39242=CARTESIAN_POINT('Ctrl Pts',(80.5215624825551,237.854381369182,51.3606053507983));
#39243=CARTESIAN_POINT('Ctrl Pts',(80.6340646824947,237.707654752757,52.6583581421423));
#39244=CARTESIAN_POINT('Ctrl Pts',(80.6306964515364,237.667006141107,53.0183537100148));
#39245=CARTESIAN_POINT('Ctrl Pts',(80.6409723448486,240.332993858894,53.0233040863504));
#39246=CARTESIAN_POINT('Ctrl Pts',(80.6411761736531,240.325223287449,53.091891390677));
#39247=CARTESIAN_POINT('Ctrl Pts',(80.6087082900944,240.105296706451,55.0329578157609));
#39248=CARTESIAN_POINT('Ctrl Pts',(78.3846879127202,239.673214115902,58.7720233877865));
#39249=CARTESIAN_POINT('Ctrl Pts',(73.0631846035857,239.14282409202,58.9445721144314));
#39250=CARTESIAN_POINT('Ctrl Pts',(70.1642998769843,238.718512072917,56.3624460082323));
#39251=CARTESIAN_POINT('Ctrl Pts',(68.7676494101067,238.294200053811,52.740253942672));
#39252=CARTESIAN_POINT('Ctrl Pts',(70.8020690104725,237.763810029931,47.8199584818442));
#39253=CARTESIAN_POINT('Ctrl Pts',(77.1104133983672,237.127342001273,46.6919843165582));
#39254=CARTESIAN_POINT('Ctrl Pts',(80.3669121402635,236.650403277595,50.2087018539011));
#39255=CARTESIAN_POINT('Ctrl Pts',(80.6342156895141,236.385620563468,52.5511807654309));
#39256=CARTESIAN_POINT('Ctrl Pts',(80.6301424893571,236.332993858894,53.0176985262882));
#39257=CARTESIAN_POINT('Origin',(74.9879498948689,423.667006141107,53.0228109606356));
#39258=CARTESIAN_POINT('',(80.6314498948689,245.667006141107,53.022810960629));
#39259=CARTESIAN_POINT('',(80.6268649774404,244.332993858894,53.0288741209513));
#39260=CARTESIAN_POINT('',(80.6314498948689,423.667006141107,53.0228109606222));
#39261=CARTESIAN_POINT('Ctrl Pts',(80.6242644646922,245.667006141107,53.0259519424172));
#39262=CARTESIAN_POINT('Ctrl Pts',(80.6283838704355,245.586860200718,53.7390185694659));
#39263=CARTESIAN_POINT('Ctrl Pts',(80.1722574471451,245.294558250776,56.3347096625558));
#39264=CARTESIAN_POINT('Ctrl Pts',(76.2700637597904,244.790100291282,59.5708210818689));
#39265=CARTESIAN_POINT('Ctrl Pts',(70.1704175211297,244.153632262625,57.6461862589446));
#39266=CARTESIAN_POINT('Ctrl Pts',(68.4956083292596,243.517164233968,51.4605133929858));
#39267=CARTESIAN_POINT('Ctrl Pts',(72.0753836691866,242.986774210088,47.5192725924447));
#39268=CARTESIAN_POINT('Ctrl Pts',(75.9470751017479,242.562462190983,47.234819894324));
#39269=CARTESIAN_POINT('Ctrl Pts',(79.3537682695749,242.157898836248,48.6822702297702));
#39270=CARTESIAN_POINT('Ctrl Pts',(80.627259993364,241.859413486289,51.3271958794769));
#39271=CARTESIAN_POINT('Ctrl Pts',(80.6392192226631,241.667006141107,53.0250766137249));
#39272=CARTESIAN_POINT('Ctrl Pts',(80.6268649774404,244.332993858894,53.0288741209513));
#39273=CARTESIAN_POINT('Ctrl Pts',(80.6315087751579,244.264826011429,53.6345321579813));
#39274=CARTESIAN_POINT('Ctrl Pts',(80.2623979033779,243.984502154412,56.11878604849));
#39275=CARTESIAN_POINT('Ctrl Pts',(77.4178204841707,243.598100292619,58.7558472860377));
#39276=CARTESIAN_POINT('Ctrl Pts',(73.5359982239256,243.173788273515,58.7072280891914));
#39277=CARTESIAN_POINT('Ctrl Pts',(70.1063587579266,242.74947625441,56.8883050507697));
#39278=CARTESIAN_POINT('Ctrl Pts',(68.415965773611,242.21908623053,51.8394693344116));
#39279=CARTESIAN_POINT('Ctrl Pts',(72.4391053296256,241.582618201872,46.8512950444875));
#39280=CARTESIAN_POINT('Ctrl Pts',(78.719845174171,240.953920744661,47.5364073786828));
#39281=CARTESIAN_POINT('Ctrl Pts',(80.6356111381715,240.537379297001,51.2192866672693));
#39282=CARTESIAN_POINT('Ctrl Pts',(80.6409723448486,240.332993858894,53.0233040863504));
#39283=CARTESIAN_POINT('Origin',(74.9879498948689,423.667006141107,53.0228109606356));
#39284=CARTESIAN_POINT('',(80.6314498948689,249.667006141107,53.0228109606291));
#39285=CARTESIAN_POINT('',(80.6227681821118,248.332993858894,53.0188409701825));
#39286=CARTESIAN_POINT('',(80.6314498948689,423.667006141107,53.0228109606222));
#39287=CARTESIAN_POINT('Ctrl Pts',(80.6314498948689,249.667006141107,53.0228109606291));
#39288=CARTESIAN_POINT('Ctrl Pts',(80.6314498948709,249.474221318505,54.7318077489481));
#39289=CARTESIAN_POINT('Ctrl Pts',(79.8060659192675,249.281436495902,56.4221521097287));
#39290=CARTESIAN_POINT('Ctrl Pts',(78.4584055093417,249.0886516733,57.4730952299799));
#39291=CARTESIAN_POINT('Ctrl Pts',(77.110745099416,248.895866850697,58.5240383502311));
#39292=CARTESIAN_POINT('Ctrl Pts',(75.2702256751601,248.703082028095,58.9126397065624));
#39293=CARTESIAN_POINT('Ctrl Pts',(73.6127451627021,248.510297205493,58.4961923829947));
#39294=CARTESIAN_POINT('Ctrl Pts',(71.9552646502442,248.31751238289,58.079745059427));
#39295=CARTESIAN_POINT('Ctrl Pts',(70.5170033810718,248.124727560288,56.8673394809161));
#39296=CARTESIAN_POINT('Ctrl Pts',(69.8261371496117,247.931942737685,55.3042099684595));
#39297=CARTESIAN_POINT('Ctrl Pts',(69.1352709181516,247.739157915083,53.741080456003));
#39298=CARTESIAN_POINT('Ctrl Pts',(69.2068803054904,247.546373092481,51.8613477992534));
#39299=CARTESIAN_POINT('Ctrl Pts',(70.0146680415447,247.353588269878,50.3553102844601));
#39300=CARTESIAN_POINT('Ctrl Pts',(70.8224557775991,247.160803447276,48.8492727696668));
#39301=CARTESIAN_POINT('Ctrl Pts',(72.3487890589407,246.968018624674,47.7498049531871));
#39302=CARTESIAN_POINT('Ctrl Pts',(74.0331492157621,246.775233802071,47.460666777573));
#39303=CARTESIAN_POINT('Ctrl Pts',(75.7175093725834,246.582448979469,47.1715286019588));
#39304=CARTESIAN_POINT('Ctrl Pts',(77.5231293307858,246.389664156866,47.6990315230378));
#39305=CARTESIAN_POINT('Ctrl Pts',(78.7869273705891,246.196879334264,48.8494595029974));
#39306=CARTESIAN_POINT('Ctrl Pts',(79.9447859852121,246.020254936545,49.9034514424903));
#39307=CARTESIAN_POINT('Ctrl Pts',(80.6314498948671,245.843630538826,51.4570729301869));
#39308=CARTESIAN_POINT('Ctrl Pts',(80.6314498948689,245.667006141107,53.022810960629));
#39309=CARTESIAN_POINT('Ctrl Pts',(80.6227681821118,248.332993858894,53.0188409701825));
#39310=CARTESIAN_POINT('Ctrl Pts',(80.6158591604151,248.20442873541,54.1611132958689));
#39311=CARTESIAN_POINT('Ctrl Pts',(79.9981558131614,247.96978560715,56.2521292880647));
#39312=CARTESIAN_POINT('Ctrl Pts',(77.6191604611375,247.629064474113,58.2666161345652));
#39313=CARTESIAN_POINT('Ctrl Pts',(73.8370732189359,247.204752455009,59.1422438972669));
#39314=CARTESIAN_POINT('Ctrl Pts',(69.2501690271641,246.674362431128,56.4388237546138));
#39315=CARTESIAN_POINT('Ctrl Pts',(69.0167443893414,246.037894402471,50.0346807540015));
#39316=CARTESIAN_POINT('Ctrl Pts',(74.2720958288138,245.401426373814,46.3889730468402));
#39317=CARTESIAN_POINT('Ctrl Pts',(79.5510126640985,244.833126192622,48.5682043349156));
#39318=CARTESIAN_POINT('Ctrl Pts',(80.6170560730475,244.476982020982,51.7495673678552));
#39319=CARTESIAN_POINT('Ctrl Pts',(80.6268649774404,244.332993858894,53.0288741209513));
#39320=CARTESIAN_POINT('Origin',(74.9879498948689,423.667006141107,53.0228109606356));
#39321=CARTESIAN_POINT('',(80.6393328775357,253.667006141107,53.0210292745041));
#39322=CARTESIAN_POINT('',(80.6374739721345,252.332993858894,53.0206546444271));
#39323=CARTESIAN_POINT('',(80.6314498948689,423.667006141107,53.0228109606222));
#39324=CARTESIAN_POINT('Ctrl Pts',(80.6393328775358,253.667006141107,53.0210292745041));
#39325=CARTESIAN_POINT('Ctrl Pts',(80.6320814513646,253.466065648679,54.7946984432943));
#39326=CARTESIAN_POINT('Ctrl Pts',(78.779047218355,253.052969146698,58.4542935954325));
#39327=CARTESIAN_POINT('Ctrl Pts',(72.531846601885,252.427716635165,59.2323865748476));
#39328=CARTESIAN_POINT('Ctrl Pts',(69.1307639245367,251.897326611285,55.1359482250076));
#39329=CARTESIAN_POINT('Ctrl Pts',(69.3913142509957,251.47301459218,51.2625748355938));
#39330=CARTESIAN_POINT('Ctrl Pts',(71.3948305414538,251.048702573075,47.9373935833451));
#39331=CARTESIAN_POINT('Ctrl Pts',(76.5284508786805,250.518312549195,46.5252630067303));
#39332=CARTESIAN_POINT('Ctrl Pts',(80.2381453491283,250.022387736946,49.8676147702881));
#39333=CARTESIAN_POINT('Ctrl Pts',(80.6311954971923,249.738618934251,52.3828494633525));
#39334=CARTESIAN_POINT('Ctrl Pts',(80.6264700991543,249.667006141107,53.0189018164475));
#39335=CARTESIAN_POINT('Ctrl Pts',(80.6374739721345,252.332993858894,53.0206546444271));
#39336=CARTESIAN_POINT('Ctrl Pts',(80.6341057873527,252.250109464167,53.7534226942952));
#39337=CARTESIAN_POINT('Ctrl Pts',(80.2883165046266,252.061147064663,55.4282110155384));
#39338=CARTESIAN_POINT('Ctrl Pts',(78.1317232526417,251.660028655607,58.3976286937398));
#39339=CARTESIAN_POINT('Ctrl Pts',(72.8959148267621,251.129638631727,59.3643140922468));
#39340=CARTESIAN_POINT('Ctrl Pts',(68.5203052848772,250.493170603069,54.6822658470019));
#39341=CARTESIAN_POINT('Ctrl Pts',(70.0974900542959,249.856702574413,48.4836860385676));
#39342=CARTESIAN_POINT('Ctrl Pts',(76.1615187036544,249.220234545756,46.4496113157072));
#39343=CARTESIAN_POINT('Ctrl Pts',(80.1472802315439,248.712331640583,49.6536433732334));
#39344=CARTESIAN_POINT('Ctrl Pts',(80.6272603120911,248.416584744962,52.276154670448));
#39345=CARTESIAN_POINT('Ctrl Pts',(80.6227681821118,248.332993858894,53.0188409701825));
#39346=CARTESIAN_POINT('Origin',(74.9879498948689,423.667006141107,53.0228109606356));
#39347=CARTESIAN_POINT('',(80.6321203983526,257.667006141107,53.0274094678416));
#39348=CARTESIAN_POINT('',(80.6352358645235,256.332993858894,53.0260672585175));
#39349=CARTESIAN_POINT('',(80.6314498948689,423.667006141107,53.0228109606222));
#39350=CARTESIAN_POINT('Ctrl Pts',(80.6321203983526,257.667006141107,53.0274094678416));
#39351=CARTESIAN_POINT('Ctrl Pts',(80.6362361148136,257.617824382212,53.4631731254976));
#39352=CARTESIAN_POINT('Ctrl Pts',(80.3908316677195,257.356486613764,55.774500525636));
#39353=CARTESIAN_POINT('Ctrl Pts',(77.2053896188859,256.882992835764,59.321559547837));
#39354=CARTESIAN_POINT('Ctrl Pts',(71.9514325914311,256.352602811883,58.458943708744));
#39355=CARTESIAN_POINT('Ctrl Pts',(69.608268828627,255.928290792779,55.3637068087443));
#39356=CARTESIAN_POINT('Ctrl Pts',(68.9405046437633,255.503978773674,51.5394423200026));
#39357=CARTESIAN_POINT('Ctrl Pts',(71.8904013482855,254.973588749793,47.1070298882851));
#39358=CARTESIAN_POINT('Ctrl Pts',(78.2977346304908,254.337120721136,47.2237125544275));
#39359=CARTESIAN_POINT('Ctrl Pts',(80.5923227223968,253.901593184907,50.9507676211459));
#39360=CARTESIAN_POINT('Ctrl Pts',(80.639737616737,253.678221658231,52.9220317220709));
#39361=CARTESIAN_POINT('Ctrl Pts',(80.6393328775358,253.667006141107,53.0210292745041));
#39362=CARTESIAN_POINT('Ctrl Pts',(80.6352358645235,256.332993858894,53.0260672585175));
#39363=CARTESIAN_POINT('Ctrl Pts',(80.6372806134956,256.295790192923,53.3554066374292));
#39364=CARTESIAN_POINT('Ctrl Pts',(80.4548977293209,256.0464305174,55.5599296850919));
#39365=CARTESIAN_POINT('Ctrl Pts',(77.5667687190911,255.584914832326,59.1824348262834));
#39366=CARTESIAN_POINT('Ctrl Pts',(71.193045766207,254.948446803668,58.5167093921053));
#39367=CARTESIAN_POINT('Ctrl Pts',(68.3192351039939,254.311978775012,52.8025939123332));
#39368=CARTESIAN_POINT('Ctrl Pts',(71.5637615965536,253.675510746354,47.2905206837289));
#39369=CARTESIAN_POINT('Ctrl Pts',(77.9675186861103,253.039042717698,47.0467384616874));
#39370=CARTESIAN_POINT('Ctrl Pts',(80.5301405732545,252.591537088544,50.7363783348355));
#39371=CARTESIAN_POINT('Ctrl Pts',(80.6384164941214,252.356187468943,52.8156035433032));
#39372=CARTESIAN_POINT('Ctrl Pts',(80.6374739721345,252.332993858894,53.0206546444271));
#39373=CARTESIAN_POINT('Origin',(74.9879498948689,423.667006141107,53.0228109606356));
#39374=CARTESIAN_POINT('',(80.622068675635,261.667006141107,53.0231071599436));
#39375=CARTESIAN_POINT('',(80.6208495127526,260.332993858894,53.0251315510043));
#39376=CARTESIAN_POINT('',(80.6314498948689,423.667006141107,53.0228109606222));
#39377=CARTESIAN_POINT('Ctrl Pts',(80.6220686756351,261.667006141107,53.0231071599436));
#39378=CARTESIAN_POINT('Ctrl Pts',(80.6212211316863,261.557427106192,53.9989613352296));
#39379=CARTESIAN_POINT('Ctrl Pts',(79.9158201063165,261.235692061725,56.8646493578844));
#39380=CARTESIAN_POINT('Ctrl Pts',(76.2600105715705,260.807879012482,59.1182057980456));
#39381=CARTESIAN_POINT('Ctrl Pts',(72.4612951821995,260.383566993377,58.317787609226));
#39382=CARTESIAN_POINT('Ctrl Pts',(69.4494584547942,259.959254974273,55.8683494259096));
#39383=CARTESIAN_POINT('Ctrl Pts',(68.7701667585371,259.428864950391,50.5875603443804));
#39384=CARTESIAN_POINT('Ctrl Pts',(73.6841987474315,258.792396921735,46.4741889478306));
#39385=CARTESIAN_POINT('Ctrl Pts',(79.3157785783291,258.205110651973,48.2397007920277));
#39386=CARTESIAN_POINT('Ctrl Pts',(80.6184820938021,257.829980391764,51.5834136213084));
#39387=CARTESIAN_POINT('Ctrl Pts',(80.6321203983526,257.667006141107,53.0274094678416));
#39388=CARTESIAN_POINT('Ctrl Pts',(80.6208495127526,260.332993858894,53.0251315510043));
#39389=CARTESIAN_POINT('Ctrl Pts',(80.6234734375329,260.235392916904,53.8929902989329));
#39390=CARTESIAN_POINT('Ctrl Pts',(80.0293014250823,259.925635965362,56.6440798635399));
#39391=CARTESIAN_POINT('Ctrl Pts',(75.7253090599096,259.403723004267,59.6591140566951));
#39392=CARTESIAN_POINT('Ctrl Pts',(69.8086851766418,258.76725497561,57.2294092881355));
#39393=CARTESIAN_POINT('Ctrl Pts',(68.64387461178,258.130786946953,50.9402821796723));
#39394=CARTESIAN_POINT('Ctrl Pts',(73.3188397393547,257.494318918296,46.5571057413125));
#39395=CARTESIAN_POINT('Ctrl Pts',(78.4794664963865,256.963928894415,47.8671065072692));
#39396=CARTESIAN_POINT('Ctrl Pts',(80.3671424458033,256.576820541282,50.8638740355873));
#39397=CARTESIAN_POINT('Ctrl Pts',(80.6314504651601,256.4018681977,52.4163684190792));
#39398=CARTESIAN_POINT('Ctrl Pts',(80.6352358645235,256.332993858894,53.0260672585175));
#39399=CARTESIAN_POINT('Origin',(74.9879498948689,423.667006141107,53.0228109606356));
#39400=CARTESIAN_POINT('',(80.6335139906277,265.667006141107,53.0179319616114));
#39401=CARTESIAN_POINT('',(80.6304551573619,264.332993858894,53.0160315296102));
#39402=CARTESIAN_POINT('',(80.6314498948689,423.667006141107,53.0228109606222));
#39403=CARTESIAN_POINT('Ctrl Pts',(80.6335139906277,265.667006141107,53.0179319616114));
#39404=CARTESIAN_POINT('Ctrl Pts',(80.6183865584892,265.497029830172,54.5213633042316));
#39405=CARTESIAN_POINT('Ctrl Pts',(79.6079955865199,265.220975514462,56.9782353383759));
#39406=CARTESIAN_POINT('Ctrl Pts',(76.5523955207542,264.838843193976,58.677302240125));
#39407=CARTESIAN_POINT('Ctrl Pts',(72.6723019530944,264.414531174871,58.8029278451709));
#39408=CARTESIAN_POINT('Ctrl Pts',(68.6966783295341,263.88414115099,55.2613763015696));
#39409=CARTESIAN_POINT('Ctrl Pts',(69.7095077253019,263.247673122334,48.9335242766798));
#39410=CARTESIAN_POINT('Ctrl Pts',(75.5720466440224,262.611205093676,46.3760761608992));
#39411=CARTESIAN_POINT('Ctrl Pts',(79.9816199514584,262.084316099935,49.3072022180086));
#39412=CARTESIAN_POINT('Ctrl Pts',(80.6228620618353,261.769583115745,52.1096097097592));
#39413=CARTESIAN_POINT('Ctrl Pts',(80.6220686756351,261.667006141107,53.0231071599436));
#39414=CARTESIAN_POINT('Ctrl Pts',(80.6304551573619,264.332993858894,53.0160315296102));
#39415=CARTESIAN_POINT('Ctrl Pts',(80.6177187628455,264.174995640884,54.417397186382));
#39416=CARTESIAN_POINT('Ctrl Pts',(79.3805880254645,263.804841413322,57.7237302943176));
#39417=CARTESIAN_POINT('Ctrl Pts',(73.83600196959,263.222531176209,59.5949695472677));
#39418=CARTESIAN_POINT('Ctrl Pts',(68.8326175982397,262.586063147551,55.6104936380737));
#39419=CARTESIAN_POINT('Ctrl Pts',(69.4880334727284,261.949595118895,49.2357022951904));
#39420=CARTESIAN_POINT('Ctrl Pts',(74.2432971283764,261.419205095013,46.8407830695233));
#39421=CARTESIAN_POINT('Ctrl Pts',(77.959377089695,260.994893075909,47.9640183999525));
#39422=CARTESIAN_POINT('Ctrl Pts',(80.1081444486407,260.668181998794,50.0419592388654));
#39423=CARTESIAN_POINT('Ctrl Pts',(80.6177697896028,260.447548926456,52.0065182520312));
#39424=CARTESIAN_POINT('Ctrl Pts',(80.6208495127526,260.332993858894,53.0251315510043));
#39425=CARTESIAN_POINT('Origin',(74.9879498948689,423.667006141107,53.0228109606356));
#39426=CARTESIAN_POINT('',(80.6362260843705,269.667006141107,53.025791082417));
#39427=CARTESIAN_POINT('',(80.6409957355089,268.332993858894,53.0245822494549));
#39428=CARTESIAN_POINT('',(80.6314498948689,423.667006141107,53.0228109606222));
#39429=CARTESIAN_POINT('Ctrl Pts',(80.6362260843705,269.667006141107,53.025791082417));
#39430=CARTESIAN_POINT('Ctrl Pts',(80.6373722385248,269.648788563706,53.1867844897909));
#39431=CARTESIAN_POINT('Ctrl Pts',(80.5960317434328,269.524492981528,54.2848165324738));
#39432=CARTESIAN_POINT('Ctrl Pts',(79.8769093444932,269.294119394574,56.2660866575358));
#39433=CARTESIAN_POINT('Ctrl Pts',(77.0298250182992,268.86980737547,58.9052188493705));
#39434=CARTESIAN_POINT('Ctrl Pts',(71.7059457747086,268.339417351589,58.8382835682292));
#39435=CARTESIAN_POINT('Ctrl Pts',(68.3212808918114,267.702949322932,53.396631405116));
#39436=CARTESIAN_POINT('Ctrl Pts',(71.0704926838037,267.066481294275,47.6215350456437));
#39437=CARTESIAN_POINT('Ctrl Pts',(77.413848888673,266.430013265619,46.8019403308202));
#39438=CARTESIAN_POINT('Ctrl Pts',(80.4345171486351,265.963521547895,50.3987411432354));
#39439=CARTESIAN_POINT('Ctrl Pts',(80.637267869771,265.709185839725,52.6448547923503));
#39440=CARTESIAN_POINT('Ctrl Pts',(80.6335139906277,265.667006141107,53.0179319616114));
#39441=CARTESIAN_POINT('Ctrl Pts',(80.6409957355089,268.332993858894,53.0245822494549));
#39442=CARTESIAN_POINT('Ctrl Pts',(80.6411428885357,268.326754374417,53.0796608730736));
#39443=CARTESIAN_POINT('Ctrl Pts',(80.6157117197006,268.108358880388,55.0073374956178));
#39444=CARTESIAN_POINT('Ctrl Pts',(78.4277792530005,267.677807376808,58.7401378270421));
#39445=CARTESIAN_POINT('Ctrl Pts',(72.0375055083273,267.04133934815,59.0127270905129));
#39446=CARTESIAN_POINT('Ctrl Pts',(68.3522149334259,266.404871319494,53.7700018438139));
#39447=CARTESIAN_POINT('Ctrl Pts',(70.3720114990969,265.874481295612,48.8436855359119));
#39448=CARTESIAN_POINT('Ctrl Pts',(73.9141788037828,265.450169276508,47.2549883740677));
#39449=CARTESIAN_POINT('Ctrl Pts',(77.7907517378467,265.025857257403,47.4625701009125));
#39450=CARTESIAN_POINT('Ctrl Pts',(80.3585521621098,264.653465451532,50.1793413821216));
#39451=CARTESIAN_POINT('Ctrl Pts',(80.6348208711523,264.387151650437,52.535678839113));
#39452=CARTESIAN_POINT('Ctrl Pts',(80.6304551573619,264.332993858894,53.0160315296102));
#39453=CARTESIAN_POINT('Origin',(74.9879498948689,423.667006141107,53.0228109606356));
#39454=CARTESIAN_POINT('',(80.6281690978408,273.667006141107,53.0254425033022));
#39455=CARTESIAN_POINT('',(80.6267765454294,272.332993858894,53.0274331835911));
#39456=CARTESIAN_POINT('',(80.6314498948689,423.667006141107,53.0228109606222));
#39457=CARTESIAN_POINT('Ctrl Pts',(80.6281690978408,273.667006141107,53.0254425033022));
#39458=CARTESIAN_POINT('Ctrl Pts',(80.6310061674789,273.588391287686,53.723925770271));
#39459=CARTESIAN_POINT('Ctrl Pts',(80.1764188506617,273.297620424713,56.303244467039));
#39460=CARTESIAN_POINT('Ctrl Pts',(76.3234123534648,272.794693552187,59.5655789311586));
#39461=CARTESIAN_POINT('Ctrl Pts',(70.1997566345717,272.158225523531,57.6765645663912));
#39462=CARTESIAN_POINT('Ctrl Pts',(68.4885131854145,271.521757494873,51.5136472948276));
#39463=CARTESIAN_POINT('Ctrl Pts',(72.740299548083,270.885289466217,46.7353404645114));
#39464=CARTESIAN_POINT('Ctrl Pts',(78.8886131272501,270.267039014961,47.7092368751911));
#39465=CARTESIAN_POINT('Ctrl Pts',(80.6240244982427,269.860944573258,51.3119073796098));
#39466=CARTESIAN_POINT('Ctrl Pts',(80.6362260843705,269.667006141107,53.025791082417));
#39467=CARTESIAN_POINT('Ctrl Pts',(80.6267765454294,272.332993858894,53.0274331835911));
#39468=CARTESIAN_POINT('Ctrl Pts',(80.6311474818016,272.266357098398,53.6190577687339));
#39469=CARTESIAN_POINT('Ctrl Pts',(80.2718050755859,271.987564328349,56.0888874902184));
#39470=CARTESIAN_POINT('Ctrl Pts',(76.6881265535354,271.496615548749,59.4798704036303));
#39471=CARTESIAN_POINT('Ctrl Pts',(70.4679411286712,270.860147520092,57.9381739632954));
#39472=CARTESIAN_POINT('Ctrl Pts',(68.7625597545307,270.329757496211,52.8943812533468));
#39473=CARTESIAN_POINT('Ctrl Pts',(70.3951339519087,269.905445477106,49.3722214931296));
#39474=CARTESIAN_POINT('Ctrl Pts',(73.4580535169106,269.481133458002,46.9869685453763));
#39475=CARTESIAN_POINT('Ctrl Pts',(78.694248321282,268.956982918598,47.5040608083218));
#39476=CARTESIAN_POINT('Ctrl Pts',(80.6361393663569,268.53891038397,51.2068681700428));
#39477=CARTESIAN_POINT('Ctrl Pts',(80.6409957355089,268.332993858894,53.0245822494549));
#39478=CARTESIAN_POINT('Origin',(74.9879498948689,423.667006141107,53.0228109606356));
#39479=CARTESIAN_POINT('',(80.6228988645023,277.667006141107,53.0197320148476));
#39480=CARTESIAN_POINT('',(80.6235335168385,276.332993858894,53.0199012860661));
#39481=CARTESIAN_POINT('',(80.6314498948689,423.667006141107,53.0228109606222));
#39482=CARTESIAN_POINT('Ctrl Pts',(80.6228988645023,277.667006141107,53.0197320148476));
#39483=CARTESIAN_POINT('Ctrl Pts',(80.6152243194595,277.527994011667,54.2547852777675));
#39484=CARTESIAN_POINT('Ctrl Pts',(79.6128226704193,277.176825872674,57.3844444804395));
#39485=CARTESIAN_POINT('Ctrl Pts',(74.4244720439219,276.613501724129,59.6761341928656));
#39486=CARTESIAN_POINT('Ctrl Pts',(69.0912915673428,275.977033695473,56.1452576101099));
#39487=CARTESIAN_POINT('Ctrl Pts',(69.1681105982651,275.340565666815,49.7496339286456));
#39488=CARTESIAN_POINT('Ctrl Pts',(74.6042813775611,274.704097638159,46.3561722901173));
#39489=CARTESIAN_POINT('Ctrl Pts',(79.412935102352,274.173707614278,48.6420025303696));
#39490=CARTESIAN_POINT('Ctrl Pts',(80.5477416441213,273.828010448594,51.5942741654804));
#39491=CARTESIAN_POINT('Ctrl Pts',(80.6271780017631,273.694469292462,52.7814357940699));
#39492=CARTESIAN_POINT('Ctrl Pts',(80.6281690978408,273.667006141107,53.0254425033022));
#39493=CARTESIAN_POINT('Ctrl Pts',(80.6235335168385,276.332993858894,53.0199012860661));
#39494=CARTESIAN_POINT('Ctrl Pts',(80.6187897801916,276.205959822378,54.1494403880117));
#39495=CARTESIAN_POINT('Ctrl Pts',(79.7423703700239,275.86676977631,57.1728458637594));
#39496=CARTESIAN_POINT('Ctrl Pts',(74.7984951898932,275.315423720691,59.6977925792757));
#39497=CARTESIAN_POINT('Ctrl Pts',(70.2035816423413,274.78503369681,57.008008197077));
#39498=CARTESIAN_POINT('Ctrl Pts',(69.1265928622935,274.360721677705,53.2782624880387));
#39499=CARTESIAN_POINT('Ctrl Pts',(69.8750124991416,273.936409658601,49.4689612484914));
#39500=CARTESIAN_POINT('Ctrl Pts',(74.2184942159277,273.406019634719,46.389620879493));
#39501=CARTESIAN_POINT('Ctrl Pts',(79.5357846862319,272.836188366559,48.5447931610259));
#39502=CARTESIAN_POINT('Ctrl Pts',(80.6172314328848,272.47851310795,51.7354621346952));
#39503=CARTESIAN_POINT('Ctrl Pts',(80.6267765454294,272.332993858894,53.0274331835911));
#39504=CARTESIAN_POINT('Origin',(74.9879498948689,423.667006141107,53.0228109606356));
#39505=CARTESIAN_POINT('',(80.64045763597,281.667006141107,53.0193177463791));
#39506=CARTESIAN_POINT('',(80.6380317763782,280.332993858894,53.0185653928147));
#39507=CARTESIAN_POINT('',(80.6314498948689,423.667006141107,53.0228109606222));
#39508=CARTESIAN_POINT('Ctrl Pts',(80.64045763597,281.667006141107,53.0193177463791));
#39509=CARTESIAN_POINT('Ctrl Pts',(80.6324997205414,281.467596735647,54.7789712462744));
#39510=CARTESIAN_POINT('Ctrl Pts',(78.7982860972629,281.056031320635,58.432189503605));
#39511=CARTESIAN_POINT('Ctrl Pts',(72.5834632791282,280.432309896071,59.2468527844925));
#39512=CARTESIAN_POINT('Ctrl Pts',(68.4476732525639,279.795841867414,54.3678012071275));
#39513=CARTESIAN_POINT('Ctrl Pts',(70.326780909695,279.159373838757,48.2410982563761));
#39514=CARTESIAN_POINT('Ctrl Pts',(75.4561843501935,278.628983814876,46.8137262387156));
#39515=CARTESIAN_POINT('Ctrl Pts',(78.8839251560877,278.204671795772,48.6362247583429));
#39516=CARTESIAN_POINT('Ctrl Pts',(80.3728574180272,277.919371906107,50.7801947467159));
#39517=CARTESIAN_POINT('Ctrl Pts',(80.6269369725781,277.740150021219,52.3698852125657));
#39518=CARTESIAN_POINT('Ctrl Pts',(80.6228988645023,277.667006141107,53.0197320148476));
#39519=CARTESIAN_POINT('Ctrl Pts',(80.6380317763782,280.332993858894,53.0185653928147));
#39520=CARTESIAN_POINT('Ctrl Pts',(80.6252133547052,280.145562546359,54.675591025712));
#39521=CARTESIAN_POINT('Ctrl Pts',(78.9779451679485,279.745975224272,58.2324232018638));
#39522=CARTESIAN_POINT('Ctrl Pts',(73.9889689229884,279.240309897408,59.1688677132986));
#39523=CARTESIAN_POINT('Ctrl Pts',(70.7301472839238,278.815997878304,57.0591309024144));
#39524=CARTESIAN_POINT('Ctrl Pts',(68.7973374677702,278.391685859198,53.6923588428567));
#39525=CARTESIAN_POINT('Ctrl Pts',(70.0574457782005,277.861295835319,48.5193232177926));
#39526=CARTESIAN_POINT('Ctrl Pts',(76.1199198830696,277.224827806661,46.4423200012274));
#39527=CARTESIAN_POINT('Ctrl Pts',(80.1305528088605,276.71539381452,49.6241218867143));
#39528=CARTESIAN_POINT('Ctrl Pts',(80.626712162767,276.418115831931,52.2630285642579));
#39529=CARTESIAN_POINT('Ctrl Pts',(80.6235335168385,276.332993858894,53.0199012860661));
#39530=CARTESIAN_POINT('Origin',(74.9879498948689,423.667006141107,53.0228109606356));
#39531=CARTESIAN_POINT('',(80.6320072490403,285.667006141107,53.0282647722842));
#39532=CARTESIAN_POINT('',(80.6355667283407,284.332993858894,53.029097899403));
#39533=CARTESIAN_POINT('',(80.6314498948689,423.667006141107,53.0228109606222));
#39534=CARTESIAN_POINT('Ctrl Pts',(80.6320072490403,285.667006141107,53.0282647722843));
#39535=CARTESIAN_POINT('Ctrl Pts',(80.6360246717883,285.61935546918,53.4507321318154));
#39536=CARTESIAN_POINT('Ctrl Pts',(80.4001389358992,285.359548787701,55.7495394486793));
#39537=CARTESIAN_POINT('Ctrl Pts',(77.2538459713296,284.887586096669,59.2986350086054));
#39538=CARTESIAN_POINT('Ctrl Pts',(70.9320055672451,284.251118068013,58.3269162510927));
#39539=CARTESIAN_POINT('Ctrl Pts',(68.3332775512137,283.614650039355,52.4690883829723));
#39540=CARTESIAN_POINT('Ctrl Pts',(71.2699962732185,283.084260015475,48.0279338393853));
#39541=CARTESIAN_POINT('Ctrl Pts',(75.0529945743877,282.65994799637,47.1562505598691));
#39542=CARTESIAN_POINT('Ctrl Pts',(78.8157359444728,282.235635977266,48.1115961875279));
#39543=CARTESIAN_POINT('Ctrl Pts',(80.5864453672283,281.904655358845,50.9229722937909));
#39544=CARTESIAN_POINT('Ctrl Pts',(80.6409663200872,281.679752745199,52.9068375629505));
#39545=CARTESIAN_POINT('Ctrl Pts',(80.64045763597,281.667006141107,53.0193177463791));
#39546=CARTESIAN_POINT('Ctrl Pts',(80.6355667283407,284.332993858894,53.029097899403));
#39547=CARTESIAN_POINT('Ctrl Pts',(80.6383807082737,284.297321279892,53.3447008893674));
#39548=CARTESIAN_POINT('Ctrl Pts',(80.4703213599792,284.049492691337,55.5336961519382));
#39549=CARTESIAN_POINT('Ctrl Pts',(78.2638620892544,283.695586098007,58.3181273708052));
#39550=CARTESIAN_POINT('Ctrl Pts',(74.4200471881275,283.271274078902,58.8621814970761));
#39551=CARTESIAN_POINT('Ctrl Pts',(70.7530948079326,282.846962059797,57.5876744834349));
#39552=CARTESIAN_POINT('Ctrl Pts',(68.3123700687952,282.316572035917,52.8557580344726));
#39553=CARTESIAN_POINT('Ctrl Pts',(71.5275734779309,281.68010400726,47.3122932630761));
#39554=CARTESIAN_POINT('Ctrl Pts',(77.9173327360281,281.043635978603,47.0278990613398));
#39555=CARTESIAN_POINT('Ctrl Pts',(80.5292436010146,280.594599262481,50.7076804397306));
#39556=CARTESIAN_POINT('Ctrl Pts',(80.6397226976433,280.357718555911,52.7999815491162));
#39557=CARTESIAN_POINT('Ctrl Pts',(80.6380317763782,280.332993858894,53.0185653928147));
#39558=CARTESIAN_POINT('Origin',(74.9879498948689,423.667006141107,53.0228109606356));
#39559=CARTESIAN_POINT('',(80.6223389969519,289.667006141107,53.0226618801889));
#39560=CARTESIAN_POINT('',(80.620338754176,288.332993858894,53.0230516208103));
#39561=CARTESIAN_POINT('',(80.6314498948689,423.667006141107,53.0228109606222));
#39562=CARTESIAN_POINT('Ctrl Pts',(80.6223389969519,289.667006141107,53.0226618801889));
#39563=CARTESIAN_POINT('Ctrl Pts',(80.6214784739939,289.558958193161,53.9839632426538));
#39564=CARTESIAN_POINT('Ctrl Pts',(79.9289801677415,289.238754235662,56.8332978081037));
#39565=CARTESIAN_POINT('Ctrl Pts',(75.4037717530398,288.706394268611,59.6869920433574));
#39566=CARTESIAN_POINT('Ctrl Pts',(69.6005983433171,288.069926239955,56.9684054601267));
#39567=CARTESIAN_POINT('Ctrl Pts',(68.9056248589062,287.539536216073,51.6896572763087));
#39568=CARTESIAN_POINT('Ctrl Pts',(71.1901917605342,287.115224196969,48.5509215501885));
#39569=CARTESIAN_POINT('Ctrl Pts',(74.6574983630918,286.690912177864,46.8048709179623));
#39570=CARTESIAN_POINT('Ctrl Pts',(79.2961199120551,286.20817282591,48.2071989139687));
#39571=CARTESIAN_POINT('Ctrl Pts',(80.6181378226749,285.831511478732,51.5697725243201));
#39572=CARTESIAN_POINT('Ctrl Pts',(80.6320072490403,285.667006141107,53.0282647722843));
#39573=CARTESIAN_POINT('Ctrl Pts',(80.620338754176,288.332993858894,53.0230516208103));
#39574=CARTESIAN_POINT('Ctrl Pts',(80.6214818087189,288.236924003872,53.8774821547362));
#39575=CARTESIAN_POINT('Ctrl Pts',(80.2371756449924,288.034776144075,55.674607152298));
#39576=CARTESIAN_POINT('Ctrl Pts',(78.3882223800832,287.726550279501,57.8039100782516));
#39577=CARTESIAN_POINT('Ctrl Pts',(74.7839532242394,287.302238260396,59.246183193397));
#39578=CARTESIAN_POINT('Ctrl Pts',(69.8383632853863,286.771848236515,57.2740496561053));
#39579=CARTESIAN_POINT('Ctrl Pts',(68.6308295619551,286.135380207858,50.9804499754289));
#39580=CARTESIAN_POINT('Ctrl Pts',(73.268595959504,285.498912179202,46.5757903654038));
#39581=CARTESIAN_POINT('Ctrl Pts',(79.1354669206025,284.898116729547,48.0014226755356));
#39582=CARTESIAN_POINT('Ctrl Pts',(80.6216450875187,284.509477289444,51.4677109764803));
#39583=CARTESIAN_POINT('Ctrl Pts',(80.6355667283407,284.332993858894,53.029097899403));
#39584=CARTESIAN_POINT('Origin',(74.9879498948689,423.667006141107,53.0228109606356));
#39585=CARTESIAN_POINT('',(80.6324604068353,293.667006141107,53.0178216104937));
#39586=CARTESIAN_POINT('',(80.631774688763,292.332993858894,53.0191408716922));
#39587=CARTESIAN_POINT('',(80.6314498948689,423.667006141107,53.0228109606222));
#39588=CARTESIAN_POINT('Ctrl Pts',(80.6324604068353,293.667006141107,53.0178216104937));
#39589=CARTESIAN_POINT('Ctrl Pts',(80.6191313922384,293.498560917141,54.5094386793754));
#39590=CARTESIAN_POINT('Ctrl Pts',(79.2484550408878,293.117959683623,57.9019599664741));
#39591=CARTESIAN_POINT('Ctrl Pts',(73.5077494891626,292.525202440553,59.5343606573951));
#39592=CARTESIAN_POINT('Ctrl Pts',(69.5216244297834,291.994812416672,56.0046329705635));
#39593=CARTESIAN_POINT('Ctrl Pts',(69.188310236716,291.570500397568,52.1368416712381));
#39594=CARTESIAN_POINT('Ctrl Pts',(70.6611837554908,291.146188378463,48.5449686940674));
#39595=CARTESIAN_POINT('Ctrl Pts',(75.519336798809,290.615798354582,46.3663178409258));
#39596=CARTESIAN_POINT('Ctrl Pts',(79.9690770453548,290.087378273871,49.2830760364057));
#39597=CARTESIAN_POINT('Ctrl Pts',(80.623168141594,289.771114202713,52.0964136416258));
#39598=CARTESIAN_POINT('Ctrl Pts',(80.6223389969519,289.667006141107,53.0226618801889));
#39599=CARTESIAN_POINT('Ctrl Pts',(80.631774688763,292.332993858894,53.0191408716922));
#39600=CARTESIAN_POINT('Ctrl Pts',(80.6289723051447,292.282604732629,53.4660254458849));
#39601=CARTESIAN_POINT('Ctrl Pts',(80.4572238746464,292.126137601588,54.8559768464921));
#39602=CARTESIAN_POINT('Ctrl Pts',(78.9147710729384,291.757514460995,57.8552070562179));
#39603=CARTESIAN_POINT('Ctrl Pts',(73.8876807942301,291.227124437114,59.6092121479762));
#39604=CARTESIAN_POINT('Ctrl Pts',(68.849107759653,290.590656408457,55.6493742208554));
#39605=CARTESIAN_POINT('Ctrl Pts',(69.4623515772426,289.9541883798,49.2827553804812));
#39606=CARTESIAN_POINT('Ctrl Pts',(75.145158953817,289.317720351143,46.3475205075674));
#39607=CARTESIAN_POINT('Ctrl Pts',(79.8562903143711,288.777322177508,49.0697980922682));
#39608=CARTESIAN_POINT('Ctrl Pts',(80.6189575424913,288.449080013425,51.9905991936166));
#39609=CARTESIAN_POINT('Ctrl Pts',(80.620338754176,288.332993858894,53.0230516208103));
#39610=CARTESIAN_POINT('Origin',(74.9879498948689,423.667006141107,53.0228109606356));
#39611=CARTESIAN_POINT('',(80.6398778085108,297.667006141107,53.0246601447562));
#39612=CARTESIAN_POINT('',(80.6388022101255,296.332993858894,53.0227366527281));
#39613=CARTESIAN_POINT('',(80.6314498948689,423.667006141107,53.0228109606222));
#39614=CARTESIAN_POINT('Ctrl Pts',(80.6398778085108,297.667006141107,53.0246601447562));
#39615=CARTESIAN_POINT('Ctrl Pts',(80.6407234024158,297.650319650674,53.1720103840775));
#39616=CARTESIAN_POINT('Ctrl Pts',(80.5684082111312,297.421477150689,55.1921130767689));
#39617=CARTESIAN_POINT('Ctrl Pts',(78.1402065526217,296.980478641151,58.909622547401));
#39618=CARTESIAN_POINT('Ctrl Pts',(72.8161519838604,296.450088617271,58.8585003306135));
#39619=CARTESIAN_POINT('Ctrl Pts',(70.0282823888382,296.025776598166,56.1568913641665));
#39620=CARTESIAN_POINT('Ctrl Pts',(68.7850071190202,295.601464579061,52.4792325314445));
#39621=CARTESIAN_POINT('Ctrl Pts',(71.0242980864921,295.071074555181,47.6487308499217));
#39622=CARTESIAN_POINT('Ctrl Pts',(77.3744534912965,294.434606526524,46.7867210073652));
#39623=CARTESIAN_POINT('Ctrl Pts',(80.4223038359955,293.966583721832,50.3688767351797));
#39624=CARTESIAN_POINT('Ctrl Pts',(80.6359192267734,293.710716926693,52.63075362281));
#39625=CARTESIAN_POINT('Ctrl Pts',(80.6324604068353,293.667006141107,53.0178216104937));
#39626=CARTESIAN_POINT('Ctrl Pts',(80.6388022101255,296.332993858894,53.0227366527281));
#39627=CARTESIAN_POINT('Ctrl Pts',(80.638798598822,296.328285461386,53.0643189418008));
#39628=CARTESIAN_POINT('Ctrl Pts',(80.6158508992825,296.111421054325,54.9794472511519));
#39629=CARTESIAN_POINT('Ctrl Pts',(78.4761358999726,295.682400637713,58.717003711871));
#39630=CARTESIAN_POINT('Ctrl Pts',(72.0754506158946,295.045932609055,59.0312687720055));
#39631=CARTESIAN_POINT('Ctrl Pts',(68.3636791850171,294.409464580399,53.8223671331437));
#39632=CARTESIAN_POINT('Ctrl Pts',(70.7294688552404,293.772996551742,47.8798977243302));
#39633=CARTESIAN_POINT('Ctrl Pts',(77.0211072714768,293.136528523085,46.6621864805733));
#39634=CARTESIAN_POINT('Ctrl Pts',(80.3413046990379,292.656527625469,50.1541699818498));
#39635=CARTESIAN_POINT('Ctrl Pts',(80.6348718172991,292.388682737405,52.5252545393511));
#39636=CARTESIAN_POINT('Ctrl Pts',(80.631774688763,292.332993858894,53.0191408716922));
#39637=CARTESIAN_POINT('Origin',(74.9879498948689,423.667006141107,53.0228109606356));
#39638=CARTESIAN_POINT('',(80.6249680425302,301.667006141107,53.0279939180991));
#39639=CARTESIAN_POINT('',(80.6269504670759,300.332993858894,53.0280711906708));
#39640=CARTESIAN_POINT('',(80.6314498948689,423.667006141107,53.0228109606222));
#39641=CARTESIAN_POINT('Ctrl Pts',(80.6249680425302,301.667006141107,53.0279939180991));
#39642=CARTESIAN_POINT('Ctrl Pts',(80.6292423549922,301.589922374655,53.7134873977605));
#39643=CARTESIAN_POINT('Ctrl Pts',(80.1958374117308,301.30068259865,56.2795585259795));
#39644=CARTESIAN_POINT('Ctrl Pts',(77.1748718396303,300.905364817869,58.8528494679402));
#39645=CARTESIAN_POINT('Ctrl Pts',(73.2985174821482,300.481052798765,58.6412253160407));
#39646=CARTESIAN_POINT('Ctrl Pts',(69.9483047892701,300.05674077966,56.6798526337298));
#39647=CARTESIAN_POINT('Ctrl Pts',(68.4714694295786,299.526350755779,51.5644711374421));
#39648=CARTESIAN_POINT('Ctrl Pts',(72.700576392418,298.889882727122,46.7496825719188));
#39649=CARTESIAN_POINT('Ctrl Pts',(78.8584126251663,298.270101188898,47.6845510583783));
#39650=CARTESIAN_POINT('Ctrl Pts',(80.629972320317,297.862475660226,51.2985643825386));
#39651=CARTESIAN_POINT('Ctrl Pts',(80.6398778085108,297.667006141107,53.0246601447562));
#39652=CARTESIAN_POINT('Ctrl Pts',(80.6269504670759,300.332993858894,53.0280711906708));
#39653=CARTESIAN_POINT('Ctrl Pts',(80.6321628473983,300.267888185366,53.6055090465738));
#39654=CARTESIAN_POINT('Ctrl Pts',(80.28646611962,299.990626502287,56.0591348011215));
#39655=CARTESIAN_POINT('Ctrl Pts',(76.728933306676,299.501208809654,59.4689876632131));
#39656=CARTESIAN_POINT('Ctrl Pts',(70.5109339842768,298.864740780998,57.9701921918225));
#39657=CARTESIAN_POINT('Ctrl Pts',(68.40045667283,298.22827275234,51.9323292456896));
#39658=CARTESIAN_POINT('Ctrl Pts',(72.3521401674818,297.591804723684,46.8873582654032));
#39659=CARTESIAN_POINT('Ctrl Pts',(77.6521973570184,297.061414699802,47.3948662159206));
#39660=CARTESIAN_POINT('Ctrl Pts',(80.1698643867066,296.641811078207,50.2930805494598));
#39661=CARTESIAN_POINT('Ctrl Pts',(80.6388799598091,296.434363466162,52.1274893195652));
#39662=CARTESIAN_POINT('Ctrl Pts',(80.6388022101255,296.332993858894,53.0227366527281));
#39663=CARTESIAN_POINT('Origin',(74.9879498948689,423.667006141107,53.0228109606356));
#39664=CARTESIAN_POINT('',(80.6245874480474,305.667006141107,53.0180653057103));
#39665=CARTESIAN_POINT('',(80.6234016113781,304.332993858894,53.0188635924083));
#39666=CARTESIAN_POINT('',(80.6314498948689,423.667006141107,53.0228109606222));
#39667=CARTESIAN_POINT('Ctrl Pts',(80.6245874480474,305.667006141107,53.0180653057103));
#39668=CARTESIAN_POINT('Ctrl Pts',(80.615226689223,305.529525098635,54.238624327565));
#39669=CARTESIAN_POINT('Ctrl Pts',(79.9225057346746,305.285966051388,56.4096693070596));
#39670=CARTESIAN_POINT('Ctrl Pts',(77.3965832675933,304.936328999363,58.372506935359));
#39671=CARTESIAN_POINT('Ctrl Pts',(73.5810548415566,304.512016980259,59.0885032457832));
#39672=CARTESIAN_POINT('Ctrl Pts',(69.1117501822202,303.981626956378,56.1948055431484));
#39673=CARTESIAN_POINT('Ctrl Pts',(69.1475242377325,303.345158927721,49.7865097594955));
#39674=CARTESIAN_POINT('Ctrl Pts',(74.551368128498,302.708690899064,46.3647595285971));
#39675=CARTESIAN_POINT('Ctrl Pts',(79.6527817257398,302.149306636859,48.7261596244971));
#39676=CARTESIAN_POINT('Ctrl Pts',(80.6174782557889,301.802078384207,51.8268182855386));
#39677=CARTESIAN_POINT('Ctrl Pts',(80.6249680425302,301.667006141107,53.0279939180991));
#39678=CARTESIAN_POINT('Ctrl Pts',(80.6234016113781,304.332993858894,53.0188635924083));
#39679=CARTESIAN_POINT('Ctrl Pts',(80.6185287438372,304.207490909347,54.1357754126701));
#39680=CARTESIAN_POINT('Ctrl Pts',(79.7563688183985,303.869831950248,57.149097718398));
#39681=CARTESIAN_POINT('Ctrl Pts',(74.8519499260711,303.320016981596,59.6937746480561));
#39682=CARTESIAN_POINT('Ctrl Pts',(69.2993505210926,302.683548952939,56.5191024939194));
#39683=CARTESIAN_POINT('Ctrl Pts',(68.9747335748927,302.047080924282,50.1189338655102));
#39684=CARTESIAN_POINT('Ctrl Pts',(73.3090500016354,301.516690900401,47.0267062469374));
#39685=CARTESIAN_POINT('Ctrl Pts',(77.1529760290398,301.092378881297,47.569974672562));
#39686=CARTESIAN_POINT('Ctrl Pts',(79.8362973275973,300.733172535719,49.4675012984646));
#39687=CARTESIAN_POINT('Ctrl Pts',(80.6151775717754,300.480044194919,51.7238464412254));
#39688=CARTESIAN_POINT('Ctrl Pts',(80.6269504670759,300.332993858894,53.0280711906708));
#39689=CARTESIAN_POINT('Origin',(74.9879498948689,423.667006141107,53.0228109606356));
#39690=CARTESIAN_POINT('',(80.6384239058391,309.667006141107,53.0216495976625));
#39691=CARTESIAN_POINT('',(80.6380282624043,308.332993858894,53.019732459396));
#39692=CARTESIAN_POINT('',(80.6314498948689,423.667006141107,53.0228109606222));
#39693=CARTESIAN_POINT('Ctrl Pts',(80.6384239058391,309.667006141107,53.0216495976625));
#39694=CARTESIAN_POINT('Ctrl Pts',(80.6362110086977,309.575205827392,53.8327216460468));
#39695=CARTESIAN_POINT('Ctrl Pts',(80.233271064791,309.377327508901,55.5847876132963));
#39696=CARTESIAN_POINT('Ctrl Pts',(77.9031908065171,308.967293180857,58.5249330072815));
#39697=CARTESIAN_POINT('Ctrl Pts',(72.6313994367438,308.436903156976,59.2708460623881));
#39698=CARTESIAN_POINT('Ctrl Pts',(68.456311111176,307.80043512832,54.4091414120066));
#39699=CARTESIAN_POINT('Ctrl Pts',(70.2924624355432,307.163967099663,48.28227828701));
#39700=CARTESIAN_POINT('Ctrl Pts',(76.4365765807934,306.527499071006,46.5047055575397));
#39701=CARTESIAN_POINT('Ctrl Pts',(80.2166985631924,306.02851208482,49.8141896419487));
#39702=CARTESIAN_POINT('Ctrl Pts',(80.6296718898329,305.741681108187,52.3550996841352));
#39703=CARTESIAN_POINT('Ctrl Pts',(80.6245874480474,305.667006141107,53.0180653057103));
#39704=CARTESIAN_POINT('Ctrl Pts',(80.6380282624043,308.332993858894,53.019732459396));
#39705=CARTESIAN_POINT('Ctrl Pts',(80.6251916315742,308.147093633328,54.662633693795));
#39706=CARTESIAN_POINT('Ctrl Pts',(79.000792842538,307.749037398208,58.1998731366368));
#39707=CARTESIAN_POINT('Ctrl Pts',(72.985687726908,307.138825153538,59.39267465869));
#39708=CARTESIAN_POINT('Ctrl Pts',(68.5438343362777,306.50235712488,54.7734243851087));
#39709=CARTESIAN_POINT('Ctrl Pts',(69.7885723489147,305.971967101,49.5966688556199));
#39710=CARTESIAN_POINT('Ctrl Pts',(73.0469626822795,305.547655081895,47.4862659742077));
#39711=CARTESIAN_POINT('Ctrl Pts',(76.909836648915,305.123343062791,47.1001149618732));
#39712=CARTESIAN_POINT('Ctrl Pts',(80.1195933644604,304.718455988457,49.5935387681186));
#39713=CARTESIAN_POINT('Ctrl Pts',(80.626766065241,304.419646918899,52.2476958443102));
#39714=CARTESIAN_POINT('Ctrl Pts',(80.6234016113781,304.332993858894,53.0188635924083));
#39715=CARTESIAN_POINT('Origin',(74.9879498948689,423.667006141107,53.0228109606356));
#39716=CARTESIAN_POINT('',(80.6335754169153,313.667006141107,53.0264184895274));
#39717=CARTESIAN_POINT('',(80.634904065444,312.332993858894,53.0272790553122));
#39718=CARTESIAN_POINT('',(80.6314498948689,423.667006141107,53.0228109606222));
#39719=CARTESIAN_POINT('Ctrl Pts',(80.6335754169154,313.667006141107,53.0264184895274));
#39720=CARTESIAN_POINT('Ctrl Pts',(80.6362304506285,313.620886556148,53.4350520299685));
#39721=CARTESIAN_POINT('Ctrl Pts',(80.4021920393429,313.362610961638,55.7197413552384));
#39722=CARTESIAN_POINT('Ctrl Pts',(77.3057707044781,312.892179357576,59.2853168000712));
#39723=CARTESIAN_POINT('Ctrl Pts',(70.9656350492383,312.255711328918,58.3524639140331));
#39724=CARTESIAN_POINT('Ctrl Pts',(68.3343700832684,311.619243300261,52.5226827760076));
#39725=CARTESIAN_POINT('Ctrl Pts',(71.8075564021643,310.982775271605,47.1517535982347));
#39726=CARTESIAN_POINT('Ctrl Pts',(78.2159016640937,310.346307242947,47.1771630008298));
#39727=CARTESIAN_POINT('Ctrl Pts',(80.5733624654555,309.907717532782,50.8955937917629));
#39728=CARTESIAN_POINT('Ctrl Pts',(80.6387680774488,309.681283832168,52.8955036656214));
#39729=CARTESIAN_POINT('Ctrl Pts',(80.6384239058391,309.667006141107,53.0216495976625));
#39730=CARTESIAN_POINT('Ctrl Pts',(80.634904065444,312.332993858894,53.0272790553122));
#39731=CARTESIAN_POINT('Ctrl Pts',(80.6374670364689,312.29885236686,53.3292671667975));
#39732=CARTESIAN_POINT('Ctrl Pts',(80.4774639995193,312.052554865274,55.5050485344305));
#39733=CARTESIAN_POINT('Ctrl Pts',(77.6531438362427,311.594101354136,59.1449803944151));
#39734=CARTESIAN_POINT('Ctrl Pts',(71.2705853255733,310.95763332548,58.5701051977721));
#39735=CARTESIAN_POINT('Ctrl Pts',(68.8158168069635,310.427243301598,53.8454589621013));
#39736=CARTESIAN_POINT('Ctrl Pts',(69.8920431913756,310.002931282494,50.1154931906856));
#39737=CARTESIAN_POINT('Ctrl Pts',(72.5552930136327,309.578619263389,47.2909563665877));
#39738=CARTESIAN_POINT('Ctrl Pts',(77.8716307581055,309.048229239508,46.9998833192451));
#39739=CARTESIAN_POINT('Ctrl Pts',(80.521218131808,308.597661436418,50.6823624775674));
#39740=CARTESIAN_POINT('Ctrl Pts',(80.6398412553964,308.35924964288,52.7876958398109));
#39741=CARTESIAN_POINT('Ctrl Pts',(80.6380282624043,308.332993858894,53.019732459396));
#39742=CARTESIAN_POINT('Origin',(74.9879498948689,423.667006141107,53.0228109606356));
#39743=CARTESIAN_POINT('',(80.6203056371871,317.667006141107,53.0239157025499));
#39744=CARTESIAN_POINT('',(80.6314498948689,316.332993858894,53.022810960631));
#39745=CARTESIAN_POINT('',(80.6314498948689,423.667006141107,53.0228109606222));
#39746=CARTESIAN_POINT('Ctrl Pts',(80.6203056371871,317.667006141107,53.0239157025499));
#39747=CARTESIAN_POINT('Ctrl Pts',(80.6211875158354,317.560489280129,53.9712705130797));
#39748=CARTESIAN_POINT('Ctrl Pts',(79.9483727986063,317.241816409599,56.8042629861476));
#39749=CARTESIAN_POINT('Ctrl Pts',(75.4459142368694,316.710987529517,59.6842286762946));
#39750=CARTESIAN_POINT('Ctrl Pts',(69.6365665351741,316.07451950086,57.0081526834969));
#39751=CARTESIAN_POINT('Ctrl Pts',(68.7369456197939,315.438051472203,50.6756503623739));
#39752=CARTESIAN_POINT('Ctrl Pts',(73.5918912351737,314.801583443546,46.4927043065974));
#39753=CARTESIAN_POINT('Ctrl Pts',(78.6929398225512,314.271193419665,48.0183103636822));
#39754=CARTESIAN_POINT('Ctrl Pts',(80.4125372384092,313.893000985519,51.0209339978467));
#39755=CARTESIAN_POINT('Ctrl Pts',(80.6301237027218,313.726964560925,52.4951686660161));
#39756=CARTESIAN_POINT('Ctrl Pts',(80.6335754169154,313.667006141107,53.0264184895274));
#39757=CARTESIAN_POINT('Ctrl Pts',(80.622881869106,316.332993858894,53.0242648148771));
#39758=CARTESIAN_POINT('Ctrl Pts',(80.6254517968293,316.238455090841,53.8652024741767));
#39759=CARTESIAN_POINT('Ctrl Pts',(80.0544782228084,315.931760313236,56.5905993295512));
#39760=CARTESIAN_POINT('Ctrl Pts',(75.8188643388059,315.412909526078,59.6485829067018));
#39761=CARTESIAN_POINT('Ctrl Pts',(70.8674386639765,314.882519502197,57.6911472579929));
#39762=CARTESIAN_POINT('Ctrl Pts',(69.2341445588646,314.458207483093,54.1693212752611));
#39763=CARTESIAN_POINT('Ctrl Pts',(69.3927639357589,314.033895463987,50.2904364123513));
#39764=CARTESIAN_POINT('Ctrl Pts',(73.2157203846311,313.503505440107,46.5846066102391));
#39765=CARTESIAN_POINT('Ctrl Pts',(79.1179469702306,312.901178903483,47.9787113040824));
#39766=CARTESIAN_POINT('Ctrl Pts',(80.6215406761124,312.511008376413,51.4527061599728));
#39767=CARTESIAN_POINT('Ctrl Pts',(80.634904065444,312.332993858894,53.0272790553122));
#39768=CARTESIAN_POINT('Origin',(74.9879498948689,423.667006141107,53.0228109606356));
#39769=CARTESIAN_POINT('',(80.6329360039533,321.667006141107,53.0160580430196));
#39770=CARTESIAN_POINT('',(80.6314498948689,320.332993858894,53.0228109606313));
#39771=CARTESIAN_POINT('',(80.6314498948689,423.667006141107,53.0228109606222));
#39772=CARTESIAN_POINT('Ctrl Pts',(80.6329360039533,321.667006141107,53.0160580430195));
#39773=CARTESIAN_POINT('Ctrl Pts',(80.6191346339023,321.50009200411,54.4947146401021));
#39774=CARTESIAN_POINT('Ctrl Pts',(79.2652823955181,321.121021857561,57.8790253272329));
#39775=CARTESIAN_POINT('Ctrl Pts',(73.5609687392484,320.529795701458,59.5407843643785));
#39776=CARTESIAN_POINT('Ctrl Pts',(68.7293595293914,319.893327672802,55.3496680594258));
#39777=CARTESIAN_POINT('Ctrl Pts',(69.6519568295469,319.256859644144,49.0080319254632));
#39778=CARTESIAN_POINT('Ctrl Pts',(74.5036175039259,318.726469620264,46.8149611940725));
#39779=CARTESIAN_POINT('Ctrl Pts',(78.1692388187073,318.302157601159,48.0932914577593));
#39780=CARTESIAN_POINT('Ctrl Pts',(80.1726242007646,317.984362443032,50.2005331564451));
#39781=CARTESIAN_POINT('Ctrl Pts',(80.6194310253304,317.772645289682,52.0843672154471));
#39782=CARTESIAN_POINT('Ctrl Pts',(80.6203056371871,317.667006141107,53.0239157025499));
#39783=CARTESIAN_POINT('Ctrl Pts',(80.6314498948689,320.332993858894,53.0228109606313));
#39784=CARTESIAN_POINT('Ctrl Pts',(80.6314498948702,320.140209036291,54.7318077489503));
#39785=CARTESIAN_POINT('Ctrl Pts',(79.8060659192661,319.947424213689,56.4221521097307));
#39786=CARTESIAN_POINT('Ctrl Pts',(78.4584055093399,319.754639391087,57.4730952299814));
#39787=CARTESIAN_POINT('Ctrl Pts',(77.1107450994137,319.561854568484,58.5240383502321));
#39788=CARTESIAN_POINT('Ctrl Pts',(75.2702256751575,319.369069745882,58.9126397065625));
#39789=CARTESIAN_POINT('Ctrl Pts',(73.6127451626997,319.176284923279,58.4961923829941));
#39790=CARTESIAN_POINT('Ctrl Pts',(71.9552646502418,318.983500100677,58.0797450594257));
#39791=CARTESIAN_POINT('Ctrl Pts',(70.51700338107,318.790715278075,56.867339480914));
#39792=CARTESIAN_POINT('Ctrl Pts',(69.8261371496106,318.597930455472,55.3042099684571));
#39793=CARTESIAN_POINT('Ctrl Pts',(69.1352709181512,318.40514563287,53.7410804560001));
#39794=CARTESIAN_POINT('Ctrl Pts',(69.206880305491,318.212360810268,51.8613477992505));
#39795=CARTESIAN_POINT('Ctrl Pts',(70.0146680415461,318.019575987665,50.3553102844576));
#39796=CARTESIAN_POINT('Ctrl Pts',(70.8224557776012,317.826791165063,48.8492727696646));
#39797=CARTESIAN_POINT('Ctrl Pts',(72.3487890589435,317.63400634246,47.7498049531857));
#39798=CARTESIAN_POINT('Ctrl Pts',(74.033149215765,317.441221519858,47.4606667775725));
#39799=CARTESIAN_POINT('Ctrl Pts',(75.7175093725865,317.248436697255,47.1715286019592));
#39800=CARTESIAN_POINT('Ctrl Pts',(77.5231293307887,317.055651874653,47.6990315230392));
#39801=CARTESIAN_POINT('Ctrl Pts',(78.7869273705914,316.862867052051,48.8494595029995));
#39802=CARTESIAN_POINT('Ctrl Pts',(79.9447859852136,316.686242654332,49.9034514424928));
#39803=CARTESIAN_POINT('Ctrl Pts',(80.6314498948676,316.509618256613,51.4570729301893));
#39804=CARTESIAN_POINT('Ctrl Pts',(80.6314498948689,316.332993858894,53.022810960631));
#39805=CARTESIAN_POINT('Origin',(74.9879498948689,423.667006141107,53.0228109606356));
#39806=CARTESIAN_POINT('',(80.6399041832245,325.667006141107,53.0259007613615));
#39807=CARTESIAN_POINT('',(80.641309217006,324.332993858894,53.0246324837175));
#39808=CARTESIAN_POINT('',(80.6314498948689,423.667006141107,53.0228109606222));
#39809=CARTESIAN_POINT('Ctrl Pts',(80.6399041832245,325.667006141107,53.0259007613615));
#39810=CARTESIAN_POINT('Ctrl Pts',(80.6406482967255,325.651850737642,53.1597610770503));
#39811=CARTESIAN_POINT('Ctrl Pts',(80.5759040625624,325.424539324626,55.1666404955042));
#39812=CARTESIAN_POINT('Ctrl Pts',(78.1845991508713,324.985071902057,58.8795750880781));
#39813=CARTESIAN_POINT('Ctrl Pts',(71.7885153548133,324.3486038734,58.8835136441829));
#39814=CARTESIAN_POINT('Ctrl Pts',(68.3266868515903,323.712135844743,53.4906222074762));
#39815=CARTESIAN_POINT('Ctrl Pts',(70.5516205825161,323.181745820863,48.6534907822217));
#39816=CARTESIAN_POINT('Ctrl Pts',(74.1573917987538,322.757433801757,47.2149770274767));
#39817=CARTESIAN_POINT('Ctrl Pts',(78.0218245725355,322.333121782654,47.5852029360215));
#39818=CARTESIAN_POINT('Ctrl Pts',(80.4145538626956,321.969645895769,50.3398610757797));
#39819=CARTESIAN_POINT('Ctrl Pts',(80.6366768484148,321.712248013662,52.6152699820339));
#39820=CARTESIAN_POINT('Ctrl Pts',(80.6329360039533,321.667006141107,53.0160580430195));
#39821=CARTESIAN_POINT('Ctrl Pts',(80.641309217006,324.332993858894,53.0246324837175));
#39822=CARTESIAN_POINT('Ctrl Pts',(80.6413395611219,324.329816548354,53.0526541263013));
#39823=CARTESIAN_POINT('Ctrl Pts',(80.627934128378,324.114483228262,54.9516482048753));
#39824=CARTESIAN_POINT('Ctrl Pts',(79.0332371365105,323.793071903394,57.7564805437124));
#39825=CARTESIAN_POINT('Ctrl Pts',(75.3173868460731,323.36875988429,58.8804754304867));
#39826=CARTESIAN_POINT('Ctrl Pts',(71.4989396689043,322.944447865185,58.1802118789516));
#39827=CARTESIAN_POINT('Ctrl Pts',(68.3650037426683,322.414057841304,53.8759562937844));
#39828=CARTESIAN_POINT('Ctrl Pts',(70.6970252219288,321.777589812648,47.9069353980174));
#39829=CARTESIAN_POINT('Ctrl Pts',(76.9686349527099,321.14112178399,46.6512225235155));
#39830=CARTESIAN_POINT('Ctrl Pts',(80.3386907684742,320.659589799406,50.1238895100213));
#39831=CARTESIAN_POINT('Ctrl Pts',(80.6339788010566,320.390213824374,52.5096602373864));
#39832=CARTESIAN_POINT('Ctrl Pts',(80.6293902184787,320.332993858894,53.0175789310935));
#39833=CARTESIAN_POINT('Origin',(74.9879498948689,423.667006141107,53.0228109606356));
#39834=CARTESIAN_POINT('',(80.6249975362087,329.667006141107,53.0267352952636));
#39835=CARTESIAN_POINT('',(80.6248446978252,328.332993858894,53.0267008926206));
#39836=CARTESIAN_POINT('',(80.6314498948689,423.667006141107,53.0228109606222));
#39837=CARTESIAN_POINT('Ctrl Pts',(80.6249975362087,329.667006141107,53.0267352952636));
#39838=CARTESIAN_POINT('Ctrl Pts',(80.6290331419222,329.591453461623,53.6980665132406));
#39839=CARTESIAN_POINT('Ctrl Pts',(80.2059687603599,329.303744772587,56.2493246988747));
#39840=CARTESIAN_POINT('Ctrl Pts',(76.4154107889894,328.803880073999,59.5455843521308));
#39841=CARTESIAN_POINT('Ctrl Pts',(70.265470501402,328.167412045342,57.7439825390367));
#39842=CARTESIAN_POINT('Ctrl Pts',(68.7734481583349,327.637022021461,52.6330100425361));
#39843=CARTESIAN_POINT('Ctrl Pts',(70.5525225770171,327.212710002356,49.182531510618));
#39844=CARTESIAN_POINT('Ctrl Pts',(73.7129266627949,326.788397983251,46.9280351364722));
#39845=CARTESIAN_POINT('Ctrl Pts',(78.8341602790448,326.273163362835,47.6520772747905));
#39846=CARTESIAN_POINT('Ctrl Pts',(80.6302316719622,325.864006747195,51.2858901186813));
#39847=CARTESIAN_POINT('Ctrl Pts',(80.6399041832245,325.667006141107,53.0259007613615));
#39848=CARTESIAN_POINT('Ctrl Pts',(80.6248446978252,328.332993858894,53.0267008926206));
#39849=CARTESIAN_POINT('Ctrl Pts',(80.6292140414995,328.269419272335,53.5910781635921));
#39850=CARTESIAN_POINT('Ctrl Pts',(80.4218299720533,328.099766681,55.094490841645));
#39851=CARTESIAN_POINT('Ctrl Pts',(79.0777073227094,327.824036084888,57.2293113977682));
#39852=CARTESIAN_POINT('Ctrl Pts',(75.7356073875843,327.399724065784,59.2044761782546));
#39853=CARTESIAN_POINT('Ctrl Pts',(70.5470739238278,326.869334041903,58.0097833191163));
#39854=CARTESIAN_POINT('Ctrl Pts',(68.3936911683374,326.232866013246,51.97401681086));
#39855=CARTESIAN_POINT('Ctrl Pts',(72.3053343322745,325.596397984589,46.9134880641335));
#39856=CARTESIAN_POINT('Ctrl Pts',(78.6463794007935,324.963107266471,47.4553532968724));
#39857=CARTESIAN_POINT('Ctrl Pts',(80.6393134177985,324.541972557907,51.1815874497272));
#39858=CARTESIAN_POINT('Ctrl Pts',(80.641309217006,324.332993858894,53.0246324837175));
#39859=CARTESIAN_POINT('Origin',(74.9879498948689,423.667006141107,53.0228109606356));
#39860=CARTESIAN_POINT('',(80.6248818348672,333.667006141107,53.0189479369226));
#39861=CARTESIAN_POINT('',(80.6272015301536,332.332993858894,53.0209924349646));
#39862=CARTESIAN_POINT('',(80.6314498948689,423.667006141107,53.0228109606222));
#39863=CARTESIAN_POINT('Ctrl Pts',(80.6248818348672,333.667006141107,53.0189479369226));
#39864=CARTESIAN_POINT('Ctrl Pts',(80.6177572981036,333.531056185603,54.2270097895939));
#39865=CARTESIAN_POINT('Ctrl Pts',(79.6454537625307,333.182950220548,57.3314456583965));
#39866=CARTESIAN_POINT('Ctrl Pts',(74.5182936803783,332.622688245941,59.6839441776349));
#39867=CARTESIAN_POINT('Ctrl Pts',(70.0404139918865,332.09229822206,56.8035337854184));
#39868=CARTESIAN_POINT('Ctrl Pts',(69.1210358704998,331.667986202955,53.0318429502156));
#39869=CARTESIAN_POINT('Ctrl Pts',(70.0287967856483,331.24367418385,49.257339273258));
#39870=CARTESIAN_POINT('Ctrl Pts',(74.4977866088157,330.71328415997,46.3631553653794));
#39871=CARTESIAN_POINT('Ctrl Pts',(79.6381532999905,330.152368810796,48.7025815115751));
#39872=CARTESIAN_POINT('Ctrl Pts',(80.6177009428506,329.803609471175,51.8129321504717));
#39873=CARTESIAN_POINT('Ctrl Pts',(80.6249975362087,329.667006141107,53.0267352952636));
#39874=CARTESIAN_POINT('Ctrl Pts',(80.6272015301536,332.332993858894,53.0209924349646));
#39875=CARTESIAN_POINT('Ctrl Pts',(80.6267710083896,332.315100001092,53.1800532435297));
#39876=CARTESIAN_POINT('Ctrl Pts',(80.5787897955094,332.191128138513,54.282321197091));
#39877=CARTESIAN_POINT('Ctrl Pts',(79.605919036016,331.855000266382,57.199692285326));
#39878=CARTESIAN_POINT('Ctrl Pts',(74.9051964886825,331.324610242502,59.6999678831728));
#39879=CARTESIAN_POINT('Ctrl Pts',(69.3215782779007,330.688142213844,56.5550128262509));
#39880=CARTESIAN_POINT('Ctrl Pts',(68.9565293265754,330.051674185188,50.1693536823915));
#39881=CARTESIAN_POINT('Ctrl Pts',(74.1251200219098,329.415206156531,46.4016523058858));
#39882=CARTESIAN_POINT('Ctrl Pts',(79.5013040728498,328.842312714433,48.4920436759634));
#39883=CARTESIAN_POINT('Ctrl Pts',(80.6146330183506,328.481575281887,51.7076836159886));
#39884=CARTESIAN_POINT('Ctrl Pts',(80.6248446978252,328.332993858894,53.0267008926206));
#39885=CARTESIAN_POINT('Origin',(74.9879498948689,423.667006141107,53.0228109606356));
#39886=CARTESIAN_POINT('',(80.6397967405656,337.667006141107,53.0196325004034));
#39887=CARTESIAN_POINT('',(80.6340573567893,336.332993858894,53.0189717794449));
#39888=CARTESIAN_POINT('',(80.6314498948689,423.667006141107,53.0228109606222));
#39889=CARTESIAN_POINT('Ctrl Pts',(80.6397967405657,337.667006141107,53.0196325004034));
#39890=CARTESIAN_POINT('Ctrl Pts',(80.6298465402105,337.470658909584,54.7539666249281));
#39891=CARTESIAN_POINT('Ctrl Pts',(78.8441868361869,337.062155668509,58.3826150558032));
#39892=CARTESIAN_POINT('Ctrl Pts',(73.7316982178695,336.547574422658,59.1214836287799));
#39893=CARTESIAN_POINT('Ctrl Pts',(70.5643676301849,336.123262403554,56.8767286678197));
#39894=CARTESIAN_POINT('Ctrl Pts',(68.7746777925706,335.698950384449,53.4317441727057));
#39895=CARTESIAN_POINT('Ctrl Pts',(70.2509566334843,335.168560360568,48.3162020395523));
#39896=CARTESIAN_POINT('Ctrl Pts',(76.3953207281506,334.532092331911,46.4956734058825));
#39897=CARTESIAN_POINT('Ctrl Pts',(80.2009776432158,334.031574258758,49.7845397703628));
#39898=CARTESIAN_POINT('Ctrl Pts',(80.6288754576064,333.743212195156,52.3417750279739));
#39899=CARTESIAN_POINT('Ctrl Pts',(80.6248818348672,333.667006141107,53.0189479369226));
#39900=CARTESIAN_POINT('Ctrl Pts',(80.6340573567893,336.332993858894,53.0189717794449));
#39901=CARTESIAN_POINT('Ctrl Pts',(80.6200188883937,336.148624720296,54.649623440592));
#39902=CARTESIAN_POINT('Ctrl Pts',(79.0297907033757,335.752099572145,58.1744941480767));
#39903=CARTESIAN_POINT('Ctrl Pts',(73.0260170282693,335.143418414444,59.4052115080782));
#39904=CARTESIAN_POINT('Ctrl Pts',(68.5631518514559,334.506950385786,54.8234282469443));
#39905=CARTESIAN_POINT('Ctrl Pts',(69.9948378458387,333.87048235713,48.5896349674149));
#39906=CARTESIAN_POINT('Ctrl Pts',(76.0271136359725,333.234014328472,46.4264929411948));
#39907=CARTESIAN_POINT('Ctrl Pts',(80.0993015055047,332.721518162394,49.5705266949811));
#39908=CARTESIAN_POINT('Ctrl Pts',(80.6293232187766,332.421178005868,52.2371121853679));
#39909=CARTESIAN_POINT('Ctrl Pts',(80.6272015301536,332.332993858894,53.0209924349646));
#39910=CARTESIAN_POINT('Origin',(74.9879498948689,423.667006141107,53.0228109606356));
#39911=CARTESIAN_POINT('',(80.6331187968458,341.667006141107,53.029546473955));
#39912=CARTESIAN_POINT('',(80.636192681801,340.332993858894,53.0268230851199));
#39913=CARTESIAN_POINT('',(80.6314498948689,423.667006141107,53.0228109606222));
#39914=CARTESIAN_POINT('Ctrl Pts',(80.6331187968458,341.667006141107,53.029546473955));
#39915=CARTESIAN_POINT('Ctrl Pts',(80.6368032847626,341.622417643117,53.4245109340992));
#39916=CARTESIAN_POINT('Ctrl Pts',(80.4185029699366,341.365673135575,55.6940048042392));
#39917=CARTESIAN_POINT('Ctrl Pts',(78.0385523165719,341.002850623257,58.4510520619348));
#39918=CARTESIAN_POINT('Ctrl Pts',(74.1752777672687,340.578538604152,58.8331746118364));
#39919=CARTESIAN_POINT('Ctrl Pts',(70.5650945300378,340.154226585048,57.4057696657705));
#39920=CARTESIAN_POINT('Ctrl Pts',(68.3252780582827,339.623836561167,52.5755116286618));
#39921=CARTESIAN_POINT('Ctrl Pts',(71.7704857081252,338.98736853251,47.1719869564409));
#39922=CARTESIAN_POINT('Ctrl Pts',(78.1665513135014,338.350900503852,47.1562322701325));
#39923=CARTESIAN_POINT('Ctrl Pts',(80.5728490636616,337.910779706719,50.8672957569095));
#39924=CARTESIAN_POINT('Ctrl Pts',(80.6405978749007,337.682814919137,52.8799936422873));
#39925=CARTESIAN_POINT('Ctrl Pts',(80.6397967405657,337.667006141107,53.0196325004034));
#39926=CARTESIAN_POINT('Ctrl Pts',(80.636192681801,340.332993858894,53.0268230851199));
#39927=CARTESIAN_POINT('Ctrl Pts',(80.6388801598045,340.300383453829,53.3149409966799));
#39928=CARTESIAN_POINT('Ctrl Pts',(80.4886957225858,340.055617039212,55.4751882644889));
#39929=CARTESIAN_POINT('Ctrl Pts',(77.6918131141847,339.598694615041,59.1280006392838));
#39930=CARTESIAN_POINT('Ctrl Pts',(71.3179589210744,338.962226586385,58.5951909515068));
#39931=CARTESIAN_POINT('Ctrl Pts',(68.3112066114293,338.325758557728,52.9498969833543));
#39932=CARTESIAN_POINT('Ctrl Pts',(71.4471267602236,337.689290529071,47.3611995095039));
#39933=CARTESIAN_POINT('Ctrl Pts',(76.762576521389,337.158900505191,47.0543373764116));
#39934=CARTESIAN_POINT('Ctrl Pts',(79.7257358927106,336.734588486085,49.5624431211091));
#39935=CARTESIAN_POINT('Ctrl Pts',(80.5669914044514,336.494645605579,51.5901499444678));
#39936=CARTESIAN_POINT('Ctrl Pts',(80.6361731399006,336.360780729848,52.773210977911));
#39937=CARTESIAN_POINT('Ctrl Pts',(80.6340573567893,336.332993858894,53.0189717794449));
#39938=CARTESIAN_POINT('Origin',(74.9879498948689,423.667006141107,53.0228109606356));
#39939=CARTESIAN_POINT('',(80.6202872556143,345.667006141106,53.0217977506596));
#39940=CARTESIAN_POINT('',(80.6311256770026,344.332993858894,53.022857263151));
#39941=CARTESIAN_POINT('',(80.6314498948689,423.667006141107,53.0228109606222));
#39942=CARTESIAN_POINT('Ctrl Pts',(80.6202875021214,345.667006141106,53.0217977730345));
#39943=CARTESIAN_POINT('Ctrl Pts',(80.6195633400336,345.562020367097,53.9555423965643));
#39944=CARTESIAN_POINT('Ctrl Pts',(80.1771837543004,345.350956588312,55.833457101896));
#39945=CARTESIAN_POINT('Ctrl Pts',(78.1844014847269,345.033814804751,57.942512067397));
#39946=CARTESIAN_POINT('Ctrl Pts',(74.5227334601851,344.609502785646,59.2321225374558));
#39947=CARTESIAN_POINT('Ctrl Pts',(69.664343426917,344.079112761766,57.0540002229753));
#39948=CARTESIAN_POINT('Ctrl Pts',(68.7222249177504,343.442644733109,50.7152347794114));
#39949=CARTESIAN_POINT('Ctrl Pts',(73.540906987327,342.806176704451,46.5092620559193));
#39950=CARTESIAN_POINT('Ctrl Pts',(79.2566196418042,342.214297173785,48.1552669397766));
#39951=CARTESIAN_POINT('Ctrl Pts',(80.6192721660009,341.834573652669,51.5452351666445));
#39952=CARTESIAN_POINT('Ctrl Pts',(80.6331187968458,341.667006141107,53.029546473955));
#39953=CARTESIAN_POINT('Ctrl Pts',(80.6225970303475,344.332993858894,53.0240752641163));
#39954=CARTESIAN_POINT('Ctrl Pts',(80.625144122426,344.239986177809,53.8521759519026));
#39955=CARTESIAN_POINT('Ctrl Pts',(80.0664343193197,343.934822487172,56.5663239398779));
#39956=CARTESIAN_POINT('Ctrl Pts',(75.8710807057947,343.417502786984,59.6364584021908));
#39957=CARTESIAN_POINT('Ctrl Pts',(69.8992144031925,342.781034758326,57.3458872283867));
#39958=CARTESIAN_POINT('Ctrl Pts',(68.6021616848208,342.14456672967,51.0701252125357));
#39959=CARTESIAN_POINT('Ctrl Pts',(72.4140943662755,341.614176705789,47.3529569671835));
#39960=CARTESIAN_POINT('Ctrl Pts',(76.2959066074933,341.189864686684,47.3035443132344));
#39961=CARTESIAN_POINT('Ctrl Pts',(79.5033506359083,340.798163072644,48.9021958940077));
#39962=CARTESIAN_POINT('Ctrl Pts',(80.6213960283487,340.512539463381,51.440510235231));
#39963=CARTESIAN_POINT('Ctrl Pts',(80.636192681801,340.332993858894,53.0268230851199));
#39964=CARTESIAN_POINT('Origin',(74.9879498948689,423.667006141107,53.0228109606356));
#39965=CARTESIAN_POINT('',(80.633451427705,349.667006141107,53.0191888592032));
#39966=CARTESIAN_POINT('',(80.6314498948689,348.332993858894,53.0228109606318));
#39967=CARTESIAN_POINT('',(80.6314498948689,423.667006141107,53.0228109606222));
#39968=CARTESIAN_POINT('Ctrl Pts',(80.633451427705,349.667006141107,53.0191888592032));
#39969=CARTESIAN_POINT('Ctrl Pts',(80.6300364855632,349.607701095854,53.5446842132234));
#39970=CARTESIAN_POINT('Ctrl Pts',(80.415720372531,349.442318045826,55.0131729290342));
#39971=CARTESIAN_POINT('Ctrl Pts',(78.7083308692968,349.064778986245,58.0158803567333));
#39972=CARTESIAN_POINT('Ctrl Pts',(73.6120037259175,348.534388962364,59.557185057255));
#39973=CARTESIAN_POINT('Ctrl Pts',(68.7442020401091,347.897920933707,55.3892069645249));
#39974=CARTESIAN_POINT('Ctrl Pts',(69.6243212317588,347.26145290505,49.0539647712928));
#39975=CARTESIAN_POINT('Ctrl Pts',(75.4254018924481,346.624984876393,46.3600147705323));
#39976=CARTESIAN_POINT('Ctrl Pts',(79.9422591554384,346.093502621745,49.2296317104394));
#39977=CARTESIAN_POINT('Ctrl Pts',(80.6210267320052,345.77417637665,52.0686245247025));
#39978=CARTESIAN_POINT('Ctrl Pts',(80.6202875021214,345.667006141106,53.0217977730345));
#39979=CARTESIAN_POINT('Ctrl Pts',(80.6314498948689,348.332993858894,53.0228109606315));
#39980=CARTESIAN_POINT('Ctrl Pts',(80.6314498948701,348.140209036291,54.7318077489505));
#39981=CARTESIAN_POINT('Ctrl Pts',(79.806065919266,347.947424213689,56.4221521097309));
#39982=CARTESIAN_POINT('Ctrl Pts',(78.4584055093397,347.754639391087,57.4730952299815));
#39983=CARTESIAN_POINT('Ctrl Pts',(77.1107450994134,347.561854568484,58.5240383502321));
#39984=CARTESIAN_POINT('Ctrl Pts',(75.2702256751573,347.369069745882,58.9126397065625));
#39985=CARTESIAN_POINT('Ctrl Pts',(73.6127451626995,347.176284923279,58.496192382994));
#39986=CARTESIAN_POINT('Ctrl Pts',(71.9552646502417,346.983500100677,58.0797450594256));
#39987=CARTESIAN_POINT('Ctrl Pts',(70.5170033810699,346.790715278075,56.8673394809138));
#39988=CARTESIAN_POINT('Ctrl Pts',(69.8261371496105,346.597930455472,55.3042099684569));
#39989=CARTESIAN_POINT('Ctrl Pts',(69.1352709181512,346.40514563287,53.7410804559999));
#39990=CARTESIAN_POINT('Ctrl Pts',(69.206880305491,346.212360810267,51.8613477992503));
#39991=CARTESIAN_POINT('Ctrl Pts',(70.0146680415462,346.019575987665,50.3553102844574));
#39992=CARTESIAN_POINT('Ctrl Pts',(70.8224557776013,345.826791165063,48.8492727696645));
#39993=CARTESIAN_POINT('Ctrl Pts',(72.3487890589437,345.63400634246,47.7498049531856));
#39994=CARTESIAN_POINT('Ctrl Pts',(74.0331492157652,345.441221519858,47.4606667775724));
#39995=CARTESIAN_POINT('Ctrl Pts',(75.7175093725867,345.248436697255,47.1715286019592));
#39996=CARTESIAN_POINT('Ctrl Pts',(77.5231293307889,345.055651874653,47.6990315230393));
#39997=CARTESIAN_POINT('Ctrl Pts',(78.7869273705916,344.862867052051,48.8494595029997));
#39998=CARTESIAN_POINT('Ctrl Pts',(79.9447859852139,344.686242654332,49.9034514424931));
#39999=CARTESIAN_POINT('Ctrl Pts',(80.6314498948679,344.509618256613,51.4570729301901));
#40000=CARTESIAN_POINT('Ctrl Pts',(80.6314498948689,344.332993858894,53.022810960632));
#40001=CARTESIAN_POINT('Origin',(74.9879498948689,423.667006141107,53.0228109606356));
#40002=CARTESIAN_POINT('',(80.6384731862346,353.667006141107,53.0238923963884));
#40003=CARTESIAN_POINT('',(80.6400049607223,352.332993858894,53.0230790512102));
#40004=CARTESIAN_POINT('',(80.6314498948689,423.667006141107,53.0228109606222));
#40005=CARTESIAN_POINT('Ctrl Pts',(80.6384731862346,353.667006141107,53.0238923963884));
#40006=CARTESIAN_POINT('Ctrl Pts',(80.6387817559317,353.653381824611,53.1442610157386));
#40007=CARTESIAN_POINT('Ctrl Pts',(80.5763907092171,353.427601498563,55.1383710357438));
#40008=CARTESIAN_POINT('Ctrl Pts',(78.2338848228655,352.989665162963,58.858492509318));
#40009=CARTESIAN_POINT('Ctrl Pts',(71.8256481706415,352.353197134305,58.9036327676611));
#40010=CARTESIAN_POINT('Ctrl Pts',(68.3359414908884,351.716729105649,53.5434228158304));
#40011=CARTESIAN_POINT('Ctrl Pts',(70.9492443786796,351.080261076991,47.7055677769413));
#40012=CARTESIAN_POINT('Ctrl Pts',(77.2864777741945,350.443793048335,46.7531983504033));
#40013=CARTESIAN_POINT('Ctrl Pts',(80.3981784562209,349.972708069706,50.314162070502));
#40014=CARTESIAN_POINT('Ctrl Pts',(80.6361447390397,349.71377910063,52.604738911161));
#40015=CARTESIAN_POINT('Ctrl Pts',(80.633451427705,349.667006141107,53.0191888592032));
#40016=CARTESIAN_POINT('Ctrl Pts',(80.6400049607223,352.332993858894,53.0230790512102));
#40017=CARTESIAN_POINT('Ctrl Pts',(80.6400149165888,352.331347635322,53.0376053373019));
#40018=CARTESIAN_POINT('Ctrl Pts',(80.6333577017943,352.117545402199,54.9241879694794));
#40019=CARTESIAN_POINT('Ctrl Pts',(78.5557872721241,351.691587159524,58.6668125349179));
#40020=CARTESIAN_POINT('Ctrl Pts',(72.1602274420798,351.055119130866,59.0722124537102));
#40021=CARTESIAN_POINT('Ctrl Pts',(69.0135210149437,350.524729106987,54.7772841430609));
#40022=CARTESIAN_POINT('Ctrl Pts',(69.5082125339175,350.100417087881,50.9268051874641));
#40023=CARTESIAN_POINT('Ctrl Pts',(71.7094642650518,349.676105068777,47.7290874540463));
#40024=CARTESIAN_POINT('Ctrl Pts',(76.9191944454673,349.145715044897,46.6305056503264));
#40025=CARTESIAN_POINT('Ctrl Pts',(80.3288397250378,348.662651973343,50.0990734332697));
#40026=CARTESIAN_POINT('Ctrl Pts',(80.634222125101,348.391744911342,52.4971262155878));
#40027=CARTESIAN_POINT('Ctrl Pts',(80.6295592093353,348.332993858894,53.0182528091584));
#40028=CARTESIAN_POINT('Origin',(74.9879498948689,423.667006141107,53.0228109606356));
#40029=CARTESIAN_POINT('',(80.6247365158406,357.667006141107,53.0276029024325));
#40030=CARTESIAN_POINT('',(80.6314498948689,356.332993858894,53.0228109606318));
#40031=CARTESIAN_POINT('',(80.6314498948689,423.667006141107,53.0228109606222));
#40032=CARTESIAN_POINT('Ctrl Pts',(80.6247365158406,357.667006141107,53.0276029024325));
#40033=CARTESIAN_POINT('Ctrl Pts',(80.6298460758694,357.592984548592,53.6847268621822));
#40034=CARTESIAN_POINT('Ctrl Pts',(80.221616630998,357.306806946524,56.2196666780232));
#40035=CARTESIAN_POINT('Ctrl Pts',(76.4566386365349,356.808473334904,59.5364252185682));
#40036=CARTESIAN_POINT('Ctrl Pts',(70.3070805562703,356.172005306247,57.777778336482));
#40037=CARTESIAN_POINT('Ctrl Pts',(68.4520736285264,355.53553727759,51.6565976712477));
#40038=CARTESIAN_POINT('Ctrl Pts',(72.6121732175607,354.899069248933,46.7820611760358));
#40039=CARTESIAN_POINT('Ctrl Pts',(77.886236228337,354.368679225053,47.5117391122231));
#40040=CARTESIAN_POINT('Ctrl Pts',(80.2290853076505,353.957991522444,50.4493699279292));
#40041=CARTESIAN_POINT('Ctrl Pts',(80.6363792531857,353.759459829387,52.2070791040902));
#40042=CARTESIAN_POINT('Ctrl Pts',(80.6384731862346,353.667006141107,53.0238923963884));
#40043=CARTESIAN_POINT('Ctrl Pts',(80.6287180057221,356.332993858894,53.0272649993926));
#40044=CARTESIAN_POINT('Ctrl Pts',(80.6334767749213,356.270950359303,53.5777950154488));
#40045=CARTESIAN_POINT('Ctrl Pts',(80.3064394217103,355.99675085016,56.0057811601085));
#40046=CARTESIAN_POINT('Ctrl Pts',(76.8197874993998,355.510395331466,59.4443095151045));
#40047=CARTESIAN_POINT('Ctrl Pts',(71.6277284938853,354.980005307585,58.2650326962652));
#40048=CARTESIAN_POINT('Ctrl Pts',(69.4763532374749,354.55569328848,55.0335481469374));
#40049=CARTESIAN_POINT('Ctrl Pts',(69.0414601665085,354.131381269376,51.175857658671));
#40050=CARTESIAN_POINT('Ctrl Pts',(72.2544222487035,353.600991245494,46.9302663935378));
#40051=CARTESIAN_POINT('Ctrl Pts',(78.6263988188862,352.966169440409,47.4335374279615));
#40052=CARTESIAN_POINT('Ctrl Pts',(80.6387318606642,352.543503644875,51.1655395103507));
#40053=CARTESIAN_POINT('Ctrl Pts',(80.6400049607223,352.332993858894,53.0230790512102));
#40054=CARTESIAN_POINT('Origin',(74.9879498948689,423.667006141107,53.0228109606356));
#40055=CARTESIAN_POINT('',(80.6248445340874,361.667006141107,53.0177036455054));
#40056=CARTESIAN_POINT('',(80.6314498948689,360.332993858894,53.0228109606317));
#40057=CARTESIAN_POINT('',(80.6314498948689,423.667006141107,53.0228109606222));
#40058=CARTESIAN_POINT('Ctrl Pts',(80.6248445340874,361.667006141107,53.0177036455054));
#40059=CARTESIAN_POINT('Ctrl Pts',(80.6175315928956,361.532587272572,54.2131392197305));
#40060=CARTESIAN_POINT('Ctrl Pts',(79.6600387342728,361.186012394485,57.3078556520816));
#40061=CARTESIAN_POINT('Ctrl Pts',(74.5718700069468,360.627281506846,59.6821750471879));
#40062=CARTESIAN_POINT('Ctrl Pts',(69.1575163315875,359.990813478189,56.2770792017615));
#40063=CARTESIAN_POINT('Ctrl Pts',(69.1020116217968,359.354345449532,49.8689239398295));
#40064=CARTESIAN_POINT('Ctrl Pts',(73.5623855454864,358.823955425652,46.9614791866025));
#40065=CARTESIAN_POINT('Ctrl Pts',(77.3801004030129,358.399643406547,47.665724281053));
#40066=CARTESIAN_POINT('Ctrl Pts',(79.9167858955864,358.049352979957,49.6244288636624));
#40067=CARTESIAN_POINT('Ctrl Pts',(80.615201377891,357.805140558144,51.801319705639));
#40068=CARTESIAN_POINT('Ctrl Pts',(80.6247365158406,357.667006141107,53.0276029024325));
#40069=CARTESIAN_POINT('Ctrl Pts',(80.6314498948689,360.332993858894,53.0228109606319));
#40070=CARTESIAN_POINT('Ctrl Pts',(80.63144989487,360.140209036291,54.7318077489509));
#40071=CARTESIAN_POINT('Ctrl Pts',(79.8060659192657,359.947424213689,56.4221521097313));
#40072=CARTESIAN_POINT('Ctrl Pts',(78.4584055093394,359.754639391086,57.4730952299818));
#40073=CARTESIAN_POINT('Ctrl Pts',(77.110745099413,359.561854568484,58.5240383502323));
#40074=CARTESIAN_POINT('Ctrl Pts',(75.2702256751568,359.369069745882,58.9126397065626));
#40075=CARTESIAN_POINT('Ctrl Pts',(73.612745162699,359.176284923279,58.4961923829939));
#40076=CARTESIAN_POINT('Ctrl Pts',(71.9552646502412,358.983500100677,58.0797450594253));
#40077=CARTESIAN_POINT('Ctrl Pts',(70.5170033810695,358.790715278075,56.8673394809134));
#40078=CARTESIAN_POINT('Ctrl Pts',(69.8261371496103,358.597930455472,55.3042099684563));
#40079=CARTESIAN_POINT('Ctrl Pts',(69.1352709181511,358.40514563287,53.7410804559993));
#40080=CARTESIAN_POINT('Ctrl Pts',(69.2068803054912,358.212360810267,51.8613477992496));
#40081=CARTESIAN_POINT('Ctrl Pts',(70.0146680415465,358.019575987665,50.3553102844568));
#40082=CARTESIAN_POINT('Ctrl Pts',(70.8224557776019,357.826791165063,48.849272769664));
#40083=CARTESIAN_POINT('Ctrl Pts',(72.3487890589444,357.63400634246,47.7498049531853));
#40084=CARTESIAN_POINT('Ctrl Pts',(74.033149215766,357.441221519858,47.4606667775723));
#40085=CARTESIAN_POINT('Ctrl Pts',(75.7175093725876,357.248436697255,47.1715286019593));
#40086=CARTESIAN_POINT('Ctrl Pts',(77.5231293307897,357.055651874653,47.6990315230396));
#40087=CARTESIAN_POINT('Ctrl Pts',(78.7869273705922,356.862867052051,48.8494595030002));
#40088=CARTESIAN_POINT('Ctrl Pts',(79.9447859852141,356.686242654332,49.9034514424936));
#40089=CARTESIAN_POINT('Ctrl Pts',(80.6314498948678,356.509618256613,51.4570729301902));
#40090=CARTESIAN_POINT('Ctrl Pts',(80.6314498948689,356.332993858894,53.0228109606318));
#40091=CARTESIAN_POINT('Origin',(74.9879498948689,423.667006141107,53.0228109606356));
#40092=CARTESIAN_POINT('',(80.6397711584222,365.667006141107,53.0208691915594));
#40093=CARTESIAN_POINT('',(80.6370474885153,364.332993858893,53.0191872378647));
#40094=CARTESIAN_POINT('',(80.6314498948689,423.667006141107,53.0228109606222));
#40095=CARTESIAN_POINT('Ctrl Pts',(80.6397711584222,365.667006141107,53.0208691915594));
#40096=CARTESIAN_POINT('Ctrl Pts',(80.6296050747201,365.472189996553,54.7412732581942));
#40097=CARTESIAN_POINT('Ctrl Pts',(78.8683419814859,365.065217842446,58.3501341198079));
#40098=CARTESIAN_POINT('Ctrl Pts',(72.7199018846829,364.446089678788,59.302952324055));
#40099=CARTESIAN_POINT('Ctrl Pts',(68.4759904733059,363.809621650131,54.5012077904277));
#40100=CARTESIAN_POINT('Ctrl Pts',(69.9370688277395,363.279231626249,49.3813034383522));
#40101=CARTESIAN_POINT('Ctrl Pts',(73.2812266717887,362.854919607146,47.4096249147279));
#40102=CARTESIAN_POINT('Ctrl Pts',(77.1569110752008,362.43060758804,47.1860666637397));
#40103=CARTESIAN_POINT('Ctrl Pts',(80.19079143513,362.034636432695,49.7542817042191));
#40104=CARTESIAN_POINT('Ctrl Pts',(80.6290737553782,361.744743282125,52.3263591577539));
#40105=CARTESIAN_POINT('Ctrl Pts',(80.6248445340874,361.667006141107,53.0177036455054));
#40106=CARTESIAN_POINT('Ctrl Pts',(80.6370474885153,364.332993858894,53.0191872378647));
#40107=CARTESIAN_POINT('Ctrl Pts',(80.6226904770127,364.150155807264,54.6340249277856));
#40108=CARTESIAN_POINT('Ctrl Pts',(79.4660425813718,363.86123975086,57.1999674524242));
#40109=CARTESIAN_POINT('Ctrl Pts',(76.2070166523586,363.466245689677,58.7616817543507));
#40110=CARTESIAN_POINT('Ctrl Pts',(72.3264382459639,363.041933670573,58.6520500150618));
#40111=CARTESIAN_POINT('Ctrl Pts',(68.572635003179,362.511543646692,54.8761882926657));
#40112=CARTESIAN_POINT('Ctrl Pts',(69.9668979799986,361.875075618035,48.6213049695892));
#40113=CARTESIAN_POINT('Ctrl Pts',(75.9735829643599,361.238607589378,46.4236610182017));
#40114=CARTESIAN_POINT('Ctrl Pts',(80.094404819463,360.724580336331,49.5385639086073));
#40115=CARTESIAN_POINT('Ctrl Pts',(80.6259624255451,360.422709092836,52.2223601240696));
#40116=CARTESIAN_POINT('Ctrl Pts',(80.622923341824,360.332993858894,53.0210345647259));
#40117=CARTESIAN_POINT('Origin',(74.9879498948689,423.667006141107,53.0228109606356));
#40118=CARTESIAN_POINT('',(80.6326307703874,369.667006141107,53.0277774696284));
#40119=CARTESIAN_POINT('',(80.6332290564755,368.332993858894,53.0268706649991));
#40120=CARTESIAN_POINT('',(80.6314498948689,423.667006141107,53.0228109606222));
#40121=CARTESIAN_POINT('Ctrl Pts',(80.6326307703874,369.667006141107,53.0277774696284));
#40122=CARTESIAN_POINT('Ctrl Pts',(80.6360347096095,369.623948730086,53.409029713798));
#40123=CARTESIAN_POINT('Ctrl Pts',(80.4262099310797,369.368735309512,55.6650143801684));
#40124=CARTESIAN_POINT('Ctrl Pts',(77.3936427899844,368.901365879386,59.2515234291501));
#40125=CARTESIAN_POINT('Ctrl Pts',(71.0408633993679,368.26489785073,58.4090694850156));
#40126=CARTESIAN_POINT('Ctrl Pts',(68.7867101717712,367.734507826848,53.5854853654303));
#40127=CARTESIAN_POINT('Ctrl Pts',(70.0186562199422,367.310195807744,49.904015982041));
#40128=CARTESIAN_POINT('Ctrl Pts',(72.7981944809444,366.885883788639,47.1938361094012));
#40129=CARTESIAN_POINT('Ctrl Pts',(78.1220664110398,366.355493764758,47.126321635835));
#40130=CARTESIAN_POINT('Ctrl Pts',(80.565317102736,365.913841880656,50.8418338582383));
#40131=CARTESIAN_POINT('Ctrl Pts',(80.6406760039593,365.684346006105,52.8677423840958));
#40132=CARTESIAN_POINT('Ctrl Pts',(80.6397711584222,365.667006141107,53.0208691915594));
#40133=CARTESIAN_POINT('Ctrl Pts',(80.6332290564755,368.332993858894,53.0268706649991));
#40134=CARTESIAN_POINT('Ctrl Pts',(80.6356848743043,368.301914540797,53.3018404448554));
#40135=CARTESIAN_POINT('Ctrl Pts',(80.5560664743386,368.164757217925,54.5142151899356));
#40136=CARTESIAN_POINT('Ctrl Pts',(79.6714791919269,367.921521890276,56.5562674935186));
#40137=CARTESIAN_POINT('Ctrl Pts',(76.6697640348178,367.497209871172,59.0180989260132));
#40138=CARTESIAN_POINT('Ctrl Pts',(71.359714904182,366.96681984729,58.6288062823227));
#40139=CARTESIAN_POINT('Ctrl Pts',(68.3108789861652,366.330351818634,52.9921286989546));
#40140=CARTESIAN_POINT('Ctrl Pts',(71.4048542721186,365.693883789976,47.3941629641248));
#40141=CARTESIAN_POINT('Ctrl Pts',(77.7862076759328,365.05741576132,46.9603056442045));
#40142=CARTESIAN_POINT('Ctrl Pts',(80.506338760825,364.603785784292,50.6294404889205));
#40143=CARTESIAN_POINT('Ctrl Pts',(80.6393496255999,364.362311816816,52.7602491064219));
#40144=CARTESIAN_POINT('Ctrl Pts',(80.6370474885153,364.332993858894,53.0191872378647));
#40145=CARTESIAN_POINT('Origin',(74.9879498948689,423.667006141107,53.0228109606356));
#40146=CARTESIAN_POINT('',(80.6223565140898,373.667006141107,53.0230511363488));
#40147=CARTESIAN_POINT('',(80.6269596911125,372.332993858894,53.0243158257365));
#40148=CARTESIAN_POINT('',(80.6314498948689,423.667006141107,53.0228109606222));
#40149=CARTESIAN_POINT('Ctrl Pts',(80.6223565140898,373.667006141107,53.0230511363488));
#40150=CARTESIAN_POINT('Ctrl Pts',(80.623318383652,373.563551454066,53.9434812983077));
#40151=CARTESIAN_POINT('Ctrl Pts',(79.9750770611082,373.247940757473,56.7508149175562));
#40152=CARTESIAN_POINT('Ctrl Pts',(75.5398292911409,372.720174051328,59.677636414875));
#40153=CARTESIAN_POINT('Ctrl Pts',(70.6749913177946,372.189784027447,57.5139538999746));
#40154=CARTESIAN_POINT('Ctrl Pts',(69.1910655822406,371.765472008342,53.9266328524801));
#40155=CARTESIAN_POINT('Ctrl Pts',(69.5124694584528,371.341159989238,50.0578336285873));
#40156=CARTESIAN_POINT('Ctrl Pts',(73.4877077677736,370.810769965357,46.5158495918775));
#40157=CARTESIAN_POINT('Ctrl Pts',(79.2397454683978,370.217359347721,48.1323470424996));
#40158=CARTESIAN_POINT('Ctrl Pts',(80.6192625408933,369.836104739638,51.5304923647657));
#40159=CARTESIAN_POINT('Ctrl Pts',(80.6326307703874,369.667006141107,53.0277774696284));
#40160=CARTESIAN_POINT('Ctrl Pts',(80.6269596911125,372.332993858894,53.0243158257365));
#40161=CARTESIAN_POINT('Ctrl Pts',(80.6287591076907,372.241517264778,53.837559733299));
#40162=CARTESIAN_POINT('Ctrl Pts',(80.071596577785,371.93788466111,56.5341906247379));
#40163=CARTESIAN_POINT('Ctrl Pts',(75.9246488708189,371.422096047889,59.6344573307068));
#40164=CARTESIAN_POINT('Ctrl Pts',(69.926659556592,370.785628019232,57.377986896543));
#40165=CARTESIAN_POINT('Ctrl Pts',(68.5918611198335,370.149159990575,51.1227317801111));
#40166=CARTESIAN_POINT('Ctrl Pts',(73.125273998855,369.512691961918,46.610739857829));
#40167=CARTESIAN_POINT('Ctrl Pts',(79.0768627736854,368.907303251357,47.9272954751586));
#40168=CARTESIAN_POINT('Ctrl Pts',(80.6189207834984,368.51407055035,51.4248207798587));
#40169=CARTESIAN_POINT('Ctrl Pts',(80.6332290564755,368.332993858894,53.0268706649991));
#40170=CARTESIAN_POINT('Origin',(74.9879498948689,423.667006141107,53.0228109606356));
#40171=CARTESIAN_POINT('',(80.6318252954934,377.667006141106,53.0173586745867));
#40172=CARTESIAN_POINT('',(80.625604522174,376.332993858894,53.0187133256936));
#40173=CARTESIAN_POINT('',(80.6314498948689,423.667006141107,53.0228109606222));
#40174=CARTESIAN_POINT('Ctrl Pts',(80.6318252954934,377.667006141107,53.0173586745867));
#40175=CARTESIAN_POINT('Ctrl Pts',(80.6180275057674,377.503154178046,54.4701804610813));
#40176=CARTESIAN_POINT('Ctrl Pts',(79.3046541470043,377.127146205434,57.8270528744592));
#40177=CARTESIAN_POINT('Ctrl Pts',(74.676644657417,376.645060228046,59.2417389742301));
#40178=CARTESIAN_POINT('Ctrl Pts',(71.2039784868037,376.220748208941,57.5063722827453));
#40179=CARTESIAN_POINT('Ctrl Pts',(68.9097584028537,375.796436189837,54.3746855019773));
#40180=CARTESIAN_POINT('Ctrl Pts',(69.5884755901131,375.266046165955,49.0938225505349));
#40181=CARTESIAN_POINT('Ctrl Pts',(75.3832511001032,374.629578137299,46.3573811711787));
#40182=CARTESIAN_POINT('Ctrl Pts',(79.9227890716234,374.096564795682,49.2006142598981));
#40183=CARTESIAN_POINT('Ctrl Pts',(80.6213458639541,373.775707463618,52.0559419724561));
#40184=CARTESIAN_POINT('Ctrl Pts',(80.6223565140898,373.667006141107,53.0230511363488));
#40185=CARTESIAN_POINT('Ctrl Pts',(80.625604522174,376.332993858894,53.0187133256936));
#40186=CARTESIAN_POINT('Ctrl Pts',(80.6145961714162,376.181119988758,54.3665391394491));
#40187=CARTESIAN_POINT('Ctrl Pts',(79.4615473568344,375.817090109071,57.6115233426936));
#40188=CARTESIAN_POINT('Ctrl Pts',(74.0224987859417,375.240904219831,59.6297861745523));
#40189=CARTESIAN_POINT('Ctrl Pts',(68.9129848210706,374.604436191174,55.7823493029185));
#40190=CARTESIAN_POINT('Ctrl Pts',(69.3770612241408,373.967968162517,49.4031223489269));
#40191=CARTESIAN_POINT('Ctrl Pts',(75.0088003293896,373.331500133859,46.3451738071356));
#40192=CARTESIAN_POINT('Ctrl Pts',(79.6701661503711,372.80111010998,48.9180786276028));
#40193=CARTESIAN_POINT('Ctrl Pts',(80.5885727818433,372.46827468499,51.8214716448624));
#40194=CARTESIAN_POINT('Ctrl Pts',(80.6266724698768,372.347595269554,52.8945065736976));
#40195=CARTESIAN_POINT('Ctrl Pts',(80.6269596911125,372.332993858894,53.0243158257365));
#40196=CARTESIAN_POINT('Origin',(74.9879498948689,423.667006141107,53.0228109606356));
#40197=CARTESIAN_POINT('',(80.6405446979746,381.667006141107,53.0261965417875));
#40198=CARTESIAN_POINT('',(80.6413661730645,380.332993858894,53.021596719646));
#40199=CARTESIAN_POINT('',(80.6314498948689,423.667006141107,53.0228109606222));
#40200=CARTESIAN_POINT('Ctrl Pts',(80.6405446979746,381.667006141107,53.0261965417875));
#40201=CARTESIAN_POINT('Ctrl Pts',(80.6410056141965,381.654912911579,53.1329056124629));
#40202=CARTESIAN_POINT('Ctrl Pts',(80.5894057523151,381.4306636725,55.1109627377459));
#40203=CARTESIAN_POINT('Ctrl Pts',(78.8308391867579,381.100336428644,57.9222168919113));
#40204=CARTESIAN_POINT('Ctrl Pts',(75.0710571136364,380.67602440954,58.8891432847));
#40205=CARTESIAN_POINT('Ctrl Pts',(71.2853928743543,380.251712390435,58.0291118004746));
#40206=CARTESIAN_POINT('Ctrl Pts',(68.3350139784818,379.721322366554,53.5970203186811));
#40207=CARTESIAN_POINT('Ctrl Pts',(70.9156937160722,379.084854337897,47.7312188622881));
#40208=CARTESIAN_POINT('Ctrl Pts',(77.2345122810668,378.448386309241,46.7400400786665));
#40209=CARTESIAN_POINT('Ctrl Pts',(80.3960885854519,377.975770243644,50.2843313906369));
#40210=CARTESIAN_POINT('Ctrl Pts',(80.6358929249802,377.715310187599,52.589062486923));
#40211=CARTESIAN_POINT('Ctrl Pts',(80.6318252954934,377.667006141107,53.0173586745867));
#40212=CARTESIAN_POINT('Ctrl Pts',(80.6413661730645,380.332993858894,53.021596719646));
#40213=CARTESIAN_POINT('Ctrl Pts',(80.6413665147454,380.332878722291,53.0226120523518));
#40214=CARTESIAN_POINT('Ctrl Pts',(80.6414404313821,380.120607576137,54.8945283089342));
#40215=CARTESIAN_POINT('Ctrl Pts',(78.5914140932141,379.696180420429,58.6441331442757));
#40216=CARTESIAN_POINT('Ctrl Pts',(72.2108730876569,379.059712391772,59.0897786478119));
#40217=CARTESIAN_POINT('Ctrl Pts',(68.3782131572467,378.423244363116,53.9691711353926));
#40218=CARTESIAN_POINT('Ctrl Pts',(70.6249796526406,377.786776334458,47.9675401113284));
#40219=CARTESIAN_POINT('Ctrl Pts',(75.8314238903965,377.256386310578,46.8534894251665));
#40220=CARTESIAN_POINT('Ctrl Pts',(79.1424775432099,376.832074291473,48.8802680501344));
#40221=CARTESIAN_POINT('Ctrl Pts',(80.4376648879746,376.559636142504,51.0099478466897));
#40222=CARTESIAN_POINT('Ctrl Pts',(80.6299739830598,376.393275998311,52.4837310832435));
#40223=CARTESIAN_POINT('Ctrl Pts',(80.625604522174,376.332993858894,53.0187133256936));
#40224=CARTESIAN_POINT('Origin',(74.9879498948689,423.667006141107,53.0228109606356));
#40225=CARTESIAN_POINT('',(80.6230176733859,385.667006141107,53.0259542642868));
#40226=CARTESIAN_POINT('',(80.6314498948689,384.332993858894,53.0228109606314));
#40227=CARTESIAN_POINT('',(80.6314498948689,423.667006141107,53.0228109606222));
#40228=CARTESIAN_POINT('Ctrl Pts',(80.6230176733859,385.667006141107,53.0259542642868));
#40229=CARTESIAN_POINT('Ctrl Pts',(80.6270946479354,385.59451563556,53.6699647111595));
#40230=CARTESIAN_POINT('Ctrl Pts',(80.3763420788995,385.415947125237,55.2537571332483));
#40231=CARTESIAN_POINT('Ctrl Pts',(78.897412769893,385.131300610139,57.3973808566349));
#40232=CARTESIAN_POINT('Ctrl Pts',(75.4752995936722,384.706988591033,59.2304245810384));
#40233=CARTESIAN_POINT('Ctrl Pts',(70.3415256590186,384.176598567153,57.8188525070491));
#40234=CARTESIAN_POINT('Ctrl Pts',(68.4435630952913,383.540130538496,51.6979642757119));
#40235=CARTESIAN_POINT('Ctrl Pts',(72.5643111612702,382.903662509839,46.8062019332478));
#40236=CARTESIAN_POINT('Ctrl Pts',(78.788125715371,382.279287710709,47.6025595677669));
#40237=CARTESIAN_POINT('Ctrl Pts',(80.632919590016,381.867068921132,51.2608688197568));
#40238=CARTESIAN_POINT('Ctrl Pts',(80.6405446979746,381.667006141107,53.0261965417875));
#40239=CARTESIAN_POINT('Ctrl Pts',(80.6285307903321,384.332993858894,53.0278704034178));
#40240=CARTESIAN_POINT('Ctrl Pts',(80.6332236772202,384.272481446272,53.5652251748871));
#40241=CARTESIAN_POINT('Ctrl Pts',(80.3164791190338,383.999813024097,55.9810146677916));
#40242=CARTESIAN_POINT('Ctrl Pts',(76.8695434714302,383.514988592372,59.4243621885054));
#40243=CARTESIAN_POINT('Ctrl Pts',(70.6181705596548,382.878520563713,58.0714985012323));
#40244=CARTESIAN_POINT('Ctrl Pts',(68.3790371462131,382.242052535058,52.0670154934588));
#40245=CARTESIAN_POINT('Ctrl Pts',(71.5793749741399,381.711662511176,47.8118999463395));
#40246=CARTESIAN_POINT('Ctrl Pts',(75.4082269213871,381.287350492072,47.1709626229601));
#40247=CARTESIAN_POINT('Ctrl Pts',(79.1051881256536,380.863153609569,48.3521518125064));
#40248=CARTESIAN_POINT('Ctrl Pts',(80.6407369179058,380.545034731844,51.1517132196232));
#40249=CARTESIAN_POINT('Ctrl Pts',(80.6413661730645,380.332993858894,53.021596719646));
#40250=CARTESIAN_POINT('Origin',(74.9879498948689,423.667006141107,53.0228109606356));
#40251=CARTESIAN_POINT('',(80.6280910915538,389.667006141107,53.0202293524412));
#40252=CARTESIAN_POINT('',(80.6314498948689,388.332993858894,53.0228109606314));
#40253=CARTESIAN_POINT('',(80.6314498948689,423.667006141107,53.0228109606222));
#40254=CARTESIAN_POINT('Ctrl Pts',(80.6280910915538,389.667006141107,53.0202293524411));
#40255=CARTESIAN_POINT('Ctrl Pts',(80.6271443157921,389.640196364317,53.2584401382313));
#40256=CARTESIAN_POINT('Ctrl Pts',(80.5499860677044,389.507308582751,54.4398090922248));
#40257=CARTESIAN_POINT('Ctrl Pts',(79.4264024191887,389.162264791632,57.3899743166933));
#40258=CARTESIAN_POINT('Ctrl Pts',(74.6248094448821,388.631874767752,59.6905993277034));
#40259=CARTESIAN_POINT('Ctrl Pts',(69.1782161333895,387.995406739095,56.3138914734408));
#40260=CARTESIAN_POINT('Ctrl Pts',(69.0817056595131,387.358938710438,49.9185346290693));
#40261=CARTESIAN_POINT('Ctrl Pts',(74.4039894636263,386.72247068178,46.3712541852796));
#40262=CARTESIAN_POINT('Ctrl Pts',(79.6053973880414,386.15849315867,48.6495978495524));
#40263=CARTESIAN_POINT('Ctrl Pts',(80.615162676363,385.806671645112,51.7851566871539));
#40264=CARTESIAN_POINT('Ctrl Pts',(80.6230176733859,385.667006141107,53.0259542642868));
#40265=CARTESIAN_POINT('Ctrl Pts',(80.6314498948689,388.332993858894,53.0228109606315));
#40266=CARTESIAN_POINT('Ctrl Pts',(80.6314498948701,388.140209036291,54.7318077489505));
#40267=CARTESIAN_POINT('Ctrl Pts',(79.806065919266,387.947424213689,56.4221521097309));
#40268=CARTESIAN_POINT('Ctrl Pts',(78.4584055093398,387.754639391087,57.4730952299815));
#40269=CARTESIAN_POINT('Ctrl Pts',(77.1107450994135,387.561854568484,58.5240383502321));
#40270=CARTESIAN_POINT('Ctrl Pts',(75.2702256751574,387.369069745882,58.9126397065625));
#40271=CARTESIAN_POINT('Ctrl Pts',(73.6127451626996,387.176284923279,58.4961923829941));
#40272=CARTESIAN_POINT('Ctrl Pts',(71.9552646502418,386.983500100677,58.0797450594256));
#40273=CARTESIAN_POINT('Ctrl Pts',(70.51700338107,386.790715278075,56.867339480914));
#40274=CARTESIAN_POINT('Ctrl Pts',(69.8261371496106,386.597930455472,55.3042099684571));
#40275=CARTESIAN_POINT('Ctrl Pts',(69.1352709181512,386.40514563287,53.7410804560002));
#40276=CARTESIAN_POINT('Ctrl Pts',(69.206880305491,386.212360810268,51.8613477992506));
#40277=CARTESIAN_POINT('Ctrl Pts',(70.014668041546,386.019575987665,50.3553102844577));
#40278=CARTESIAN_POINT('Ctrl Pts',(70.8224557776011,385.826791165063,48.8492727696647));
#40279=CARTESIAN_POINT('Ctrl Pts',(72.3487890589434,385.63400634246,47.7498049531858));
#40280=CARTESIAN_POINT('Ctrl Pts',(74.0331492157648,385.441221519858,47.4606667775725));
#40281=CARTESIAN_POINT('Ctrl Pts',(75.7175093725863,385.248436697256,47.1715286019592));
#40282=CARTESIAN_POINT('Ctrl Pts',(77.5231293307885,385.055651874653,47.6990315230391));
#40283=CARTESIAN_POINT('Ctrl Pts',(78.7869273705912,384.862867052051,48.8494595029993));
#40284=CARTESIAN_POINT('Ctrl Pts',(79.9447859852136,384.686242654332,49.9034514424927));
#40285=CARTESIAN_POINT('Ctrl Pts',(80.6314498948677,384.509618256613,51.4570729301894));
#40286=CARTESIAN_POINT('Ctrl Pts',(80.6314498948689,384.332993858894,53.0228109606314));
#40287=CARTESIAN_POINT('Origin',(74.9879498948689,423.667006141107,53.0228109606356));
#40288=CARTESIAN_POINT('',(80.6360923571988,393.667006141107,53.0197627911133));
#40289=CARTESIAN_POINT('',(80.6356989504312,392.332993858894,53.0186124760575));
#40290=CARTESIAN_POINT('',(80.6314498948689,423.667006141107,53.0228109606222));
#40291=CARTESIAN_POINT('Ctrl Pts',(80.6360923571988,393.667006141107,53.0197627911133));
#40292=CARTESIAN_POINT('Ctrl Pts',(80.6237110197019,393.473721083521,54.7279555626006));
#40293=CARTESIAN_POINT('Ctrl Pts',(78.8984604558714,393.068280016383,58.3253991383234));
#40294=CARTESIAN_POINT('Ctrl Pts',(72.7596690106956,392.450682939694,59.3171720578613));
#40295=CARTESIAN_POINT('Ctrl Pts',(68.4931906324375,391.814214911036,54.5519789152622));
#40296=CARTESIAN_POINT('Ctrl Pts',(70.1854506547193,391.177746882379,48.3838220223643));
#40297=CARTESIAN_POINT('Ctrl Pts',(76.3032611663828,390.541278853722,46.4759621802336));
#40298=CARTESIAN_POINT('Ctrl Pts',(80.1713126028281,390.037698606631,49.7306407766893));
#40299=CARTESIAN_POINT('Ctrl Pts',(80.6308904150066,389.746274369093,52.3159136460942));
#40300=CARTESIAN_POINT('Ctrl Pts',(80.6280910915538,389.667006141107,53.0202293524411));
#40301=CARTESIAN_POINT('Ctrl Pts',(80.6356989504312,392.332993858894,53.0186124760575));
#40302=CARTESIAN_POINT('Ctrl Pts',(80.6226233173025,392.151686894233,54.621714738745));
#40303=CARTESIAN_POINT('Ctrl Pts',(79.071569540894,391.75822392002,58.1232600357524));
#40304=CARTESIAN_POINT('Ctrl Pts',(73.1160470792531,391.152604936255,59.4327448560289));
#40305=CARTESIAN_POINT('Ctrl Pts',(69.3510454836729,390.622214912373,55.6680491820767));
#40306=CARTESIAN_POINT('Ctrl Pts',(69.2526248134902,390.197902893269,51.7871702535196));
#40307=CARTESIAN_POINT('Ctrl Pts',(70.9403623007099,389.773590874164,48.2911081744554));
#40308=CARTESIAN_POINT('Ctrl Pts',(75.9215609897948,389.243200850283,46.4107278533347));
#40309=CARTESIAN_POINT('Ctrl Pts',(80.082648031994,388.727642510268,49.5142379536945));
#40310=CARTESIAN_POINT('Ctrl Pts',(80.6262685739933,388.424240179805,52.2093882971212));
#40311=CARTESIAN_POINT('Ctrl Pts',(80.6232078042707,388.332993858894,53.0209321700845));
#40312=CARTESIAN_POINT('Origin',(74.9879498948689,423.667006141107,53.0228109606356));
#40313=CARTESIAN_POINT('',(80.6337031614845,397.667006141107,53.0276437365256));
#40314=CARTESIAN_POINT('',(80.6372725134855,396.332993858893,53.0262406841596));
#40315=CARTESIAN_POINT('',(80.6314498948689,423.667006141107,53.0228109606222));
#40316=CARTESIAN_POINT('Ctrl Pts',(80.6337031614845,397.667006141107,53.0276437365256));
#40317=CARTESIAN_POINT('Ctrl Pts',(80.6373890898133,397.625479817054,53.3949129559387));
#40318=CARTESIAN_POINT('Ctrl Pts',(80.4383554548793,397.371797483449,55.6351493604705));
#40319=CARTESIAN_POINT('Ctrl Pts',(77.4329911410624,396.905959140291,59.2361828813744));
#40320=CARTESIAN_POINT('Ctrl Pts',(71.0871415122597,396.269491111636,58.436122929515));
#40321=CARTESIAN_POINT('Ctrl Pts',(68.3201615171243,395.633023082977,52.6695186301911));
#40322=CARTESIAN_POINT('Ctrl Pts',(71.6880557805561,394.996555054321,47.2174710456321));
#40323=CARTESIAN_POINT('Ctrl Pts',(77.0117036986669,394.46616503044,47.1341441224853));
#40324=CARTESIAN_POINT('Ctrl Pts',(79.8669002864431,394.041853011336,49.7644977739172));
#40325=CARTESIAN_POINT('Ctrl Pts',(80.5941763410107,393.810826049817,51.7491572431493));
#40326=CARTESIAN_POINT('Ctrl Pts',(80.637301181244,393.685877093074,52.852987230998));
#40327=CARTESIAN_POINT('Ctrl Pts',(80.6360923571988,393.667006141107,53.0197627911133));
#40328=CARTESIAN_POINT('Ctrl Pts',(80.6372725134855,396.332993858894,53.0262406841596));
#40329=CARTESIAN_POINT('Ctrl Pts',(80.6394471176278,396.303445627766,53.2874601812273));
#40330=CARTESIAN_POINT('Ctrl Pts',(80.5040174270057,396.061741387085,55.4222191120998));
#40331=CARTESIAN_POINT('Ctrl Pts',(77.7778399493888,395.607881136854,59.0897530386598));
#40332=CARTESIAN_POINT('Ctrl Pts',(72.4666579798875,395.077491112972,58.7162338035805));
#40333=CARTESIAN_POINT('Ctrl Pts',(69.8475504599716,394.653179093868,55.8507175000904));
#40334=CARTESIAN_POINT('Ctrl Pts',(68.8293227947622,394.228867074763,52.1045033700332));
#40335=CARTESIAN_POINT('Ctrl Pts',(71.3570971813203,393.698477050882,47.4185107128847));
#40336=CARTESIAN_POINT('Ctrl Pts',(77.7478064874976,393.062009022225,46.942727991698));
#40337=CARTESIAN_POINT('Ctrl Pts',(80.495439138097,392.606847958229,50.5995879290105));
#40338=CARTESIAN_POINT('Ctrl Pts',(80.6379237452377,392.363842903785,52.7458475893924));
#40339=CARTESIAN_POINT('Ctrl Pts',(80.6356989504312,392.332993858894,53.0186124760575));
#40340=CARTESIAN_POINT('Origin',(74.9879498948689,423.667006141107,53.0228109606356));
#40341=CARTESIAN_POINT('',(80.6220844309609,401.667006141107,53.022623341048));
#40342=CARTESIAN_POINT('',(80.6229913075356,400.332993858894,53.0262785622937));
#40343=CARTESIAN_POINT('',(80.6314498948689,423.667006141107,53.0228109606222));
#40344=CARTESIAN_POINT('Ctrl Pts',(80.6220844309609,401.667006141107,53.022623341048));
#40345=CARTESIAN_POINT('Ctrl Pts',(80.62301189764,401.565082541034,53.9302973036867));
#40346=CARTESIAN_POINT('Ctrl Pts',(79.9875795301274,401.25100293141,56.7266784249494));
#40347=CARTESIAN_POINT('Ctrl Pts',(75.5925088429904,400.724767312234,59.6677158495928));
#40348=CARTESIAN_POINT('Ctrl Pts',(69.7221234542071,400.088299283577,57.1283303225627));
#40349=CARTESIAN_POINT('Ctrl Pts',(68.6898157193372,399.451831254919,50.8036267423682));
#40350=CARTESIAN_POINT('Ctrl Pts',(72.6545162366563,398.921441231039,47.2498512386062));
#40351=CARTESIAN_POINT('Ctrl Pts',(76.5349782081459,398.497129211934,47.3635296330406));
#40352=CARTESIAN_POINT('Ctrl Pts',(79.6010285553096,398.114343516882,49.0560694265861));
#40353=CARTESIAN_POINT('Ctrl Pts',(80.6185578577317,397.837635826606,51.5185520258631));
#40354=CARTESIAN_POINT('Ctrl Pts',(80.6337031614845,397.667006141107,53.0276437365256));
#40355=CARTESIAN_POINT('Ctrl Pts',(80.6229913075356,400.332993858894,53.0262785622937));
#40356=CARTESIAN_POINT('Ctrl Pts',(80.6259200030489,400.243048351746,53.8269052679644));
#40357=CARTESIAN_POINT('Ctrl Pts',(80.0921841224516,399.940946835046,56.5114176061463));
#40358=CARTESIAN_POINT('Ctrl Pts',(76.817716662541,399.53276731357,58.9746115424238));
#40359=CARTESIAN_POINT('Ctrl Pts',(72.9612986351318,399.108455294466,58.5285757956383));
#40360=CARTESIAN_POINT('Ctrl Pts',(69.7360426834167,398.684143275361,56.3678740736957));
#40361=CARTESIAN_POINT('Ctrl Pts',(68.5717701362819,398.153753251481,51.1724299186502));
#40362=CARTESIAN_POINT('Ctrl Pts',(73.0847550464725,397.517285222823,46.622649502512));
#40363=CARTESIAN_POINT('Ctrl Pts',(79.0482790583822,396.910365425296,47.9016912192682));
#40364=CARTESIAN_POINT('Ctrl Pts',(80.6238334812249,396.515601637318,51.4119067555371));
#40365=CARTESIAN_POINT('Ctrl Pts',(80.6372725134855,396.332993858894,53.0262406841596));
#40366=CARTESIAN_POINT('Origin',(74.9879498948689,423.667006141107,53.0228109606356));
#40367=CARTESIAN_POINT('',(80.6319421555458,405.667006141107,53.0182025218874));
#40368=CARTESIAN_POINT('',(80.6278395430646,404.332993858894,53.0174600182511));
#40369=CARTESIAN_POINT('',(80.6314498948689,423.667006141107,53.0228109606222));
#40370=CARTESIAN_POINT('Ctrl Pts',(80.6319421555458,405.667006141107,53.0182025218874));
#40371=CARTESIAN_POINT('Ctrl Pts',(80.6183780990486,405.504685265015,54.4565202766007));
#40372=CARTESIAN_POINT('Ctrl Pts',(79.3242260166029,405.130208379371,57.7945566874126));
#40373=CARTESIAN_POINT('Ctrl Pts',(73.704367667017,404.543575484175,59.575416161524));
#40374=CARTESIAN_POINT('Ctrl Pts',(68.7776943304863,403.907107455519,55.477194252816));
#40375=CARTESIAN_POINT('Ctrl Pts',(69.4407233960758,403.376717431636,50.194338734914));
#40376=CARTESIAN_POINT('Ctrl Pts',(72.4450042051697,402.952405412533,47.7356388492427));
#40377=CARTESIAN_POINT('Ctrl Pts',(76.2412371124112,402.528093393428,46.9235284074953));
#40378=CARTESIAN_POINT('Ctrl Pts',(79.9095618030171,402.09962696962,49.1692426271042));
#40379=CARTESIAN_POINT('Ctrl Pts',(80.6210813572206,401.777238550587,52.0409558189692));
#40380=CARTESIAN_POINT('Ctrl Pts',(80.6220844309609,401.667006141107,53.022623341048));
#40381=CARTESIAN_POINT('Ctrl Pts',(80.6278395430645,404.332993858894,53.0174600182511));
#40382=CARTESIAN_POINT('Ctrl Pts',(80.6153316186647,404.182651075727,54.3503900415285));
#40383=CARTESIAN_POINT('Ctrl Pts',(79.8054162775193,403.926230287784,56.6359043562006));
#40384=CARTESIAN_POINT('Ctrl Pts',(77.0681164794659,403.563731495065,58.5085806146201));
#40385=CARTESIAN_POINT('Ctrl Pts',(73.2162245052195,403.13941947596,58.9921464057559));
#40386=CARTESIAN_POINT('Ctrl Pts',(68.9304046244017,402.609029452079,55.8330454857165));
#40387=CARTESIAN_POINT('Ctrl Pts',(69.3542790093376,401.972561423423,49.4386835020307));
#40388=CARTESIAN_POINT('Ctrl Pts',(74.9554640876222,401.336093394765,46.3505401944445));
#40389=CARTESIAN_POINT('Ctrl Pts',(79.7906837745455,400.789570873256,48.9553092231759));
#40390=CARTESIAN_POINT('Ctrl Pts',(80.619012038738,400.455204361299,51.9384533329752));
#40391=CARTESIAN_POINT('Ctrl Pts',(80.6229913075356,400.332993858894,53.0262785622937));
#40392=CARTESIAN_POINT('Origin',(74.9879498948689,423.667006141107,53.0228109606356));
#40393=CARTESIAN_POINT('',(80.6394151663028,409.667006141107,53.0244911165473));
#40394=CARTESIAN_POINT('',(80.6387414332306,408.332993858894,53.0233301036444));
#40395=CARTESIAN_POINT('',(80.6314498948689,423.667006141107,53.0228109606222));
#40396=CARTESIAN_POINT('Ctrl Pts',(80.6394151663029,409.667006141107,53.0244911165473));
#40397=CARTESIAN_POINT('Ctrl Pts',(80.6397780627352,409.656443998548,53.1177179807749));
#40398=CARTESIAN_POINT('Ctrl Pts',(80.5952691262063,409.433725846437,55.0831851225367));
#40399=CARTESIAN_POINT('Ctrl Pts',(78.3155544127733,408.998851684773,58.8116972627153));
#40400=CARTESIAN_POINT('Ctrl Pts',(71.90864214512,408.362383656117,58.9480975871434));
#40401=CARTESIAN_POINT('Ctrl Pts',(68.9450950083279,407.831993632236,54.524794049794));
#40402=CARTESIAN_POINT('Ctrl Pts',(69.6010890929968,407.407681613131,50.6984892817582));
#40403=CARTESIAN_POINT('Ctrl Pts',(71.9347077043872,406.983369594027,47.5960537873647));
#40404=CARTESIAN_POINT('Ctrl Pts',(77.1859865465286,406.452979570146,46.7172645440322));
#40405=CARTESIAN_POINT('Ctrl Pts',(80.386744270138,405.97883241758,50.2593803039047));
#40406=CARTESIAN_POINT('Ctrl Pts',(80.6361065402022,405.716841274567,52.5766157156117));
#40407=CARTESIAN_POINT('Ctrl Pts',(80.6319421555458,405.667006141107,53.0182025218874));
#40408=CARTESIAN_POINT('Ctrl Pts',(80.6387414332307,408.332993858894,53.0233301036444));
#40409=CARTESIAN_POINT('Ctrl Pts',(80.6399063121554,408.228331804484,53.9476020009326));
#40410=CARTESIAN_POINT('Ctrl Pts',(80.1469930043062,408.017591745297,55.8101772106293));
#40411=CARTESIAN_POINT('Ctrl Pts',(77.5645627245594,407.594695676559,58.6914128709184));
#40412=CARTESIAN_POINT('Ctrl Pts',(72.2572669003642,407.064305652677,59.1166316929431));
#40413=CARTESIAN_POINT('Ctrl Pts',(68.3843315795067,406.427837624022,54.0109585396062));
#40414=CARTESIAN_POINT('Ctrl Pts',(70.5882295550609,405.791369595364,48.0065658313019));
#40415=CARTESIAN_POINT('Ctrl Pts',(76.8287342059321,405.154901566707,46.6044208685245));
#40416=CARTESIAN_POINT('Ctrl Pts',(80.3093621919521,404.668776321217,50.0457497443635));
#40417=CARTESIAN_POINT('Ctrl Pts',(80.6329821588008,404.394807085279,52.4694276913957));
#40418=CARTESIAN_POINT('Ctrl Pts',(80.6278395430645,404.332993858894,53.0174600182511));
#40419=CARTESIAN_POINT('Origin',(74.9879498948689,423.667006141107,53.0228109606356));
#40420=CARTESIAN_POINT('',(80.6269259201534,413.667006141107,53.0266694084182));
#40421=CARTESIAN_POINT('',(80.6310716108719,412.332993858894,53.0264521482468));
#40422=CARTESIAN_POINT('',(80.6314498948689,423.667006141107,53.0228109606222));
#40423=CARTESIAN_POINT('Ctrl Pts',(80.6269259201534,413.667006141107,53.0266694084182));
#40424=CARTESIAN_POINT('Ctrl Pts',(80.6312435980057,413.596046722529,53.6570115578714));
#40425=CARTESIAN_POINT('Ctrl Pts',(80.2411937413767,413.312931294398,56.1667899653849));
#40426=CARTESIAN_POINT('Ctrl Pts',(76.5500783965337,412.817659856716,59.5150838971706));
#40427=CARTESIAN_POINT('Ctrl Pts',(71.4097383128725,412.287269832834,58.1195031021403));
#40428=CARTESIAN_POINT('Ctrl Pts',(69.397075484847,411.86295781373,54.8001736486049));
#40429=CARTESIAN_POINT('Ctrl Pts',(69.1240494715453,411.438645794625,50.9277902465141));
#40430=CARTESIAN_POINT('Ctrl Pts',(72.5128743250655,410.908255770745,46.8207854764477));
#40431=CARTESIAN_POINT('Ctrl Pts',(78.7687719438231,410.282349884646,47.5804943468211));
#40432=CARTESIAN_POINT('Ctrl Pts',(80.632488759591,409.868600008101,51.2451206940265));
#40433=CARTESIAN_POINT('Ctrl Pts',(80.6394151663029,409.667006141107,53.0244911165473));
#40434=CARTESIAN_POINT('Ctrl Pts',(80.6310716108719,412.332993858894,53.0264521482468));
#40435=CARTESIAN_POINT('Ctrl Pts',(80.6342885006541,412.27401253324,53.5496918395882));
#40436=CARTESIAN_POINT('Ctrl Pts',(80.3195049291274,412.002875198035,55.9505212394806));
#40437=CARTESIAN_POINT('Ctrl Pts',(76.922041457819,411.519581853277,59.4142434298776));
#40438=CARTESIAN_POINT('Ctrl Pts',(70.6502604163708,410.88311382462,58.0990212603595));
#40439=CARTESIAN_POINT('Ctrl Pts',(68.3768445575805,410.246645795963,52.120585584734));
#40440=CARTESIAN_POINT('Ctrl Pts',(72.1690405094426,409.610177767306,46.9698855255472));
#40441=CARTESIAN_POINT('Ctrl Pts',(78.5640475947216,408.973709738649,47.3834241974277));
#40442=CARTESIAN_POINT('Ctrl Pts',(80.6295583507564,408.547981769178,51.1247901462488));
#40443=CARTESIAN_POINT('Ctrl Pts',(80.6387256738349,408.33440980926,53.0108258284451));
#40444=CARTESIAN_POINT('Ctrl Pts',(80.6387414332307,408.332993858894,53.0233301036444));
#40445=CARTESIAN_POINT('Origin',(74.9879498948689,509.5,53.0228109606356));
#40446=CARTESIAN_POINT('',(69.9879498948689,509.,53.0228109606356));
#40447=CARTESIAN_POINT('Origin',(74.9879498948689,509.,53.0228109606356));
#40448=CARTESIAN_POINT('',(70.9879498948689,510.,53.0228109606356));
#40449=CARTESIAN_POINT('',(70.4879498948689,509.5,53.0228109606356));
#40450=CARTESIAN_POINT('Origin',(74.9879498948689,510.,53.0228109606356));
#40451=CARTESIAN_POINT('Origin',(74.9879498948689,416.,53.0228109606356));
#40452=CARTESIAN_POINT('',(69.9879498948689,455.,53.0228109606356));
#40453=CARTESIAN_POINT('',(69.9879498948689,416.,53.0228109606356));
#40454=CARTESIAN_POINT('Origin',(74.9879498948689,455.,53.0228109606356));
#40455=CARTESIAN_POINT('Origin',(74.9879498948689,510.,53.0228109606356));
#40456=CARTESIAN_POINT('Origin',(74.9879498948689,0.5,53.0228109606356));
#40457=CARTESIAN_POINT('',(78.9879498948689,0.,53.0228109606356));
#40458=CARTESIAN_POINT('Origin',(74.9879498948689,0.,53.0228109606356));
#40459=CARTESIAN_POINT('',(79.9879498948689,1.,53.0228109606356));
#40460=CARTESIAN_POINT('',(79.4879498948689,0.5,53.0228109606356));
#40461=CARTESIAN_POINT('Origin',(74.9879498948689,1.,53.0228109606356));
#40462=CARTESIAN_POINT('Origin',(74.9879498948689,0.,53.0228109606356));
#40463=CARTESIAN_POINT('',(79.9879498948689,15.,53.0228109606356));
#40464=CARTESIAN_POINT('',(79.9879498948689,0.,53.0228109606356));
#40465=CARTESIAN_POINT('Origin',(74.9879498948689,15.,53.0228109606356));
#40466=CARTESIAN_POINT('Origin',(74.9879498948689,0.,53.0228109606356));
#40467=CARTESIAN_POINT('Origin',(74.9879498948689,15.,53.0228109606356));
#40468=CARTESIAN_POINT('',(78.3434537325938,15.,60.2023805156308));
#40469=CARTESIAN_POINT('Ctrl Pts',(72.1688064861966,15.,57.9117293166054));
#40470=CARTESIAN_POINT('Ctrl Pts',(72.2546784237327,15.,58.0248630587345));
#40471=CARTESIAN_POINT('Ctrl Pts',(72.3449777763099,15.,58.13427856792));
#40472=CARTESIAN_POINT('Ctrl Pts',(72.4393010647226,15.,58.2398866170317));
#40473=CARTESIAN_POINT('Ctrl Pts',(72.5351751631816,15.,58.3472310138289));
#40474=CARTESIAN_POINT('Ctrl Pts',(72.635206430336,15.,58.4506423776243));
#40475=CARTESIAN_POINT('Ctrl Pts',(72.7390204213387,15.,58.5500517066503));
#40476=CARTESIAN_POINT('Ctrl Pts',(72.8444033767096,15.,58.65096343139));
#40477=CARTESIAN_POINT('Ctrl Pts',(72.9536841924254,15.,58.7477519171545));
#40478=CARTESIAN_POINT('Ctrl Pts',(73.0665233585081,15.,58.8403600304194));
#40479=CARTESIAN_POINT('Ctrl Pts',(73.180863358548,15.,58.9341998915422));
#40480=CARTESIAN_POINT('Ctrl Pts',(73.2988570389478,15.0000000000001,59.0237481324304));
#40481=CARTESIAN_POINT('Ctrl Pts',(73.4202044759237,15.0000000000001,59.1089501698777));
#40482=CARTESIAN_POINT('Ctrl Pts',(73.4609348987315,15.0000000000001,59.1375483429896));
#40483=CARTESIAN_POINT('Ctrl Pts',(73.5020435972152,14.9999999999999,59.1656568588392));
#40484=CARTESIAN_POINT('Ctrl Pts',(73.5435205270524,14.9999999999999,59.193273565218));
#40485=CARTESIAN_POINT('Ctrl Pts',(73.5707922927962,14.9999999999999,59.2114320053422));
#40486=CARTESIAN_POINT('Ctrl Pts',(73.5982267011967,15.,59.2293799234602));
#40487=CARTESIAN_POINT('Ctrl Pts',(73.6257970261555,15.,59.2471015554436));
#40488=CARTESIAN_POINT('Ctrl Pts',(73.7583003035948,15.,59.3322719088175));
#40489=CARTESIAN_POINT('Ctrl Pts',(73.8940373217576,15.,59.4122821412029));
#40490=CARTESIAN_POINT('Ctrl Pts',(74.032592582409,15.,59.4870928430669));
#40491=CARTESIAN_POINT('Ctrl Pts',(74.1743088382327,15.,59.5636102738297));
#40492=CARTESIAN_POINT('Ctrl Pts',(74.3189734092911,15.,59.6346888756922));
#40493=CARTESIAN_POINT('Ctrl Pts',(74.4661965872584,15.,59.7002916495573));
#40494=CARTESIAN_POINT('Ctrl Pts',(74.5848379276424,15.,59.7531583321798));
#40495=CARTESIAN_POINT('Ctrl Pts',(74.7051419796555,14.9999999999999,59.8024691803922));
#40496=CARTESIAN_POINT('Ctrl Pts',(74.8269292956354,14.9999999999999,59.8482028687199));
#40497=CARTESIAN_POINT('Ctrl Pts',(74.9660800226104,14.9999999999998,59.9004568816017));
#40498=CARTESIAN_POINT('Ctrl Pts',(75.1071665460714,14.9999999999999,59.9480416246017));
#40499=CARTESIAN_POINT('Ctrl Pts',(75.2499003342714,14.9999999999999,59.9909802687671));
#40500=CARTESIAN_POINT('Ctrl Pts',(75.3123463666089,14.9999999999999,60.0097659255895));
#40501=CARTESIAN_POINT('Ctrl Pts',(75.3751081297216,14.9999999999998,60.0276621259232));
#40502=CARTESIAN_POINT('Ctrl Pts',(75.4381633889478,14.9999999999998,60.0446699346699));
#40503=CARTESIAN_POINT('Ctrl Pts',(75.4670091976466,14.9999999999998,60.0524504751596));
#40504=CARTESIAN_POINT('Ctrl Pts',(75.4959164438666,14.9999999999999,60.0600450869122));
#40505=CARTESIAN_POINT('Ctrl Pts',(75.5248830744914,14.9999999999999,60.0674538280609));
#40506=CARTESIAN_POINT('Ctrl Pts',(75.5520898605735,14.9999999999999,60.0744124570496));
#40507=CARTESIAN_POINT('Ctrl Pts',(75.5793414200024,15.,60.0812051333796));
#40508=CARTESIAN_POINT('Ctrl Pts',(75.6066283015114,15.,60.0878303861922));
#40509=CARTESIAN_POINT('Ctrl Pts',(75.7740637033796,15.,60.1284836893846));
#40510=CARTESIAN_POINT('Ctrl Pts',(75.94290994267,14.9999999999998,60.1628557189233));
#40511=CARTESIAN_POINT('Ctrl Pts',(76.1126821629086,14.9999999999998,60.1910302695823));
#40512=CARTESIAN_POINT('Ctrl Pts',(76.2856185048526,14.9999999999998,60.2197299220934));
#40513=CARTESIAN_POINT('Ctrl Pts',(76.4595159481927,14.9999999999998,60.2419994636294));
#40514=CARTESIAN_POINT('Ctrl Pts',(76.6339143325404,14.9999999999998,60.257913982013));
#40515=CARTESIAN_POINT('Ctrl Pts',(76.8129175877103,14.9999999999999,60.2742487124395));
#40516=CARTESIAN_POINT('Ctrl Pts',(76.9924489312741,14.9999999999999,60.283888978601));
#40517=CARTESIAN_POINT('Ctrl Pts',(77.1720606699146,14.9999999999999,60.286893235395));
#40518=CARTESIAN_POINT('Ctrl Pts',(77.3538461982158,14.9999999999999,60.2899338518525));
#40519=CARTESIAN_POINT('Ctrl Pts',(77.5357146523819,14.9999999999999,60.2861774033693));
#40520=CARTESIAN_POINT('Ctrl Pts',(77.717245145824,14.9999999999999,60.2756529017544));
#40521=CARTESIAN_POINT('Ctrl Pts',(77.9003905459956,14.9999999999999,60.2650347735088));
#40522=CARTESIAN_POINT('Ctrl Pts',(78.0831926380365,15.,60.2475281592605));
#40523=CARTESIAN_POINT('Ctrl Pts',(78.2652533350261,15.,60.2231228362824));
#40524=CARTESIAN_POINT('Ctrl Pts',(78.2930224296742,15.,60.2194003759442));
#40525=CARTESIAN_POINT('Ctrl Pts',(78.3207743284586,14.9999999999999,60.2155173378091));
#40526=CARTESIAN_POINT('Ctrl Pts',(78.3485076714003,14.9999999999999,60.2114735929952));
#40527=CARTESIAN_POINT('Ctrl Pts',(78.3434537325882,14.9999999999999,45.8432414056378));
#40528=CARTESIAN_POINT('Ctrl Pts',(78.1604444691944,14.9999999999999,45.8163432874972));
#40529=CARTESIAN_POINT('Ctrl Pts',(77.9768364993718,14.9999999999998,45.7963747706827));
#40530=CARTESIAN_POINT('Ctrl Pts',(77.7929605518461,14.9999999999999,45.7833395953758));
#40531=CARTESIAN_POINT('Ctrl Pts',(77.6105716158271,14.9999999999999,45.7704098360079));
#40532=CARTESIAN_POINT('Ctrl Pts',(77.4279184304687,15.,45.7643022285713));
#40533=CARTESIAN_POINT('Ctrl Pts',(77.2453576416075,15.,45.7650583218053));
#40534=CARTESIAN_POINT('Ctrl Pts',(77.0651782861446,14.9999999999999,45.7658045521018));
#40535=CARTESIAN_POINT('Ctrl Pts',(76.8850884586316,15.,45.7732371101817));
#40536=CARTESIAN_POINT('Ctrl Pts',(76.7054719634877,15.,45.787425385552));
#40537=CARTESIAN_POINT('Ctrl Pts',(76.5221532410464,15.,45.8019061074504));
#40538=CARTESIAN_POINT('Ctrl Pts',(76.3393268374206,14.9999999999999,45.8234243776713));
#40539=CARTESIAN_POINT('Ctrl Pts',(76.1574531402198,14.9999999999998,45.8520775781582));
#40540=CARTESIAN_POINT('Ctrl Pts',(76.0789744509187,14.9999999999998,45.8644414639377));
#40541=CARTESIAN_POINT('Ctrl Pts',(76.0006738665816,15.,45.8781340766259));
#40542=CARTESIAN_POINT('Ctrl Pts',(75.922591806848,15.,45.8931641940993));
#40543=CARTESIAN_POINT('Ctrl Pts',(75.8968634177424,15.,45.8981166852602));
#40544=CARTESIAN_POINT('Ctrl Pts',(75.8711585155862,14.9999999999999,45.9032145034763));
#40545=CARTESIAN_POINT('Ctrl Pts',(75.845493153525,14.9999999999999,45.9084548388638));
#40546=CARTESIAN_POINT('Ctrl Pts',(75.6809018784442,14.9999999999999,45.9420609684487));
#40547=CARTESIAN_POINT('Ctrl Pts',(75.5177825848442,14.9999999999999,45.9815544092212));
#40548=CARTESIAN_POINT('Ctrl Pts',(75.3564446018102,14.9999999999998,46.0269586008827));
#40549=CARTESIAN_POINT('Ctrl Pts',(75.1977486437348,14.9999999999998,46.0716192664052));
#40550=CARTESIAN_POINT('Ctrl Pts',(75.0407758107613,14.9999999999999,46.1219992700254));
#40551=CARTESIAN_POINT('Ctrl Pts',(74.8858656690889,14.9999999999999,46.1781423428412));
#40552=CARTESIAN_POINT('Ctrl Pts',(74.7791862064282,14.9999999999999,46.2168054850696));
#40553=CARTESIAN_POINT('Ctrl Pts',(74.6734859004813,14.9999999999999,46.2582021789035));
#40554=CARTESIAN_POINT('Ctrl Pts',(74.5688895733295,14.9999999999999,46.3023505313413));
#40555=CARTESIAN_POINT('Ctrl Pts',(74.4230808149576,14.9999999999999,46.3638939586146));
#40556=CARTESIAN_POINT('Ctrl Pts',(74.2794151390612,14.9999999999999,46.4307849909926));
#40557=CARTESIAN_POINT('Ctrl Pts',(74.1383311642972,14.9999999999999,46.5029908494939));
#40558=CARTESIAN_POINT('Ctrl Pts',(74.0399765949272,14.9999999999999,46.5533280768848));
#40559=CARTESIAN_POINT('Ctrl Pts',(73.9428777407458,14.9999999999999,46.6062483716059));
#40560=CARTESIAN_POINT('Ctrl Pts',(73.8471982719262,14.9999999999999,46.6617392239536));
#40561=CARTESIAN_POINT('Ctrl Pts',(73.8193292090864,14.9999999999999,46.6779023367947));
#40562=CARTESIAN_POINT('Ctrl Pts',(73.7915764524053,14.9999999999998,46.6942861391598));
#40563=CARTESIAN_POINT('Ctrl Pts',(73.7639697491469,14.9999999999998,46.7108746871263));
#40564=CARTESIAN_POINT('Ctrl Pts',(73.635325383924,14.9999999999998,46.788175594922));
#40565=CARTESIAN_POINT('Ctrl Pts',(73.50975027916,14.9999999999999,46.8699766963246));
#40566=CARTESIAN_POINT('Ctrl Pts',(73.3875696928616,14.9999999999999,46.9562183983009));
#40567=CARTESIAN_POINT('Ctrl Pts',(73.2682057974333,14.9999999999999,47.0404719266896));
#40568=CARTESIAN_POINT('Ctrl Pts',(73.1520816382575,14.9999999999998,47.128964325939));
#40569=CARTESIAN_POINT('Ctrl Pts',(73.0395496569516,14.9999999999998,47.2216433484764));
#40570=CARTESIAN_POINT('Ctrl Pts',(72.9285853368353,14.9999999999998,47.3130312775395));
#40571=CARTESIAN_POINT('Ctrl Pts',(72.8211137584,14.9999999999998,47.4084906138113));
#40572=CARTESIAN_POINT('Ctrl Pts',(72.7175222237852,14.9999999999998,47.5079652205717));
#40573=CARTESIAN_POINT('Ctrl Pts',(72.6162286608911,14.9999999999998,47.6052331814503));
#40574=CARTESIAN_POINT('Ctrl Pts',(72.5186450261201,14.9999999999999,47.7063408125022));
#40575=CARTESIAN_POINT('Ctrl Pts',(72.4251803497841,14.9999999999999,47.8112211767485));
#40576=CARTESIAN_POINT('Ctrl Pts',(72.3343088870862,14.9999999999999,47.9131915946753));
#40577=CARTESIAN_POINT('Ctrl Pts',(72.2473312334373,14.9999999999999,48.0187287888016));
#40578=CARTESIAN_POINT('Ctrl Pts',(72.1646654645466,14.9999999999999,48.1277497923169));
#40579=CARTESIAN_POINT('Origin',(74.9879498948689,15.,53.0228109606356));
#40580=CARTESIAN_POINT('Ctrl Pts',(68.1225865616467,416.611326082532,56.981650601597));
#40581=CARTESIAN_POINT('Ctrl Pts',(67.4629372253086,416.505248077756,55.8376961156356));
#40582=CARTESIAN_POINT('Ctrl Pts',(66.7429036265161,416.293092068203,53.2244189993033));
#40583=CARTESIAN_POINT('Ctrl Pts',(67.9167913369144,415.868780049099,47.8794315286107));
#40584=CARTESIAN_POINT('Ctrl Pts',(74.0953234943061,415.338390025218,43.6918638654563));
#40585=CARTESIAN_POINT('Ctrl Pts',(82.3660788114064,414.701921996561,47.2361689914527));
#40586=CARTESIAN_POINT('Ctrl Pts',(83.8426349834315,414.065453967903,56.0973433337628));
#40587=CARTESIAN_POINT('Ctrl Pts',(77.1816007100824,413.428985939248,62.1397176713732));
#40588=CARTESIAN_POINT('Ctrl Pts',(69.9631732868513,412.898595915366,60.1799448706925));
#40589=CARTESIAN_POINT('Ctrl Pts',(67.1368504531333,412.474283896262,55.518708772654));
#40590=CARTESIAN_POINT('Ctrl Pts',(66.7534481043442,412.049971877156,50.0808353852934));
#40591=CARTESIAN_POINT('Ctrl Pts',(71.5122745354891,411.519581853277,44.3134901557799));
#40592=CARTESIAN_POINT('Ctrl Pts',(80.445492513773,410.883113824618,45.3983296708595));
#40593=CARTESIAN_POINT('Ctrl Pts',(84.3461800842815,410.246645795963,53.4889644224392));
#40594=CARTESIAN_POINT('Ctrl Pts',(79.6608064208477,409.610177767304,61.1519726411528));
#40595=CARTESIAN_POINT('Ctrl Pts',(70.6637691707098,408.973709738649,61.3435155792337));
#40596=CARTESIAN_POINT('Ctrl Pts',(66.5021476487722,408.443319714767,55.1320013533967));
#40597=CARTESIAN_POINT('Ctrl Pts',(67.4233407241729,408.019007695663,49.7588348278931));
#40598=CARTESIAN_POINT('Ctrl Pts',(70.7003722640477,407.594695676558,45.4021764965285));
#40599=CARTESIAN_POINT('Ctrl Pts',(78.0745877019812,407.064305652678,44.168118774657));
#40600=CARTESIAN_POINT('Ctrl Pts',(84.1080553689783,406.427837624021,50.8450505375157));
#40601=CARTESIAN_POINT('Ctrl Pts',(81.7476715690704,405.791369595364,59.5111857266153));
#40602=CARTESIAN_POINT('Ctrl Pts',(73.1854533668698,405.154901566707,62.2244404843412));
#40603=CARTESIAN_POINT('Ctrl Pts',(66.2670718320099,404.518433538049,56.4694287670495));
#40604=CARTESIAN_POINT('Ctrl Pts',(67.19814392288,403.988043514169,49.0508711380302));
#40605=CARTESIAN_POINT('Ctrl Pts',(71.4169665351032,403.563731495064,45.598191667147));
#40606=CARTESIAN_POINT('Ctrl Pts',(76.7479040366348,403.13941947596,44.4577690126192));
#40607=CARTESIAN_POINT('Ctrl Pts',(83.1246198509995,402.609029452079,48.3615350602155));
#40608=CARTESIAN_POINT('Ctrl Pts',(83.3016244349796,401.972561423422,57.358914436859));
#40609=CARTESIAN_POINT('Ctrl Pts',(75.8369141305076,401.336093394765,62.3540542041882));
#40610=CARTESIAN_POINT('Ctrl Pts',(67.5933056949457,400.699625366108,58.7880702754657));
#40611=CARTESIAN_POINT('Ctrl Pts',(66.1436664996217,400.063157337451,49.9064762517133));
#40612=CARTESIAN_POINT('Ctrl Pts',(71.7111780792753,399.53276731357,44.9160145050502));
#40613=CARTESIAN_POINT('Ctrl Pts',(77.1603959625132,399.108455294466,45.0756497094295));
#40614=CARTESIAN_POINT('Ctrl Pts',(81.9330467436625,398.684143275361,47.7102774725632));
#40615=CARTESIAN_POINT('Ctrl Pts',(84.1876426409602,398.15375325148,54.83900042918));
#40616=CARTESIAN_POINT('Ctrl Pts',(78.4214489426319,397.517285222823,61.7480652304801));
#40617=CARTESIAN_POINT('Ctrl Pts',(69.5101601487526,396.880817194167,60.6245647221929));
#40618=CARTESIAN_POINT('Ctrl Pts',(65.6245720453742,396.244349165508,52.5266929985891));
#40619=CARTESIAN_POINT('Ctrl Pts',(70.3540062684141,395.607881136854,44.8705439585235));
#40620=CARTESIAN_POINT('Ctrl Pts',(77.829847457575,395.077491112971,44.7535304268656));
#40621=CARTESIAN_POINT('Ctrl Pts',(81.8393155107531,394.653179093867,48.4472581999877));
#40622=CARTESIAN_POINT('Ctrl Pts',(83.7150557611386,394.228867074762,53.5659550502071));
#40623=CARTESIAN_POINT('Ctrl Pts',(80.7427680213086,393.698477050882,60.4265234846684));
#40624=CARTESIAN_POINT('Ctrl Pts',(71.8588410072801,393.062009022225,61.8617959337022));
#40625=CARTESIAN_POINT('Ctrl Pts',(65.8675517102712,392.425540993567,55.1701762552898));
#40626=CARTESIAN_POINT('Ctrl Pts',(68.2439423679512,391.789072964911,46.508416110662));
#40627=CARTESIAN_POINT('Ctrl Pts',(76.8350025796891,391.152604936254,43.8292650078264));
#40628=CARTESIAN_POINT('Ctrl Pts',(82.5559722100773,390.622214912373,48.6430369322593));
#40629=CARTESIAN_POINT('Ctrl Pts',(83.1610301794806,390.197902893269,54.0609114033989));
#40630=CARTESIAN_POINT('Ctrl Pts',(81.2207373946848,389.773590874163,59.1554891916591));
#40631=CARTESIAN_POINT('Ctrl Pts',(74.4780025100577,389.243200850283,62.3861887951374));
#40632=CARTESIAN_POINT('Ctrl Pts',(66.8295127442103,388.606732821626,57.6443779073797));
#40633=CARTESIAN_POINT('Ctrl Pts',(66.6939859425028,387.97026479297,48.6635675961109));
#40634=CARTESIAN_POINT('Ctrl Pts',(74.1679115467585,387.333796764312,43.682226669912));
#40635=CARTESIAN_POINT('Ctrl Pts',(82.4109334435622,386.697328735656,47.29287151569));
#40636=CARTESIAN_POINT('Ctrl Pts',(83.5737265630747,386.166938711774,54.6786555508142));
#40637=CARTESIAN_POINT('Ctrl Pts',(80.4778928884972,385.742626692671,59.1658899764619));
#40638=CARTESIAN_POINT('Ctrl Pts',(75.6723206511343,385.318314673565,61.7399790197646));
#40639=CARTESIAN_POINT('Ctrl Pts',(68.4631138765931,384.787924649685,59.7577501393902));
#40640=CARTESIAN_POINT('Ctrl Pts',(65.7978612288556,384.151456621028,51.1623679770162));
#40641=CARTESIAN_POINT('Ctrl Pts',(71.5845057620196,383.51498859237,44.2930109177437));
#40642=CARTESIAN_POINT('Ctrl Pts',(80.4937037924029,382.878520563714,45.4329722400649));
#40643=CARTESIAN_POINT('Ctrl Pts',(84.3495636598611,382.242052535057,53.5641782315556));
#40644=CARTESIAN_POINT('Ctrl Pts',(80.3844055763066,381.711662511175,59.9029016854306));
#40645=CARTESIAN_POINT('Ctrl Pts',(75.1046549021694,381.287350492072,61.2607277973877));
#40646=CARTESIAN_POINT('Ctrl Pts',(69.788558668218,380.863038472966,60.0530110413841));
#40647=CARTESIAN_POINT('Ctrl Pts',(65.6454289172183,380.332648449086,53.8291561652914));
#40648=CARTESIAN_POINT('Ctrl Pts',(69.2694010835046,379.696180420429,45.5919848102989));
#40649=CARTESIAN_POINT('Ctrl Pts',(78.1427309546104,379.059712391772,44.2001017837785));
#40650=CARTESIAN_POINT('Ctrl Pts',(84.1216479173398,378.423244363115,50.9027783621136));
#40651=CARTESIAN_POINT('Ctrl Pts',(81.7009543132028,377.786776334458,59.5702121615964));
#40652=CARTESIAN_POINT('Ctrl Pts',(74.5507931646769,377.256386310578,61.755867487212));
#40653=CARTESIAN_POINT('Ctrl Pts',(69.6742308536814,376.832074291472,59.3189434099489));
#40654=CARTESIAN_POINT('Ctrl Pts',(66.4525254996838,376.407762272368,54.9212083629745));
#40655=CARTESIAN_POINT('Ctrl Pts',(67.4056279554398,375.877372248488,47.505448836054));
#40656=CARTESIAN_POINT('Ctrl Pts',(75.543059676302,375.24090421983,43.6627452068579));
#40657=CARTESIAN_POINT('Ctrl Pts',(83.1550969766561,374.604436191174,48.4303661543525));
#40658=CARTESIAN_POINT('Ctrl Pts',(83.2740323816697,373.967968162516,57.4114115127954));
#40659=CARTESIAN_POINT('Ctrl Pts',(75.7629377951823,373.33150013386,62.3679853603609));
#40660=CARTESIAN_POINT('Ctrl Pts',(68.9313898304873,372.801110109979,59.3295900506045));
#40661=CARTESIAN_POINT('Ctrl Pts',(66.8475568448849,372.376798090874,54.2920212898348));
#40662=CARTESIAN_POINT('Ctrl Pts',(67.2988947945623,371.952486071769,48.859181057825));
#40663=CARTESIAN_POINT('Ctrl Pts',(72.8812042835999,371.422096047889,43.8852777193108));
#40664=CARTESIAN_POINT('Ctrl Pts',(81.5447115814599,370.785628019232,46.3199866328066));
#40665=CARTESIAN_POINT('Ctrl Pts',(84.1655183393139,370.149159990575,54.9109524282782));
#40666=CARTESIAN_POINT('Ctrl Pts',(78.3661932179409,369.512691961918,61.769607507635));
#40667=CARTESIAN_POINT('Ctrl Pts',(69.4451731646705,368.876223933261,60.5865743708756));
#40668=CARTESIAN_POINT('Ctrl Pts',(66.2797325110554,368.34583390938,53.8129579718812));
#40669=CARTESIAN_POINT('Ctrl Pts',(68.0097178803784,367.921521890275,48.6431794898481));
#40670=CARTESIAN_POINT('Ctrl Pts',(71.9129411847918,367.497209871171,44.8373541171795));
#40671=CARTESIAN_POINT('Ctrl Pts',(79.3890969473516,366.96681984729,44.7425455404127));
#40672=CARTESIAN_POINT('Ctrl Pts',(84.3335160685705,366.330351818633,52.2616469326837));
#40673=CARTESIAN_POINT('Ctrl Pts',(80.6788833058256,365.693883789976,60.4663395369466));
#40674=CARTESIAN_POINT('Ctrl Pts',(71.8029972093442,365.05741576132,61.8418275824281));
#40675=CARTESIAN_POINT('Ctrl Pts',(65.8433980359348,364.420947732661,55.0988798675317));
#40676=CARTESIAN_POINT('Ctrl Pts',(67.89514712053,363.890557708782,47.9091497372594));
#40677=CARTESIAN_POINT('Ctrl Pts',(72.591248992436,363.466245689677,45.1403799490598));
#40678=CARTESIAN_POINT('Ctrl Pts',(78.0337578782412,363.041933670573,44.8264437146201));
#40679=CARTESIAN_POINT('Ctrl Pts',(83.7404046046765,362.511543646691,49.6571865966155));
#40680=CARTESIAN_POINT('Ctrl Pts',(82.5429443961398,361.875075618035,58.5762815755079));
#40681=CARTESIAN_POINT('Ctrl Pts',(74.4036612243952,361.238607589377,62.3743588273717));
#40682=CARTESIAN_POINT('Ctrl Pts',(66.8004446252625,360.602139560721,57.5926835239192));
#40683=CARTESIAN_POINT('Ctrl Pts',(66.7225010042729,359.965671532063,48.5939007737091));
#40684=CARTESIAN_POINT('Ctrl Pts',(72.9860720763478,359.435281508183,44.5110621683577));
#40685=CARTESIAN_POINT('Ctrl Pts',(78.3471760447884,359.010969489078,45.500012708544));
#40686=CARTESIAN_POINT('Ctrl Pts',(82.6621127768296,358.586657469973,48.8317960042954));
#40687=CARTESIAN_POINT('Ctrl Pts',(83.8029638126729,358.056267446093,56.2210011419468));
#40688=CARTESIAN_POINT('Ctrl Pts',(77.050386020973,357.419799417436,62.1696866572998));
#40689=CARTESIAN_POINT('Ctrl Pts',(68.4147436383932,356.783331388779,59.7000708974758));
#40690=CARTESIAN_POINT('Ctrl Pts',(65.8098123187626,356.146863360122,51.1042780788362));
#40691=CARTESIAN_POINT('Ctrl Pts',(71.6517170309307,355.510395331465,44.2591107669676));
#40692=CARTESIAN_POINT('Ctrl Pts',(79.0579276024554,354.980005307585,45.2837758939829));
#40693=CARTESIAN_POINT('Ctrl Pts',(82.4570647662865,354.555693288479,49.5458558407725));
#40694=CARTESIAN_POINT('Ctrl Pts',(83.530087844715,354.131381269375,54.8907674775094));
#40695=CARTESIAN_POINT('Ctrl Pts',(79.5461202331947,353.600991245494,61.2176858207979));
#40696=CARTESIAN_POINT('Ctrl Pts',(70.5472231890065,352.964523216837,61.2810749494122));
#40697=CARTESIAN_POINT('Ctrl Pts',(65.6467313954362,352.328055188181,53.7538907785469));
#40698=CARTESIAN_POINT('Ctrl Pts',(69.3165152858901,351.691587159523,45.5559637504295));
#40699=CARTESIAN_POINT('Ctrl Pts',(78.2157045584089,351.055119130867,44.2185795552879));
#40700=CARTESIAN_POINT('Ctrl Pts',(83.1354728280878,350.524729106985,49.8486571590997));
#40701=CARTESIAN_POINT('Ctrl Pts',(82.9070482515139,350.100417087882,55.2954251130503));
#40702=CARTESIAN_POINT('Ctrl Pts',(80.2123707723944,349.676105068776,60.0344305166016));
#40703=CARTESIAN_POINT('Ctrl Pts',(73.0557494183956,349.145715044896,62.1988390842647));
#40704=CARTESIAN_POINT('Ctrl Pts',(66.2200396000194,348.509247016238,56.3458708225633));
#40705=CARTESIAN_POINT('Ctrl Pts',(67.4559649289566,347.872778987582,47.4494777364714));
#40706=CARTESIAN_POINT('Ctrl Pts',(75.6022507863105,347.236310958925,43.6664434924748));
#40707=CARTESIAN_POINT('Ctrl Pts',(83.1980754689443,346.599842930268,48.4921676437515));
#40708=CARTESIAN_POINT('Ctrl Pts',(83.2206893294649,346.069452906387,55.9688903392643));
#40709=CARTESIAN_POINT('Ctrl Pts',(79.4766322461752,345.645140887283,59.9314015996187));
#40710=CARTESIAN_POINT('Ctrl Pts',(74.3346602262409,345.220828868178,61.7423634097004));
#40711=CARTESIAN_POINT('Ctrl Pts',(67.5121669129356,344.690438844297,58.6836907168177));
#40712=CARTESIAN_POINT('Ctrl Pts',(66.1891777776275,344.05397081564,49.7823500345728));
#40713=CARTESIAN_POINT('Ctrl Pts',(72.9559103728996,343.417502786983,43.8760270375587));
#40714=CARTESIAN_POINT('Ctrl Pts',(81.5869756465227,342.781034758326,46.361592084672));
#40715=CARTESIAN_POINT('Ctrl Pts',(84.15744203475,342.144566729669,54.9857945834842));
#40716=CARTESIAN_POINT('Ctrl Pts',(79.2718205765323,341.614176705788,60.645529260948));
#40717=CARTESIAN_POINT('Ctrl Pts',(73.8467384815149,341.189864686684,61.182132646781));
#40718=CARTESIAN_POINT('Ctrl Pts',(68.777065024432,340.765552667579,59.1776701328107));
#40719=CARTESIAN_POINT('Ctrl Pts',(65.6317570526712,340.235162643698,52.3946817489889));
#40720=CARTESIAN_POINT('Ctrl Pts',(70.4697601757384,339.598694615042,44.8066719984206));
#40721=CARTESIAN_POINT('Ctrl Pts',(79.4515657791064,338.962226586384,44.7845481587893));
#40722=CARTESIAN_POINT('Ctrl Pts',(84.3381434764118,338.325758557728,52.3207726624231));
#40723=CARTESIAN_POINT('Ctrl Pts',(80.6237096357617,337.689290529071,60.5175493116288));
#40724=CARTESIAN_POINT('Ctrl Pts',(73.2238328504367,337.15890050519,61.5869964652049));
#40725=CARTESIAN_POINT('Ctrl Pts',(68.7760442604858,336.734588486085,58.434753519227));
#40726=CARTESIAN_POINT('Ctrl Pts',(66.2628357971074,336.31027646698,53.5970637657427));
#40727=CARTESIAN_POINT('Ctrl Pts',(68.3359304749261,335.7798864431,46.4134593703794));
#40728=CARTESIAN_POINT('Ctrl Pts',(76.9642790972773,335.143418414443,43.8569448985446));
#40729=CARTESIAN_POINT('Ctrl Pts',(83.7600261255697,334.506950385786,49.7298610130848));
#40730=CARTESIAN_POINT('Ctrl Pts',(82.5076676927869,333.870482357129,58.6239556672253));
#40731=CARTESIAN_POINT('Ctrl Pts',(74.3284255748771,333.234014328472,62.3768431648914));
#40732=CARTESIAN_POINT('Ctrl Pts',(68.0402716754738,332.703624304591,58.3319681124699));
#40733=CARTESIAN_POINT('Ctrl Pts',(66.7492161935976,332.279312285487,53.0354943162464));
#40734=CARTESIAN_POINT('Ctrl Pts',(68.0239579766349,331.855000266382,47.7350705296098));
#40735=CARTESIAN_POINT('Ctrl Pts',(74.2996281013125,331.324610242501,43.6708537368546));
#40736=CARTESIAN_POINT('Ctrl Pts',(82.49038640365,330.688142213844,47.3985399664363));
#40737=CARTESIAN_POINT('Ctrl Pts',(83.7701233751467,330.051674185187,56.2887365134628));
#40738=CARTESIAN_POINT('Ctrl Pts',(76.9924909750265,329.41520615653,62.1825485574472));
#40739=CARTESIAN_POINT('Ctrl Pts',(68.3563118700172,328.778738127874,59.6526124594933));
#40740=CARTESIAN_POINT('Ctrl Pts',(66.261109058149,328.248348103992,52.4754250696154));
#40741=CARTESIAN_POINT('Ctrl Pts',(68.7594106029481,327.824036084888,47.6300202028764));
#40742=CARTESIAN_POINT('Ctrl Pts',(73.1974725113032,327.399724065783,44.4640976787181));
#40743=CARTESIAN_POINT('Ctrl Pts',(80.6006069959407,326.869334041903,45.5107559107372));
#40744=CARTESIAN_POINT('Ctrl Pts',(84.3402606976814,326.232866013246,53.6960571504341));
#40745=CARTESIAN_POINT('Ctrl Pts',(79.4769098228901,325.596397984588,61.2472914620972));
#40746=CARTESIAN_POINT('Ctrl Pts',(70.4950786748861,324.959929955932,61.2528222598463));
#40747=CARTESIAN_POINT('Ctrl Pts',(65.6337353794111,324.323461927275,53.6797444471556));
#40748=CARTESIAN_POINT('Ctrl Pts',(68.7581439587704,323.793071903394,46.8871039678202));
#40749=CARTESIAN_POINT('Ctrl Pts',(73.8216217453728,323.368759884289,44.867041682654));
#40750=CARTESIAN_POINT('Ctrl Pts',(79.2483303007407,322.944447865185,45.3869389671831));
#40751=CARTESIAN_POINT('Ctrl Pts',(84.1513546426586,322.414057841304,51.0316042322666));
#40752=CARTESIAN_POINT('Ctrl Pts',(81.6074539287359,321.777589812647,59.6636801906463));
#40753=CARTESIAN_POINT('Ctrl Pts',(72.984082497274,321.14112178399,62.1758080767258));
#40754=CARTESIAN_POINT('Ctrl Pts',(66.1991967015628,320.504653755333,56.290347508501));
#40755=CARTESIAN_POINT('Ctrl Pts',(67.4947727809053,319.868185726676,47.3849756007047));
#40756=CARTESIAN_POINT('Ctrl Pts',(74.3078162547182,319.337795702796,44.3053112884437));
#40757=CARTESIAN_POINT('Ctrl Pts',(79.4553397631149,318.913483683691,46.1004326386231));
#40758=CARTESIAN_POINT('Ctrl Pts',(83.2115794746481,318.489171664586,50.0513973513058));
#40759=CARTESIAN_POINT('Ctrl Pts',(83.2119861784514,317.958781640706,57.5281542342649));
#40760=CARTESIAN_POINT('Ctrl Pts',(75.6310556643944,317.322313612048,62.3772426779387));
#40761=CARTESIAN_POINT('Ctrl Pts',(67.473160646069,316.685845583392,58.6193083742348));
#40762=CARTESIAN_POINT('Ctrl Pts',(66.2098496237681,316.049377554734,49.7267628094426));
#40763=CARTESIAN_POINT('Ctrl Pts',(73.0275060429953,315.412909526078,43.8527754803025));
#40764=CARTESIAN_POINT('Ctrl Pts',(80.1907575810404,314.882519502196,45.9951389076834));
#40765=CARTESIAN_POINT('Ctrl Pts',(82.9000134492689,314.458207483093,50.7258250705812));
#40766=CARTESIAN_POINT('Ctrl Pts',(83.1452072706115,314.033895463987,56.1718638990638));
#40767=CARTESIAN_POINT('Ctrl Pts',(78.2427970493154,313.503505440107,61.8170625381211));
#40768=CARTESIAN_POINT('Ctrl Pts',(69.3395322193748,312.86703741145,60.5070848430938));
#40769=CARTESIAN_POINT('Ctrl Pts',(65.6445247142307,312.230569382793,52.3204957549632));
#40770=CARTESIAN_POINT('Ctrl Pts',(70.5218174540695,311.594101354136,44.7782588924076));
#40771=CARTESIAN_POINT('Ctrl Pts',(79.5208670156516,310.957633325478,44.8139405643491));
#40772=CARTESIAN_POINT('Ctrl Pts',(83.5242960099995,310.427243301599,51.1285624801488));
#40773=CARTESIAN_POINT('Ctrl Pts',(82.4677347346415,310.002931282493,56.4767525667836));
#40774=CARTESIAN_POINT('Ctrl Pts',(79.0817364147207,309.578619263389,60.7492780855906));
#40775=CARTESIAN_POINT('Ctrl Pts',(71.6787158414133,309.048229239508,61.7967417095284));
#40776=CARTESIAN_POINT('Ctrl Pts',(65.8157628902134,308.411761210851,54.9695937775186));
#40777=CARTESIAN_POINT('Ctrl Pts',(68.3942158441679,307.775293182194,46.3658212488418));
#40778=CARTESIAN_POINT('Ctrl Pts',(77.022213469953,307.138825153537,43.8696284817613));
#40779=CARTESIAN_POINT('Ctrl Pts',(83.7930749612714,306.50235712488,49.7974949494634));
#40780=CARTESIAN_POINT('Ctrl Pts',(82.674980327966,305.971967100999,57.1901776860114));
#40781=CARTESIAN_POINT('Ctrl Pts',(78.3703224436088,305.547655081895,60.5352306646661));
#40782=CARTESIAN_POINT('Ctrl Pts',(73.0122888161883,305.12334306279,61.5406830895957));
#40783=CARTESIAN_POINT('Ctrl Pts',(66.736176576404,304.59295303891,57.4771490604643));
#40784=CARTESIAN_POINT('Ctrl Pts',(66.7864130236384,303.956485010252,48.4781689797607));
#40785=CARTESIAN_POINT('Ctrl Pts',(74.3748710433667,303.320016981596,43.6731064157774));
#40786=CARTESIAN_POINT('Ctrl Pts',(82.5258097259484,302.683548952939,47.4461052169655));
#40787=CARTESIAN_POINT('Ctrl Pts',(83.7507257081707,302.047080924282,56.3614709991433));
#40788=CARTESIAN_POINT('Ctrl Pts',(78.0589796480722,301.516690900401,61.2097614648264));
#40789=CARTESIAN_POINT('Ctrl Pts',(72.6155299655976,301.092378881296,60.9125839324752));
#40790=CARTESIAN_POINT('Ctrl Pts',(67.9109254487115,300.668066862192,58.1582863321683));
#40791=CARTESIAN_POINT('Ctrl Pts',(65.8370492680559,300.137676838311,50.9749075143978));
#40792=CARTESIAN_POINT('Ctrl Pts',(71.7758589926117,299.501208809654,44.2136424516264));
#40793=CARTESIAN_POINT('Ctrl Pts',(80.6559380768304,298.864740780997,45.5617955657014));
#40794=CARTESIAN_POINT('Ctrl Pts',(84.3358153569538,298.22827275234,53.7551968474773));
#40795=CARTESIAN_POINT('Ctrl Pts',(79.4145706112079,297.591804723683,61.2894862198068));
#40796=CARTESIAN_POINT('Ctrl Pts',(71.9381583745758,297.061414699802,61.2176968040063));
#40797=CARTESIAN_POINT('Ctrl Pts',(68.0232356244143,296.637102680698,57.4239073011965));
#40798=CARTESIAN_POINT('Ctrl Pts',(66.2773409644892,296.212790661593,52.2594798626694));
#40799=CARTESIAN_POINT('Ctrl Pts',(69.4219109861495,295.682400637713,45.4761493362127));
#40800=CARTESIAN_POINT('Ctrl Pts',(78.3392462538169,295.045932609055,44.2656544301752));
#40801=CARTESIAN_POINT('Ctrl Pts',(84.1596613442124,294.409464580399,51.1064211661828));
#40802=CARTESIAN_POINT('Ctrl Pts',(81.5653181651201,293.772996551741,59.7054155742559));
#40803=CARTESIAN_POINT('Ctrl Pts',(72.9093482796908,293.136528523085,62.1667874551533));
#40804=CARTESIAN_POINT('Ctrl Pts',(67.3117508498048,292.606138499203,57.2100953459727));
#40805=CARTESIAN_POINT('Ctrl Pts',(66.8436875947261,292.1818264801,51.7786705125969));
#40806=CARTESIAN_POINT('Ctrl Pts',(68.9120002794622,291.757514460994,46.7347096117251));
#40807=CARTESIAN_POINT('Ctrl Pts',(75.7341607948001,291.227124437114,43.6752947076548));
#40808=CARTESIAN_POINT('Ctrl Pts',(83.2604808230956,290.590656408457,48.6087187746907));
#40809=CARTESIAN_POINT('Ctrl Pts',(83.1691981735905,289.9541883798,57.5900877593652));
#40810=CARTESIAN_POINT('Ctrl Pts',(75.571876221788,289.317720351143,62.3811231925081));
#40811=CARTESIAN_POINT('Ctrl Pts',(67.422651578918,288.681252322486,58.5634925249907));
#40812=CARTESIAN_POINT('Ctrl Pts',(66.4467208862754,288.150862298605,51.1507027036456));
#40813=CARTESIAN_POINT('Ctrl Pts',(69.6548705620827,287.7265502795,46.7430690313694));
#40814=CARTESIAN_POINT('Ctrl Pts',(74.5239065903062,287.302238260396,44.2911418123788));
#40815=CARTESIAN_POINT('Ctrl Pts',(81.6807633712101,286.771848236515,46.4547717876539));
#40816=CARTESIAN_POINT('Ctrl Pts',(84.1281320986843,286.135380207858,55.1147113085348));
#40817=CARTESIAN_POINT('Ctrl Pts',(78.1698806835492,285.498912179201,61.835764904141));
#40818=CARTESIAN_POINT('Ctrl Pts',(69.2923073332586,284.862444150544,60.4712090162484));
#40819=CARTESIAN_POINT('Ctrl Pts',(65.6429905038059,284.225976121887,52.2452347352405));
#40820=CARTESIAN_POINT('Ctrl Pts',(69.7669376769983,283.695586098006,46.0086528697471));
#40821=CARTESIAN_POINT('Ctrl Pts',(75.0792902129726,283.271274078902,44.7845738425221));
#40822=CARTESIAN_POINT('Ctrl Pts',(80.3631965402376,282.846962059797,46.1261374288099));
#40823=CARTESIAN_POINT('Ctrl Pts',(84.3478524431245,282.316572035916,52.4526223128409));
#40824=CARTESIAN_POINT('Ctrl Pts',(80.5170464309942,281.68010400726,60.5956617632522));
#40825=CARTESIAN_POINT('Ctrl Pts',(71.6114005142047,281.043635978602,61.7630486595907));
#40826=CARTESIAN_POINT('Ctrl Pts',(65.8036330010486,280.407167949946,54.9115409514946));
#40827=CARTESIAN_POINT('Ctrl Pts',(68.442408261578,279.770699921289,46.3079933507691));
#40828=CARTESIAN_POINT('Ctrl Pts',(75.6454776805482,279.240309897407,44.303577077192));
#40829=CARTESIAN_POINT('Ctrl Pts',(80.4589526316782,278.815997878304,46.8628578015768));
#40830=CARTESIAN_POINT('Ctrl Pts',(83.5685876035802,278.391685859198,51.3405390399957));
#40831=CARTESIAN_POINT('Ctrl Pts',(82.4285404572061,277.861295835319,58.7298682488162));
#40832=CARTESIAN_POINT('Ctrl Pts',(74.1966746279617,277.22482780666,62.3658758344585));
#40833=CARTESIAN_POINT('Ctrl Pts',(66.7074471491151,276.588359778005,57.407570364738));
#40834=CARTESIAN_POINT('Ctrl Pts',(66.8153218403697,275.951891749346,48.4263853420385));
#40835=CARTESIAN_POINT('Ctrl Pts',(74.4491755527711,275.315423720691,43.6610476109663));
#40836=CARTESIAN_POINT('Ctrl Pts',(81.2018256402978,274.785033696809,46.8709713558098));
#40837=CARTESIAN_POINT('Ctrl Pts',(83.1577951796486,274.360721677705,51.9595509309462));
#40838=CARTESIAN_POINT('Ctrl Pts',(82.5694214441079,273.9364096586,57.3792626648571));
#40839=CARTESIAN_POINT('Ctrl Pts',(76.8633002952122,273.406019634719,62.210626352928));
#40840=CARTESIAN_POINT('Ctrl Pts',(68.2640318319858,272.769551606063,59.5579393961078));
#40841=CARTESIAN_POINT('Ctrl Pts',(65.8609833098742,272.133083577405,50.9035370966215));
#40842=CARTESIAN_POINT('Ctrl Pts',(71.8316410442895,271.496615548749,44.1935022547268));
#40843=CARTESIAN_POINT('Ctrl Pts',(80.7199450811446,270.860147520091,45.6014147313923));
#40844=CARTESIAN_POINT('Ctrl Pts',(83.7133420812205,270.329757496211,52.4527991208584));
#40845=CARTESIAN_POINT('Ctrl Pts',(81.8533709346943,269.905445477106,57.5772470194573));
#40846=CARTESIAN_POINT('Ctrl Pts',(77.8552946903246,269.481133458002,61.2833022370128));
#40847=CARTESIAN_POINT('Ctrl Pts',(70.3791286576398,268.950743434121,61.189307003014));
#40848=CARTESIAN_POINT('Ctrl Pts',(65.6261439501125,268.314275405464,53.5477559455689));
#40849=CARTESIAN_POINT('Ctrl Pts',(69.4867806917746,267.677807376807,45.4379590732729));
#40850=CARTESIAN_POINT('Ctrl Pts',(78.394568044232,267.04133934815,44.2870264756042));
#40851=CARTESIAN_POINT('Ctrl Pts',(84.1820070775441,266.404871319493,51.1783047045848));
#40852=CARTESIAN_POINT('Ctrl Pts',(81.9493708504318,265.874481295612,58.3139356598449));
#40853=CARTESIAN_POINT('Ctrl Pts',(77.1848545790382,265.450169276508,60.9632456890776));
#40854=CARTESIAN_POINT('Ctrl Pts',(71.7361540343936,265.025857257403,61.1396580076683));
#40855=CARTESIAN_POINT('Ctrl Pts',(66.1533034599807,264.495467233522,56.1663620064171));
#40856=CARTESIAN_POINT('Ctrl Pts',(67.5755898002831,263.858999204865,47.2803467149763));
#40857=CARTESIAN_POINT('Ctrl Pts',(75.8081796701991,263.222531176208,43.6889980275431));
#40858=CARTESIAN_POINT('Ctrl Pts',(83.2882343864571,262.586063147551,48.6611306487392));
#40859=CARTESIAN_POINT('Ctrl Pts',(83.1389331100811,261.949595118894,57.6590123618092));
#40860=CARTESIAN_POINT('Ctrl Pts',(76.7742670496182,261.419205095014,61.5823935045322));
#40861=CARTESIAN_POINT('Ctrl Pts',(71.4398434719161,260.994893075909,60.4583899346883));
#40862=CARTESIAN_POINT('Ctrl Pts',(67.2104103072712,260.570581056805,57.0187163982657));
#40863=CARTESIAN_POINT('Ctrl Pts',(66.2565010855456,260.040191032923,49.6030606046766));
#40864=CARTESIAN_POINT('Ctrl Pts',(73.1571307501172,259.403723004267,43.8267749100486));
#40865=CARTESIAN_POINT('Ctrl Pts',(81.7276617814507,258.767254975609,46.5136539921665));
#40866=CARTESIAN_POINT('Ctrl Pts',(84.1147180442186,258.130786946953,55.1724809196061));
#40867=CARTESIAN_POINT('Ctrl Pts',(78.1018348621412,257.494318918295,61.867957156008));
#40868=CARTESIAN_POINT('Ctrl Pts',(70.7238585278493,256.963928894415,60.6566112669601));
#40869=CARTESIAN_POINT('Ctrl Pts',(67.4334230143906,256.53961687531,56.3100617086169));
#40870=CARTESIAN_POINT('Ctrl Pts',(66.4957015356938,256.115304856205,50.9397602869315));
#40871=CARTESIAN_POINT('Ctrl Pts',(70.6381541596617,255.584914832325,44.7154547103664));
#40872=CARTESIAN_POINT('Ctrl Pts',(79.6357826280725,254.948446803668,44.8793087245797));
#40873=CARTESIAN_POINT('Ctrl Pts',(84.3446499226267,254.311978775011,52.5278308147126));
#40874=CARTESIAN_POINT('Ctrl Pts',(80.4690377153397,253.675510746354,60.6304817006697));
#40875=CARTESIAN_POINT('Ctrl Pts',(71.5389167422275,253.039042717697,61.7427341895921));
#40876=CARTESIAN_POINT('Ctrl Pts',(66.762877011925,252.508652693816,55.9902270712261));
#40877=CARTESIAN_POINT('Ctrl Pts',(67.1287601229746,252.084340674712,50.5509634739719));
#40878=CARTESIAN_POINT('Ctrl Pts',(69.9422387447338,251.660028655607,45.8815098682203));
#40879=CARTESIAN_POINT('Ctrl Pts',(77.1512298269574,251.129638631726,43.8984966991504));
#40880=CARTESIAN_POINT('Ctrl Pts',(83.8369722296532,250.493170603069,49.9222011007897));
#40881=CARTESIAN_POINT('Ctrl Pts',(82.3768062577141,249.856702574412,58.7845504899393));
#40882=CARTESIAN_POINT('Ctrl Pts',(74.1375957721407,249.220234545756,62.3606841473118));
#40883=CARTESIAN_POINT('Ctrl Pts',(66.6660428528195,248.583766517098,57.3447033691071));
#40884=CARTESIAN_POINT('Ctrl Pts',(66.8322241000219,248.053376493218,49.8697935070852));
#40885=CARTESIAN_POINT('Ctrl Pts',(70.6751412031906,247.629064474113,46.0030833977625));
#40886=CARTESIAN_POINT('Ctrl Pts',(75.8612007292659,247.204752455009,44.3225342246141));
#40887=CARTESIAN_POINT('Ctrl Pts',(82.6042870466499,246.674362431127,47.5525002567253));
#40888=CARTESIAN_POINT('Ctrl Pts',(83.7020947420946,246.037894402471,56.4844084771085));
#40889=CARTESIAN_POINT('Ctrl Pts',(76.7883844442563,245.401426373813,62.2179877500005));
#40890=CARTESIAN_POINT('Ctrl Pts',(68.2228317834295,244.764958345157,59.5152800381715));
#40891=CARTESIAN_POINT('Ctrl Pts',(65.8709468103568,244.128490316499,50.8289227310511));
#40892=CARTESIAN_POINT('Ctrl Pts',(70.8979193573472,243.598100292619,45.2943549372585));
#40893=CARTESIAN_POINT('Ctrl Pts',(76.3348210323808,243.173788273514,44.8949064332121));
#40894=CARTESIAN_POINT('Ctrl Pts',(81.3522652511927,242.74947625441,47.0267395510882));
#40895=CARTESIAN_POINT('Ctrl Pts',(84.3252993449719,242.219086230529,53.8869845853058));
#40896=CARTESIAN_POINT('Ctrl Pts',(79.297240837648,241.582618201872,61.3504150191248));
#40897=CARTESIAN_POINT('Ctrl Pts',(70.3177403128524,240.946150173215,61.1457404330823));
#40898=CARTESIAN_POINT('Ctrl Pts',(65.6230109474603,240.309682144558,53.4885322246883));
#40899=CARTESIAN_POINT('Ctrl Pts',(69.5432298218416,239.673214115901,45.3881587659845));
#40900=CARTESIAN_POINT('Ctrl Pts',(76.967750906386,239.142824092021,44.5059001205523));
#40901=CARTESIAN_POINT('Ctrl Pts',(81.3345269806457,238.718512072916,47.769445071773));
#40902=CARTESIAN_POINT('Ctrl Pts',(83.724782060455,238.294200053811,52.6690511360203));
#40903=CARTESIAN_POINT('Ctrl Pts',(81.4709617211638,237.76381002993,59.7980193313823));
#40904=CARTESIAN_POINT('Ctrl Pts',(72.7808118995323,237.127342001274,62.1358521464321));
#40905=CARTESIAN_POINT('Ctrl Pts',(66.1355232304304,236.490873972616,56.0932153159349));
#40906=CARTESIAN_POINT('Ctrl Pts',(67.612059031172,235.85440594396,47.2335785632174));
#40907=CARTESIAN_POINT('Ctrl Pts',(75.8834540617522,235.217937915302,43.6884141888023));
#40908=CARTESIAN_POINT('Ctrl Pts',(82.0674696356908,234.687547891422,47.8907760287162));
#40909=CARTESIAN_POINT('Ctrl Pts',(83.2243770613147,234.263235872317,53.2181603906615));
#40910=CARTESIAN_POINT('Ctrl Pts',(81.8162055485238,233.838923853213,58.4847068797696));
#40911=CARTESIAN_POINT('Ctrl Pts',(75.4399144954396,233.308533829332,62.3891666450382));
#40912=CARTESIAN_POINT('Ctrl Pts',(67.345892088715,232.672065800675,58.4558515708228));
#40913=CARTESIAN_POINT('Ctrl Pts',(66.291041376437,232.035597772018,49.5361760534184));
#40914=CARTESIAN_POINT('Ctrl Pts',(73.2153321012232,231.399129743361,43.8153789656575));
#40915=CARTESIAN_POINT('Ctrl Pts',(81.7848765901179,230.762661714704,46.5625727059977));
#40916=CARTESIAN_POINT('Ctrl Pts',(83.698186774302,230.232271690823,53.7903758156054));
#40917=CARTESIAN_POINT('Ctrl Pts',(81.0783348798918,229.807959671719,58.5711534701399));
#40918=CARTESIAN_POINT('Ctrl Pts',(76.5617481587882,229.383647652614,61.6240051409511));
#40919=CARTESIAN_POINT('Ctrl Pts',(69.1874022588527,228.853257628733,60.3907508304615));
#40920=CARTESIAN_POINT('Ctrl Pts',(65.6556204535641,228.216789600076,52.1136327645463));
#40921=CARTESIAN_POINT('Ctrl Pts',(70.7080900492044,227.580321571419,44.687606077119));
#40922=CARTESIAN_POINT('Ctrl Pts',(79.687197132215,226.943853542762,44.9088690599485));
#40923=CARTESIAN_POINT('Ctrl Pts',(84.3557695970477,226.307385514105,52.6022816558166));
#40924=CARTESIAN_POINT('Ctrl Pts',(81.0608424149524,225.776995490225,59.3138648216729));
#40925=CARTESIAN_POINT('Ctrl Pts',(75.9479723037787,225.35268347112,61.2054297859663));
#40926=CARTESIAN_POINT('Ctrl Pts',(70.5361213944014,224.928371452016,60.5486734034489));
#40927=CARTESIAN_POINT('Ctrl Pts',(65.7771886512274,224.397981428134,54.7820060528674));
#40928=CARTESIAN_POINT('Ctrl Pts',(68.5382388443865,223.761513399478,46.216916024055));
#40929=CARTESIAN_POINT('Ctrl Pts',(77.2222924846526,223.125045370821,43.9233299437037));
#40930=CARTESIAN_POINT('Ctrl Pts',(83.8564062843967,222.488577342164,49.9782330272043));
#40931=CARTESIAN_POINT('Ctrl Pts',(82.3363825504368,221.852109313506,58.848052098875));
#40932=CARTESIAN_POINT('Ctrl Pts',(75.4477482643877,221.321719289626,61.7547047329954));
#40933=CARTESIAN_POINT('Ctrl Pts',(70.3471947930426,220.897407270521,59.8301800696257));
#40934=CARTESIAN_POINT('Ctrl Pts',(66.6919112490471,220.473095251417,55.7856301591708));
#40935=CARTESIAN_POINT('Ctrl Pts',(66.880301523413,219.942705227536,48.3112457941265));
#40936=CARTESIAN_POINT('Ctrl Pts',(74.5812401565408,219.306237198879,43.6551244884603));
#40937=CARTESIAN_POINT('Ctrl Pts',(82.6416720877777,218.669769170222,47.6178447743592));
#40938=CARTESIAN_POINT('Ctrl Pts',(83.6799939691614,218.033301141565,56.5394601953136));
#40939=CARTESIAN_POINT('Ctrl Pts',(76.7162878641993,217.396833112908,62.2394157987944));
#40940=CARTESIAN_POINT('Ctrl Pts',(69.6092409969674,216.866443089027,59.9168855034723));
#40941=CARTESIAN_POINT('Ctrl Pts',(67.0205576898783,216.442131069923,55.1192648449001));
#40942=CARTESIAN_POINT('Ctrl Pts',(66.9124473478813,216.017819050818,49.6688377131259));
#40943=CARTESIAN_POINT('Ctrl Pts',(71.9569601804353,215.487429026937,44.1490780730461));
#40944=CARTESIAN_POINT('Ctrl Pts',(80.8222636492987,214.85096099828,45.6837141077411));
#40945=CARTESIAN_POINT('Ctrl Pts',(84.3130014825699,214.214492969623,53.9605188524692));
#40946=CARTESIAN_POINT('Ctrl Pts',(79.2400908333381,213.578024940966,61.3780748791543));
#40947=CARTESIAN_POINT('Ctrl Pts',(70.2576310661073,212.94155691231,61.1135443626181));
#40948=CARTESIAN_POINT('Ctrl Pts',(65.6207844274967,212.305088883652,53.420014571099));
#40949=CARTESIAN_POINT('Ctrl Pts',(69.5979250829234,211.668620854996,45.3496325751228));
#40950=CARTESIAN_POINT('Ctrl Pts',(77.0293989008466,211.138230831115,44.5201429154035));
#40951=CARTESIAN_POINT('Ctrl Pts',(81.3721622592396,210.71391881201,47.8154805578659));
#40952=CARTESIAN_POINT('Ctrl Pts',(83.7271839203301,210.289606792905,52.7320157427041));
#40953=CARTESIAN_POINT('Ctrl Pts',(81.4218657451715,209.759216769025,59.8446643532429));
#40954=CARTESIAN_POINT('Ctrl Pts',(72.7151407986123,209.122748740368,62.1196670571768));
#40955=CARTESIAN_POINT('Ctrl Pts',(66.1135889180742,208.486280711711,56.0292773473689));
#40956=CARTESIAN_POINT('Ctrl Pts',(67.6540268194141,207.849812683054,47.1805053390905));
#40957=CARTESIAN_POINT('Ctrl Pts',(75.9507747452419,207.213344654397,43.6951222468685));
#40958=CARTESIAN_POINT('Ctrl Pts',(82.1043148718093,206.682954630516,47.9419865539333));
#40959=CARTESIAN_POINT('Ctrl Pts',(83.2227524914535,206.258642611411,53.2775820273672));
#40960=CARTESIAN_POINT('Ctrl Pts',(81.7766207124032,205.834330592307,58.5338300971972));
#40961=CARTESIAN_POINT('Ctrl Pts',(75.3723240203356,205.303940568426,62.3921841170279));
#40962=CARTESIAN_POINT('Ctrl Pts',(67.3068916918394,204.667472539769,58.4005724286968));
#40963=CARTESIAN_POINT('Ctrl Pts',(66.3164237824365,204.031004511112,49.4735185709573));
#40964=CARTESIAN_POINT('Ctrl Pts',(73.2818100437565,203.394536482455,43.802829109735));
#40965=CARTESIAN_POINT('Ctrl Pts',(81.8313103627761,202.758068453799,46.6117808120413));
#40966=CARTESIAN_POINT('Ctrl Pts',(83.6924220806197,202.227678429917,53.853200311008));
#40967=CARTESIAN_POINT('Ctrl Pts',(81.0381449774921,201.803366410813,58.6149512779444));
#40968=CARTESIAN_POINT('Ctrl Pts',(76.499649456248,201.379054391708,61.635136237765));
#40969=CARTESIAN_POINT('Ctrl Pts',(69.1343934412748,200.848664367828,60.3487080192437));
#40970=CARTESIAN_POINT('Ctrl Pts',(65.6624230963692,200.21219633917,52.0463235332207));
#40971=CARTESIAN_POINT('Ctrl Pts',(70.7683400725564,199.575728310514,44.6569437792745));
#40972=CARTESIAN_POINT('Ctrl Pts',(79.7456170301404,198.939260281857,44.9429853917731));
#40973=CARTESIAN_POINT('Ctrl Pts',(84.3585598878715,198.3027922532,52.6698815596127));
#40974=CARTESIAN_POINT('Ctrl Pts',(81.0152943056921,197.772402229319,59.3575170829689));
#40975=CARTESIAN_POINT('Ctrl Pts',(75.8889095924911,197.348090210215,61.2121433810362));
#40976=CARTESIAN_POINT('Ctrl Pts',(70.4819380791528,196.92377819111,60.5163575054332));
#40977=CARTESIAN_POINT('Ctrl Pts',(65.7647357358894,196.393388167229,54.7155044901546));
#40978=CARTESIAN_POINT('Ctrl Pts',(68.5875114199334,195.756920138572,46.1705584030409));
#40979=CARTESIAN_POINT('Ctrl Pts',(77.2878870962725,195.120452109915,43.9396876198568));
#40980=CARTESIAN_POINT('Ctrl Pts',(83.8781423559844,194.483984081258,50.042298288482));
#40981=CARTESIAN_POINT('Ctrl Pts',(82.2941616241956,193.847516052601,58.9009195827315));
#40982=CARTESIAN_POINT('Ctrl Pts',(75.3847363513986,193.31712602872,61.7577948078464));
#40983=CARTESIAN_POINT('Ctrl Pts',(70.2981992521546,192.892814009616,59.796519898665));
#40984=CARTESIAN_POINT('Ctrl Pts',(66.6721959932454,192.468501990511,55.7257018853234));
#40985=CARTESIAN_POINT('Ctrl Pts',(66.9145010625479,191.938111966631,48.2528723070669));
#40986=CARTESIAN_POINT('Ctrl Pts',(74.648847973789,191.301643937973,43.6524327574035));
#40987=CARTESIAN_POINT('Ctrl Pts',(82.680452897193,190.665175909317,47.6732092639168));
#40988=CARTESIAN_POINT('Ctrl Pts',(83.6544270164244,190.028707880659,56.6020779367127));
#40989=CARTESIAN_POINT('Ctrl Pts',(76.6496815131711,189.392239852003,62.2516537285915));
#40990=CARTESIAN_POINT('Ctrl Pts',(69.5597509643709,188.861849828122,59.8778848970763));
#40991=CARTESIAN_POINT('Ctrl Pts',(67.0054911824049,188.437537809017,55.0617437137643));
#40992=CARTESIAN_POINT('Ctrl Pts',(66.9372166834158,188.013225789912,49.6106156172916));
#40993=CARTESIAN_POINT('Ctrl Pts',(72.0202984177305,187.482835766032,44.1275349380969));
#40994=CARTESIAN_POINT('Ctrl Pts',(80.8763462373005,186.846367737374,45.7258412951564));
#40995=CARTESIAN_POINT('Ctrl Pts',(84.3036521127895,186.209899708718,54.0280636360005));
#40996=CARTESIAN_POINT('Ctrl Pts',(79.1840926941306,185.573431680061,61.4079981018203));
#40997=CARTESIAN_POINT('Ctrl Pts',(70.1909442437265,184.936963651404,61.0802067924056));
#40998=CARTESIAN_POINT('Ctrl Pts',(66.394611359777,184.406573627523,54.6389530102197));
#40999=CARTESIAN_POINT('Ctrl Pts',(67.6242295079782,183.982261608419,49.3278798473855));
#41000=CARTESIAN_POINT('Ctrl Pts',(71.1471386294461,183.557949589314,45.167522861111));
#41001=CARTESIAN_POINT('Ctrl Pts',(78.5802604721558,183.027559565433,44.3609292064653));
#41002=CARTESIAN_POINT('Ctrl Pts',(84.2184995867349,182.391091536776,51.3748030205826));
#41003=CARTESIAN_POINT('Ctrl Pts',(81.3621086629095,181.754623508119,59.8903389550533));
#41004=CARTESIAN_POINT('Ctrl Pts',(72.6576265185261,181.118155479462,62.1051328414189));
#41005=CARTESIAN_POINT('Ctrl Pts',(66.0827647583405,180.481687450805,55.9605938816611));
#41006=CARTESIAN_POINT('Ctrl Pts',(67.4402524491558,179.951297426925,48.6081030913529));
#41007=CARTESIAN_POINT('Ctrl Pts',(71.8512292228023,179.52698540782,45.4045514944974));
#41008=CARTESIAN_POINT('Ctrl Pts',(77.2390781242549,179.102673388715,44.5735622367552));
#41009=CARTESIAN_POINT('Ctrl Pts',(83.3799716108488,178.572283364835,48.8386907035881));
#41010=CARTESIAN_POINT('Ctrl Pts',(83.0376354525052,177.935815336178,57.83129723052));
#41011=CARTESIAN_POINT('Ctrl Pts',(75.2971941772932,177.299347307521,62.3874897446671));
#41012=CARTESIAN_POINT('Ctrl Pts',(67.2730309492928,176.662879278864,58.351882497749));
#41013=CARTESIAN_POINT('Ctrl Pts',(66.3381724278209,176.026411250207,49.4014520199251));
#41014=CARTESIAN_POINT('Ctrl Pts',(72.1843046459954,175.496021226326,44.7404830498607));
#41015=CARTESIAN_POINT('Ctrl Pts',(77.6152384240311,175.071709207222,45.2142100070392));
#41016=CARTESIAN_POINT('Ctrl Pts',(82.2279530476807,174.647397188116,48.1197775474917));
#41017=CARTESIAN_POINT('Ctrl Pts',(84.0675483467432,174.117007164236,55.3666929456424));
#41018=CARTESIAN_POINT('Ctrl Pts',(77.9123834182491,173.480539135579,61.9316080933473));
#41019=CARTESIAN_POINT('Ctrl Pts',(69.0807483806694,172.844071106922,60.2958990960111));
#41020=CARTESIAN_POINT('Ctrl Pts',(65.668785894465,172.207603078265,51.9873593113253));
#41021=CARTESIAN_POINT('Ctrl Pts',(70.8320161622452,171.571135049608,44.6167949234776));
#41022=CARTESIAN_POINT('Ctrl Pts',(78.3021576349833,171.040745025728,44.9312468745954));
#41023=CARTESIAN_POINT('Ctrl Pts',(82.0918625454198,170.616433006623,48.850123706441));
#41024=CARTESIAN_POINT('Ctrl Pts',(83.6691886717045,170.192120987518,54.0685047985716));
#41025=CARTESIAN_POINT('Ctrl Pts',(80.3060744937362,169.661730963637,60.7461807923759));
#41026=CARTESIAN_POINT('Ctrl Pts',(71.3541437074611,169.025262934981,61.6665619043428));
#41027=CARTESIAN_POINT('Ctrl Pts',(65.7588621303524,168.388794906323,54.6404573339678));
#41028=CARTESIAN_POINT('Ctrl Pts',(68.6309797965831,167.752326877667,46.1302128326447));
#41029=CARTESIAN_POINT('Ctrl Pts',(77.3622890976487,167.11585884901,43.9511295201827));
#41030=CARTESIAN_POINT('Ctrl Pts',(82.7960315486792,166.585468825129,49.0869192966586));
#41031=CARTESIAN_POINT('Ctrl Pts',(83.0875324231865,166.161156806024,54.5306759197567));
#41032=CARTESIAN_POINT('Ctrl Pts',(80.8565720249266,165.73684478692,59.5048366160715));
#41033=CARTESIAN_POINT('Ctrl Pts',(73.9386918548011,165.206454763039,62.3411771464144));
#41034=CARTESIAN_POINT('Ctrl Pts',(66.5764879777522,164.569986734382,57.166032678258));
#41035=CARTESIAN_POINT('Ctrl Pts',(66.9592770116748,163.933518705725,48.1923604134332));
#41036=CARTESIAN_POINT('Ctrl Pts',(74.7081221966236,163.297050677068,43.6504753795876));
#41037=CARTESIAN_POINT('Ctrl Pts',(82.7291234421973,162.660582648411,47.7306353289073));
#41038=CARTESIAN_POINT('Ctrl Pts',(83.463904735118,162.13019262453,55.1711991586084));
#41039=CARTESIAN_POINT('Ctrl Pts',(80.1143646250949,161.705880605426,59.4723664400229));
#41040=CARTESIAN_POINT('Ctrl Pts',(75.1682999312516,161.281568586321,61.7649420605167));
#41041=CARTESIAN_POINT('Ctrl Pts',(68.0854511270769,160.75117856244,59.3701254768339));
#41042=CARTESIAN_POINT('Ctrl Pts',(65.9204924507741,160.114710533783,50.6353032048341));
#41043=CARTESIAN_POINT('Ctrl Pts',(72.0937834729716,159.478242505126,44.1112094504318));
#41044=CARTESIAN_POINT('Ctrl Pts',(80.9223816280249,158.841774476469,45.7632312352661));
#41045=CARTESIAN_POINT('Ctrl Pts',(84.3027423805713,158.205306447812,54.1033347943454));
#41046=CARTESIAN_POINT('Ctrl Pts',(79.9785158501795,157.674916423932,60.2027576003278));
#41047=CARTESIAN_POINT('Ctrl Pts',(74.6292268764211,157.250604404827,61.2537411428208));
#41048=CARTESIAN_POINT('Ctrl Pts',(69.3916553792759,156.826292385722,59.7413576783326));
#41049=CARTESIAN_POINT('Ctrl Pts',(65.6144707901074,156.295902361841,53.288856594905));
#41050=CARTESIAN_POINT('Ctrl Pts',(69.7075983555732,155.659434333185,45.274464981916));
#41051=CARTESIAN_POINT('Ctrl Pts',(78.64644657324,155.022966304528,44.3967896988572));
#41052=CARTESIAN_POINT('Ctrl Pts',(84.2287385638327,154.386498275871,51.4332190129864));
#41053=CARTESIAN_POINT('Ctrl Pts',(81.3120644269999,153.750030247214,59.9465719466464));
#41054=CARTESIAN_POINT('Ctrl Pts',(74.0477236227788,153.219640223333,61.7161047472509));
#41055=CARTESIAN_POINT('Ctrl Pts',(69.3198652774232,152.795328204229,59.0019171344252));
#41056=CARTESIAN_POINT('Ctrl Pts',(66.3572243229997,152.371016185123,54.4256503691965));
#41057=CARTESIAN_POINT('Ctrl Pts',(67.7365440944563,151.840626161243,47.0772239648329));
#41058=CARTESIAN_POINT('Ctrl Pts',(76.0821040501351,151.204158132586,43.710356693956));
#41059=CARTESIAN_POINT('Ctrl Pts',(83.406427223103,150.567690103929,48.9091653477627));
#41060=CARTESIAN_POINT('Ctrl Pts',(83.0070608638056,149.931222075272,57.8821151343176));
#41061=CARTESIAN_POINT('Ctrl Pts',(75.2225373742539,149.294754046615,62.3971301103889));
#41062=CARTESIAN_POINT('Ctrl Pts',(68.5776471717109,148.764364022734,58.9696926057169));
#41063=CARTESIAN_POINT('Ctrl Pts',(66.7878946983978,148.34005200363,53.8202999215615));
#41064=CARTESIAN_POINT('Ctrl Pts',(67.5518938036794,147.915739984525,48.4225444344639));
#41065=CARTESIAN_POINT('Ctrl Pts',(73.4118440549937,147.385349960644,43.7789599672223));
#41066=CARTESIAN_POINT('Ctrl Pts',(81.9204685029185,146.748881931987,46.7093995584277));
#41067=CARTESIAN_POINT('Ctrl Pts',(84.0413100822046,146.112413903331,55.4372487984491));
#41068=CARTESIAN_POINT('Ctrl Pts',(77.8559769716525,145.475945874673,61.9499268706774));
#41069=CARTESIAN_POINT('Ctrl Pts',(69.0180612333034,144.839477846017,60.2542230063861));
#41070=CARTESIAN_POINT('Ctrl Pts',(66.2486524828672,144.309087822136,53.3092774468237));
#41071=CARTESIAN_POINT('Ctrl Pts',(68.2739939265614,143.884775803031,48.2479089591696));
#41072=CARTESIAN_POINT('Ctrl Pts',(72.3902695459265,143.460463783926,44.6735930866159));
#41073=CARTESIAN_POINT('Ctrl Pts',(79.8594440960063,142.930073760046,45.0102311603966));
#41074=CARTESIAN_POINT('Ctrl Pts',(84.3618626866762,142.293605731389,52.8020469325975));
#41075=CARTESIAN_POINT('Ctrl Pts',(80.2399992388539,141.657137702732,60.7822451180113));
#41076=CARTESIAN_POINT('Ctrl Pts',(71.2995448559428,141.020669674075,61.6434052587863));
#41077=CARTESIAN_POINT('Ctrl Pts',(65.7388616677646,140.384201645418,54.5678862902412));
#41078=CARTESIAN_POINT('Ctrl Pts',(68.2019590988151,139.853811621537,47.5084922158581));
#41079=CARTESIAN_POINT('Ctrl Pts',(73.049966590537,139.429499602433,45.0152448772302));
#41080=CARTESIAN_POINT('Ctrl Pts',(78.5015222053076,139.005187583328,45.0158020357968));
#41081=CARTESIAN_POINT('Ctrl Pts',(83.919986575027,138.474797559447,50.1677082389766));
#41082=CARTESIAN_POINT('Ctrl Pts',(82.2099907202014,137.83832953079,59.0028698317267));
#41083=CARTESIAN_POINT('Ctrl Pts',(73.8651568290306,137.201861502133,62.3250782372519));
#41084=CARTESIAN_POINT('Ctrl Pts',(66.5504504432737,136.565393473476,57.1127474868928));
#41085=CARTESIAN_POINT('Ctrl Pts',(66.9917635648296,135.928925444819,48.124454605468));
#41086=CARTESIAN_POINT('Ctrl Pts',(73.480436591811,135.398535420938,44.4097519254127));
#41087=CARTESIAN_POINT('Ctrl Pts',(78.7755611796576,134.974223401834,45.7063299333033));
#41088=CARTESIAN_POINT('Ctrl Pts',(82.8911061103094,134.549911382729,49.2814871123865));
#41089=CARTESIAN_POINT('Ctrl Pts',(83.6037845027795,134.019521358848,56.7242005397054));
#41090=CARTESIAN_POINT('Ctrl Pts',(76.5192810884573,133.383053330192,62.2734326997418));
#41091=CARTESIAN_POINT('Ctrl Pts',(68.0404888765095,132.746585301534,59.3097518823143));
#41092=CARTESIAN_POINT('Ctrl Pts',(65.935774761008,132.110117272878,50.577999489296));
#41093=CARTESIAN_POINT('Ctrl Pts',(72.1628384614155,131.473649244221,44.08124307824));
#41094=CARTESIAN_POINT('Ctrl Pts',(79.4976034645514,130.94325922034,45.531455476841));
#41095=CARTESIAN_POINT('Ctrl Pts',(82.6452064879334,130.518947201235,49.9825288461035));
#41096=CARTESIAN_POINT('Ctrl Pts',(83.4081022570692,130.094635182131,55.3804403845415));
#41097=CARTESIAN_POINT('Ctrl Pts',(79.0657785435674,129.56424515825,61.4669926450126));
#41098=CARTESIAN_POINT('Ctrl Pts',(70.0782111864052,128.927777129593,61.0111426762753));
#41099=CARTESIAN_POINT('Ctrl Pts',(65.6201130519864,128.291309100936,53.2137916911737));
#41100=CARTESIAN_POINT('Ctrl Pts',(69.7567120988123,127.654841072279,45.241221861641));
#41101=CARTESIAN_POINT('Ctrl Pts',(78.7182326925333,127.018373043622,44.4194464410791));
#41102=CARTESIAN_POINT('Ctrl Pts',(83.3050165716072,126.487983019741,50.323962280583));
#41103=CARTESIAN_POINT('Ctrl Pts',(82.7627561352269,126.063671000637,55.7484818492179));
#41104=CARTESIAN_POINT('Ctrl Pts',(79.7991798376885,125.639358981532,60.3241429446261));
#41105=CARTESIAN_POINT('Ctrl Pts',(72.5296152817953,125.108968957651,62.0720916910074));
#41106=CARTESIAN_POINT('Ctrl Pts',(66.0429388543689,124.472500928994,55.8345284553034));
#41107=CARTESIAN_POINT('Ctrl Pts',(67.7900261310386,123.836032900337,47.0242499461599));
#41108=CARTESIAN_POINT('Ctrl Pts',(76.1409832360778,123.19956487168,43.7174634712323));
#41109=CARTESIAN_POINT('Ctrl Pts',(83.4457689004487,122.563096843024,48.9733432825609));
#41110=CARTESIAN_POINT('Ctrl Pts',(83.0370236359612,122.032706819143,56.438919011267));
#41111=CARTESIAN_POINT('Ctrl Pts',(79.0706101813766,121.608394800038,60.1788419033402));
#41112=CARTESIAN_POINT('Ctrl Pts',(73.8327296571528,121.184082780934,61.6901547582187));
#41113=CARTESIAN_POINT('Ctrl Pts',(67.1980487999333,120.653692757053,58.2429959897354));
#41114=CARTESIAN_POINT('Ctrl Pts',(66.3907685778263,120.017224728396,49.2801579996498));
#41115=CARTESIAN_POINT('Ctrl Pts',(73.48695938946,119.380756699739,43.774034379002));
#41116=CARTESIAN_POINT('Ctrl Pts',(81.9602620234156,118.744288671082,46.7533738753299));
#41117=CARTESIAN_POINT('Ctrl Pts',(84.0289296905471,118.107820642425,55.5115004031035));
#41118=CARTESIAN_POINT('Ctrl Pts',(78.8249425935863,117.577430618544,60.8799649831249));
#41119=CARTESIAN_POINT('Ctrl Pts',(73.3779393972438,117.153118599439,61.1027094789036));
#41120=CARTESIAN_POINT('Ctrl Pts',(68.4323434172374,116.728806580335,58.8091229133018));
#41121=CARTESIAN_POINT('Ctrl Pts',(65.6835744766738,116.198416556454,51.8559824024478));
#41122=CARTESIAN_POINT('Ctrl Pts',(70.9512619784509,115.561948527797,44.5597070117332));
#41123=CARTESIAN_POINT('Ctrl Pts',(79.9193858227639,114.92548049914,45.055767566542));
#41124=CARTESIAN_POINT('Ctrl Pts',(84.3630715091719,114.289012470483,52.8613411445304));
#41125=CARTESIAN_POINT('Ctrl Pts',(80.1819632346659,113.652544441826,60.8301867190402));
#41126=CARTESIAN_POINT('Ctrl Pts',(72.7327151200314,113.122154417945,61.4709645111751));
#41127=CARTESIAN_POINT('Ctrl Pts',(68.4741821526868,112.697842398841,58.0673846461795));
#41128=CARTESIAN_POINT('Ctrl Pts',(66.2442385369553,112.273530379736,53.0927680376334));
#41129=CARTESIAN_POINT('Ctrl Pts',(68.7282926279591,111.743140355855,46.0407208933463));
#41130=CARTESIAN_POINT('Ctrl Pts',(77.4897535082816,111.106672327198,43.9862210914205));
#41131=CARTESIAN_POINT('Ctrl Pts',(83.9353829353853,110.470204298542,50.2413935630175));
#41132=CARTESIAN_POINT('Ctrl Pts',(82.1720225153696,109.833736269885,59.0484294656406));
#41133=CARTESIAN_POINT('Ctrl Pts',(73.7899031570053,109.197268241228,62.3232182001498));
#41134=CARTESIAN_POINT('Ctrl Pts',(67.7455644465447,108.666878217347,57.922324744781));
#41135=CARTESIAN_POINT('Ctrl Pts',(66.7622050692158,108.242566198242,52.5601924015445));
#41136=CARTESIAN_POINT('Ctrl Pts',(68.3405978179793,107.818254179138,47.34213382943));
#41137=CARTESIAN_POINT('Ctrl Pts',(74.8402754823346,107.287864155257,43.6467199267987));
#41138=CARTESIAN_POINT('Ctrl Pts',(82.802348221357,106.6513961266,47.8407113302285));
#41139=CARTESIAN_POINT('Ctrl Pts',(83.5670911998759,106.014928097943,56.7899285886139));
#41140=CARTESIAN_POINT('Ctrl Pts',(76.4607404746586,105.378460069286,62.2829332974389));
#41141=CARTESIAN_POINT('Ctrl Pts',(67.9848922283654,104.741992040629,59.2590016349609));
#41142=CARTESIAN_POINT('Ctrl Pts',(66.3072204096844,104.211602016748,51.972897674607));
#41143=CARTESIAN_POINT('Ctrl Pts',(69.0808858451976,103.787289997644,47.2796856632862));
#41144=CARTESIAN_POINT('Ctrl Pts',(73.6941942806995,103.362977978539,44.3750610386075));
#41145=CARTESIAN_POINT('Ctrl Pts',(81.0246195689312,102.832587954658,45.847052460437));
#41146=CARTESIAN_POINT('Ctrl Pts',(84.2858470046237,102.196119926001,54.2344574110884));
#41147=CARTESIAN_POINT('Ctrl Pts',(78.9949754871697,101.559651897344,61.4925563320708));
#41148=CARTESIAN_POINT('Ctrl Pts',(70.0277833696733,100.923183868687,60.9799288953412));
#41149=CARTESIAN_POINT('Ctrl Pts',(65.6114160752346,100.28671584003,53.1390191194198));
#41150=CARTESIAN_POINT('Ctrl Pts',(69.1224790880608,99.7563258161497,46.5379335895811));
#41151=CARTESIAN_POINT('Ctrl Pts',(74.2940588091507,99.3320137970449,44.8133402694683));
#41152=CARTESIAN_POINT('Ctrl Pts',(79.6817377409247,98.9077017779405,45.645430805096));
#41153=CARTESIAN_POINT('Ctrl Pts',(84.2509640357489,98.3773117540596,51.5635440786798));
#41154=CARTESIAN_POINT('Ctrl Pts',(81.2133277182638,97.7408437254026,60.0344904128399));
#41155=CARTESIAN_POINT('Ctrl Pts',(72.4593963387556,97.1043756967459,62.0449646762496));
#41156=CARTESIAN_POINT('Ctrl Pts',(66.0253337278694,96.4679076680886,55.7778952111669));
#41157=CARTESIAN_POINT('Ctrl Pts',(67.8324903896393,95.8314396394319,46.9620940000828));
#41158=CARTESIAN_POINT('Ctrl Pts',(74.8118490485081,95.3010496155511,44.2805932331342));
#41159=CARTESIAN_POINT('Ctrl Pts',(79.8472420235469,94.8767375964464,46.3696783243398));
#41160=CARTESIAN_POINT('Ctrl Pts',(83.3693006798349,94.4524255773417,50.5307553187046));
#41161=CARTESIAN_POINT('Ctrl Pts',(82.9383832695932,93.9220355534611,57.995084078736));
#41162=CARTESIAN_POINT('Ctrl Pts',(75.0903408348937,93.285567524804,62.3987639191292));
#41163=CARTESIAN_POINT('Ctrl Pts',(67.162821618513,92.6490994961473,58.1764706518527));
#41164=CARTESIAN_POINT('Ctrl Pts',(66.414612745349,92.0126314674902,49.2258558772637));
#41165=CARTESIAN_POINT('Ctrl Pts',(73.5597771752602,91.3761634388332,43.7549517963041));
#41166=CARTESIAN_POINT('Ctrl Pts',(80.5875093419881,90.8457734149524,46.3069851513022));
#41167=CARTESIAN_POINT('Ctrl Pts',(83.0193467550868,90.4214613958478,51.186086065161));
#41168=CARTESIAN_POINT('Ctrl Pts',(82.9499580277891,89.9971493767431,56.6372000922097));
#41169=CARTESIAN_POINT('Ctrl Pts',(77.7300486906101,89.4667593528625,61.9901843219554));
#41170=CARTESIAN_POINT('Ctrl Pts',(68.9171818569722,88.8302913242055,60.168771582871));
#41171=CARTESIAN_POINT('Ctrl Pts',(65.700600559468,88.1938232955485,51.7826565039134));
#41172=CARTESIAN_POINT('Ctrl Pts',(71.0048716735689,87.5573552668916,44.5343443342367));
#41173=CARTESIAN_POINT('Ctrl Pts',(79.9868760409975,86.9208872382345,45.0891089122556));
#41174=CARTESIAN_POINT('Ctrl Pts',(83.6193563062945,86.3904972143539,51.6241667371345));
#41175=CARTESIAN_POINT('Ctrl Pts',(82.2560251437057,85.9661851952492,56.902498582754));
#41176=CARTESIAN_POINT('Ctrl Pts',(78.6291898710409,85.5418731761446,60.9725753432482));
#41177=CARTESIAN_POINT('Ctrl Pts',(71.1780714024604,85.0114831522638,61.5912248558673));
#41178=CARTESIAN_POINT('Ctrl Pts',(65.7187308749215,84.3750151236068,54.4372212775972));
#41179=CARTESIAN_POINT('Ctrl Pts',(68.7892291056127,83.7385470949501,45.996524506815));
#41180=CARTESIAN_POINT('Ctrl Pts',(77.5468597008283,83.1020790662928,44.0022257030456));
#41181=CARTESIAN_POINT('Ctrl Pts',(83.9644750271765,82.4656110376362,50.3108214038772));
#41182=CARTESIAN_POINT('Ctrl Pts',(82.4217691187119,81.9352210137552,57.6266912860082));
#41183=CARTESIAN_POINT('Ctrl Pts',(77.9313087594824,81.5109089946506,60.717843934059));
#41184=CARTESIAN_POINT('Ctrl Pts',(72.5241951379537,81.0865969755461,61.4125245910826));
#41185=CARTESIAN_POINT('Ctrl Pts',(66.4929544430065,80.5562069516651,56.9936978993126));
#41186=CARTESIAN_POINT('Ctrl Pts',(67.062245548944,79.9197389230083,48.0126025412713));
#41187=CARTESIAN_POINT('Ctrl Pts',(74.9152631630308,79.2832708943513,43.6533095121423));
#41188=CARTESIAN_POINT('Ctrl Pts',(82.8349685791922,78.6468028656944,47.8902408878197));
#41189=CARTESIAN_POINT('Ctrl Pts',(83.5435298885395,78.0103348370374,56.8614229205523));
#41190=CARTESIAN_POINT('Ctrl Pts',(77.5815717462269,77.4799448131566,61.3732904675436));
#41191=CARTESIAN_POINT('Ctrl Pts',(72.164331182832,77.0556327940521,60.7625830010131));
#41192=CARTESIAN_POINT('Ctrl Pts',(67.6264530835239,76.6313207749473,57.7414704100648));
#41193=CARTESIAN_POINT('Ctrl Pts',(65.9704295539125,76.1009307510667,50.4504156357781));
#41194=CARTESIAN_POINT('Ctrl Pts',(72.2893966827277,75.4644627224096,44.0430120572231));
#41195=CARTESIAN_POINT('Ctrl Pts',(81.0769140980902,74.8279946937527,45.9011990864744));
#41196=CARTESIAN_POINT('Ctrl Pts',(84.2779973823023,74.1915266650957,54.2932421731437));
#41197=CARTESIAN_POINT('Ctrl Pts',(78.9303059381265,73.5550586364389,61.5310845596158));
#41198=CARTESIAN_POINT('Ctrl Pts',(71.4704861415877,73.024668612558,61.0281111453561));
#41199=CARTESIAN_POINT('Ctrl Pts',(67.7809414994357,72.6003565934535,57.0147934075068));
#41200=CARTESIAN_POINT('Ctrl Pts',(66.3358828547326,72.1760445743488,51.7582484923816));
#41201=CARTESIAN_POINT('Ctrl Pts',(69.8665366556498,71.645654550468,45.167620495722));
#41202=CARTESIAN_POINT('Ctrl Pts',(78.8388529626364,71.009186521811,44.4735698629039));
#41203=CARTESIAN_POINT('Ctrl Pts',(84.2549408213817,70.3727184931542,51.6387156162939));
#41204=CARTESIAN_POINT('Ctrl Pts',(81.1688544716568,69.7362504644971,60.0737255394068));
#41205=CARTESIAN_POINT('Ctrl Pts',(72.385306968269,69.0997824358402,62.0316477669905));
#41206=CARTESIAN_POINT('Ctrl Pts',(67.0829761186137,68.5693924119593,56.7602929873277));
#41207=CARTESIAN_POINT('Ctrl Pts',(66.9290235122682,68.1450803928548,51.3109115979991));
#41208=CARTESIAN_POINT('Ctrl Pts',(69.2848705936376,67.7207683737502,46.3946687784702));
#41209=CARTESIAN_POINT('Ctrl Pts',(76.2721629512954,67.1903783498693,43.7339096460225));
#41210=CARTESIAN_POINT('Ctrl Pts',(83.5013466579915,66.5539103212124,49.0933003882955));
#41211=CARTESIAN_POINT('Ctrl Pts',(82.8920936660021,65.9174422925556,58.0544460824981));
#41212=CARTESIAN_POINT('Ctrl Pts',(75.0310360867532,65.2809742638985,62.3992239935898));
#41213=CARTESIAN_POINT('Ctrl Pts',(67.1156166044769,64.6445062352416,58.11783396077));
#41214=CARTESIAN_POINT('Ctrl Pts',(66.568944468159,64.1141162113608,50.6610891463319));
#41215=CARTESIAN_POINT('Ctrl Pts',(70.0260214775475,63.6898041922562,46.4458694032433));
#41216=CARTESIAN_POINT('Ctrl Pts',(75.028396930057,63.2654921731517,44.2789132976665));
#41217=CARTESIAN_POINT('Ctrl Pts',(82.0485181524915,62.7351021492707,46.8518088794201));
#41218=CARTESIAN_POINT('Ctrl Pts',(83.9922315445127,62.0986341206139,55.6385115853959));
#41219=CARTESIAN_POINT('Ctrl Pts',(77.6561748449408,61.4621660919568,62.0046491004664));
#41220=CARTESIAN_POINT('Ctrl Pts',(68.8721052431446,60.8256980632999,60.13023116634));
#41221=CARTESIAN_POINT('Ctrl Pts',(65.7034106049201,60.189230034643,51.7074323154109));
#41222=CARTESIAN_POINT('Ctrl Pts',(70.1802693794732,59.6588400107622,45.719141310041));
#41223=CARTESIAN_POINT('Ctrl Pts',(75.5543902423377,59.2345279916576,44.8035628684599));
#41224=CARTESIAN_POINT('Ctrl Pts',(80.7521040083146,58.8102159725529,46.4477132686177));
#41225=CARTESIAN_POINT('Ctrl Pts',(84.3651580886292,58.2798259486721,52.993531312606));
#41226=CARTESIAN_POINT('Ctrl Pts',(80.0709714679809,57.6433579200152,60.902015836241));
#41227=CARTESIAN_POINT('Ctrl Pts',(71.112811884322,57.0068898913583,61.5537045922262));
#41228=CARTESIAN_POINT('Ctrl Pts',(65.7099701712437,56.3704218627013,54.3785653751525));
#41229=CARTESIAN_POINT('Ctrl Pts',(68.8406772736282,55.7339538340444,45.9415730655311));
#41230=CARTESIAN_POINT('Ctrl Pts',(76.1473828139961,55.2035638101635,44.3560296890693));
#41231=CARTESIAN_POINT('Ctrl Pts',(80.805200283045,54.779251791059,47.1887307598465));
#41232=CARTESIAN_POINT('Ctrl Pts',(83.6513455125856,54.3549397719544,51.8383453958925));
#41233=CARTESIAN_POINT('Ctrl Pts',(82.0869171103928,53.8245497480736,59.1496009260114));
#41234=CARTESIAN_POINT('Ctrl Pts',(73.6590043141352,53.1880817194166,62.3046686102621));
#41235=CARTESIAN_POINT('Ctrl Pts',(66.4682867565965,52.5516136907597,56.9225777183616));
#41236=CARTESIAN_POINT('Ctrl Pts',(67.0940935459028,51.9151456621027,47.9625728509838));
#41237=CARTESIAN_POINT('Ctrl Pts',(74.9901395829951,51.2786776334457,43.6455573108627));
#41238=CARTESIAN_POINT('Ctrl Pts',(81.5463680720391,50.748287609565,47.2396860859249));
#41239=CARTESIAN_POINT('Ctrl Pts',(83.2055272982663,50.3239755904603,52.4326283726629));
#41240=CARTESIAN_POINT('Ctrl Pts',(82.3054779870697,49.8996635713557,57.8093718265372));
#41241=CARTESIAN_POINT('Ctrl Pts',(76.3301451774869,49.369273547475,62.303511506943));
#41242=CARTESIAN_POINT('Ctrl Pts',(67.8982274249162,48.7328055188179,59.1591627337605));
#41243=CARTESIAN_POINT('Ctrl Pts',(65.9984409942062,48.096337490161,50.380544797054));
#41244=CARTESIAN_POINT('Ctrl Pts',(72.3462476957355,47.4598694615041,44.0261233882245));
#41245=CARTESIAN_POINT('Ctrl Pts',(81.1385289337613,46.8234014328471,45.9444447442511));
#41246=CARTESIAN_POINT('Ctrl Pts',(83.7316942230129,46.2930114089664,52.9571038287145));
#41247=CARTESIAN_POINT('Ctrl Pts',(81.5791985335305,45.8686993898618,57.9657185312172));
#41248=CARTESIAN_POINT('Ctrl Pts',(77.3739835375813,45.4443873707569,61.4349584723578));
#41249=CARTESIAN_POINT('Ctrl Pts',(69.9156905569373,44.9139973468764,60.9098304240122));
#41250=CARTESIAN_POINT('Ctrl Pts',(65.6114515168285,44.2775293182193,53.0068124891259));
#41251=CARTESIAN_POINT('Ctrl Pts',(69.9335014708324,43.6410612895624,45.1332360745562));
#41252=CARTESIAN_POINT('Ctrl Pts',(78.8928496988574,43.0045932609056,44.4980977510727));
#41253=CARTESIAN_POINT('Ctrl Pts',(84.2731024819777,42.3681252322484,51.7117685353029));
#41254=CARTESIAN_POINT('Ctrl Pts',(81.6325400570954,41.8377352083678,58.7067184087889));
#41255=CARTESIAN_POINT('Ctrl Pts',(76.7231235643936,41.413423189263,61.0767582043516));
#41256=CARTESIAN_POINT('Ctrl Pts',(71.2733201606874,40.9891111701586,60.9385489705161));
#41257=CARTESIAN_POINT('Ctrl Pts',(65.9866694623412,40.4587211462777,55.6514686754988));
#41258=CARTESIAN_POINT('Ctrl Pts',(67.9192087097107,39.8222531176208,46.8623015789586));
#41259=CARTESIAN_POINT('Ctrl Pts',(76.3452680327245,39.1857850889638,43.7518601880908));
#41260=CARTESIAN_POINT('Ctrl Pts',(83.5260304351007,38.5493170603069,49.1472260405232));
#41261=CARTESIAN_POINT('Ctrl Pts',(82.8579028431224,37.9128490316499,58.1215099514755));
#41262=CARTESIAN_POINT('Ctrl Pts',(76.2775020620698,37.3824590077692,61.6711886993321));
#41263=CARTESIAN_POINT('Ctrl Pts',(71.0168044487598,36.9581469886645,60.2413217290587));
#41264=CARTESIAN_POINT('Ctrl Pts',(66.9928447242639,36.5338349695599,56.5633865655431));
#41265=CARTESIAN_POINT('Ctrl Pts',(66.4683227187594,36.0034449456791,49.1050509390183));
#41266=CARTESIAN_POINT('Ctrl Pts',(73.6906859447653,35.3669769170221,43.7364723910789));
#41267=CARTESIAN_POINT('Ctrl Pts',(82.0919416290415,34.7305088883652,46.9132985255213));
#41268=CARTESIAN_POINT('Ctrl Pts',(83.9755071830147,34.0940408597083,55.6954111508481));
#41269=CARTESIAN_POINT('Ctrl Pts',(77.5863852200769,33.4575728310513,62.0328622739661));
#41270=CARTESIAN_POINT('Ctrl Pts',(70.2905767805001,32.9271828071705,60.3979087989981));
#41271=CARTESIAN_POINT('Ctrl Pts',(67.2563673100594,32.5028707880659,55.8687773349566));
#41272=CARTESIAN_POINT('Ctrl Pts',(66.6300125136881,32.0785587689612,50.4533236506808));
#41273=CARTESIAN_POINT('Ctrl Pts',(71.1246377186793,31.5481687450805,44.4783560439785));
#41274=CARTESIAN_POINT('Ctrl Pts',(80.0978292805397,30.9117007164235,45.1609975264086));
#41275=CARTESIAN_POINT('Ctrl Pts',(84.3576222297789,30.2752326877666,53.0684298181443));
#41276=CARTESIAN_POINT('Ctrl Pts',(80.0210339933028,29.6387646591097,60.9340082261254));
#41277=CARTESIAN_POINT('Ctrl Pts',(71.0416207354475,29.0022966304526,61.5292424780427));
#41278=CARTESIAN_POINT('Ctrl Pts',(66.6053888241581,28.471906606572,55.5107924815076));
#41279=CARTESIAN_POINT('Ctrl Pts',(67.2844459508887,28.0475945874673,50.1016945997134));
#41280=CARTESIAN_POINT('Ctrl Pts',(70.3626132162843,27.6232825683627,45.6023228604246));
#41281=CARTESIAN_POINT('Ctrl Pts',(77.6739958051555,27.0928925444818,44.0384887347478));
#41282=CARTESIAN_POINT('Ctrl Pts',(84.0011051141402,26.456424515825,50.4378520405945));
#41283=CARTESIAN_POINT('Ctrl Pts',(82.0321144470125,25.8199564871679,59.2012080002241));
#41284=CARTESIAN_POINT('Ctrl Pts',(73.6003234993231,25.183488458511,62.2960766909906));
#41285=CARTESIAN_POINT('Ctrl Pts',(66.4305778201804,24.5470204298541,56.8574282604532));
#41286=CARTESIAN_POINT('Ctrl Pts',(67.0277000252806,24.0166304059734,49.404549832749));
#41287=CARTESIAN_POINT('Ctrl Pts',(71.087281001366,23.5923183868687,45.7659773340634));
#41288=CARTESIAN_POINT('Ctrl Pts',(76.3616547019156,23.1680063677641,44.3873920955271));
#41289=CARTESIAN_POINT('Ctrl Pts',(82.9071737981875,22.6376163438832,48.0010028147332));
#41290=CARTESIAN_POINT('Ctrl Pts',(83.4878939142026,22.0011483152263,56.9813219696603));
#41291=CARTESIAN_POINT('Ctrl Pts',(76.2549182840066,21.3646802865694,62.3065904942583));
#41292=CARTESIAN_POINT('Ctrl Pts',(67.8595780289596,20.7282122579124,59.1140998978481));
#41293=CARTESIAN_POINT('Ctrl Pts',(66.0126504674273,20.0917442292555,50.306823428731));
#41294=CARTESIAN_POINT('Ctrl Pts',(71.3506474699067,19.5613542053747,45.0709387852651));
#41295=CARTESIAN_POINT('Ctrl Pts',(76.8013676315427,19.13704218627,44.986593912523));
#41296=CARTESIAN_POINT('Ctrl Pts',(81.6878086862886,18.7127301671654,47.4027719979591));
#41297=CARTESIAN_POINT('Ctrl Pts',(84.2593913555,18.1823401432847,54.4265435254333));
#41298=CARTESIAN_POINT('Ctrl Pts',(78.8105057472924,17.5458721146277,61.5812140877453));
#41299=CARTESIAN_POINT('Ctrl Pts',(69.8553503280536,16.9094040859708,60.8700036609127));
#41300=CARTESIAN_POINT('Ctrl Pts',(65.6148282883278,16.2729360573138,52.9336653886293));
#41301=CARTESIAN_POINT('Ctrl Pts',(69.2571180034507,15.742546033433,46.4187817991452));
#41302=CARTESIAN_POINT('Ctrl Pts',(74.4817461662636,15.3182340143284,44.7908493746173));
#41303=CARTESIAN_POINT('Ctrl Pts',(77.1471440252829,15.1060780047761,45.284124068141));
#41304=CARTESIAN_POINT('Ctrl Pts',(78.3434537325882,14.9999999999999,45.8432414056378));
#41305=CARTESIAN_POINT('Ctrl Pts',(68.7814015540657,416.407550721688,56.6017518575033));
#41306=CARTESIAN_POINT('Ctrl Pts',(68.1850535830631,416.301472716912,55.5675736979236));
#41307=CARTESIAN_POINT('Ctrl Pts',(67.5341159529618,416.089316707359,53.2050722594426));
#41308=CARTESIAN_POINT('Ctrl Pts',(68.5953548805507,415.665004688255,48.3730012520256));
#41309=CARTESIAN_POINT('Ctrl Pts',(74.1809818384847,415.134614664374,44.5872815646217));
#41310=CARTESIAN_POINT('Ctrl Pts',(81.6580577336735,414.498146635717,47.7914675678002));
#41311=CARTESIAN_POINT('Ctrl Pts',(82.9929204080563,413.86167860706,55.8023046120247));
#41312=CARTESIAN_POINT('Ctrl Pts',(76.9710932722329,413.225210578403,61.2648397466391));
#41313=CARTESIAN_POINT('Ctrl Pts',(70.4453616288584,412.694820554522,59.4931309478417));
#41314=CARTESIAN_POINT('Ctrl Pts',(67.8902587970379,412.270508535417,55.2791970646377));
#41315=CARTESIAN_POINT('Ctrl Pts',(67.5436485600779,411.846196516313,50.3631536723669));
#41316=CARTESIAN_POINT('Ctrl Pts',(71.8458077986813,411.315806492433,45.1492552626692));
#41317=CARTESIAN_POINT('Ctrl Pts',(79.9217750170301,410.679338463775,46.1299912507797));
#41318=CARTESIAN_POINT('Ctrl Pts',(83.4481442408686,410.042870435119,53.4442313362922));
#41319=CARTESIAN_POINT('Ctrl Pts',(79.2123890848229,409.40640240646,60.3718808483404));
#41320=CARTESIAN_POINT('Ctrl Pts',(71.0787268288466,408.769934377806,60.5450429152035));
#41321=CARTESIAN_POINT('Ctrl Pts',(67.3164634352907,408.239544353923,54.9295989188625));
#41322=CARTESIAN_POINT('Ctrl Pts',(68.1492568471143,407.815232334819,50.0720529791814));
#41323=CARTESIAN_POINT('Ctrl Pts',(71.1118174108275,407.390920315714,46.1334689268072));
#41324=CARTESIAN_POINT('Ctrl Pts',(77.7783873168303,406.860530291834,45.0178340311155));
#41325=CARTESIAN_POINT('Ctrl Pts',(83.2328704840493,406.224062263176,51.0540330992533));
#41326=CARTESIAN_POINT('Ctrl Pts',(81.0989941768656,405.58759423452,58.8885473657906));
#41327=CARTESIAN_POINT('Ctrl Pts',(73.3584248002522,404.951126205863,61.3414323767353));
#41328=CARTESIAN_POINT('Ctrl Pts',(67.1039459981687,404.314658177206,56.1386839289719));
#41329=CARTESIAN_POINT('Ctrl Pts',(67.9456704139453,403.784268153325,49.432027003658));
#41330=CARTESIAN_POINT('Ctrl Pts',(71.7596457584586,403.359956134221,46.310674061179));
#41331=CARTESIAN_POINT('Ctrl Pts',(76.5790150618936,402.935644115116,45.2796888109111));
#41332=CARTESIAN_POINT('Ctrl Pts',(82.343807547953,402.405254091235,48.8088410945701));
#41333=CARTESIAN_POINT('Ctrl Pts',(82.5038263923615,401.768786062578,56.9428126458584));
#41334=CARTESIAN_POINT('Ctrl Pts',(75.7554457013352,401.132318033921,61.4586080859898));
#41335=CARTESIAN_POINT('Ctrl Pts',(68.3029116146995,400.495850005264,58.234823624498));
#41336=CARTESIAN_POINT('Ctrl Pts',(66.9923829061935,399.859381976607,50.205526415265));
#41337=CARTESIAN_POINT('Ctrl Pts',(72.0256241317357,399.328991952726,45.6939600829022));
#41338=CARTESIAN_POINT('Ctrl Pts',(76.951923377724,398.904679933622,45.8382763506332));
#41339=CARTESIAN_POINT('Ctrl Pts',(81.266580352052,398.480367914517,48.2200795820483));
#41340=CARTESIAN_POINT('Ctrl Pts',(83.3048203906889,397.949977890636,54.6647149918501));
#41341=CARTESIAN_POINT('Ctrl Pts',(78.0919630087754,397.313509861979,60.9107711141114));
#41342=CARTESIAN_POINT('Ctrl Pts',(70.035820603255,396.677041833323,59.8950841246337));
#41343=CARTESIAN_POINT('Ctrl Pts',(66.5231018692908,396.040573804665,52.5743015424564));
#41344=CARTESIAN_POINT('Ctrl Pts',(70.7986894391281,395.404105776009,45.6528529875597));
#41345=CARTESIAN_POINT('Ctrl Pts',(77.5571328712723,394.873715752128,45.5470683254055));
#41346=CARTESIAN_POINT('Ctrl Pts',(81.1818437693164,394.449403733023,48.8863380579642));
#41347=CARTESIAN_POINT('Ctrl Pts',(82.8775839616058,394.025091713919,53.5138337782664));
#41348=CARTESIAN_POINT('Ctrl Pts',(80.1905233291765,393.494701690038,59.7160473490804));
#41349=CARTESIAN_POINT('Ctrl Pts',(72.1591170084185,392.858233661381,61.0135879750886));
#41350=CARTESIAN_POINT('Ctrl Pts',(66.7427646843267,392.221765632724,54.9641104752807));
#41351=CARTESIAN_POINT('Ctrl Pts',(68.8911117968739,391.585297604067,47.1335514145627));
#41352=CARTESIAN_POINT('Ctrl Pts',(76.6577554419204,390.94882957541,44.7114973986289));
#41353=CARTESIAN_POINT('Ctrl Pts',(81.8297285544656,390.418439551529,49.0633294431198));
#41354=CARTESIAN_POINT('Ctrl Pts',(82.37672386321,389.994127532425,53.96129305807));
#41355=CARTESIAN_POINT('Ctrl Pts',(80.622625736186,389.569815513319,58.566984233337));
#41356=CARTESIAN_POINT('Ctrl Pts',(74.5269381549992,389.03942548944,61.4876589726595));
#41357=CARTESIAN_POINT('Ctrl Pts',(67.6124138739367,388.402957460782,57.2008824294));
#41358=CARTESIAN_POINT('Ctrl Pts',(67.4898925148396,387.766489432125,49.0818899404304));
#41359=CARTESIAN_POINT('Ctrl Pts',(74.2466041857144,387.130021403468,44.5785691750345));
#41360=CARTESIAN_POINT('Ctrl Pts',(81.6986080191094,386.493553374812,47.8427287961786));
#41361=CARTESIAN_POINT('Ctrl Pts',(82.749817016555,385.96316335093,54.5197571519698));
#41362=CARTESIAN_POINT('Ctrl Pts',(79.9510661822958,385.538851331826,58.5763869365196));
#41363=CARTESIAN_POINT('Ctrl Pts',(75.6066469653137,385.114539312722,60.9034608735224));
#41364=CARTESIAN_POINT('Ctrl Pts',(69.0892511374014,384.58414928884,59.1114509286099));
#41365=CARTESIAN_POINT('Ctrl Pts',(66.679761851001,383.947681260184,51.3409000765814));
#41366=CARTESIAN_POINT('Ctrl Pts',(71.9111075617697,383.311213231526,45.1307412562451));
#41367=CARTESIAN_POINT('Ctrl Pts',(79.9653598379443,382.67474520287,46.1613094447321));
#41368=CARTESIAN_POINT('Ctrl Pts',(83.4512031212773,382.038277174213,53.512227466944));
#41369=CARTESIAN_POINT('Ctrl Pts',(79.8665501131237,381.507887150332,59.2426734209241));
#41370=CARTESIAN_POINT('Ctrl Pts',(75.093455639325,381.083575131227,60.4701996264918));
#41371=CARTESIAN_POINT('Ctrl Pts',(70.2875034035968,380.659263112123,59.3783779610809));
#41372=CARTESIAN_POINT('Ctrl Pts',(66.5419572709727,380.128873088242,53.7517775497547));
#41373=CARTESIAN_POINT('Ctrl Pts',(69.8181652943605,379.492405059585,46.3050628276286));
#41374=CARTESIAN_POINT('Ctrl Pts',(77.8399913967625,378.855937030928,45.0467478820745));
#41375=CARTESIAN_POINT('Ctrl Pts',(83.2451586623123,378.219469002271,51.1062212379702));
#41376=CARTESIAN_POINT('Ctrl Pts',(81.056760009085,377.583000973614,58.9419094974527));
#41377=CARTESIAN_POINT('Ctrl Pts',(74.5927436622569,377.052610949733,60.9178246495513));
#41378=CARTESIAN_POINT('Ctrl Pts',(70.1841467313888,376.628298930629,58.7147530342143));
#41379=CARTESIAN_POINT('Ctrl Pts',(67.2716031340737,376.203986911524,54.7390340759755));
#41380=CARTESIAN_POINT('Ctrl Pts',(68.1332438336644,375.673596887643,48.0349067408809));
#41381=CARTESIAN_POINT('Ctrl Pts',(75.4897901509022,375.037128858987,44.5609571949648));
#41382=CARTESIAN_POINT('Ctrl Pts',(82.3713600232549,374.40066083033,48.8710670092633));
#41383=CARTESIAN_POINT('Ctrl Pts',(82.4788821316752,373.764192801672,56.990271989776));
#41384=CARTESIAN_POINT('Ctrl Pts',(75.6885682938352,373.127724773016,61.4712023785323));
#41385=CARTESIAN_POINT('Ctrl Pts',(69.5125903262564,372.597334749135,58.7243780003945));
#41386=CARTESIAN_POINT('Ctrl Pts',(67.6287264240034,372.17302273003,54.1702251440499));
#41387=CARTESIAN_POINT('Ctrl Pts',(68.0367530158591,371.748710710926,49.2587319147457));
#41388=CARTESIAN_POINT('Ctrl Pts',(73.0833721116578,371.218320687044,44.7621350101664));
#41389=CARTESIAN_POINT('Ctrl Pts',(80.9155106650358,370.581852658388,46.9632040336022));
#41390=CARTESIAN_POINT('Ctrl Pts',(83.2848191844876,369.945384629731,54.7297623227698));
#41391=CARTESIAN_POINT('Ctrl Pts',(78.0420097419556,369.308916601074,60.93024614814));
#41392=CARTESIAN_POINT('Ctrl Pts',(69.9770699095695,368.672448572417,59.8607394089223));
#41393=CARTESIAN_POINT('Ctrl Pts',(67.1153917312942,368.142058548536,53.7371337697309));
#41394=CARTESIAN_POINT('Ctrl Pts',(68.6793639935662,367.717746529432,49.0634583205791));
#41395=CARTESIAN_POINT('Ctrl Pts',(72.2080256168429,367.293434510327,45.6228481145867));
#41396=CARTESIAN_POINT('Ctrl Pts',(78.9667534352475,366.763044486446,45.5371375722202));
#41397=CARTESIAN_POINT('Ctrl Pts',(83.4366954912707,366.126576457789,52.3346898655854));
#41398=CARTESIAN_POINT('Ctrl Pts',(80.1327691280308,365.490108429132,59.7520425675722));
#41399=CARTESIAN_POINT('Ctrl Pts',(72.1086321011238,364.853640400476,60.995535829637));
#41400=CARTESIAN_POINT('Ctrl Pts',(66.7209288483918,364.217172371818,54.8996558418304));
#41401=CARTESIAN_POINT('Ctrl Pts',(68.5757876895998,363.686782347938,48.3998676376236));
#41402=CARTESIAN_POINT('Ctrl Pts',(72.8212415522201,363.262470328833,45.8967949376159));
#41403=CARTESIAN_POINT('Ctrl Pts',(77.7414756105612,362.838158309728,45.6129846976599));
#41404=CARTESIAN_POINT('Ctrl Pts',(82.900500275741,362.307768285847,49.9801591302214));
#41405=CARTESIAN_POINT('Ctrl Pts',(81.8179509175015,361.671300257191,58.0433586224958));
#41406=CARTESIAN_POINT('Ctrl Pts',(74.459730818579,361.034832228533,61.4769642339771));
#41407=CARTESIAN_POINT('Ctrl Pts',(67.5861351940375,360.398364199877,57.1541487498666));
#41408=CARTESIAN_POINT('Ctrl Pts',(67.5156712101143,359.761896171219,49.0189084957493));
#41409=CARTESIAN_POINT('Ctrl Pts',(73.1781765660606,359.231506147339,45.327867841106));
#41410=CARTESIAN_POINT('Ctrl Pts',(78.02481749753,358.807194128234,46.221916566047));
#41411=CARTESIAN_POINT('Ctrl Pts',(81.9256836447492,358.38288210913,49.2339747896943));
#41412=CARTESIAN_POINT('Ctrl Pts',(82.9570561679429,357.852492085249,55.9140959516758));
#41413=CARTESIAN_POINT('Ctrl Pts',(76.8524702261602,357.216024056593,61.2919328443892));
#41414=CARTESIAN_POINT('Ctrl Pts',(69.045522611019,356.579556027934,59.059306710478));
#41415=CARTESIAN_POINT('Ctrl Pts',(66.6905660886839,355.943087999279,51.2883846096399));
#41416=CARTESIAN_POINT('Ctrl Pts',(71.9718690931407,355.30661997062,45.1000942366571));
#41417=CARTESIAN_POINT('Ctrl Pts',(78.6673638110826,354.776229946742,46.0264303000629));
#41418=CARTESIAN_POINT('Ctrl Pts',(81.7403124811487,354.351917927635,49.879511912526));
#41419=CARTESIAN_POINT('Ctrl Pts',(82.710365963219,353.927605908532,54.7115143631759));
#41420=CARTESIAN_POINT('Ctrl Pts',(79.1087084297517,353.39721588465,60.4312880503046));
#41421=CARTESIAN_POINT('Ctrl Pts',(70.9733648495515,352.760747855993,60.4885942221618));
#41422=CARTESIAN_POINT('Ctrl Pts',(66.5431347605869,352.124279827337,53.6837347909748));
#41423=CARTESIAN_POINT('Ctrl Pts',(69.86075831682,351.487811798679,46.2724984259334));
#41424=CARTESIAN_POINT('Ctrl Pts',(77.9059622970041,350.851343770022,45.063452486993));
#41425=CARTESIAN_POINT('Ctrl Pts',(82.3536190500792,350.320953746142,50.1532557668041));
#41426=CARTESIAN_POINT('Ctrl Pts',(82.1471145858705,349.896641727037,55.077340183975));
#41427=CARTESIAN_POINT('Ctrl Pts',(79.7110241380284,349.472329707933,59.3615804633122));
#41428=CARTESIAN_POINT('Ctrl Pts',(73.241167520903,348.941939684051,61.3182877419281));
#41429=CARTESIAN_POINT('Ctrl Pts',(67.0614270800493,348.305471655395,56.0269828698838));
#41430=CARTESIAN_POINT('Ctrl Pts',(68.178750363224,347.669003626737,47.9843067480785));
#41431=CARTESIAN_POINT('Ctrl Pts',(75.5433011550229,347.032535598082,44.5643005851607));
#41432=CARTESIAN_POINT('Ctrl Pts',(82.4102142072295,346.396067569423,48.9269378951685));
#41433=CARTESIAN_POINT('Ctrl Pts',(82.4306579931864,345.865677545544,55.6861782424242));
#41434=CARTESIAN_POINT('Ctrl Pts',(79.0458886590258,345.441365526438,59.2684384222114));
#41435=CARTESIAN_POINT('Ctrl Pts',(74.3973513042222,345.017053507334,60.9056164522856));
#41436=CARTESIAN_POINT('Ctrl Pts',(68.2295590842627,344.486663483453,58.1404605522035));
#41437=CARTESIAN_POINT('Ctrl Pts',(67.0335268243352,343.850195454796,50.0933116161857));
#41438=CARTESIAN_POINT('Ctrl Pts',(73.1509092443753,343.213727426139,44.753772043679));
#41439=CARTESIAN_POINT('Ctrl Pts',(80.9537189797542,342.577259397483,47.0008169370583));
#41440=CARTESIAN_POINT('Ctrl Pts',(83.2775178994342,341.940791368825,54.7974224642177));
#41441=CARTESIAN_POINT('Ctrl Pts',(78.8607311565456,341.410401344945,59.9140368612769));
#41442=CARTESIAN_POINT('Ctrl Pts',(73.9562515767661,340.98608932584,60.3991466351328));
#41443=CARTESIAN_POINT('Ctrl Pts',(69.3730748596339,340.561777306736,58.5870366437974));
#41444=CARTESIAN_POINT('Ctrl Pts',(66.529597387875,340.031387282854,52.4549583755465));
#41445=CARTESIAN_POINT('Ctrl Pts',(70.9033353532007,339.394919254198,45.5951103177607));
#41446=CARTESIAN_POINT('Ctrl Pts',(79.0232276239048,338.75845122554,45.575109529237));
#41447=CARTESIAN_POINT('Ctrl Pts',(83.4408788431293,338.121983196884,52.3881417634678));
#41448=CARTESIAN_POINT('Ctrl Pts',(80.0828900417,337.485515168226,59.7983381424253));
#41449=CARTESIAN_POINT('Ctrl Pts',(73.3931213062477,336.955125144346,60.7651588530632));
#41450=CARTESIAN_POINT('Ctrl Pts',(69.3721520503855,336.530813125241,57.9154119020912));
#41451=CARTESIAN_POINT('Ctrl Pts',(67.1001164622618,336.106501106137,53.5419572347303));
#41452=CARTESIAN_POINT('Ctrl Pts',(68.9742725277789,335.576111082256,47.0477069267705));
#41453=CARTESIAN_POINT('Ctrl Pts',(76.7746263075684,334.939643053599,44.7365210676572));
#41454=CARTESIAN_POINT('Ctrl Pts',(82.9182388733991,334.303175024942,50.0458595537917));
#41455=CARTESIAN_POINT('Ctrl Pts',(81.7860594422747,333.666706996285,58.0864578061059));
#41456=CARTESIAN_POINT('Ctrl Pts',(74.3917149433775,333.030238967628,61.4792101691393));
#41457=CARTESIAN_POINT('Ctrl Pts',(68.7069857809447,332.499848943747,57.8224900034527));
#41458=CARTESIAN_POINT('Ctrl Pts',(67.5398227525649,332.075536924643,53.0342771942362));
#41459=CARTESIAN_POINT('Ctrl Pts',(68.6922375796396,331.651224905538,48.2424934441593));
#41460=CARTESIAN_POINT('Ctrl Pts',(74.3656809371467,331.120834881658,44.5682876130294));
#41461=CARTESIAN_POINT('Ctrl Pts',(81.7704365027121,330.484366853,47.9382570757208));
#41462=CARTESIAN_POINT('Ctrl Pts',(82.9273671692477,329.847898824343,55.9753312916411));
#41463=CARTESIAN_POINT('Ctrl Pts',(76.8001309130144,329.211430795687,61.3035604890083));
#41464=CARTESIAN_POINT('Ctrl Pts',(68.9926980804786,328.574962767029,59.0164024860079));
#41465=CARTESIAN_POINT('Ctrl Pts',(67.0985554248778,328.044572743149,52.5279533939223));
#41466=CARTESIAN_POINT('Ctrl Pts',(69.3571145943043,327.620260724044,48.1475239721236));
#41467=CARTESIAN_POINT('Ctrl Pts',(73.3692905618005,327.19594870494,45.2854101646361));
#41468=CARTESIAN_POINT('Ctrl Pts',(80.0620043807514,326.665558681058,46.2316288275121));
#41469=CARTESIAN_POINT('Ctrl Pts',(83.4427928913044,326.029090652402,53.6314510018721));
#41470=CARTESIAN_POINT('Ctrl Pts',(79.0461395988837,325.392622623745,60.4580526707575));
#41471=CARTESIAN_POINT('Ctrl Pts',(70.9262242348619,324.756154595088,60.4630527212918));
#41472=CARTESIAN_POINT('Ctrl Pts',(66.5313858701374,324.119686566431,53.6167037005958));
#41473=CARTESIAN_POINT('Ctrl Pts',(69.3559695000191,323.58929654255,47.4758995726207));
#41474=CARTESIAN_POINT('Ctrl Pts',(73.9335450964997,323.164984523445,45.6496867975949));
#41475=CARTESIAN_POINT('Ctrl Pts',(78.8394950580058,322.740672504341,46.1196936234625));
#41476=CARTESIAN_POINT('Ctrl Pts',(83.2720146665453,322.21028248046,51.2226847012778));
#41477=CARTESIAN_POINT('Ctrl Pts',(80.9722321220802,321.573814451804,59.0264081339356));
#41478=CARTESIAN_POINT('Ctrl Pts',(73.1763779112654,320.937346423146,61.2974668392768));
#41479=CARTESIAN_POINT('Ctrl Pts',(67.042584310839,320.300878394489,55.9767876921426));
#41480=CARTESIAN_POINT('Ctrl Pts',(68.2138341304525,319.664410365832,47.9259943756242));
#41481=CARTESIAN_POINT('Ctrl Pts',(74.3730833377875,319.134020341951,45.1418612569866));
#41482=CARTESIAN_POINT('Ctrl Pts',(79.0266394483123,318.709708322847,46.7647189116685));
#41483=CARTESIAN_POINT('Ctrl Pts',(82.4224223395787,318.285396303742,50.336540575266));
#41484=CARTESIAN_POINT('Ctrl Pts',(82.4227900152136,317.755006279862,57.0958118292673));
#41485=CARTESIAN_POINT('Ctrl Pts',(75.5693418552194,317.118538251204,61.4795713440574));
#41486=CARTESIAN_POINT('Ctrl Pts',(68.1942959424373,316.482070222548,58.0822564773221));
#41487=CARTESIAN_POINT('Ctrl Pts',(67.0522149557767,315.845602193891,50.0430586604197));
#41488=CARTESIAN_POINT('Ctrl Pts',(73.2156344403881,315.209134165234,44.7327517557342));
#41489=CARTESIAN_POINT('Ctrl Pts',(79.6914849948774,314.678744141353,46.6695293930162));
#41490=CARTESIAN_POINT('Ctrl Pts',(82.1407548583383,314.254432122248,50.9462487638779));
#41491=CARTESIAN_POINT('Ctrl Pts',(82.3624193546182,313.830120103144,55.8696740240246));
#41492=CARTESIAN_POINT('Ctrl Pts',(77.9304549343695,313.299730079263,60.9731472921046));
#41493=CARTESIAN_POINT('Ctrl Pts',(69.8815664959961,312.663262050606,59.7888778667402));
#41494=CARTESIAN_POINT('Ctrl Pts',(66.5411398372432,312.026794021949,52.3878914286447));
#41495=CARTESIAN_POINT('Ctrl Pts',(70.9503971034345,311.390325993292,45.5694237943499));
#41496=CARTESIAN_POINT('Ctrl Pts',(79.0858785651323,310.753857964635,45.6016813765094));
#41497=CARTESIAN_POINT('Ctrl Pts',(82.7051299253863,310.223467940754,51.310338627707));
#41498=CARTESIAN_POINT('Ctrl Pts',(81.7499585364533,309.79915592165,56.1453049211703));
#41499=CARTESIAN_POINT('Ctrl Pts',(78.6888878786527,309.374843902545,60.0078297261541));
#41500=CARTESIAN_POINT('Ctrl Pts',(71.9962770398569,308.844453878664,60.9547764938151));
#41501=CARTESIAN_POINT('Ctrl Pts',(66.6959456305342,308.207985850007,54.7827763223478));
#41502=CARTESIAN_POINT('Ctrl Pts',(69.0269647079598,307.57151782135,47.0046402615646));
#41503=CARTESIAN_POINT('Ctrl Pts',(76.8270011735663,306.935049792693,44.7479875070206));
#41504=CARTESIAN_POINT('Ctrl Pts',(82.9481162719336,306.298581764036,50.1070031925532));
#41505=CARTESIAN_POINT('Ctrl Pts',(81.9373163980776,305.768191740156,56.7902682355812));
#41506=CARTESIAN_POINT('Ctrl Pts',(78.0457427182703,305.343879721051,59.8143227548971));
#41507=CARTESIAN_POINT('Ctrl Pts',(73.2018774913111,304.919567701947,60.7232898083249));
#41508=CARTESIAN_POINT('Ctrl Pts',(67.5280344450094,304.389177678065,57.049701221359));
#41509=CARTESIAN_POINT('Ctrl Pts',(67.5734500950031,303.752709649409,48.9142825730056));
#41510=CARTESIAN_POINT('Ctrl Pts',(74.4337034050772,303.116241620751,44.5703241200507));
#41511=CARTESIAN_POINT('Ctrl Pts',(81.8024605270155,302.479773592095,47.9812578627763));
#41512=CARTESIAN_POINT('Ctrl Pts',(82.9098309440052,301.843305563437,56.0410860200523));
#41513=CARTESIAN_POINT('Ctrl Pts',(77.7642770452582,301.312915539558,60.424124132531));
#41514=CARTESIAN_POINT('Ctrl Pts',(72.8431924711145,300.888603520452,60.1554643936637));
#41515=CARTESIAN_POINT('Ctrl Pts',(68.5900518955643,300.464291501348,57.6654750993555));
#41516=CARTESIAN_POINT('Ctrl Pts',(66.7151893218969,299.933901477467,51.1714287220792));
#41517=CARTESIAN_POINT('Ctrl Pts',(72.0840981258804,299.29743344881,45.0589891583906));
#41518=CARTESIAN_POINT('Ctrl Pts',(80.1120257724278,298.660965420153,46.2777706077001));
#41519=CARTESIAN_POINT('Ctrl Pts',(83.4387741350087,298.024497391496,53.6849155267259));
#41520=CARTESIAN_POINT('Ctrl Pts',(78.9897825916792,297.388029362839,60.4961983290048));
#41521=CARTESIAN_POINT('Ctrl Pts',(72.230822911004,296.857639338958,60.4312979795421));
#41522=CARTESIAN_POINT('Ctrl Pts',(68.6915845458889,296.433327319854,57.0015686555198));
#41523=CARTESIAN_POINT('Ctrl Pts',(67.1132296826662,296.009015300749,52.3327307522611));
#41524=CARTESIAN_POINT('Ctrl Pts',(69.956040019597,295.478625276869,46.2003431741158));
#41525=CARTESIAN_POINT('Ctrl Pts',(78.0176486663101,294.842157248211,45.1060099559052));
#41526=CARTESIAN_POINT('Ctrl Pts',(83.2795242391994,294.205689219555,51.2903220417248));
#41527=CARTESIAN_POINT('Ctrl Pts',(80.9341397967266,293.569221190898,59.064138500607));
#41528=CARTESIAN_POINT('Ctrl Pts',(73.1088153495147,292.93275316224,61.2893118559007));
#41529=CARTESIAN_POINT('Ctrl Pts',(68.0483753764643,292.40236313836,56.8082745541695));
#41530=CARTESIAN_POINT('Ctrl Pts',(67.6252284753894,291.978051119255,51.8980608988107));
#41531=CARTESIAN_POINT('Ctrl Pts',(69.4950614381384,291.553739100151,47.3381293058391));
#41532=CARTESIAN_POINT('Ctrl Pts',(75.6625527961363,291.02334907627,44.5723024187452));
#41533=CARTESIAN_POINT('Ctrl Pts',(82.46663100973,290.386881047613,49.0323045295677));
#41534=CARTESIAN_POINT('Ctrl Pts',(82.3841080390843,289.750413018956,57.1518020804449));
#41535=CARTESIAN_POINT('Ctrl Pts',(75.5158413988719,289.113944990299,61.4830794761245));
#41536=CARTESIAN_POINT('Ctrl Pts',(68.1486338337177,288.477476961643,58.0317968367027));
#41537=CARTESIAN_POINT('Ctrl Pts',(67.2663555438189,287.947086937761,51.3303542278666));
#41538=CARTESIAN_POINT('Ctrl Pts',(70.1666442948999,287.522774918657,47.3456865376424));
#41539=CARTESIAN_POINT('Ctrl Pts',(74.5684371812347,287.098462899552,45.1290515142399));
#41540=CARTESIAN_POINT('Ctrl Pts',(81.0385066331955,286.568072875671,47.0850549158614));
#41541=CARTESIAN_POINT('Ctrl Pts',(83.2510206077065,285.931604847015,54.9139680637917));
#41542=CARTESIAN_POINT('Ctrl Pts',(77.8645357794759,285.295136818357,60.9900549389625));
#41543=CARTESIAN_POINT('Ctrl Pts',(69.8388734112542,284.658668789701,59.7564447611965));
#41544=CARTESIAN_POINT('Ctrl Pts',(66.5397528529418,284.022200761043,52.3198526178177));
#41545=CARTESIAN_POINT('Ctrl Pts',(70.2679572090717,283.491810737163,46.6817465262931));
#41546=CARTESIAN_POINT('Ctrl Pts',(75.0705250001109,283.067498718058,45.5751327483045));
#41547=CARTESIAN_POINT('Ctrl Pts',(79.8473763416493,282.643186698953,46.7879570150492));
#41548=CARTESIAN_POINT('Ctrl Pts',(83.4496561165695,282.112796675073,52.5073388385993));
#41549=CARTESIAN_POINT('Ctrl Pts',(79.9864624668663,281.476328646416,59.8689547556312));
#41550=CARTESIAN_POINT('Ctrl Pts',(71.9354214358458,280.839860617759,60.9243167012247));
#41551=CARTESIAN_POINT('Ctrl Pts',(66.6849797515537,280.203392589102,54.7302943700388));
#41552=CARTESIAN_POINT('Ctrl Pts',(69.0705324776169,279.566924560445,46.9523616526382));
#41553=CARTESIAN_POINT('Ctrl Pts',(75.5823799037634,279.036534536564,45.1402934643665));
#41554=CARTESIAN_POINT('Ctrl Pts',(79.9339434731479,278.61222251746,47.4539801204988));
#41555=CARTESIAN_POINT('Ctrl Pts',(82.7451712026369,278.187910498354,51.501973462158));
#41556=CARTESIAN_POINT('Ctrl Pts',(81.7145254259567,277.657520474474,58.1822067891732));
#41557=CARTESIAN_POINT('Ctrl Pts',(74.2726070999485,277.021052445817,61.4692952872608));
#41558=CARTESIAN_POINT('Ctrl Pts',(67.5020619551909,276.38458441716,56.9867994465287));
#41559=CARTESIAN_POINT('Ctrl Pts',(67.5995847596681,275.748116388503,48.8674682042408));
#41560=CARTESIAN_POINT('Ctrl Pts',(74.5008774943678,275.111648359846,44.5594225040166));
#41561=CARTESIAN_POINT('Ctrl Pts',(80.6055287943158,274.581258335966,47.4613150806631));
#41562=CARTESIAN_POINT('Ctrl Pts',(82.3737993009008,274.156946316861,52.061583644204));
#41563=CARTESIAN_POINT('Ctrl Pts',(81.84188717115,273.732634297756,56.9612082142489));
#41564=CARTESIAN_POINT('Ctrl Pts',(76.683337647963,273.202244273875,61.3289438790048));
#41565=CARTESIAN_POINT('Ctrl Pts',(68.9092734328478,272.565776245219,58.930814452869));
#41566=CARTESIAN_POINT('Ctrl Pts',(66.736826601721,271.929308216562,51.1069071626902));
#41567=CARTESIAN_POINT('Ctrl Pts',(72.1345272122206,271.292840187904,45.0407816579883));
#41568=CARTESIAN_POINT('Ctrl Pts',(80.169890527306,270.656372159248,46.3135878332638));
#41569=CARTESIAN_POINT('Ctrl Pts',(82.8760347300884,270.125982135366,52.5074986797403));
#41570=CARTESIAN_POINT('Ctrl Pts',(81.1945504046273,269.701670116263,57.1401935654835));
#41571=CARTESIAN_POINT('Ctrl Pts',(77.5801381329828,269.277358097157,60.4906077744654));
#41572=CARTESIAN_POINT('Ctrl Pts',(70.8214010299961,268.746968073278,60.4056325247524));
#41573=CARTESIAN_POINT('Ctrl Pts',(66.5245229306788,268.110500044619,53.4973810987512));
#41574=CARTESIAN_POINT('Ctrl Pts',(70.0146846891176,267.474032015963,46.1658177307299));
#41575=CARTESIAN_POINT('Ctrl Pts',(78.0676616590457,266.837563987306,45.1253310940095));
#41576=CARTESIAN_POINT('Ctrl Pts',(83.2997256280266,266.201095958649,51.3553074815834));
#41577=CARTESIAN_POINT('Ctrl Pts',(81.2813379625202,265.670705934768,57.8061879836611));
#41578=CARTESIAN_POINT('Ctrl Pts',(76.9740348929436,265.246393915664,60.2012645394267));
#41579=CARTESIAN_POINT('Ctrl Pts',(72.0482033406272,264.822081896559,60.3607479535025));
#41580=CARTESIAN_POINT('Ctrl Pts',(67.0010950831651,264.291691872678,55.8647001048012));
#41581=CARTESIAN_POINT('Ctrl Pts',(68.2868957752895,263.655223844021,47.8314059022108));
#41582=CARTESIAN_POINT('Ctrl Pts',(75.7294686614734,263.018755815364,44.5846907386619));
#41583=CARTESIAN_POINT('Ctrl Pts',(82.491721281617,262.382287786707,49.0796868477532));
#41584=CARTESIAN_POINT('Ctrl Pts',(82.3567472759911,261.74581975805,57.2141125301874));
#41585=CARTESIAN_POINT('Ctrl Pts',(76.6028482236023,261.21542973417,60.7609976023698));
#41586=CARTESIAN_POINT('Ctrl Pts',(71.7803273753439,260.791117715065,59.744855826201));
#41587=CARTESIAN_POINT('Ctrl Pts',(67.9567596897789,260.366805695961,56.6352607408135));
#41588=CARTESIAN_POINT('Ctrl Pts',(67.0943896432094,259.836415672079,49.9312271845779));
#41589=CARTESIAN_POINT('Ctrl Pts',(73.3328200825553,259.199947643423,44.7092462559759));
#41590=CARTESIAN_POINT('Ctrl Pts',(81.0809045713872,258.563479614766,47.1382866577201));
#41591=CARTESIAN_POINT('Ctrl Pts',(83.2388937946819,257.927011586109,54.9661939790624));
#41592=CARTESIAN_POINT('Ctrl Pts',(77.8030197810562,257.290543557452,61.0191579532844));
#41593=CARTESIAN_POINT('Ctrl Pts',(71.1330498823766,256.760153533571,59.9240554142214));
#41594=CARTESIAN_POINT('Ctrl Pts',(68.1583716191361,256.335841514467,55.9946100753261));
#41595=CARTESIAN_POINT('Ctrl Pts',(67.3106359050502,255.911529495361,51.1396542979552));
#41596=CARTESIAN_POINT('Ctrl Pts',(71.0555698892031,255.381139471481,45.5126464363393));
#41597=CARTESIAN_POINT('Ctrl Pts',(79.1897666288785,254.744671442824,45.6607766678622));
#41598=CARTESIAN_POINT('Ctrl Pts',(83.4467609168083,254.108203414167,52.5753301713011));
#41599=CARTESIAN_POINT('Ctrl Pts',(79.94306077055,253.47173538551,59.9004332971613));
#41600=CARTESIAN_POINT('Ctrl Pts',(71.8698933621133,252.835267356853,60.905951651344));
#41601=CARTESIAN_POINT('Ctrl Pts',(67.5521726494623,252.304877332973,55.7054674558198));
#41602=CARTESIAN_POINT('Ctrl Pts',(67.8829448323149,251.880565313867,50.7881672611792));
#41603=CARTESIAN_POINT('Ctrl Pts',(70.4264360103071,251.456253294763,46.5668044399285));
#41604=CARTESIAN_POINT('Ctrl Pts',(76.9436368441984,250.925863270882,44.7740854683437));
#41605=CARTESIAN_POINT('Ctrl Pts',(82.9878010642769,250.289395242225,50.2197422740896));
#41606=CARTESIAN_POINT('Ctrl Pts',(81.6677557512237,249.652927213568,58.2316416051388));
#41607=CARTESIAN_POINT('Ctrl Pts',(74.2191975778626,249.016459184912,61.4646018055494));
#41608=CARTESIAN_POINT('Ctrl Pts',(67.4646309039848,248.379991156254,56.9299653026552));
#41609=CARTESIAN_POINT('Ctrl Pts',(67.6148650422271,247.849601132374,50.1723638254997));
#41610=CARTESIAN_POINT('Ctrl Pts',(71.0890075766938,247.425289113269,46.6767115127872));
#41611=CARTESIAN_POINT('Ctrl Pts',(75.7774017059763,247.000977094165,45.1574314432569));
#41612=CARTESIAN_POINT('Ctrl Pts',(81.87340699568,246.470587070284,48.0774430062916));
#41613=CARTESIAN_POINT('Ctrl Pts',(82.8658667097527,245.834119041627,56.1522261539176));
#41614=CARTESIAN_POINT('Ctrl Pts',(76.6156108827676,245.19765101297,61.3355988606232));
#41615=CARTESIAN_POINT('Ctrl Pts',(68.8720270293296,244.561182984313,58.8922487784292));
#41616=CARTESIAN_POINT('Ctrl Pts',(66.7458339833244,243.924714955656,51.039452951696));
#41617=CARTESIAN_POINT('Ctrl Pts',(71.2904074612936,243.394324931775,46.0359941556539));
#41618=CARTESIAN_POINT('Ctrl Pts',(76.2055723888366,242.970012912671,45.6748775869161));
#41619=CARTESIAN_POINT('Ctrl Pts',(80.7415318974397,242.545700893566,47.6021354257825));
#41620=CARTESIAN_POINT('Ctrl Pts',(83.4292672620948,242.015310869685,53.8040566305332));
#41621=CARTESIAN_POINT('Ctrl Pts',(78.8837120348752,241.378842841028,60.5512802700413));
#41622=CARTESIAN_POINT('Ctrl Pts',(70.7659036424594,240.742374812371,60.3662466963265));
#41623=CARTESIAN_POINT('Ctrl Pts',(66.5216905776815,240.105906783714,53.4438406131678));
#41624=CARTESIAN_POINT('Ctrl Pts',(70.0657168395739,239.469438755057,46.1207963677559));
#41625=CARTESIAN_POINT('Ctrl Pts',(76.7777649544276,238.939048731177,45.3232011544806));
#41626=CARTESIAN_POINT('Ctrl Pts',(80.7254958293852,238.514736712072,48.273569331517));
#41627=CARTESIAN_POINT('Ctrl Pts',(82.8863769043757,238.090424692968,52.702998687643));
#41628=CARTESIAN_POINT('Ctrl Pts',(80.8488379995376,237.560034669086,59.1478558025543));
#41629=CARTESIAN_POINT('Ctrl Pts',(72.9926135961208,236.92356664043,61.261345165764));
#41630=CARTESIAN_POINT('Ctrl Pts',(66.9850210825831,236.287098611772,55.7985727276454));
#41631=CARTESIAN_POINT('Ctrl Pts',(68.3198653405516,235.650630583116,47.7891257226176));
#41632=CARTESIAN_POINT('Ctrl Pts',(75.7975195609413,235.014162554458,44.5841629263389));
#41633=CARTESIAN_POINT('Ctrl Pts',(81.3881037350091,234.483772530579,48.3832571095637));
#41634=CARTESIAN_POINT('Ctrl Pts',(82.433991842377,234.059460511473,53.1994142403088));
#41635=CARTESIAN_POINT('Ctrl Pts',(81.1609514886376,233.635148492369,57.9605716309985));
#41636=CARTESIAN_POINT('Ctrl Pts',(75.3965430028564,233.104758468487,61.4903510616958));
#41637=CARTESIAN_POINT('Ctrl Pts',(68.0792403488523,232.468290439831,57.9344853393984));
#41638=CARTESIAN_POINT('Ctrl Pts',(67.1256153736941,231.831822411174,49.8707610183333));
#41639=CARTESIAN_POINT('Ctrl Pts',(73.3854363071609,231.195354382517,44.698943890854));
#41640=CARTESIAN_POINT('Ctrl Pts',(81.1326289242826,230.55888635386,47.182511026836));
#41641=CARTESIAN_POINT('Ctrl Pts',(82.8623337589318,230.028496329979,53.7167186456097));
#41642=CARTESIAN_POINT('Ctrl Pts',(80.4938884721818,229.604184310875,58.0387226211197));
#41643=CARTESIAN_POINT('Ctrl Pts',(76.4107231014128,229.17987229177,60.7986160968965));
#41644=CARTESIAN_POINT('Ctrl Pts',(69.7440352528211,228.649482267889,59.6837075155094));
#41645=CARTESIAN_POINT('Ctrl Pts',(66.5511708056287,228.013014239233,52.2008794545322));
#41646=CARTESIAN_POINT('Ctrl Pts',(71.1187945807649,227.376546210575,45.4874702176766));
#41647=CARTESIAN_POINT('Ctrl Pts',(79.2362472869139,226.740078181919,45.687500330039));
#41648=CARTESIAN_POINT('Ctrl Pts',(83.4568135234188,226.103610153261,52.6426365499872));
#41649=CARTESIAN_POINT('Ctrl Pts',(80.4780746217014,225.573220129381,58.7101617981617));
#41650=CARTESIAN_POINT('Ctrl Pts',(75.8558464940669,225.148908110276,60.4202081308665));
#41651=CARTESIAN_POINT('Ctrl Pts',(70.9633284069712,224.724596091172,59.8264754996315));
#41652=CARTESIAN_POINT('Ctrl Pts',(66.6610730582673,224.194206067291,54.6131899181505));
#41653=CARTESIAN_POINT('Ctrl Pts',(69.157166952132,223.557738038634,46.8700243015665));
#41654=CARTESIAN_POINT('Ctrl Pts',(77.0078801768239,222.921270009977,44.7965356614796));
#41655=CARTESIAN_POINT('Ctrl Pts',(83.005370185439,222.28480198132,50.2703972566507));
#41656=CARTESIAN_POINT('Ctrl Pts',(81.6312111896099,221.648333952663,58.289049463463));
#41657=CARTESIAN_POINT('Ctrl Pts',(75.403625026532,221.117943928782,60.9167734757233));
#41658=CARTESIAN_POINT('Ctrl Pts',(70.7925316075469,220.693631909677,59.1769303273695));
#41659=CARTESIAN_POINT('Ctrl Pts',(67.4880169134195,220.269319890573,55.5205041023283));
#41660=CARTESIAN_POINT('Ctrl Pts',(67.658328852938,219.738929866692,48.7633776943335));
#41661=CARTESIAN_POINT('Ctrl Pts',(74.6202688954666,219.102461838035,44.5540677770521));
#41662=CARTESIAN_POINT('Ctrl Pts',(81.9072044880662,218.465993809378,48.1365169238422));
#41663=CARTESIAN_POINT('Ctrl Pts',(82.8458867743987,217.829525780721,56.2019949911516));
#41664=CARTESIAN_POINT('Ctrl Pts',(76.5504328451881,217.193057752064,61.3549706278894));
#41665=CARTESIAN_POINT('Ctrl Pts',(70.1253934407355,216.662667728183,59.2553153217915));
#41666=CARTESIAN_POINT('Ctrl Pts',(67.7851257368055,216.238355709079,54.9180846330423));
#41667=CARTESIAN_POINT('Ctrl Pts',(67.6873898951343,215.814043689974,49.9906921806011));
#41668=CARTESIAN_POINT('Ctrl Pts',(72.2478204552385,215.283653666094,45.0006205160765));
#41669=CARTESIAN_POINT('Ctrl Pts',(80.2623903861754,214.647185637436,46.3879895849169));
#41670=CARTESIAN_POINT('Ctrl Pts',(83.4181495289489,214.01071760878,53.8705343916804));
#41671=CARTESIAN_POINT('Ctrl Pts',(78.8320462675723,213.374249580122,60.576285830569));
#41672=CARTESIAN_POINT('Ctrl Pts',(70.7115626079727,212.737781551466,60.3371402298481));
#41673=CARTESIAN_POINT('Ctrl Pts',(66.51967771935,212.101313522809,53.3818980605949));
#41674=CARTESIAN_POINT('Ctrl Pts',(70.1151634260747,211.464845494152,46.0859672328122));
#41675=CARTESIAN_POINT('Ctrl Pts',(76.8334970750981,210.934455470271,45.3360771801855));
#41676=CARTESIAN_POINT('Ctrl Pts',(80.7595195459134,210.510143451166,48.3151871536133));
#41677=CARTESIAN_POINT('Ctrl Pts',(82.888548276625,210.085831432062,52.7599210756032));
#41678=CARTESIAN_POINT('Ctrl Pts',(80.8044533787177,209.555441408181,59.1900246680587));
#41679=CARTESIAN_POINT('Ctrl Pts',(72.9332444349171,208.918973379524,61.2467132323923));
#41680=CARTESIAN_POINT('Ctrl Pts',(66.9651916338919,208.282505350867,55.7407703836971));
#41681=CARTESIAN_POINT('Ctrl Pts',(68.3578058098086,207.64603732221,47.7411455189258));
#41682=CARTESIAN_POINT('Ctrl Pts',(75.858380007233,207.009569293553,44.5902272647635));
#41683=CARTESIAN_POINT('Ctrl Pts',(81.4214132232327,206.479179269672,48.4295533629287));
#41684=CARTESIAN_POINT('Ctrl Pts',(82.4325231697244,206.054867250568,53.2531336492902));
#41685=CARTESIAN_POINT('Ctrl Pts',(81.1251652983051,205.630555231463,58.0049808791072));
#41686=CARTESIAN_POINT('Ctrl Pts',(75.3354386547323,205.100165207582,61.4930789706004));
#41687=CARTESIAN_POINT('Ctrl Pts',(68.0439825137209,204.463697178926,57.8845109023309));
#41688=CARTESIAN_POINT('Ctrl Pts',(67.1485620295659,203.827229150268,49.8141162822962));
#41689=CARTESIAN_POINT('Ctrl Pts',(73.4455348837261,203.190761121612,44.6875983460268));
#41690=CARTESIAN_POINT('Ctrl Pts',(81.1746068125109,202.554293092954,47.2269970174668));
#41691=CARTESIAN_POINT('Ctrl Pts',(82.8571222576213,202.023903069074,53.773514367668));
#41692=CARTESIAN_POINT('Ctrl Pts',(80.457555279028,201.599591049969,58.0783174973361));
#41693=CARTESIAN_POINT('Ctrl Pts',(76.3545835235771,201.175279030865,60.8086790297828));
#41694=CARTESIAN_POINT('Ctrl Pts',(69.6961132750877,200.644889006984,59.6456992226426));
#41695=CARTESIAN_POINT('Ctrl Pts',(66.5573206522378,200.008420978327,52.1400293614303));
#41696=CARTESIAN_POINT('Ctrl Pts',(71.1732628826331,199.37195294967,45.4597503397074));
#41697=CARTESIAN_POINT('Ctrl Pts',(79.2890610861173,198.735484921013,45.7183427854784));
#41698=CARTESIAN_POINT('Ctrl Pts',(83.4593360519497,198.099016892356,52.7037494220058));
#41699=CARTESIAN_POINT('Ctrl Pts',(80.4368974067114,197.568626868475,58.7496250948249));
#41700=CARTESIAN_POINT('Ctrl Pts',(75.8024515672505,197.144314849371,60.4262774749522));
#41701=CARTESIAN_POINT('Ctrl Pts',(70.9143446388831,196.720002830266,59.7972607045105));
#41702=CARTESIAN_POINT('Ctrl Pts',(66.649815151398,196.189612806385,54.553069988049));
#41703=CARTESIAN_POINT('Ctrl Pts',(69.2017112256344,195.553144777728,46.8281152573069));
#41704=CARTESIAN_POINT('Ctrl Pts',(77.0671801888051,194.916676749071,44.8113236199402));
#41705=CARTESIAN_POINT('Ctrl Pts',(83.0250204169708,194.280208720415,50.328314678029));
#41706=CARTESIAN_POINT('Ctrl Pts',(81.5930418740195,193.643740691757,58.3368436701622));
#41707=CARTESIAN_POINT('Ctrl Pts',(75.3466598718807,193.113350667877,60.9195670203631));
#41708=CARTESIAN_POINT('Ctrl Pts',(70.7482377838634,192.689038648772,59.146500258619));
#41709=CARTESIAN_POINT('Ctrl Pts',(67.4701935758559,192.264726629667,55.4663266741922));
#41710=CARTESIAN_POINT('Ctrl Pts',(67.6892465309357,191.734336605787,48.7106058523097));
#41711=CARTESIAN_POINT('Ctrl Pts',(74.6813889215455,191.09786857713,44.5516343502816));
#41712=CARTESIAN_POINT('Ctrl Pts',(81.9422638078207,190.461400548472,48.1865685182189));
#41713=CARTESIAN_POINT('Ctrl Pts',(82.8227732812904,189.824932519816,56.2586037997643));
#41714=CARTESIAN_POINT('Ctrl Pts',(76.4902181824824,189.188464491159,61.3660341796913));
#41715=CARTESIAN_POINT('Ctrl Pts',(70.0806525778287,188.658074467278,59.2200572972461));
#41716=CARTESIAN_POINT('Ctrl Pts',(67.7715050437085,188.233762448174,54.8660833530394));
#41717=CARTESIAN_POINT('Ctrl Pts',(67.709782312098,187.809450429068,49.938057201976));
#41718=CARTESIAN_POINT('Ctrl Pts',(72.3050806194153,187.279060405188,44.9811447065694));
#41719=CARTESIAN_POINT('Ctrl Pts',(80.3112830930193,186.642592376531,46.4260741570604));
#41720=CARTESIAN_POINT('Ctrl Pts',(83.4096973447483,186.006124347874,53.9315974328931));
#41721=CARTESIAN_POINT('Ctrl Pts',(78.7814218299252,185.369656319217,60.6033375565992));
#41722=CARTESIAN_POINT('Ctrl Pts',(70.6512751961183,184.73318829056,60.307001804386));
#41723=CARTESIAN_POINT('Ctrl Pts',(67.2192465592645,184.202798266679,54.4838645523399));
#41724=CARTESIAN_POINT('Ctrl Pts',(68.3308679122969,183.778486247575,49.6824533630493));
#41725=CARTESIAN_POINT('Ctrl Pts',(71.5157111174391,183.35417422847,45.9213331576022));
#41726=CARTESIAN_POINT('Ctrl Pts',(78.2355346432551,182.823784204589,45.1921419602876));
#41727=CARTESIAN_POINT('Ctrl Pts',(83.3327162377549,182.187316175932,51.5329493976676));
#41728=CARTESIAN_POINT('Ctrl Pts',(80.7504307142551,181.550848147276,59.2313162371021));
#41729=CARTESIAN_POINT('Ctrl Pts',(72.8812493485224,180.914380118618,61.2335737511561));
#41730=CARTESIAN_POINT('Ctrl Pts',(66.9373254266475,180.277912089962,55.6786779306922));
#41731=CARTESIAN_POINT('Ctrl Pts',(68.1645456866902,179.747522066081,49.0317479285263));
#41732=CARTESIAN_POINT('Ctrl Pts',(72.1522356671046,179.323210046976,46.1356160148762));
#41733=CARTESIAN_POINT('Ctrl Pts',(77.023055030443,178.898898027871,45.3843702688699));
#41734=CARTESIAN_POINT('Ctrl Pts',(82.5746552051696,178.368508003991,49.2402078588529));
#41735=CARTESIAN_POINT('Ctrl Pts',(82.2651703589308,177.732039975334,57.3698645733266));
#41736=CARTESIAN_POINT('Ctrl Pts',(75.2675184325902,177.095571946677,61.4888350802814));
#41737=CARTESIAN_POINT('Ctrl Pts',(68.0133711206639,176.45910391802,57.840493361602));
#41738=CARTESIAN_POINT('Ctrl Pts',(67.1682236282861,175.822635889363,49.7489653920918));
#41739=CARTESIAN_POINT('Ctrl Pts',(72.4533484582045,175.292245865482,45.5352730026869));
#41740=CARTESIAN_POINT('Ctrl Pts',(77.3631181809475,174.867933846378,45.963540104857));
#41741=CARTESIAN_POINT('Ctrl Pts',(81.53318681453,174.443621827273,48.5902831513639));
#41742=CARTESIAN_POINT('Ctrl Pts',(83.1962506025606,173.913231803392,55.1417690024739));
#41743=CARTESIAN_POINT('Ctrl Pts',(77.6317485041141,173.276763774735,61.0767008101384));
#41744=CARTESIAN_POINT('Ctrl Pts',(69.6476161095727,172.640295746078,59.5979579569643));
#41745=CARTESIAN_POINT('Ctrl Pts',(66.5630728625792,172.003827717421,52.0867234727528));
#41746=CARTESIAN_POINT('Ctrl Pts',(71.2308284781632,171.367359688764,45.4234542542364));
#41747=CARTESIAN_POINT('Ctrl Pts',(77.984119150899,170.836969664883,45.7077307215896));
#41748=CARTESIAN_POINT('Ctrl Pts',(81.4101558487953,170.412657645779,49.2505437262273));
#41749=CARTESIAN_POINT('Ctrl Pts',(82.8361183764638,169.988345626674,53.968157774753));
#41750=CARTESIAN_POINT('Ctrl Pts',(79.7957358492659,169.457955602793,60.0050296558403));
#41751=CARTESIAN_POINT('Ctrl Pts',(71.7028515441215,168.821487574137,60.8370890219851));
#41752=CARTESIAN_POINT('Ctrl Pts',(66.6445051896481,168.18501954548,54.4852245179543));
#41753=CARTESIAN_POINT('Ctrl Pts',(69.2410082836161,167.548551516823,46.7916413343917));
#41754=CARTESIAN_POINT('Ctrl Pts',(77.1344424145289,166.912083488166,44.8216675309665));
#41755=CARTESIAN_POINT('Ctrl Pts',(82.0467512839816,166.381693464285,49.4646159036547));
#41756=CARTESIAN_POINT('Ctrl Pts',(82.3102791092707,165.95738144518,54.3859779637414));
#41757=CARTESIAN_POINT('Ctrl Pts',(80.2934064564848,165.533069426076,58.8828075295142));
#41758=CARTESIAN_POINT('Ctrl Pts',(74.039380907102,165.002679402195,61.446966738303));
#41759=CARTESIAN_POINT('Ctrl Pts',(67.3836699068338,164.366211373538,56.7684402345682));
#41760=CARTESIAN_POINT('Ctrl Pts',(67.7297256839352,163.729743344881,48.6559008097939));
#41761=CARTESIAN_POINT('Ctrl Pts',(74.7349750628069,163.093275316224,44.5498648066396));
#41762=CARTESIAN_POINT('Ctrl Pts',(81.9862638229229,162.456807287567,48.2384838548278));
#41763=CARTESIAN_POINT('Ctrl Pts',(82.6505339267891,161.926417263686,54.9650352185995));
#41764=CARTESIAN_POINT('Ctrl Pts',(79.6224228708578,161.502105244582,58.8534532612115));
#41765=CARTESIAN_POINT('Ctrl Pts',(75.1509931548911,161.077793225477,60.9260284073355));
#41766=CARTESIAN_POINT('Ctrl Pts',(68.7478297154571,160.547403201596,58.7610235601704));
#41767=CARTESIAN_POINT('Ctrl Pts',(66.7906251178065,159.910935172939,50.8644135705499));
#41768=CARTESIAN_POINT('Ctrl Pts',(72.3715138911219,159.274467144282,44.9663858477208));
#41769=CARTESIAN_POINT('Ctrl Pts',(80.3529008288988,158.637999115625,46.4598760783115));
#41770=CARTESIAN_POINT('Ctrl Pts',(83.4088749123851,158.001531086968,53.9996454094183));
#41771=CARTESIAN_POINT('Ctrl Pts',(79.4996104357941,157.471141063088,59.5137545190037));
#41772=CARTESIAN_POINT('Ctrl Pts',(74.6636507067732,157.046829043983,60.4638834262844));
#41773=CARTESIAN_POINT('Ctrl Pts',(69.9286878056629,156.622517024879,59.0966315232787));
#41774=CARTESIAN_POINT('Ctrl Pts',(66.5139699521479,156.092127000998,53.2633262851448));
#41775=CARTESIAN_POINT('Ctrl Pts',(70.2143122162198,155.455658972341,46.0180128830924));
#41776=CARTESIAN_POINT('Ctrl Pts',(78.2953693841028,154.819190943683,45.2245612029049));
#41777=CARTESIAN_POINT('Ctrl Pts',(83.3419726606467,154.182722915027,51.5857596661316));
#41778=CARTESIAN_POINT('Ctrl Pts',(80.7051888305738,153.54625488637,59.282152990196));
#41779=CARTESIAN_POINT('Ctrl Pts',(74.1379497527392,153.015864862489,60.8818776274124));
#41780=CARTESIAN_POINT('Ctrl Pts',(69.8637868359816,152.591552843385,58.4281492801464));
#41781=CARTESIAN_POINT('Ctrl Pts',(67.1854472627357,152.16724082428,54.2910308903069));
#41782=CARTESIAN_POINT('Ctrl Pts',(68.432404550129,151.636850800399,47.647775246892));
#41783=CARTESIAN_POINT('Ctrl Pts',(75.9771066703128,151.000382771742,44.6039997816288));
#41784=CARTESIAN_POINT('Ctrl Pts',(82.5985720801216,150.363914743085,49.3039196049969));
#41785=CARTESIAN_POINT('Ctrl Pts',(82.2375297733488,149.727446714428,57.4158058820656));
#41786=CARTESIAN_POINT('Ctrl Pts',(75.2000258565176,149.090978685771,61.497550335829));
#41787=CARTESIAN_POINT('Ctrl Pts',(69.1927935718333,148.56058866189,58.3990170863381));
#41788=CARTESIAN_POINT('Ctrl Pts',(67.5747895850749,148.136276642786,53.7437711701705));
#41789=CARTESIAN_POINT('Ctrl Pts',(68.2654736973507,147.711964623681,48.8639958783961));
#41790=CARTESIAN_POINT('Ctrl Pts',(73.5630905523075,147.1815745998,44.6660197376315));
#41791=CARTESIAN_POINT('Ctrl Pts',(81.2552091462713,146.545106571144,47.315248059547));
#41792=CARTESIAN_POINT('Ctrl Pts',(83.172530218171,145.908638542486,55.2055541642953));
#41793=CARTESIAN_POINT('Ctrl Pts',(77.5807549411311,145.27217051383,61.0932616783001));
#41794=CARTESIAN_POINT('Ctrl Pts',(69.5909445553386,144.635702485172,59.5602811942995));
#41795=CARTESIAN_POINT('Ctrl Pts',(67.0872942092809,144.105312461292,53.2817875083084));
#41796=CARTESIAN_POINT('Ctrl Pts',(68.9182795434562,143.681000442187,48.7061187979232));
#41797=CARTESIAN_POINT('Ctrl Pts',(72.6395485245209,143.256688423083,45.4748019438016));
#41798=CARTESIAN_POINT('Ctrl Pts',(79.3919650625709,142.726298399202,45.7791355058949));
#41799=CARTESIAN_POINT('Ctrl Pts',(83.4623219070964,142.089830370545,52.8232319222899));
#41800=CARTESIAN_POINT('Ctrl Pts',(79.7360013175807,141.453362341888,60.0376331714256));
#41801=CARTESIAN_POINT('Ctrl Pts',(71.6534921155156,140.816894313231,60.8161545378098));
#41802=CARTESIAN_POINT('Ctrl Pts',(66.6264240143533,140.180426284574,54.4196175472566));
#41803=CARTESIAN_POINT('Ctrl Pts',(68.8531573323029,139.650036260693,48.0376580714305));
#41804=CARTESIAN_POINT('Ctrl Pts',(73.2359396256076,139.225724241589,45.7836680957074));
#41805=CARTESIAN_POINT('Ctrl Pts',(78.164352269396,138.801412222484,45.784171788142));
#41806=CARTESIAN_POINT('Ctrl Pts',(83.0628491749938,138.271022198603,50.4416900206561));
#41807=CARTESIAN_POINT('Ctrl Pts',(81.5169481905285,137.634554169946,58.4290105545691));
#41808=CARTESIAN_POINT('Ctrl Pts',(73.9729024601451,136.998086141289,61.4324127149976));
#41809=CARTESIAN_POINT('Ctrl Pts',(67.3601309900174,136.361618112632,56.7202684044691));
#41810=CARTESIAN_POINT('Ctrl Pts',(67.7590947577619,135.725150083975,48.5945113888264));
#41811=CARTESIAN_POINT('Ctrl Pts',(73.6251008021535,135.194760060095,45.2362795463956));
#41812=CARTESIAN_POINT('Ctrl Pts',(78.4120938759237,134.77044804099,46.408435147345));
#41813=CARTESIAN_POINT('Ctrl Pts',(82.1327022867324,134.346136021885,49.640512574416));
#41814=CARTESIAN_POINT('Ctrl Pts',(82.7769905318885,133.815745998004,56.369007255807));
#41815=CARTESIAN_POINT('Ctrl Pts',(76.3723312622475,133.179277969348,61.385723194052));
#41816=CARTESIAN_POINT('Ctrl Pts',(68.7071821389033,132.542809940691,58.7064435452887));
#41817=CARTESIAN_POINT('Ctrl Pts',(66.804440904768,131.906341912034,50.8126088424777));
#41818=CARTESIAN_POINT('Ctrl Pts',(72.4339422147442,131.269873883377,44.9392951128856));
#41819=CARTESIAN_POINT('Ctrl Pts',(79.0648474342985,130.739483859496,46.2503420188497));
#41820=CARTESIAN_POINT('Ctrl Pts',(81.9103997196017,130.315171840391,50.2742808395536));
#41821=CARTESIAN_POINT('Ctrl Pts',(82.6000863742362,129.890859821287,55.1541972076467));
#41822=CARTESIAN_POINT('Ctrl Pts',(78.6744613590471,129.360469797406,60.6566708568771));
#41823=CARTESIAN_POINT('Ctrl Pts',(70.5493602448022,128.724001768749,60.2445652289898));
#41824=CARTESIAN_POINT('Ctrl Pts',(66.5190707704739,128.087533740092,53.1954647705981));
#41825=CARTESIAN_POINT('Ctrl Pts',(70.2587128993032,127.451065711435,45.987959843949));
#41826=CARTESIAN_POINT('Ctrl Pts',(78.3602667533996,126.814597682778,45.245043755542));
#41827=CARTESIAN_POINT('Ctrl Pts',(82.5068930122806,126.284207658897,50.5829495892478));
#41828=CARTESIAN_POINT('Ctrl Pts',(82.0166690505848,125.859895639793,55.4869206238833));
#41829=CARTESIAN_POINT('Ctrl Pts',(79.3374838917574,125.435583620688,59.6234914652784));
#41830=CARTESIAN_POINT('Ctrl Pts',(72.7655223446663,124.905193596807,61.203703300415));
#41831=CARTESIAN_POINT('Ctrl Pts',(66.9013213018522,124.268725568151,55.564710013072));
#41832=CARTESIAN_POINT('Ctrl Pts',(68.4807543357559,123.632257539493,47.599884728686));
#41833=CARTESIAN_POINT('Ctrl Pts',(76.0303356832701,122.995789510837,44.610424577313));
#41834=CARTESIAN_POINT('Ctrl Pts',(82.634138445717,122.359321482179,49.3619388875029));
#41835=CARTESIAN_POINT('Ctrl Pts',(82.2646172536146,121.828931458299,56.1111019547982));
#41836=CARTESIAN_POINT('Ctrl Pts',(78.6788293425275,121.404619439194,59.4921338236011));
#41837=CARTESIAN_POINT('Ctrl Pts',(73.9435870692403,120.98030742009,60.8584178549934));
#41838=CARTESIAN_POINT('Ctrl Pts',(67.9455844192023,120.449917396209,57.742055836471));
#41839=CARTESIAN_POINT('Ctrl Pts',(67.2157725389121,119.813449367552,49.6393110061912));
#41840=CARTESIAN_POINT('Ctrl Pts',(73.630997658148,119.176981338895,44.6615668194227));
#41841=CARTESIAN_POINT('Ctrl Pts',(81.2911839951798,118.540513310238,47.3550025066695));
#41842=CARTESIAN_POINT('Ctrl Pts',(83.1613378754544,117.904045281581,55.2726804256891));
#41843=CARTESIAN_POINT('Ctrl Pts',(78.4567365434457,117.3736552577,60.1259756286634));
#41844=CARTESIAN_POINT('Ctrl Pts',(73.5324394582474,116.949343238595,60.3273450848164));
#41845=CARTESIAN_POINT('Ctrl Pts',(69.0614334773316,116.525031219491,58.2538560060471));
#41846=CARTESIAN_POINT('Ctrl Pts',(66.5764423007162,115.99464119561,51.967953773869));
#41847=CARTESIAN_POINT('Ctrl Pts',(71.3386312100502,115.358173166953,45.3718446209629));
#41848=CARTESIAN_POINT('Ctrl Pts',(79.4461546526474,114.721705138296,45.8203021408262));
#41849=CARTESIAN_POINT('Ctrl Pts',(83.4634147283923,114.085237109639,52.8768361344529));
#41850=CARTESIAN_POINT('Ctrl Pts',(79.6835345728483,113.448769080982,60.0809741935798));
#41851=CARTESIAN_POINT('Ctrl Pts',(72.9491322867537,112.918379057102,60.6602615742436));
#41852=CARTESIAN_POINT('Ctrl Pts',(69.0992572779785,112.494067037997,57.5832965341482));
#41853=CARTESIAN_POINT('Ctrl Pts',(67.0833038350869,112.069755018892,53.0860548064605));
#41854=CARTESIAN_POINT('Ctrl Pts',(69.3289827669467,111.539364995011,46.7107372335584));
#41855=CARTESIAN_POINT('Ctrl Pts',(77.249675066892,110.902896966355,44.853391639753));
#41856=CARTESIAN_POINT('Ctrl Pts',(83.0767680675852,110.266428937698,50.5083043429388));
#41857=CARTESIAN_POINT('Ctrl Pts',(81.4826234960783,109.629960909041,58.4701981882822));
#41858=CARTESIAN_POINT('Ctrl Pts',(73.9048702919147,108.993492880384,61.4307311710459));
#41859=CARTESIAN_POINT('Ctrl Pts',(68.440559289883,108.463102856503,57.4521568920576));
#41860=CARTESIAN_POINT('Ctrl Pts',(67.5515651878163,108.038790837398,52.6045862708441));
#41861=CARTESIAN_POINT('Ctrl Pts',(68.9784919825808,107.614478818294,47.8872637926212));
#41862=CARTESIAN_POINT('Ctrl Pts',(74.8544466357378,107.084088794413,44.5464697351562));
#41863=CARTESIAN_POINT('Ctrl Pts',(82.0524617951992,106.447620765756,48.337996726937));
#41864=CARTESIAN_POINT('Ctrl Pts',(82.7438183970427,105.811152737099,56.4284279001484));
#41865=CARTESIAN_POINT('Ctrl Pts',(76.319408331325,105.174684708442,61.3943120940143));
#41866=CARTESIAN_POINT('Ctrl Pts',(68.6569206643761,104.538216679785,58.6605634005361));
#41867=CARTESIAN_POINT('Ctrl Pts',(67.1402418322057,104.007826655904,52.0736496057157));
#41868=CARTESIAN_POINT('Ctrl Pts',(69.6477403827077,103.5835146368,47.8308082864586));
#41869=CARTESIAN_POINT('Ctrl Pts',(73.8183458446825,103.159202617695,45.204917671504));
#41870=CARTESIAN_POINT('Ctrl Pts',(80.4453277976839,102.628812593814,46.5356536389092));
#41871=CARTESIAN_POINT('Ctrl Pts',(83.3936008529561,101.992344565157,54.1181852185861));
#41872=CARTESIAN_POINT('Ctrl Pts',(78.6104527158214,101.355876536501,60.6797813976882));
#41873=CARTESIAN_POINT('Ctrl Pts',(70.5037715895374,100.719408507843,60.2163467894311));
#41874=CARTESIAN_POINT('Ctrl Pts',(66.5112083742668,100.082940479187,53.1278675352251));
#41875=CARTESIAN_POINT('Ctrl Pts',(69.6853422487638,99.5525504553057,47.1602363328864));
#41876=CARTESIAN_POINT('Ctrl Pts',(74.3606460862077,99.1282384362012,45.6011386872139));
#41877=CARTESIAN_POINT('Ctrl Pts',(79.2313117905229,98.7039264170964,46.3533800301158));
#41878=CARTESIAN_POINT('Ctrl Pts',(83.3620653286017,98.1735363932159,51.7035784589593));
#41879=CARTESIAN_POINT('Ctrl Pts',(80.6159271082092,97.5370683645586,59.3616346117788));
#41880=CARTESIAN_POINT('Ctrl Pts',(72.7020417620283,96.9006003359019,61.1791794521838));
#41881=CARTESIAN_POINT('Ctrl Pts',(66.8854056010564,96.2641323072449,55.5135114165275));
#41882=CARTESIAN_POINT('Ctrl Pts',(68.5191436330107,95.6276642785879,47.5436934005256));
#41883=CARTESIAN_POINT('Ctrl Pts',(74.8287480634794,95.0972742547072,45.1195151992875));
#41884=CARTESIAN_POINT('Ctrl Pts',(79.3809339271596,94.6729622356025,47.008127203822));
#41885=CARTESIAN_POINT('Ctrl Pts',(82.5650082795865,94.2486502164979,50.7698983238375));
#41886=CARTESIAN_POINT('Ctrl Pts',(82.175442628398,93.7182601926172,57.5179340842469));
#41887=CARTESIAN_POINT('Ctrl Pts',(75.0805151806506,93.0817921639601,61.4990273607779));
#41888=CARTESIAN_POINT('Ctrl Pts',(67.913737713677,92.4453241353032,57.6819144127156));
#41889=CARTESIAN_POINT('Ctrl Pts',(67.2373285689711,91.8088561066465,49.5902198319534));
#41890=CARTESIAN_POINT('Ctrl Pts',(73.6968276930205,91.1723880779892,44.6443154422948));
#41891=CARTESIAN_POINT('Ctrl Pts',(80.0501636057682,90.6419980541087,46.9514502021527));
#41892=CARTESIAN_POINT('Ctrl Pts',(82.248636684147,90.2176860350039,51.3623421261072));
#41893=CARTESIAN_POINT('Ctrl Pts',(82.1859066479681,89.7933740158994,56.2903555578788));
#41894=CARTESIAN_POINT('Ctrl Pts',(77.4669110080675,89.2629839920186,61.1296559381968));
#41895=CARTESIAN_POINT('Ctrl Pts',(69.4997457803577,88.6265159633616,59.4830298726876));
#41896=CARTESIAN_POINT('Ctrl Pts',(66.5918345240826,87.9900479347046,51.9016643858503));
#41897=CARTESIAN_POINT('Ctrl Pts',(71.387096403826,87.3535799060477,45.3489158004046));
#41898=CARTESIAN_POINT('Ctrl Pts',(79.5071683647652,86.7171118773907,45.8504439794842));
#41899=CARTESIAN_POINT('Ctrl Pts',(82.7910680317342,86.18672185351,51.7583836370666));
#41900=CARTESIAN_POINT('Ctrl Pts',(81.5585650520041,85.7624098344053,56.530195436176));
#41901=CARTESIAN_POINT('Ctrl Pts',(78.2797686720669,85.3380978153008,60.2096988999699));
#41902=CARTESIAN_POINT('Ctrl Pts',(71.5436755152033,84.8077077914198,60.7689814782875));
#41903=CARTESIAN_POINT('Ctrl Pts',(66.608225015574,84.1712397627631,54.3014914295169));
#41904=CARTESIAN_POINT('Ctrl Pts',(69.3840716494891,83.534771734106,46.6707820270848));
#41905=CARTESIAN_POINT('Ctrl Pts',(77.3013012267029,82.8983037054491,44.8678604145149));
#41906=CARTESIAN_POINT('Ctrl Pts',(83.1030684198422,82.2618356767922,50.5710697392593));
#41907=CARTESIAN_POINT('Ctrl Pts',(81.7084038796298,81.7314456529114,57.1848930541526));
#41908=CARTESIAN_POINT('Ctrl Pts',(77.6488577290056,81.3071336338068,59.9794120632335));
#41909=CARTESIAN_POINT('Ctrl Pts',(72.7606223294546,80.882821614702,60.6074296742434));
#41910=CARTESIAN_POINT('Ctrl Pts',(67.308152429271,80.3524315908214,56.6126430706874));
#41911=CARTESIAN_POINT('Ctrl Pts',(67.8228131394891,79.7159635621643,48.4933928886451));
#41912=CARTESIAN_POINT('Ctrl Pts',(74.9222383377375,79.0794955335076,44.5524269697548));
#41913=CARTESIAN_POINT('Ctrl Pts',(82.0819518335224,78.4430275048504,48.3827733219354));
#41914=CARTESIAN_POINT('Ctrl Pts',(82.7225180796838,77.8065594761937,56.4930614826308));
#41915=CARTESIAN_POINT('Ctrl Pts',(77.3326822297666,77.2761694523128,60.5719605413598));
#41916=CARTESIAN_POINT('Ctrl Pts',(72.4352916914142,76.8518574332081,60.0198578733533));
#41917=CARTESIAN_POINT('Ctrl Pts',(68.3328781087648,76.4275454141036,57.2886577272533));
#41918=CARTESIAN_POINT('Ctrl Pts',(66.8357701494069,75.8971553902227,50.6972682092248));
#41919=CARTESIAN_POINT('Ctrl Pts',(72.548355637658,75.2606873615658,44.9047328226551));
#41920=CARTESIAN_POINT('Ctrl Pts',(80.4926040316474,74.6242193329087,46.5846042385617));
#41921=CARTESIAN_POINT('Ctrl Pts',(83.3865044972309,73.987751304252,54.1713288687746));
#41922=CARTESIAN_POINT('Ctrl Pts',(78.5519889954277,73.3512832755949,60.7146123738708));
#41923=CARTESIAN_POINT('Ctrl Pts',(71.808029508702,72.8208932517142,60.2599053673781));
#41924=CARTESIAN_POINT('Ctrl Pts',(68.4725414848908,72.3965812326095,56.6317142086632));
#41925=CARTESIAN_POINT('Ctrl Pts',(67.166153767543,71.9722692135049,51.8795986194627));
#41926=CARTESIAN_POINT('Ctrl Pts',(70.3579984560808,71.4418791896241,45.9214214229869));
#41927=CARTESIAN_POINT('Ctrl Pts',(78.4693120436398,70.8054111609672,45.2939733777076));
#41928=CARTESIAN_POINT('Ctrl Pts',(83.3656604933546,70.1689431323102,51.7715363745729));
#41929=CARTESIAN_POINT('Ctrl Pts',(80.5757216097465,69.5324751036534,59.3971046514366));
#41930=CARTESIAN_POINT('Ctrl Pts',(72.6350621664635,68.8960070749963,61.1671404621037));
#41931=CARTESIAN_POINT('Ctrl Pts',(67.8415543592253,68.3656170511155,56.401636194736));
#41932=CARTESIAN_POINT('Ctrl Pts',(67.7023753752291,67.9413050320109,51.4751891330521));
#41933=CARTESIAN_POINT('Ctrl Pts',(69.8321503171176,67.5169930129063,47.0307195203685));
#41934=CARTESIAN_POINT('Ctrl Pts',(76.1489271116202,66.9866029890255,44.6252925418915));
#41935=CARTESIAN_POINT('Ctrl Pts',(82.6843828424258,66.3501349603685,49.47038465205));
#41936=CARTESIAN_POINT('Ctrl Pts',(82.1335950744637,65.7136669317117,57.57159958279));
#41937=CARTESIAN_POINT('Ctrl Pts',(75.0269014433569,65.0771989030547,61.4994432855063));
#41938=CARTESIAN_POINT('Ctrl Pts',(67.8710625940478,64.4407308743976,57.6289046242914));
#41939=CARTESIAN_POINT('Ctrl Pts',(67.3768502886019,63.910340850517,50.8877250377879));
#41940=CARTESIAN_POINT('Ctrl Pts',(70.5021787723569,63.4860288314123,47.0770068233573));
#41941=CARTESIAN_POINT('Ctrl Pts',(75.0245155457956,63.0617168123077,45.1179964740309));
#41942=CARTESIAN_POINT('Ctrl Pts',(81.3709708767905,62.531326788427,47.4439914766132));
#41943=CARTESIAN_POINT('Ctrl Pts',(83.1281613622351,61.8948587597698,55.3875033424759));
#41944=CARTESIAN_POINT('Ctrl Pts',(77.4001262550961,61.258390731113,61.1427326455332));
#41945=CARTESIAN_POINT('Ctrl Pts',(69.4589948150873,60.621922702456,59.4481878772006));
#41946=CARTESIAN_POINT('Ctrl Pts',(66.5943749115452,59.9854546737991,51.8336588718405));
#41947=CARTESIAN_POINT('Ctrl Pts',(70.6416247147348,59.4550646499183,46.4200171168907));
#41948=CARTESIAN_POINT('Ctrl Pts',(75.5000334115163,59.0307526308137,45.5922995465797));
#41949=CARTESIAN_POINT('Ctrl Pts',(80.1989634148402,58.6064406117091,47.0786737474534));
#41950=CARTESIAN_POINT('Ctrl Pts',(83.4653010752091,58.0760505878282,52.9963410504375));
#41951=CARTESIAN_POINT('Ctrl Pts',(79.5831938141838,57.4395825591714,60.1459104346127));
#41952=CARTESIAN_POINT('Ctrl Pts',(71.4846784404145,56.8031145305144,60.7350617396308));
#41953=CARTESIAN_POINT('Ctrl Pts',(66.6003050078138,56.1666465018575,54.248464273294));
#41954=CARTESIAN_POINT('Ctrl Pts',(69.4305827409398,55.5301784732006,46.6211038439836));
#41955=CARTESIAN_POINT('Ctrl Pts',(76.0361211439636,54.9997884493197,45.1877126110912));
#41956=CARTESIAN_POINT('Ctrl Pts',(80.2469644571503,54.575476430215,47.7485816106596));
#41957=CARTESIAN_POINT('Ctrl Pts',(82.819987485169,54.1511644111105,51.9520092522931));
#41958=CARTESIAN_POINT('Ctrl Pts',(81.4056849883237,53.6207743872297,58.561661018292));
#41959=CARTESIAN_POINT('Ctrl Pts',(73.7865327827989,52.9843063585727,61.4139616395946));
#41960=CARTESIAN_POINT('Ctrl Pts',(67.2858519069638,52.3478383299158,56.5483477348614));
#41961=CARTESIAN_POINT('Ctrl Pts',(67.8516049343422,51.7113703012588,48.4481641547567));
#41962=CARTESIAN_POINT('Ctrl Pts',(74.9899294558238,51.0749022726019,44.5454186863394));
#41963=CARTESIAN_POINT('Ctrl Pts',(80.9170081952258,50.5445122487211,47.7946471543425));
#41964=CARTESIAN_POINT('Ctrl Pts',(82.4169509430253,50.1202002296165,52.4892635598102));
#41965=CARTESIAN_POINT('Ctrl Pts',(81.6032722944373,49.6958882105118,57.3500431781426));
#41966=CARTESIAN_POINT('Ctrl Pts',(76.2013452390112,49.1654981866312,61.4129155743917));
#41967=CARTESIAN_POINT('Ctrl Pts',(68.5785724013713,48.529030157974,58.5703052544606));
#41968=CARTESIAN_POINT('Ctrl Pts',(66.8610935518025,47.8925621293172,50.6341023260653));
#41969=CARTESIAN_POINT('Ctrl Pts',(72.5997511055059,47.2560941006602,44.8894648265617));
#41970=CARTESIAN_POINT('Ctrl Pts',(80.5483061755169,46.6196260720033,46.6236999502513));
#41971=CARTESIAN_POINT('Ctrl Pts',(82.8926257609871,46.0892360481225,52.9634092260413));
#41972=CARTESIAN_POINT('Ctrl Pts',(80.9466881752093,45.6649240290179,57.4913865176607));
#41973=CARTESIAN_POINT('Ctrl Pts',(77.1450146309224,45.2406120099132,60.6277107521473));
#41974=CARTESIAN_POINT('Ctrl Pts',(70.4024354435628,44.7102219860325,60.1529751177799));
#41975=CARTESIAN_POINT('Ctrl Pts',(66.5112404148095,44.0737539573755,53.0083477367719));
#41976=CARTESIAN_POINT('Ctrl Pts',(70.4185371839515,43.4372859287186,45.8903366046345));
#41977=CARTESIAN_POINT('Ctrl Pts',(78.5181271372242,42.8008179000617,45.3161475171128));
#41978=CARTESIAN_POINT('Ctrl Pts',(83.3820793220409,42.1643498714047,51.8375789787671));
#41979=CARTESIAN_POINT('Ctrl Pts',(80.9949109317497,41.6339598475238,58.161278457454));
#41980=CARTESIAN_POINT('Ctrl Pts',(76.5566125769281,41.2096478284193,60.3038841502383));
#41981=CARTESIAN_POINT('Ctrl Pts',(71.6297839982718,40.7853358093146,60.1789377709565));
#41982=CARTESIAN_POINT('Ctrl Pts',(66.8504516413873,40.2549457854338,55.399217042421));
#41983=CARTESIAN_POINT('Ctrl Pts',(68.5975402770678,39.6184777567769,47.4534772741982));
#41984=CARTESIAN_POINT('Ctrl Pts',(76.2150168726171,38.9820097281199,44.641520511437));
#41985=CARTESIAN_POINT('Ctrl Pts',(82.7066979113341,38.345541699463,49.5191354830133));
#41986=CARTESIAN_POINT('Ctrl Pts',(82.1026852762907,37.709073670806,57.6322278590409));
#41987=CARTESIAN_POINT('Ctrl Pts',(76.1537538698749,37.1786836469253,60.8412718198015));
#41988=CARTESIAN_POINT('Ctrl Pts',(71.3978840843149,36.7543716278207,59.5486179512189));
#41989=CARTESIAN_POINT('Ctrl Pts',(67.7600721668191,36.330059608716,56.2236253355719));
#41990=CARTESIAN_POINT('Ctrl Pts',(67.2858844181191,35.7996695848353,49.4810075947219));
#41991=CARTESIAN_POINT('Ctrl Pts',(73.8151741761902,35.1632015561782,44.6276093604353));
#41992=CARTESIAN_POINT('Ctrl Pts',(81.4102273433826,34.5267335275214,47.4995804443723));
#41993=CARTESIAN_POINT('Ctrl Pts',(83.1130419063421,33.8902654988644,55.4389427035715));
#41994=CARTESIAN_POINT('Ctrl Pts',(77.3370337923406,33.2537974702075,61.1682384223835));
#41995=CARTESIAN_POINT('Ctrl Pts',(70.7413467809401,32.7234074463267,59.6901785900305));
#41996=CARTESIAN_POINT('Ctrl Pts',(67.9983065599966,32.2990954272219,55.5956722967659));
#41997=CARTESIAN_POINT('Ctrl Pts',(67.4320581134842,31.8747834081174,50.6998971647794));
#41998=CARTESIAN_POINT('Ctrl Pts',(71.4953694423362,31.3443933842366,45.2983002665808));
#41999=CARTESIAN_POINT('Ctrl Pts',(79.607474293434,30.7079253555797,45.915434008014));
#42000=CARTESIAN_POINT('Ctrl Pts',(83.4584883735393,30.0714573269227,53.0640521347187));
#42001=CARTESIAN_POINT('Ctrl Pts',(79.5380484466973,29.4349892982659,60.1748327661367));
#42002=CARTESIAN_POINT('Ctrl Pts',(71.4203189468987,28.7985212696087,60.712947062398));
#42003=CARTESIAN_POINT('Ctrl Pts',(67.4097973660229,28.2681312457281,55.2720404377711));
#42004=CARTESIAN_POINT('Ctrl Pts',(68.0236907142191,27.8438192266234,50.3820111918258));
#42005=CARTESIAN_POINT('Ctrl Pts',(70.8064704458179,27.4195072075188,46.3144088162878));
#42006=CARTESIAN_POINT('Ctrl Pts',(77.416237077738,26.889117183638,44.9006435679068));
#42007=CARTESIAN_POINT('Ctrl Pts',(83.1361834050853,26.2526491549811,50.6859102435824));
#42008=CARTESIAN_POINT('Ctrl Pts',(81.3561413060791,25.6161811263241,58.6083157669602));
#42009=CARTESIAN_POINT('Ctrl Pts',(73.7334831048529,24.9797130976671,61.4061942193271));
#42010=CARTESIAN_POINT('Ctrl Pts',(67.2517616009762,24.3432450690103,56.4894501586866));
#42011=CARTESIAN_POINT('Ctrl Pts',(67.7915826783805,23.8128550451294,49.7517659321519));
#42012=CARTESIAN_POINT('Ctrl Pts',(71.4615975557508,23.3885430260248,46.4623586555792));
#42013=CARTESIAN_POINT('Ctrl Pts',(76.2298310418815,22.9642310069202,45.2160654137496));
#42014=CARTESIAN_POINT('Ctrl Pts',(82.1472280848147,22.4338409830394,48.4829062967456));
#42015=CARTESIAN_POINT('Ctrl Pts',(82.6722210527895,21.7973729543824,56.6014547617899));
#42016=CARTESIAN_POINT('Ctrl Pts',(76.1333372795995,21.1609049257255,61.4156990954795));
#42017=CARTESIAN_POINT('Ctrl Pts',(68.5436318843579,20.5244368970686,58.529566744947));
#42018=CARTESIAN_POINT('Ctrl Pts',(66.8739394534925,19.8879688684117,50.5674554183872));
#42019=CARTESIAN_POINT('Ctrl Pts',(71.69969081302,19.3575788445308,45.834017496858));
#42020=CARTESIAN_POINT('Ctrl Pts',(76.6273481755489,18.9332668254262,45.7577665390324));
#42021=CARTESIAN_POINT('Ctrl Pts',(81.0448758647264,18.5089548063216,47.9420829924205));
#42022=CARTESIAN_POINT('Ctrl Pts',(83.3696839446724,17.9785647824408,54.2918383373525));
#42023=CARTESIAN_POINT('Ctrl Pts',(78.4436850878909,17.3420967537838,60.7599313649476));
#42024=CARTESIAN_POINT('Ctrl Pts',(70.3478855924792,16.7056287251269,60.1169702163001));
#42025=CARTESIAN_POINT('Ctrl Pts',(66.5142931440722,16.06916069647,52.9422199889477));
#42026=CARTESIAN_POINT('Ctrl Pts',(69.8070609250172,15.5387706725891,47.0525186038545));
#42027=CARTESIAN_POINT('Ctrl Pts',(74.5303225619222,15.1144586534845,45.5808060668782));
#42028=CARTESIAN_POINT('Ctrl Pts',(76.9399431248174,14.9023026439322,46.0267450626822));
#42029=CARTESIAN_POINT('Ctrl Pts',(78.0214523863932,14.7962246391561,46.5322083011042));
#42030=CARTESIAN_POINT('Ctrl Pts',(69.4402165464847,416.203775360844,56.2218531134097));
#42031=CARTESIAN_POINT('Ctrl Pts',(68.9071699408176,416.097697356068,55.2974512802116));
#42032=CARTESIAN_POINT('Ctrl Pts',(68.3253282794076,415.885541346515,53.1857255195819));
#42033=CARTESIAN_POINT('Ctrl Pts',(69.2739184241871,415.461229327411,48.8665709754406));
#42034=CARTESIAN_POINT('Ctrl Pts',(74.2666401826634,414.93083930353,45.482699263787));
#42035=CARTESIAN_POINT('Ctrl Pts',(80.9500366559405,414.294371274873,48.3467661441477));
#42036=CARTESIAN_POINT('Ctrl Pts',(82.1432058326811,413.657903246216,55.5072658902866));
#42037=CARTESIAN_POINT('Ctrl Pts',(76.7605858343834,413.021435217559,60.3899618219047));
#42038=CARTESIAN_POINT('Ctrl Pts',(70.9275499708654,412.491045193678,58.8063170249911));
#42039=CARTESIAN_POINT('Ctrl Pts',(68.6436671409425,412.066733174574,55.0396853566212));
#42040=CARTESIAN_POINT('Ctrl Pts',(68.3338490158116,411.642421155469,50.6454719594405));
#42041=CARTESIAN_POINT('Ctrl Pts',(72.1793410618734,411.112031131589,45.9850203695584));
#42042=CARTESIAN_POINT('Ctrl Pts',(79.3980575202873,410.475563102931,46.8616528307));
#42043=CARTESIAN_POINT('Ctrl Pts',(82.5501083974558,409.839095074275,53.3994982501454));
#42044=CARTESIAN_POINT('Ctrl Pts',(78.763971748798,409.202627045617,59.5917890555278));
#42045=CARTESIAN_POINT('Ctrl Pts',(71.4936844869833,408.566159016961,59.7465702511734));
#42046=CARTESIAN_POINT('Ctrl Pts',(68.1307792218093,408.03576899308,54.7271964843283));
#42047=CARTESIAN_POINT('Ctrl Pts',(68.8751729700556,407.611456973975,50.3852711304698));
#42048=CARTESIAN_POINT('Ctrl Pts',(71.5232625576074,407.187144954871,46.8647613570859));
#42049=CARTESIAN_POINT('Ctrl Pts',(77.4821869316795,406.656754930989,45.8675492875739));
#42050=CARTESIAN_POINT('Ctrl Pts',(82.3576855991202,406.020286902333,51.2630156609909));
#42051=CARTESIAN_POINT('Ctrl Pts',(80.450316784661,405.383818873675,58.2659090049658));
#42052=CARTESIAN_POINT('Ctrl Pts',(73.5313962336346,404.747350845019,60.4584242691296));
#42053=CARTESIAN_POINT('Ctrl Pts',(67.9408201643275,404.110882816362,55.807939090894));
#42054=CARTESIAN_POINT('Ctrl Pts',(68.6931969050106,403.580492792481,49.8131828692861));
#42055=CARTESIAN_POINT('Ctrl Pts',(72.1023249818142,403.156180773377,47.0231564552108));
#42056=CARTESIAN_POINT('Ctrl Pts',(76.4101260871524,402.731868754271,46.1016086092032));
#42057=CARTESIAN_POINT('Ctrl Pts',(81.5629952449066,402.201478730392,49.2561471289245));
#42058=CARTESIAN_POINT('Ctrl Pts',(81.7060283497433,401.565010701734,56.526710854858));
#42059=CARTESIAN_POINT('Ctrl Pts',(75.6739772721628,400.928542673077,60.5631619677914));
#42060=CARTESIAN_POINT('Ctrl Pts',(69.0125175344533,400.29207464442,57.6815769735303));
#42061=CARTESIAN_POINT('Ctrl Pts',(67.8410993127655,399.655606615764,50.5045765788166));
#42062=CARTESIAN_POINT('Ctrl Pts',(72.3400701841959,399.125216591882,46.4719056607541));
#42063=CARTESIAN_POINT('Ctrl Pts',(76.7434507929351,398.700904572778,46.6009029918369));
#42064=CARTESIAN_POINT('Ctrl Pts',(80.6001139604411,398.276592553673,48.7298816915336));
#42065=CARTESIAN_POINT('Ctrl Pts',(82.4219981404177,397.746202529792,54.4904295545201));
#42066=CARTESIAN_POINT('Ctrl Pts',(77.7624770749188,397.109734501136,60.0734769977429));
#42067=CARTESIAN_POINT('Ctrl Pts',(70.5614810577574,396.473266472479,59.1656035270743));
#42068=CARTESIAN_POINT('Ctrl Pts',(67.4216316932075,395.836798443821,52.6219100863238));
#42069=CARTESIAN_POINT('Ctrl Pts',(71.2433726098421,395.200330415165,46.4351620165959));
#42070=CARTESIAN_POINT('Ctrl Pts',(77.2844182849696,394.669940391284,46.3406062239454));
#42071=CARTESIAN_POINT('Ctrl Pts',(80.5243720278798,394.24562837218,49.3254179159407));
#42072=CARTESIAN_POINT('Ctrl Pts',(82.040112162073,393.821316353075,53.4617125063257));
#42073=CARTESIAN_POINT('Ctrl Pts',(79.6382786370442,393.290926329193,59.0055712134925));
#42074=CARTESIAN_POINT('Ctrl Pts',(72.459393009557,392.654458300537,60.165380016475));
#42075=CARTESIAN_POINT('Ctrl Pts',(67.6179776583822,392.01799027188,54.7580446952715));
#42076=CARTESIAN_POINT('Ctrl Pts',(69.5382812257965,391.381522243223,47.7586867184634));
#42077=CARTESIAN_POINT('Ctrl Pts',(76.4805083041517,390.745054214566,45.5937297894312));
#42078=CARTESIAN_POINT('Ctrl Pts',(81.103484898854,390.214664190685,49.4836219539805));
#42079=CARTESIAN_POINT('Ctrl Pts',(81.5924175469392,389.790352171581,53.861674712741));
#42080=CARTESIAN_POINT('Ctrl Pts',(80.0245140776873,389.366040152476,57.9784792750151));
#42081=CARTESIAN_POINT('Ctrl Pts',(74.5758737999407,388.835650128596,60.5891291501815));
#42082=CARTESIAN_POINT('Ctrl Pts',(68.3953150036631,388.199182099938,56.7573869514204));
#42083=CARTESIAN_POINT('Ctrl Pts',(68.2857990871763,387.562714071282,49.5002122847499));
#42084=CARTESIAN_POINT('Ctrl Pts',(74.3252968246704,386.926246042624,45.4749116801571));
#42085=CARTESIAN_POINT('Ctrl Pts',(80.9862825946566,386.289778013968,48.392586076667));
#42086=CARTESIAN_POINT('Ctrl Pts',(81.9259074700354,385.759387990087,54.3608587531254));
#42087=CARTESIAN_POINT('Ctrl Pts',(79.4242394760944,385.335075970982,57.9868838965773));
#42088=CARTESIAN_POINT('Ctrl Pts',(75.540973279493,384.910763951878,60.0669427272804));
#42089=CARTESIAN_POINT('Ctrl Pts',(69.71538839821,384.380373927996,58.4651517178295));
#42090=CARTESIAN_POINT('Ctrl Pts',(67.5616624731461,383.743905899341,51.5194321761466));
#42091=CARTESIAN_POINT('Ctrl Pts',(72.23770936152,383.107437870682,45.9684715947465));
#42092=CARTESIAN_POINT('Ctrl Pts',(79.4370158834858,382.470969842026,46.8896466493991));
#42093=CARTESIAN_POINT('Ctrl Pts',(82.5528425826936,381.834501813369,53.4602767023325));
#42094=CARTESIAN_POINT('Ctrl Pts',(79.3486946499408,381.304111789488,58.5824451564176));
#42095=CARTESIAN_POINT('Ctrl Pts',(75.0822563764807,380.879799770384,59.6796714555959));
#42096=CARTESIAN_POINT('Ctrl Pts',(70.7864481389756,380.455487751278,58.7037448807778));
#42097=CARTESIAN_POINT('Ctrl Pts',(67.4384856247272,379.925097727399,53.6743989342178));
#42098=CARTESIAN_POINT('Ctrl Pts',(70.3669295052165,379.288629698741,47.0181408449584));
#42099=CARTESIAN_POINT('Ctrl Pts',(77.5372518389146,378.652161670085,45.8933939803704));
#42100=CARTESIAN_POINT('Ctrl Pts',(82.3686694072851,378.015693641427,51.309664113827));
#42101=CARTESIAN_POINT('Ctrl Pts',(80.4125657049669,377.379225612771,58.3136068333089));
#42102=CARTESIAN_POINT('Ctrl Pts',(74.6346941598371,376.84883558889,60.0797818118907));
#42103=CARTESIAN_POINT('Ctrl Pts',(70.6940626090962,376.424523569785,58.1105626584799));
#42104=CARTESIAN_POINT('Ctrl Pts',(68.0906807684637,376.000211550681,54.5568597889763));
#42105=CARTESIAN_POINT('Ctrl Pts',(68.8608597118887,375.469821526799,48.564364645708));
#42106=CARTESIAN_POINT('Ctrl Pts',(75.4365206255027,374.833353498142,45.4591691830717));
#42107=CARTESIAN_POINT('Ctrl Pts',(81.5876230698536,374.196885469486,49.3117678641741));
#42108=CARTESIAN_POINT('Ctrl Pts',(81.6837318816807,373.560417440829,56.5691324667567));
#42109=CARTESIAN_POINT('Ctrl Pts',(75.6141987924881,372.923949412171,60.5744193967036));
#42110=CARTESIAN_POINT('Ctrl Pts',(70.0937908220254,372.393559388291,58.1191659501846));
#42111=CARTESIAN_POINT('Ctrl Pts',(68.4098960031221,371.969247369186,54.048428998265));
#42112=CARTESIAN_POINT('Ctrl Pts',(68.774611237156,371.544935350082,49.6582827716665));
#42113=CARTESIAN_POINT('Ctrl Pts',(73.2855399397156,371.014545326201,45.6389923010219));
#42114=CARTESIAN_POINT('Ctrl Pts',(80.2863097486117,370.378077297544,47.6064214343979));
#42115=CARTESIAN_POINT('Ctrl Pts',(82.4041200296613,369.741609268888,54.5485722172613));
#42116=CARTESIAN_POINT('Ctrl Pts',(77.71782626597,369.105141240229,60.0908847886452));
#42117=CARTESIAN_POINT('Ctrl Pts',(70.5089666544688,368.468673211574,59.1349044469688));
#42118=CARTESIAN_POINT('Ctrl Pts',(67.9510509515326,367.938283187692,53.6613095675806));
#42119=CARTESIAN_POINT('Ctrl Pts',(69.3490101067543,367.513971168588,49.48373715131));
#42120=CARTESIAN_POINT('Ctrl Pts',(72.5031100488934,367.089659149483,46.4083421119939));
#42121=CARTESIAN_POINT('Ctrl Pts',(78.5444099231439,366.559269125602,46.3317296040275));
#42122=CARTESIAN_POINT('Ctrl Pts',(82.5398749139707,365.922801096946,52.4077327984871));
#42123=CARTESIAN_POINT('Ctrl Pts',(79.5866549502363,365.286333068288,59.0377455981978));
#42124=CARTESIAN_POINT('Ctrl Pts',(72.4142669929032,364.649865039632,60.149244076846));
#42125=CARTESIAN_POINT('Ctrl Pts',(67.5984596608489,364.013397010975,54.700431816129));
#42126=CARTESIAN_POINT('Ctrl Pts',(69.2564282586696,363.483006987094,48.8905855379879));
#42127=CARTESIAN_POINT('Ctrl Pts',(73.0512341120044,363.058694967989,46.6532099261719));
#42128=CARTESIAN_POINT('Ctrl Pts',(77.4491933428809,362.634382948884,46.3995256806998));
#42129=CARTESIAN_POINT('Ctrl Pts',(82.0605959468057,362.103992925004,50.3031316638272));
#42130=CARTESIAN_POINT('Ctrl Pts',(81.092957438863,361.467524896347,57.5104356694839));
#42131=CARTESIAN_POINT('Ctrl Pts',(74.5158004127629,360.83105686769,60.5795696405825));
#42132=CARTESIAN_POINT('Ctrl Pts',(68.3718257628123,360.194588839033,56.715613975814));
#42133=CARTESIAN_POINT('Ctrl Pts',(68.3088414159556,359.558120810376,49.4439162177894));
#42134=CARTESIAN_POINT('Ctrl Pts',(73.3702810557735,359.027730786495,46.1446735138543));
#42135=CARTESIAN_POINT('Ctrl Pts',(77.7024589502714,358.603418767391,46.94382042355));
#42136=CARTESIAN_POINT('Ctrl Pts',(81.1892545126691,358.179106748286,49.6361535750933));
#42137=CARTESIAN_POINT('Ctrl Pts',(82.1111485232127,357.648716724405,55.6071907614047));
#42138=CARTESIAN_POINT('Ctrl Pts',(76.6545544313477,357.012248695748,60.4141790314787));
#42139=CARTESIAN_POINT('Ctrl Pts',(69.6763015836446,356.375780667091,58.41854252348));
#42140=CARTESIAN_POINT('Ctrl Pts',(67.5713198586051,355.739312638434,51.4724911404437));
#42141=CARTESIAN_POINT('Ctrl Pts',(72.2920211553507,355.102844609777,45.9410777063465));
#42142=CARTESIAN_POINT('Ctrl Pts',(78.2768000197099,354.572454585897,46.7690847061429));
#42143=CARTESIAN_POINT('Ctrl Pts',(81.0235601960107,354.148142566792,50.2131679842795));
#42144=CARTESIAN_POINT('Ctrl Pts',(81.8906440817231,353.723830547688,54.5322612488422));
#42145=CARTESIAN_POINT('Ctrl Pts',(78.6712966263086,353.193440523806,59.6448902798114));
#42146=CARTESIAN_POINT('Ctrl Pts',(71.3995065100964,352.55697249515,59.6961134949115));
#42147=CARTESIAN_POINT('Ctrl Pts',(67.4395381257376,351.920504466493,53.6135788034026));
#42148=CARTESIAN_POINT('Ctrl Pts',(70.4050013477498,351.284036437836,46.9890331014375));
#42149=CARTESIAN_POINT('Ctrl Pts',(77.5962200355992,350.647568409179,45.908325418698));
#42150=CARTESIAN_POINT('Ctrl Pts',(81.5717652720708,350.117178385298,50.4578543745087));
#42151=CARTESIAN_POINT('Ctrl Pts',(81.3871809202268,349.692866366193,54.8592552548996));
#42152=CARTESIAN_POINT('Ctrl Pts',(79.2096775036626,349.268554347089,58.6887304100229));
#42153=CARTESIAN_POINT('Ctrl Pts',(73.4265856234102,348.738164323208,60.4377363995915));
#42154=CARTESIAN_POINT('Ctrl Pts',(67.9028145600792,348.101696294551,55.7080949172044));
#42155=CARTESIAN_POINT('Ctrl Pts',(68.9015357974914,347.465228265894,48.5191357596856));
#42156=CARTESIAN_POINT('Ctrl Pts',(75.4843515237355,346.828760237237,45.4621576778466));
#42157=CARTESIAN_POINT('Ctrl Pts',(81.6223529455147,346.19229220858,49.3617081465855));
#42158=CARTESIAN_POINT('Ctrl Pts',(81.640626656908,345.661902184699,55.4034661455841));
#42159=CARTESIAN_POINT('Ctrl Pts',(78.6151450718763,345.237590165595,58.6054752448041));
#42160=CARTESIAN_POINT('Ctrl Pts',(74.4600423822037,344.81327814649,60.0688694948707));
#42161=CARTESIAN_POINT('Ctrl Pts',(68.9469512555899,344.282888122609,57.5972303875894));
#42162=CARTESIAN_POINT('Ctrl Pts',(67.8778758710427,343.646420093952,50.4042731977985));
#42163=CARTESIAN_POINT('Ctrl Pts',(73.3459081158512,343.009952065295,45.6315170497992));
#42164=CARTESIAN_POINT('Ctrl Pts',(80.3204623129854,342.373484036639,47.6400417894447));
#42165=CARTESIAN_POINT('Ctrl Pts',(82.3975937641188,341.737016007981,54.6090503449511));
#42166=CARTESIAN_POINT('Ctrl Pts',(78.4496417365585,341.206625984101,59.1825444616058));
#42167=CARTESIAN_POINT('Ctrl Pts',(74.0657646720175,340.782313964996,59.6161606234846));
#42168=CARTESIAN_POINT('Ctrl Pts',(69.9690846948357,340.358001945891,57.9964031547838));
#42169=CARTESIAN_POINT('Ctrl Pts',(67.427437723079,339.827611922011,52.5152350021043));
#42170=CARTESIAN_POINT('Ctrl Pts',(71.3369105306629,339.191143893354,46.3835486371008));
#42171=CARTESIAN_POINT('Ctrl Pts',(78.594889468703,338.554675864697,46.3656708996847));
#42172=CARTESIAN_POINT('Ctrl Pts',(82.5436142098468,337.91820783604,52.4555108645124));
#42173=CARTESIAN_POINT('Ctrl Pts',(79.5420704476381,337.281739807383,59.0791269732218));
#42174=CARTESIAN_POINT('Ctrl Pts',(73.5624097620586,336.751349783503,59.9433212409216));
#42175=CARTESIAN_POINT('Ctrl Pts',(69.9682598402852,336.327037764397,57.3960702849555));
#42176=CARTESIAN_POINT('Ctrl Pts',(67.9373971274161,335.902725745293,53.486850703718));
#42177=CARTESIAN_POINT('Ctrl Pts',(69.6126145806316,335.372335721412,47.6819544831614));
#42178=CARTESIAN_POINT('Ctrl Pts',(76.5849735178594,334.735867692755,45.6160972367699));
#42179=CARTESIAN_POINT('Ctrl Pts',(82.0764516212286,334.099399664098,50.3618580944983));
#42180=CARTESIAN_POINT('Ctrl Pts',(81.0644511917625,333.462931635441,57.5489599449865));
#42181=CARTESIAN_POINT('Ctrl Pts',(74.4550043118779,332.826463606784,60.581577173387));
#42182=CARTESIAN_POINT('Ctrl Pts',(69.3736998864156,332.296073582903,57.3130118944356));
#42183=CARTESIAN_POINT('Ctrl Pts',(68.3304293115324,331.871761563799,53.0330600722258));
#42184=CARTESIAN_POINT('Ctrl Pts',(69.3605171826439,331.447449544694,48.7499163587087));
#42185=CARTESIAN_POINT('Ctrl Pts',(74.4317337729813,330.917059520814,45.4657214892044));
#42186=CARTESIAN_POINT('Ctrl Pts',(81.0504866017737,330.280591492156,48.4779741850053));
#42187=CARTESIAN_POINT('Ctrl Pts',(82.0846109633492,329.6441234635,55.6619260698194));
#42188=CARTESIAN_POINT('Ctrl Pts',(76.6077708510018,329.007655434842,60.4245724205696));
#42189=CARTESIAN_POINT('Ctrl Pts',(69.6290842909404,328.371187406186,58.3801925125222));
#42190=CARTESIAN_POINT('Ctrl Pts',(67.9360017916063,327.840797382305,52.5804817182293));
#42191=CARTESIAN_POINT('Ctrl Pts',(69.9548185856608,327.4164853632,48.6650277413706));
#42192=CARTESIAN_POINT('Ctrl Pts',(73.5411086122976,326.992173344096,46.1067226505543));
#42193=CARTESIAN_POINT('Ctrl Pts',(79.5234017655623,326.461783320215,46.9525017442868));
#42194=CARTESIAN_POINT('Ctrl Pts',(82.5453250849273,325.825315291558,53.5668448533101));
#42195=CARTESIAN_POINT('Ctrl Pts',(78.6153693748776,325.188847262901,59.6688138794178));
#42196=CARTESIAN_POINT('Ctrl Pts',(71.3573697948376,324.552379234244,59.6732831827373));
#42197=CARTESIAN_POINT('Ctrl Pts',(67.4290363608638,323.915911205587,53.553662954036));
#42198=CARTESIAN_POINT('Ctrl Pts',(69.9537950412676,323.385521181707,48.0646951774213));
#42199=CARTESIAN_POINT('Ctrl Pts',(74.0454684476267,322.961209162602,46.4323319125358));
#42200=CARTESIAN_POINT('Ctrl Pts',(78.4306598152707,322.536897143497,46.8524482797421));
#42201=CARTESIAN_POINT('Ctrl Pts',(82.3926746904323,322.006507119616,51.4137651702888));
#42202=CARTESIAN_POINT('Ctrl Pts',(80.3370103154243,321.37003909096,58.3891360772251));
#42203=CARTESIAN_POINT('Ctrl Pts',(73.368673325257,320.733571062302,60.4191256018276));
#42204=CARTESIAN_POINT('Ctrl Pts',(67.8859719201152,320.097103033646,55.6632278757842));
#42205=CARTESIAN_POINT('Ctrl Pts',(68.9328954799997,319.460635004988,48.4670131505437));
#42206=CARTESIAN_POINT('Ctrl Pts',(74.4383504208568,318.930244981108,45.9784112255296));
#42207=CARTESIAN_POINT('Ctrl Pts',(78.5979391335097,318.505932962003,47.4290051847139));
#42208=CARTESIAN_POINT('Ctrl Pts',(81.6332652045092,318.081620942898,50.6216837992263));
#42209=CARTESIAN_POINT('Ctrl Pts',(81.6335938519759,317.551230919018,56.6634694242698));
#42210=CARTESIAN_POINT('Ctrl Pts',(75.5076280460444,316.91476289036,60.5819000101759));
#42211=CARTESIAN_POINT('Ctrl Pts',(68.9154312388058,316.278294861704,57.5452045804096));
#42212=CARTESIAN_POINT('Ctrl Pts',(67.8945802877852,315.641826833047,50.3593545113968));
#42213=CARTESIAN_POINT('Ctrl Pts',(73.403762837781,315.00535880439,45.6127280311658));
#42214=CARTESIAN_POINT('Ctrl Pts',(79.1922124087143,314.474968780509,47.3439198783492));
#42215=CARTESIAN_POINT('Ctrl Pts',(81.3814962674079,314.050656761405,51.1666724571746));
#42216=CARTESIAN_POINT('Ctrl Pts',(81.5796314386246,313.626344742299,55.5674841489855));
#42217=CARTESIAN_POINT('Ctrl Pts',(77.6181128194239,313.095954718419,60.1292320460879));
#42218=CARTESIAN_POINT('Ctrl Pts',(70.423600772617,312.459486689762,59.0706708903866));
#42219=CARTESIAN_POINT('Ctrl Pts',(67.4377549602559,311.823018661105,52.4552871023261));
#42220=CARTESIAN_POINT('Ctrl Pts',(71.3789767527993,311.186550632448,46.3605886962923));
#42221=CARTESIAN_POINT('Ctrl Pts',(78.6508901146131,310.550082603791,46.3894221886695));
#42222=CARTESIAN_POINT('Ctrl Pts',(81.8859638407731,310.019692579911,51.4921147752653));
#42223=CARTESIAN_POINT('Ctrl Pts',(81.0321823382649,309.595380560806,55.813857275557));
#42224=CARTESIAN_POINT('Ctrl Pts',(78.2960393425849,309.171068541701,59.2663813667178));
#42225=CARTESIAN_POINT('Ctrl Pts',(72.3138382383004,308.640678517821,60.1128112781015));
#42226=CARTESIAN_POINT('Ctrl Pts',(67.576128370855,308.004210489163,54.5959588671773));
#42227=CARTESIAN_POINT('Ctrl Pts',(69.6597135717515,307.367742460507,47.6434592742872));
#42228=CARTESIAN_POINT('Ctrl Pts',(76.6317888771799,306.731274431849,45.6263465322803));
#42229=CARTESIAN_POINT('Ctrl Pts',(82.1031575825955,306.094806403193,50.4165114356426));
#42230=CARTESIAN_POINT('Ctrl Pts',(81.1996524681894,305.564416379312,56.3903587851514));
#42231=CARTESIAN_POINT('Ctrl Pts',(77.7211629929319,305.140104360207,59.0934148451279));
#42232=CARTESIAN_POINT('Ctrl Pts',(73.3914661664338,304.715792341103,59.9058965270541));
#42233=CARTESIAN_POINT('Ctrl Pts',(68.3198923136149,304.185402317221,56.6222533822537));
#42234=CARTESIAN_POINT('Ctrl Pts',(68.3604871663677,303.548934288565,49.3503961662505));
#42235=CARTESIAN_POINT('Ctrl Pts',(74.4925357667877,302.912466259908,45.4675418243239));
#42236=CARTESIAN_POINT('Ctrl Pts',(81.0791113280825,302.275998231251,48.5164105085873));
#42237=CARTESIAN_POINT('Ctrl Pts',(82.0689361798398,301.639530202594,55.7207010409613));
#42238=CARTESIAN_POINT('Ctrl Pts',(77.4695744424442,301.109140178713,59.6384868002357));
#42239=CARTESIAN_POINT('Ctrl Pts',(73.0708549766314,300.684828159609,59.3983448548522));
#42240=CARTESIAN_POINT('Ctrl Pts',(69.2691783424173,300.260516140504,57.1726638665426));
#42241=CARTESIAN_POINT('Ctrl Pts',(67.5933293757376,299.730126116623,51.3679499297607));
#42242=CARTESIAN_POINT('Ctrl Pts',(72.3923372591493,299.093658087966,45.9043358651546));
#42243=CARTESIAN_POINT('Ctrl Pts',(79.568113468025,298.457190059309,46.9937456496989));
#42244=CARTESIAN_POINT('Ctrl Pts',(82.5417329130637,297.820722030653,53.6146342059745));
#42245=CARTESIAN_POINT('Ctrl Pts',(78.5649945721503,297.184254001995,59.7029104382029));
#42246=CARTESIAN_POINT('Ctrl Pts',(72.5234874474323,296.653863978115,59.6448991550778));
#42247=CARTESIAN_POINT('Ctrl Pts',(69.3599334673634,296.22955195901,56.5792300098432));
#42248=CARTESIAN_POINT('Ctrl Pts',(67.9491184008433,295.805239939905,52.4059816418528));
#42249=CARTESIAN_POINT('Ctrl Pts',(70.4901690530445,295.274849916025,46.9245370120187));
#42250=CARTESIAN_POINT('Ctrl Pts',(77.6960510788033,294.638381887367,45.9463654816353));
#42251=CARTESIAN_POINT('Ctrl Pts',(82.3993871341864,294.001913858711,51.4742229172667));
#42252=CARTESIAN_POINT('Ctrl Pts',(80.3029614283332,293.365445830054,58.4228614269583));
#42253=CARTESIAN_POINT('Ctrl Pts',(73.3082824193387,292.728977801396,60.4118362566478));
#42254=CARTESIAN_POINT('Ctrl Pts',(68.7849999031238,292.198587777516,56.4064537623666));
#42255=CARTESIAN_POINT('Ctrl Pts',(68.4067693560527,291.774275758411,52.0174512850244));
#42256=CARTESIAN_POINT('Ctrl Pts',(70.0781225968146,291.349963739307,47.9415489999532));
#42257=CARTESIAN_POINT('Ctrl Pts',(75.5909447974727,290.819573715426,45.4693101298355));
#42258=CARTESIAN_POINT('Ctrl Pts',(81.6727811963644,290.183105686769,49.4558902844448));
#42259=CARTESIAN_POINT('Ctrl Pts',(81.5990179045781,289.546637658112,56.7135164015244));
#42260=CARTESIAN_POINT('Ctrl Pts',(75.4598065759558,288.910169629455,60.5850357597409));
#42261=CARTESIAN_POINT('Ctrl Pts',(68.8746160885175,288.273701600798,57.5001011484147));
#42262=CARTESIAN_POINT('Ctrl Pts',(68.0859902013625,287.743311576918,51.5100057520876));
#42263=CARTESIAN_POINT('Ctrl Pts',(70.6784180277171,287.318999557812,47.9483040439154));
#42264=CARTESIAN_POINT('Ctrl Pts',(74.6129677721632,286.894687538709,45.9669612161011));
#42265=CARTESIAN_POINT('Ctrl Pts',(80.3962498951809,286.364297514827,47.7153380440689));
#42266=CARTESIAN_POINT('Ctrl Pts',(82.3739091167288,285.727829486171,54.7132248190485));
#42267=CARTESIAN_POINT('Ctrl Pts',(77.5591908754027,285.091361457513,60.144344973784));
#42268=CARTESIAN_POINT('Ctrl Pts',(70.3854394892496,284.454893428857,59.0416805061446));
#42269=CARTESIAN_POINT('Ctrl Pts',(67.4365152020778,283.8184254002,52.3944705003951));
#42270=CARTESIAN_POINT('Ctrl Pts',(70.7689767411451,283.288035376319,47.3548401828391));
#42271=CARTESIAN_POINT('Ctrl Pts',(75.0617597872492,282.863723357214,46.3656916540868));
#42272=CARTESIAN_POINT('Ctrl Pts',(79.3315561430612,282.43941133811,47.4497766012886));
#42273=CARTESIAN_POINT('Ctrl Pts',(82.5514597900143,281.909021314229,52.5620553643578));
#42274=CARTESIAN_POINT('Ctrl Pts',(79.4558785027385,281.272553285572,59.14224774801));
#42275=CARTESIAN_POINT('Ctrl Pts',(72.259442357487,280.636085256915,60.0855847428586));
#42276=CARTESIAN_POINT('Ctrl Pts',(67.5663265020588,279.999617228258,54.5490477885832));
#42277=CARTESIAN_POINT('Ctrl Pts',(69.698656693656,279.363149199601,47.5967299545071));
#42278=CARTESIAN_POINT('Ctrl Pts',(75.5192821269783,278.83275917572,45.977009851541));
#42279=CARTESIAN_POINT('Ctrl Pts',(79.408934314618,278.408447156615,48.0451024394208));
#42280=CARTESIAN_POINT('Ctrl Pts',(81.9217548016931,277.984135137511,51.6634078843202));
#42281=CARTESIAN_POINT('Ctrl Pts',(81.0005103947078,277.45374511363,57.6345453295302));
#42282=CARTESIAN_POINT('Ctrl Pts',(74.348539571935,276.817277084973,60.5727147400631));
#42283=CARTESIAN_POINT('Ctrl Pts',(68.296676761267,276.180809056316,56.5660285283193));
#42284=CARTESIAN_POINT('Ctrl Pts',(68.3838476789665,275.54434102766,49.3085510664432));
#42285=CARTESIAN_POINT('Ctrl Pts',(74.5525794359645,274.907872999002,45.4577973970669));
#42286=CARTESIAN_POINT('Ctrl Pts',(80.0092319483338,274.377482975122,48.0516588055164));
#42287=CARTESIAN_POINT('Ctrl Pts',(81.5898034221531,273.953170956017,52.1636163574618));
#42288=CARTESIAN_POINT('Ctrl Pts',(81.1143528981921,273.528858936913,56.5431537636407));
#42289=CARTESIAN_POINT('Ctrl Pts',(76.5033750007141,272.998468913031,60.4472614050817));
#42290=CARTESIAN_POINT('Ctrl Pts',(69.5545150337097,272.362000884375,58.3036895096301));
#42291=CARTESIAN_POINT('Ctrl Pts',(67.6126698935678,271.725532855717,51.3102772287588));
#42292=CARTESIAN_POINT('Ctrl Pts',(72.4374133801518,271.089064827061,45.88806106125));
#42293=CARTESIAN_POINT('Ctrl Pts',(79.6198359734671,270.452596798404,47.0257609351353));
#42294=CARTESIAN_POINT('Ctrl Pts',(82.0387273789565,269.922206774523,52.5621982386224));
#42295=CARTESIAN_POINT('Ctrl Pts',(80.5357298745602,269.497894755419,56.7031401115096));
#42296=CARTESIAN_POINT('Ctrl Pts',(77.304981575641,269.073582736314,59.697913311918));
#42297=CARTESIAN_POINT('Ctrl Pts',(71.2636734023524,268.543192712433,59.6219580464909));
#42298=CARTESIAN_POINT('Ctrl Pts',(67.422901911245,267.906724683776,53.4470062519336));
#42299=CARTESIAN_POINT('Ctrl Pts',(70.5425886864608,267.270256655119,46.8936763881869));
#42300=CARTESIAN_POINT('Ctrl Pts',(77.7407552738591,266.633788626463,45.9636357124148));
#42301=CARTESIAN_POINT('Ctrl Pts',(82.4174441785092,265.997320597805,51.5323102585822));
#42302=CARTESIAN_POINT('Ctrl Pts',(80.6133050746085,265.466930573925,57.2984403074771));
#42303=CARTESIAN_POINT('Ctrl Pts',(76.763215206849,265.042618554819,59.4392833897759));
#42304=CARTESIAN_POINT('Ctrl Pts',(72.3602526468608,264.618306535715,59.5818378993367));
#42305=CARTESIAN_POINT('Ctrl Pts',(67.8488867063496,264.087916511834,55.5630382031854));
#42306=CARTESIAN_POINT('Ctrl Pts',(68.9982017502957,263.451448483178,48.3824650894454));
#42307=CARTESIAN_POINT('Ctrl Pts',(75.6507576527478,262.81498045452,45.4803834497805));
#42308=CARTESIAN_POINT('Ctrl Pts',(81.6952081767768,262.178512425863,49.4982430467674));
#42309=CARTESIAN_POINT('Ctrl Pts',(81.5745614419011,261.542044397206,56.7692126985655));
#42310=CARTESIAN_POINT('Ctrl Pts',(76.4314293975865,261.011654373326,59.9396017002077));
#42311=CARTESIAN_POINT('Ctrl Pts',(72.1208112787717,260.587342354221,59.0313217177135));
#42312=CARTESIAN_POINT('Ctrl Pts',(68.7031090722866,260.163030335117,56.2518050833615));
#42313=CARTESIAN_POINT('Ctrl Pts',(67.9322782008732,259.632640311235,50.2593937644792));
#42314=CARTESIAN_POINT('Ctrl Pts',(73.5085094149935,258.996172282579,45.5917176019033));
#42315=CARTESIAN_POINT('Ctrl Pts',(80.4341473613234,258.359704253922,47.7629193232736));
#42316=CARTESIAN_POINT('Ctrl Pts',(82.3630695451455,257.723236225265,54.7599070385188));
#42317=CARTESIAN_POINT('Ctrl Pts',(77.5042046999709,257.086768196608,60.1703587505607));
#42318=CARTESIAN_POINT('Ctrl Pts',(71.542241236904,256.556378172727,59.1914995614827));
#42319=CARTESIAN_POINT('Ctrl Pts',(68.8833202238815,256.132066153623,55.6791584420352));
#42320=CARTESIAN_POINT('Ctrl Pts',(68.1255702744068,255.707754134518,51.3395483089789));
#42321=CARTESIAN_POINT('Ctrl Pts',(71.4729856187442,255.177364110637,46.3098381623122));
#42322=CARTESIAN_POINT('Ctrl Pts',(78.7437506296847,254.54089608198,46.4422446111449));
#42323=CARTESIAN_POINT('Ctrl Pts',(82.5488719109899,253.904428053323,52.6228295278893));
#42324=CARTESIAN_POINT('Ctrl Pts',(79.4170838257604,253.267960024666,59.1703848936531));
#42325=CARTESIAN_POINT('Ctrl Pts',(72.200869981999,252.631491996009,60.0691691130958));
#42326=CARTESIAN_POINT('Ctrl Pts',(68.3414682869996,252.101101972129,55.4207078404137));
#42327=CARTESIAN_POINT('Ctrl Pts',(68.6371295416553,251.676789953024,51.0253710483865));
#42328=CARTESIAN_POINT('Ctrl Pts',(70.9106332758805,251.252477933919,47.2520990116368));
#42329=CARTESIAN_POINT('Ctrl Pts',(76.7360438614395,250.722087910039,45.649674237537));
#42330=CARTESIAN_POINT('Ctrl Pts',(82.1386298989004,250.085619881381,50.5172834473894));
#42331=CARTESIAN_POINT('Ctrl Pts',(80.9587052447333,249.449151852725,57.6787327203381));
#42332=CARTESIAN_POINT('Ctrl Pts',(74.3007993835847,248.812683824068,60.5685194637872));
#42333=CARTESIAN_POINT('Ctrl Pts',(68.2632189551499,248.176215795411,56.5152272362032));
#42334=CARTESIAN_POINT('Ctrl Pts',(68.3975059844324,247.64582577153,50.4749341439143));
#42335=CARTESIAN_POINT('Ctrl Pts',(71.5028739501969,247.221513752425,47.3503396278119));
#42336=CARTESIAN_POINT('Ctrl Pts',(75.6936026826867,246.797201733321,45.9923286618994));
#42337=CARTESIAN_POINT('Ctrl Pts',(81.1425269447101,246.26681170944,48.6023857558582));
#42338=CARTESIAN_POINT('Ctrl Pts',(82.0296386774106,245.630343680783,55.8200438307264));
#42339=CARTESIAN_POINT('Ctrl Pts',(76.4428373212789,244.993875652126,60.4532099712461));
#42340=CARTESIAN_POINT('Ctrl Pts',(69.5212222752298,244.357407623469,58.2692175186869));
#42341=CARTESIAN_POINT('Ctrl Pts',(67.6207211562919,243.720939594812,51.2499831723409));
#42342=CARTESIAN_POINT('Ctrl Pts',(71.6828955652401,243.190549570931,46.7776333740493));
#42343=CARTESIAN_POINT('Ctrl Pts',(76.0763237452923,242.766237551827,46.45484874062));
#42344=CARTESIAN_POINT('Ctrl Pts',(80.1307985436868,242.341925532722,48.1775313004769));
#42345=CARTESIAN_POINT('Ctrl Pts',(82.5332351792175,241.811535508841,53.7211286757604));
#42346=CARTESIAN_POINT('Ctrl Pts',(78.4701832321027,241.175067480184,59.7521455209579));
#42347=CARTESIAN_POINT('Ctrl Pts',(71.2140669720661,240.538599451527,59.5867529595707));
#42348=CARTESIAN_POINT('Ctrl Pts',(67.4203702079031,239.90213142287,53.3991490016473));
#42349=CARTESIAN_POINT('Ctrl Pts',(70.5882038573061,239.265663394213,46.8534339695275));
#42350=CARTESIAN_POINT('Ctrl Pts',(76.5877790024693,238.735273370333,46.1405021884087));
#42351=CARTESIAN_POINT('Ctrl Pts',(80.1164646781247,238.310961351228,48.777693591261));
#42352=CARTESIAN_POINT('Ctrl Pts',(82.0479717482962,237.886649332123,52.7369462392655));
#42353=CARTESIAN_POINT('Ctrl Pts',(80.2267142779113,237.356259308243,58.4976922737264));
#42354=CARTESIAN_POINT('Ctrl Pts',(73.2044152927096,236.719791279586,60.3868381850957));
#42355=CARTESIAN_POINT('Ctrl Pts',(67.8345189347357,236.083323250929,55.503930139356));
#42356=CARTESIAN_POINT('Ctrl Pts',(69.0276716499313,235.446855222272,48.3446728820177));
#42357=CARTESIAN_POINT('Ctrl Pts',(75.7115850601304,234.810387193615,45.4799116638757));
#42358=CARTESIAN_POINT('Ctrl Pts',(80.7087378343276,234.279997169734,48.875738190411));
#42359=CARTESIAN_POINT('Ctrl Pts',(81.6436066234392,233.855685150629,53.180668089956));
#42360=CARTESIAN_POINT('Ctrl Pts',(80.5056974287515,233.431373131525,57.4364363822277));
#42361=CARTESIAN_POINT('Ctrl Pts',(75.3531715102732,232.900983107644,60.5915354783531));
#42362=CARTESIAN_POINT('Ctrl Pts',(68.8125886089893,232.264515078988,57.4131191079744));
#42363=CARTESIAN_POINT('Ctrl Pts',(67.9601893709513,231.62804705033,50.2053459832478));
#42364=CARTESIAN_POINT('Ctrl Pts',(73.5555405130985,230.991579021674,45.5825088160508));
#42365=CARTESIAN_POINT('Ctrl Pts',(80.4803812584472,230.355110993016,47.8024493476742));
#42366=CARTESIAN_POINT('Ctrl Pts',(82.0264807435618,229.824720969135,53.643061475614));
#42367=CARTESIAN_POINT('Ctrl Pts',(79.9094420644716,229.400408950031,57.5062917720994));
#42368=CARTESIAN_POINT('Ctrl Pts',(76.2596980440375,228.976096930926,59.973227052842));
#42369=CARTESIAN_POINT('Ctrl Pts',(70.3006682467896,228.445706907045,58.9766642005573));
#42370=CARTESIAN_POINT('Ctrl Pts',(67.4467211576931,227.809238878389,52.2881261445181));
#42371=CARTESIAN_POINT('Ctrl Pts',(71.5294991123255,227.172770849731,46.2873343582343));
#42372=CARTESIAN_POINT('Ctrl Pts',(78.7852974416126,226.536302821075,46.4661316001294));
#42373=CARTESIAN_POINT('Ctrl Pts',(82.5578574497902,225.899834792418,52.6829914441579));
#42374=CARTESIAN_POINT('Ctrl Pts',(79.8953068284501,225.369444768537,58.1064587746505));
#42375=CARTESIAN_POINT('Ctrl Pts',(75.7637206843553,224.945132749432,59.6349864757668));
#42376=CARTESIAN_POINT('Ctrl Pts',(71.3905354195408,224.520820730328,59.1042775958139));
#42377=CARTESIAN_POINT('Ctrl Pts',(67.5449574653074,223.990430706447,54.4443737834338));
#42378=CARTESIAN_POINT('Ctrl Pts',(69.7760950598774,223.35396267779,47.5231325790778));
#42379=CARTESIAN_POINT('Ctrl Pts',(76.7934678689953,222.717494649133,45.6697413792555));
#42380=CARTESIAN_POINT('Ctrl Pts',(82.1543340864813,222.081026620476,50.5625614860971));
#42381=CARTESIAN_POINT('Ctrl Pts',(80.9260398287832,221.444558591819,57.7300468280508));
#42382=CARTESIAN_POINT('Ctrl Pts',(75.359501788676,220.914168567939,60.0788422184516));
#42383=CARTESIAN_POINT('Ctrl Pts',(71.2378684220514,220.489856548833,58.5236805851131));
#42384=CARTESIAN_POINT('Ctrl Pts',(68.2841225777918,220.065544529729,55.2553780454862));
#42385=CARTESIAN_POINT('Ctrl Pts',(68.4363561824632,219.535154505848,49.2155095945404));
#42386=CARTESIAN_POINT('Ctrl Pts',(74.6592976343922,218.898686477191,45.4530110656439));
#42387=CARTESIAN_POINT('Ctrl Pts',(81.1727368883548,218.262218448534,48.6551890733252));
#42388=CARTESIAN_POINT('Ctrl Pts',(82.0117795796358,217.625750419878,55.8645297869897));
#42389=CARTESIAN_POINT('Ctrl Pts',(76.384577826177,216.98928239122,60.4705254569844));
#42390=CARTESIAN_POINT('Ctrl Pts',(70.6415458845036,216.45889236734,58.5937451401108));
#42391=CARTESIAN_POINT('Ctrl Pts',(68.5496937837328,216.034580348235,54.7169044211844));
#42392=CARTESIAN_POINT('Ctrl Pts',(68.4623324423871,215.61026832913,50.3125466480765));
#42393=CARTESIAN_POINT('Ctrl Pts',(72.5386807300418,215.07987830525,45.8521629591067));
#42394=CARTESIAN_POINT('Ctrl Pts',(79.7025171230519,214.443410276593,47.0922650620929));
#42395=CARTESIAN_POINT('Ctrl Pts',(82.5232975753281,213.806942247936,53.7805499308915));
#42396=CARTESIAN_POINT('Ctrl Pts',(78.4240017018063,213.170474219279,59.7744967819837));
#42397=CARTESIAN_POINT('Ctrl Pts',(71.1654941498381,212.534006190622,59.5607360970782));
#42398=CARTESIAN_POINT('Ctrl Pts',(67.4185710112033,211.897538161965,53.3437815500908));
#42399=CARTESIAN_POINT('Ctrl Pts',(70.6324017692262,211.261070133308,46.8223018905017));
#42400=CARTESIAN_POINT('Ctrl Pts',(76.6375952493495,210.730680109427,46.1520114449674));
#42401=CARTESIAN_POINT('Ctrl Pts',(80.1468768325872,210.306368090323,48.8148937493606));
#42402=CARTESIAN_POINT('Ctrl Pts',(82.0499126329196,209.882056071218,52.7878264085024));
#42403=CARTESIAN_POINT('Ctrl Pts',(80.187041012264,209.351666047337,58.5353849828742));
#42404=CARTESIAN_POINT('Ctrl Pts',(73.1513480712217,208.71519801868,60.3737594076079));
#42405=CARTESIAN_POINT('Ctrl Pts',(67.8167943497098,208.078729990023,55.4522634200252));
#42406=CARTESIAN_POINT('Ctrl Pts',(69.061584800203,207.442261961366,48.3017856987611));
#42407=CARTESIAN_POINT('Ctrl Pts',(75.7659852692241,206.805793932709,45.4853322826586));
#42408=CARTESIAN_POINT('Ctrl Pts',(80.7385115746561,206.275403908829,48.917120171924));
#42409=CARTESIAN_POINT('Ctrl Pts',(81.6422938479955,205.851091889724,53.2286852712132));
#42410=CARTESIAN_POINT('Ctrl Pts',(80.4737098842069,205.426779870619,57.4761316610172));
#42411=CARTESIAN_POINT('Ctrl Pts',(75.2985532891292,204.896389846738,60.5939738241731));
#42412=CARTESIAN_POINT('Ctrl Pts',(68.7810733356024,204.259921818082,57.3684493759649));
#42413=CARTESIAN_POINT('Ctrl Pts',(67.9807002766952,203.623453789425,50.1547139936352));
#42414=CARTESIAN_POINT('Ctrl Pts',(73.6092597236957,202.986985760768,45.5723675823186));
#42415=CARTESIAN_POINT('Ctrl Pts',(80.5179032622457,202.350517732111,47.8422132228922));
#42416=CARTESIAN_POINT('Ctrl Pts',(82.0218224346228,201.82012770823,53.6938284243281));
#42417=CARTESIAN_POINT('Ctrl Pts',(79.876965580564,201.395815689125,57.5416837167277));
#42418=CARTESIAN_POINT('Ctrl Pts',(76.2095175909059,200.971503670021,59.9822218218007));
#42419=CARTESIAN_POINT('Ctrl Pts',(70.2578331089008,200.44111364614,58.9426904260413));
#42420=CARTESIAN_POINT('Ctrl Pts',(67.4522182081061,199.804645617483,52.23373518964));
#42421=CARTESIAN_POINT('Ctrl Pts',(71.57818569271,199.168177588826,46.2625569001401));
#42422=CARTESIAN_POINT('Ctrl Pts',(78.8325051420938,198.531709560169,46.4937001791837));
#42423=CARTESIAN_POINT('Ctrl Pts',(82.5601122160283,197.895241531512,52.7376172843988));
#42424=CARTESIAN_POINT('Ctrl Pts',(79.8585005077304,197.364851507631,58.1417331066808));
#42425=CARTESIAN_POINT('Ctrl Pts',(75.7159935420101,196.940539488527,59.6404115688682));
#42426=CARTESIAN_POINT('Ctrl Pts',(71.3467511986132,196.516227469422,59.0781639035877));
#42427=CARTESIAN_POINT('Ctrl Pts',(67.5348945669068,195.985837445541,54.3906354859434));
#42428=CARTESIAN_POINT('Ctrl Pts',(69.8159110313352,195.349369416884,47.485672111573));
#42429=CARTESIAN_POINT('Ctrl Pts',(76.8464732813378,194.712901388227,45.6829596200234));
#42430=CARTESIAN_POINT('Ctrl Pts',(82.1718984779573,194.07643335957,50.6143310675762));
#42431=CARTESIAN_POINT('Ctrl Pts',(80.8919221238434,193.439965330914,57.7727677575927));
#42432=CARTESIAN_POINT('Ctrl Pts',(75.3085833923628,192.909575307032,60.0813392328799));
#42433=CARTESIAN_POINT('Ctrl Pts',(71.1982763155723,192.485263287928,58.496480618573));
#42434=CARTESIAN_POINT('Ctrl Pts',(68.2681911584664,192.060951268823,55.2069514630609));
#42435=CARTESIAN_POINT('Ctrl Pts',(68.4639919993237,191.530561244943,49.1683393975527));
#42436=CARTESIAN_POINT('Ctrl Pts',(74.7139298693017,190.894093216286,45.4508359431595));
#42437=CARTESIAN_POINT('Ctrl Pts',(81.2040747184487,190.257625187628,48.6999277725212));
#42438=CARTESIAN_POINT('Ctrl Pts',(81.9911195461561,189.621157158972,55.9151296628155));
#42439=CARTESIAN_POINT('Ctrl Pts',(76.3307548517939,188.984689130314,60.4804146307914));
#42440=CARTESIAN_POINT('Ctrl Pts',(70.6015541912865,188.454299106434,58.5622296974156));
#42441=CARTESIAN_POINT('Ctrl Pts',(68.5375189050122,188.029987087329,54.6704229923146));
#42442=CARTESIAN_POINT('Ctrl Pts',(68.48234794078,187.605675068225,50.2654987866604));
#42443=CARTESIAN_POINT('Ctrl Pts',(72.5898628211001,187.075285044344,45.8347544750419));
#42444=CARTESIAN_POINT('Ctrl Pts',(79.7462199487381,186.438817015687,47.1263070189644));
#42445=CARTESIAN_POINT('Ctrl Pts',(82.515742576707,185.80234898703,53.8351312297857));
#42446=CARTESIAN_POINT('Ctrl Pts',(78.3787509657197,185.165880958373,59.7986770113781));
#42447=CARTESIAN_POINT('Ctrl Pts',(71.1116061485101,184.529412929716,59.5337968163666));
#42448=CARTESIAN_POINT('Ctrl Pts',(68.0438817587522,183.999022905836,54.3287760944599));
#42449=CARTESIAN_POINT('Ctrl Pts',(69.0375063166156,183.574710886731,50.0370268787132));
#42450=CARTESIAN_POINT('Ctrl Pts',(71.8842836054319,183.150398867626,46.6751434540935));
#42451=CARTESIAN_POINT('Ctrl Pts',(77.8908088143546,182.620008843745,46.0233547141099));
#42452=CARTESIAN_POINT('Ctrl Pts',(82.4469328887749,181.983540815089,51.6910957747526));
#42453=CARTESIAN_POINT('Ctrl Pts',(80.1387527656007,181.347072786431,58.572293519151));
#42454=CARTESIAN_POINT('Ctrl Pts',(73.1048721785186,180.710604757775,60.3620146608933));
#42455=CARTESIAN_POINT('Ctrl Pts',(67.7918860949547,180.074136729118,55.3967619797233));
#42456=CARTESIAN_POINT('Ctrl Pts',(68.8888389242243,179.543746705237,49.4553927656997));
#42457=CARTESIAN_POINT('Ctrl Pts',(72.4532421114072,179.119434686132,46.866680535255));
#42458=CARTESIAN_POINT('Ctrl Pts',(76.8070319366311,178.695122667027,46.1951783009844));
#42459=CARTESIAN_POINT('Ctrl Pts',(81.7693387994904,178.164732643147,49.6417250141177));
#42460=CARTESIAN_POINT('Ctrl Pts',(81.4927052653565,177.52826461449,56.9084319161333));
#42461=CARTESIAN_POINT('Ctrl Pts',(75.2378426878872,176.891796585833,60.5901804158958));
#42462=CARTESIAN_POINT('Ctrl Pts',(68.7537112920353,176.255328557176,57.329104225455));
#42463=CARTESIAN_POINT('Ctrl Pts',(67.998274828751,175.618860528519,50.0964787642586));
#42464=CARTESIAN_POINT('Ctrl Pts',(72.7223922704138,175.088470504638,46.3300629555132));
#42465=CARTESIAN_POINT('Ctrl Pts',(77.1109979378639,174.664158485534,46.7128702026749));
#42466=CARTESIAN_POINT('Ctrl Pts',(80.8384205813792,174.239846466429,49.0607887552361));
#42467=CARTESIAN_POINT('Ctrl Pts',(82.324952858378,173.709456442548,54.9168450593055));
#42468=CARTESIAN_POINT('Ctrl Pts',(77.3511135899792,173.072988413891,60.2217935269295));
#42469=CARTESIAN_POINT('Ctrl Pts',(70.2144838384759,172.436520385234,58.9000168179176));
#42470=CARTESIAN_POINT('Ctrl Pts',(67.4573598306935,171.800052356578,52.1860876341802));
#42471=CARTESIAN_POINT('Ctrl Pts',(71.6296407940811,171.16358432792,46.2301135849953));
#42472=CARTESIAN_POINT('Ctrl Pts',(77.6660806668148,170.63319430404,46.4842145685839));
#42473=CARTESIAN_POINT('Ctrl Pts',(80.7284491521708,170.208882284935,49.6509637460135));
#42474=CARTESIAN_POINT('Ctrl Pts',(82.0030480812232,169.78457026583,53.8678107509346));
#42475=CARTESIAN_POINT('Ctrl Pts',(79.2853972047954,169.25418024195,59.2638785193046));
#42476=CARTESIAN_POINT('Ctrl Pts',(72.051559380782,168.617712213293,60.0076161396274));
#42477=CARTESIAN_POINT('Ctrl Pts',(67.5301482489436,167.981244184636,54.3299917019408));
#42478=CARTESIAN_POINT('Ctrl Pts',(69.8510367706492,167.344776155979,47.4530698361387));
#42479=CARTESIAN_POINT('Ctrl Pts',(76.9065957314089,166.708308127322,45.6922055417502));
#42480=CARTESIAN_POINT('Ctrl Pts',(81.297471019284,166.177918103441,49.8423125106509));
#42481=CARTESIAN_POINT('Ctrl Pts',(81.5330257953548,165.753606084336,54.2412800077259));
#42482=CARTESIAN_POINT('Ctrl Pts',(79.730240888043,165.329294065231,58.2607784429569));
#42483=CARTESIAN_POINT('Ctrl Pts',(74.1400699594029,164.798904041351,60.5527563301915));
#42484=CARTESIAN_POINT('Ctrl Pts',(68.1908518359154,164.162436012694,56.3708477908785));
#42485=CARTESIAN_POINT('Ctrl Pts',(68.5001743561956,163.525967984037,49.1194412061544));
#42486=CARTESIAN_POINT('Ctrl Pts',(74.7618279289903,162.88949995538,45.4492542336917));
#42487=CARTESIAN_POINT('Ctrl Pts',(81.2434042036485,162.253031926723,48.7463323807481));
#42488=CARTESIAN_POINT('Ctrl Pts',(81.8371631184601,161.722641902843,54.7588712785909));
#42489=CARTESIAN_POINT('Ctrl Pts',(79.1304811166209,161.298329883738,58.2345400824001));
#42490=CARTESIAN_POINT('Ctrl Pts',(75.1336863785303,160.874017864633,60.0871147541545));
#42491=CARTESIAN_POINT('Ctrl Pts',(69.4102083038376,160.343627840753,58.1519216435066));
#42492=CARTESIAN_POINT('Ctrl Pts',(67.6607577848386,159.707159812095,51.0935239362658));
#42493=CARTESIAN_POINT('Ctrl Pts',(72.6492443092724,159.070691783438,45.8215622450095));
#42494=CARTESIAN_POINT('Ctrl Pts',(79.7834200297725,158.434223754782,47.1565209213571));
#42495=CARTESIAN_POINT('Ctrl Pts',(82.5150074441991,157.797755726124,53.8959560244911));
#42496=CARTESIAN_POINT('Ctrl Pts',(79.0207050214086,157.267365702244,58.8247514376798));
#42497=CARTESIAN_POINT('Ctrl Pts',(74.6980745371252,156.843053683139,59.674025709748));
#42498=CARTESIAN_POINT('Ctrl Pts',(70.46572023205,156.418741664035,58.4519053682248));
#42499=CARTESIAN_POINT('Ctrl Pts',(67.4134691141883,155.888351640154,53.2377959753846));
#42500=CARTESIAN_POINT('Ctrl Pts',(70.7210260768666,155.251883611497,46.7615607842688));
#42501=CARTESIAN_POINT('Ctrl Pts',(77.9442921949654,154.61541558284,46.0523327069526));
#42502=CARTESIAN_POINT('Ctrl Pts',(82.4552067574609,153.978947554183,51.7383003192767));
#42503=CARTESIAN_POINT('Ctrl Pts',(80.0983132341476,153.342479525526,58.6177340337456));
#42504=CARTESIAN_POINT('Ctrl Pts',(74.2281758826995,152.812089501645,60.0476505075739));
#42505=CARTESIAN_POINT('Ctrl Pts',(70.40770839454,152.387777482541,57.8543814258676));
#42506=CARTESIAN_POINT('Ctrl Pts',(68.0136702024717,151.963465463436,54.1564114114174));
#42507=CARTESIAN_POINT('Ctrl Pts',(69.1282650058018,151.433075439555,48.2183265289509));
#42508=CARTESIAN_POINT('Ctrl Pts',(75.8721092904904,150.796607410898,45.4976428693019));
#42509=CARTESIAN_POINT('Ctrl Pts',(81.7907169371403,150.160139382241,49.6986738622307));
#42510=CARTESIAN_POINT('Ctrl Pts',(81.467998682892,149.523671353584,56.949496629814));
#42511=CARTESIAN_POINT('Ctrl Pts',(75.1775143387812,148.887203324927,60.597970561269));
#42512=CARTESIAN_POINT('Ctrl Pts',(69.8079399719556,148.356813301047,57.8283415669595));
#42513=CARTESIAN_POINT('Ctrl Pts',(68.3616844717522,147.932501281942,53.6672424187795));
#42514=CARTESIAN_POINT('Ctrl Pts',(68.9790535910217,147.508189262837,49.3054473223284));
#42515=CARTESIAN_POINT('Ctrl Pts',(73.7143370496216,146.977799238956,45.5530795080406));
#42516=CARTESIAN_POINT('Ctrl Pts',(80.589949789624,146.3413312103,47.9210965606662));
#42517=CARTESIAN_POINT('Ctrl Pts',(82.3037503541374,145.704863181643,54.9738595301416));
#42518=CARTESIAN_POINT('Ctrl Pts',(77.3055329106097,145.068395152986,60.2365964859227));
#42519=CARTESIAN_POINT('Ctrl Pts',(70.1638278773739,144.431927124329,58.8663393822131));
#42520=CARTESIAN_POINT('Ctrl Pts',(67.9259359356944,143.901537100448,53.2542975697928));
#42521=CARTESIAN_POINT('Ctrl Pts',(69.5625651603511,143.477225081343,49.1643286366771));
#42522=CARTESIAN_POINT('Ctrl Pts',(72.8888275031151,143.052913062239,46.276010800987));
#42523=CARTESIAN_POINT('Ctrl Pts',(78.9244860291356,142.522523038358,46.5480398513935));
#42524=CARTESIAN_POINT('Ctrl Pts',(82.5627811275167,141.886055009701,52.844416911982));
#42525=CARTESIAN_POINT('Ctrl Pts',(79.2320033963073,141.249586981044,59.29302122484));
#42526=CARTESIAN_POINT('Ctrl Pts',(72.0074393750885,140.613118952387,59.9889038168333));
#42527=CARTESIAN_POINT('Ctrl Pts',(67.5139863609418,139.97665092373,54.2713488042719));
#42528=CARTESIAN_POINT('Ctrl Pts',(69.5043555657909,139.446260899849,48.5668239270031));
#42529=CARTESIAN_POINT('Ctrl Pts',(73.4219126606781,139.021948880745,46.5520913141847));
#42530=CARTESIAN_POINT('Ctrl Pts',(77.8271823334845,138.59763686164,46.5525415404871));
#42531=CARTESIAN_POINT('Ctrl Pts',(82.2057117749606,138.06724683776,50.7156718023356));
#42532=CARTESIAN_POINT('Ctrl Pts',(80.8239056608555,137.430778809102,57.8551512774115));
#42533=CARTESIAN_POINT('Ctrl Pts',(74.0806480912595,136.794310780446,60.5397471927433));
#42534=CARTESIAN_POINT('Ctrl Pts',(68.1698115367609,136.157842751788,56.3277893220453));
#42535=CARTESIAN_POINT('Ctrl Pts',(68.5264259506943,135.521374723132,49.0645681721848));
#42536=CARTESIAN_POINT('Ctrl Pts',(73.769765012496,134.990984699251,46.0628071673783));
#42537=CARTESIAN_POINT('Ctrl Pts',(78.0486265721898,134.566672680146,47.1105403613868));
#42538=CARTESIAN_POINT('Ctrl Pts',(81.3742984631555,134.142360661042,49.9995380364455));
#42539=CARTESIAN_POINT('Ctrl Pts',(81.9501965609975,133.611970637161,56.0138139719088));
#42540=CARTESIAN_POINT('Ctrl Pts',(76.2253814360378,132.975502608504,60.4980136883621));
#42541=CARTESIAN_POINT('Ctrl Pts',(69.373875401297,132.339034579847,58.1031352082631));
#42542=CARTESIAN_POINT('Ctrl Pts',(67.673107048528,131.70256655119,51.0472181956595));
#42543=CARTESIAN_POINT('Ctrl Pts',(72.7050459680729,131.066098522533,45.797347147531));
#42544=CARTESIAN_POINT('Ctrl Pts',(78.6320914040458,130.535708498652,46.9692285608586));
#42545=CARTESIAN_POINT('Ctrl Pts',(81.1755929512698,130.111396479547,50.5660328330036));
#42546=CARTESIAN_POINT('Ctrl Pts',(81.7920704914035,129.687084460443,54.927954030752));
#42547=CARTESIAN_POINT('Ctrl Pts',(78.2831441745266,129.156694436562,59.8463490687415));
#42548=CARTESIAN_POINT('Ctrl Pts',(71.0205093031994,128.520226407905,59.4779877817043));
#42549=CARTESIAN_POINT('Ctrl Pts',(67.4180284889611,127.883758379248,53.1771378500223));
#42550=CARTESIAN_POINT('Ctrl Pts',(70.7607136997943,127.247290350591,46.7346978262573));
#42551=CARTESIAN_POINT('Ctrl Pts',(78.0023008142659,126.610822321934,46.0706410700047));
#42552=CARTESIAN_POINT('Ctrl Pts',(81.7087694529541,126.080432298053,50.8419368979128));
#42553=CARTESIAN_POINT('Ctrl Pts',(81.2705819659427,125.656120278949,55.2253593985487));
#42554=CARTESIAN_POINT('Ctrl Pts',(78.8757879458262,125.231808259844,58.9228399859306));
#42555=CARTESIAN_POINT('Ctrl Pts',(73.0014294075374,124.701418235964,60.3353149098227));
#42556=CARTESIAN_POINT('Ctrl Pts',(67.7597037493354,124.064950207307,55.2948915708406));
#42557=CARTESIAN_POINT('Ctrl Pts',(69.1714825404732,123.42848217865,48.1755195112118));
#42558=CARTESIAN_POINT('Ctrl Pts',(75.9196881304625,122.792014149993,45.5033856833937));
#42559=CARTESIAN_POINT('Ctrl Pts',(81.8225079909851,122.155546121336,49.7505344924449));
#42560=CARTESIAN_POINT('Ctrl Pts',(81.4922108712684,121.625156097455,55.7832848983293));
#42561=CARTESIAN_POINT('Ctrl Pts',(78.2870485036781,121.20084407835,58.805425743862));
#42562=CARTESIAN_POINT('Ctrl Pts',(74.0544444813281,120.776532059246,60.0266809517681));
#42563=CARTESIAN_POINT('Ctrl Pts',(68.6931200384709,120.246142035365,57.2411156832066));
#42564=CARTESIAN_POINT('Ctrl Pts',(68.0407764999982,119.609674006708,49.9984640127326));
#42565=CARTESIAN_POINT('Ctrl Pts',(73.7750359268359,118.973205978051,45.5490992598435));
#42566=CARTESIAN_POINT('Ctrl Pts',(80.6221059669441,118.336737949394,47.9566311380089));
#42567=CARTESIAN_POINT('Ctrl Pts',(82.2937460603617,117.700269920737,55.0338604482749));
#42568=CARTESIAN_POINT('Ctrl Pts',(78.088530493305,117.169879896857,59.3719862742016));
#42569=CARTESIAN_POINT('Ctrl Pts',(73.6869395192513,116.745567877751,59.5519806907294));
#42570=CARTESIAN_POINT('Ctrl Pts',(69.6905235374256,116.321255858647,57.6985890987921));
#42571=CARTESIAN_POINT('Ctrl Pts',(67.4693101247587,115.790865834766,52.0799251452905));
#42572=CARTESIAN_POINT('Ctrl Pts',(71.7260004416496,115.15439780611,46.1839822301925));
#42573=CARTESIAN_POINT('Ctrl Pts',(78.9729234825307,114.517929777452,46.5848367151104));
#42574=CARTESIAN_POINT('Ctrl Pts',(82.5637579476127,113.881461748796,52.8923311243753));
#42575=CARTESIAN_POINT('Ctrl Pts',(79.1851059110305,113.244993720138,59.3317616681195));
#42576=CARTESIAN_POINT('Ctrl Pts',(73.1655494534761,112.714603696258,59.849558637312));
#42577=CARTESIAN_POINT('Ctrl Pts',(69.72433240327,112.290291677153,57.099208422117));
#42578=CARTESIAN_POINT('Ctrl Pts',(67.9223691332186,111.865979658048,53.0793415752875));
#42579=CARTESIAN_POINT('Ctrl Pts',(69.9296729059342,111.335589634168,47.3807535737706));
#42580=CARTESIAN_POINT('Ctrl Pts',(77.0095966255024,110.699121605511,45.7205621880855));
#42581=CARTESIAN_POINT('Ctrl Pts',(82.2181531997852,110.062653576854,50.7752151228603));
#42582=CARTESIAN_POINT('Ctrl Pts',(80.7932244767869,109.426185548197,57.8919669109238));
#42583=CARTESIAN_POINT('Ctrl Pts',(74.0198374268243,108.78971751954,60.5382441419418));
#42584=CARTESIAN_POINT('Ctrl Pts',(69.1355541332214,108.259327495659,56.9819890393342));
#42585=CARTESIAN_POINT('Ctrl Pts',(68.3409253064168,107.835015476555,52.6489801401436));
#42586=CARTESIAN_POINT('Ctrl Pts',(69.6163861471822,107.41070345745,48.4323937558124));
#42587=CARTESIAN_POINT('Ctrl Pts',(74.8686177891412,106.880313433569,45.4462195435136));
#42588=CARTESIAN_POINT('Ctrl Pts',(81.3025753690411,106.243845404912,48.8352821236455));
#42589=CARTESIAN_POINT('Ctrl Pts',(81.9205455942097,105.607377376255,56.066927211683));
#42590=CARTESIAN_POINT('Ctrl Pts',(76.1780761879914,104.970909347598,60.5056908905895));
#42591=CARTESIAN_POINT('Ctrl Pts',(69.3289491003867,104.334441318941,58.0621251661116));
#42592=CARTESIAN_POINT('Ctrl Pts',(67.9732632547269,103.80405129506,52.1744015368241));
#42593=CARTESIAN_POINT('Ctrl Pts',(70.2145949202179,103.379739275956,48.3819309096312));
#42594=CARTESIAN_POINT('Ctrl Pts',(73.9424974086653,102.955427256851,46.0347743044002));
#42595=CARTESIAN_POINT('Ctrl Pts',(79.8660360264369,102.42503723297,47.2242548173817));
#42596=CARTESIAN_POINT('Ctrl Pts',(82.5013547012883,101.788569204314,54.0019130260837));
#42597=CARTESIAN_POINT('Ctrl Pts',(78.2259299444734,101.152101175657,59.8670064633057));
#42598=CARTESIAN_POINT('Ctrl Pts',(70.9797598094013,100.515633147,59.452764683521));
#42599=CARTESIAN_POINT('Ctrl Pts',(67.4110006732993,99.8791651183428,53.1167159510304));
#42600=CARTESIAN_POINT('Ctrl Pts',(70.2482054094664,99.3487750944619,47.7825390761917));
#42601=CARTESIAN_POINT('Ctrl Pts',(74.4272333632649,98.9244630753572,46.3889371049594));
#42602=CARTESIAN_POINT('Ctrl Pts',(78.7808858401211,98.5001510562527,47.0613292551355));
#42603=CARTESIAN_POINT('Ctrl Pts',(82.4731666214545,97.9697610323718,51.8436128392389));
#42604=CARTESIAN_POINT('Ctrl Pts',(80.0185264981547,97.333293003715,58.6887788107176));
#42605=CARTESIAN_POINT('Ctrl Pts',(72.9446871853008,96.696824975058,60.3133942281181));
#42606=CARTESIAN_POINT('Ctrl Pts',(67.7454774742435,96.0603569464011,55.249127621888));
#42607=CARTESIAN_POINT('Ctrl Pts',(69.2057968763822,95.4238889177441,48.1252928009685));
#42608=CARTESIAN_POINT('Ctrl Pts',(74.8456470784505,94.8934988938634,45.9584371654408));
#42609=CARTESIAN_POINT('Ctrl Pts',(78.9146258307725,94.4691868747586,47.6465760833042));
#42610=CARTESIAN_POINT('Ctrl Pts',(81.7607158793379,94.0448748556541,51.0090413289703));
#42611=CARTESIAN_POINT('Ctrl Pts',(81.4125019872028,93.5144848317732,57.0407840897579));
#42612=CARTESIAN_POINT('Ctrl Pts',(75.0706895264074,92.8780168031164,60.5992908024265));
#42613=CARTESIAN_POINT('Ctrl Pts',(68.6646538088411,92.2415487744594,57.1873581735787));
#42614=CARTESIAN_POINT('Ctrl Pts',(68.0600443925932,91.6050807458025,49.954583786643));
#42615=CARTESIAN_POINT('Ctrl Pts',(73.8338782107808,90.9686127171454,45.5336790882854));
#42616=CARTESIAN_POINT('Ctrl Pts',(79.5128178695483,90.4382226932647,47.5959152530032));
#42617=CARTESIAN_POINT('Ctrl Pts',(81.4779266132071,90.0139106741601,51.5385981870534));
#42618=CARTESIAN_POINT('Ctrl Pts',(81.4218552681473,89.5895986550554,55.9435110235478));
#42619=CARTESIAN_POINT('Ctrl Pts',(77.2037733255249,89.0592086311748,60.2691275544382));
#42620=CARTESIAN_POINT('Ctrl Pts',(70.0823097037432,88.4227406025177,58.7972881625044));
#42621=CARTESIAN_POINT('Ctrl Pts',(67.4830684886971,87.7862725738608,52.020672267787));
#42622=CARTESIAN_POINT('Ctrl Pts',(71.7693211340833,87.1498045452038,46.1634872665727));
#42623=CARTESIAN_POINT('Ctrl Pts',(79.0274606885328,86.5133365165468,46.6117790467127));
#42624=CARTESIAN_POINT('Ctrl Pts',(81.9627797571738,85.9829464926663,51.8926005369987));
#42625=CARTESIAN_POINT('Ctrl Pts',(80.8611049603024,85.5586344735614,56.157892289598));
#42626=CARTESIAN_POINT('Ctrl Pts',(77.9303474730929,85.134322454457,59.4468224566914));
#42627=CARTESIAN_POINT('Ctrl Pts',(71.9092796279463,84.603932430576,59.9467381007079));
#42628=CARTESIAN_POINT('Ctrl Pts',(67.4977191562266,83.9674644019192,54.1657615814364));
#42629=CARTESIAN_POINT('Ctrl Pts',(69.9789141933655,83.3309963732622,47.3450395473547));
#42630=CARTESIAN_POINT('Ctrl Pts',(77.0557427525776,82.6945283446052,45.7334951259842));
#42631=CARTESIAN_POINT('Ctrl Pts',(82.241661812508,82.0580603159484,50.8313180746414));
#42632=CARTESIAN_POINT('Ctrl Pts',(80.9950386405475,81.5276702920675,56.7430948222971));
#42633=CARTESIAN_POINT('Ctrl Pts',(77.3664066985287,81.1033582729629,59.2409801924079));
#42634=CARTESIAN_POINT('Ctrl Pts',(72.9970495209555,80.6790462538583,59.802334757404));
#42635=CARTESIAN_POINT('Ctrl Pts',(68.1233504155356,80.1486562299775,56.2315882420625));
#42636=CARTESIAN_POINT('Ctrl Pts',(68.5833807300341,79.5121882013205,48.9741832360189));
#42637=CARTESIAN_POINT('Ctrl Pts',(74.9292135124444,78.8757201726637,45.4515444273673));
#42638=CARTESIAN_POINT('Ctrl Pts',(81.3289350878523,78.2392521440066,48.875305756051));
#42639=CARTESIAN_POINT('Ctrl Pts',(81.901506270828,77.6027841153497,56.1247000447093));
#42640=CARTESIAN_POINT('Ctrl Pts',(77.0837927133066,77.0723940914689,59.7706306151759));
#42641=CARTESIAN_POINT('Ctrl Pts',(72.7062521999963,76.6480820723642,59.2771327456936));
#42642=CARTESIAN_POINT('Ctrl Pts',(69.0393031340058,76.2237700532596,56.8358450444417));
#42643=CARTESIAN_POINT('Ctrl Pts',(67.7011107449014,75.6933800293789,50.9441207826716));
#42644=CARTESIAN_POINT('Ctrl Pts',(72.8073145925882,75.0569120007219,45.7664535880871));
#42645=CARTESIAN_POINT('Ctrl Pts',(79.9082939652046,74.4204439720649,47.2680093906491));
#42646=CARTESIAN_POINT('Ctrl Pts',(82.4950116121594,73.783975943408,54.0494155644056));
#42647=CARTESIAN_POINT('Ctrl Pts',(78.1736720527292,73.1475079147511,59.8981401881259));
#42648=CARTESIAN_POINT('Ctrl Pts',(72.1455728758162,72.6171178908703,59.4916995894));
#42649=CARTESIAN_POINT('Ctrl Pts',(69.164141470346,72.1928058717657,56.2486350098195));
#42650=CARTESIAN_POINT('Ctrl Pts',(67.9964246803533,71.768493852661,52.0009487465438));
#42651=CARTESIAN_POINT('Ctrl Pts',(70.8494602565119,71.2381038287802,46.6752223502516));
#42652=CARTESIAN_POINT('Ctrl Pts',(78.0997711246432,70.6016358001233,46.1143768925114));
#42653=CARTESIAN_POINT('Ctrl Pts',(82.4763801653275,69.9651677714664,51.9043571328517));
#42654=CARTESIAN_POINT('Ctrl Pts',(79.9825887478364,69.3286997428094,58.7204837634665));
#42655=CARTESIAN_POINT('Ctrl Pts',(72.8848173646578,68.6922317141525,60.3026331572165));
#42656=CARTESIAN_POINT('Ctrl Pts',(68.6001325998369,68.1618416902717,56.0429794021445));
#42657=CARTESIAN_POINT('Ctrl Pts',(68.4757272381901,67.737529671167,51.6394666681051));
#42658=CARTESIAN_POINT('Ctrl Pts',(70.3794300405974,67.3132176520624,47.6667702622669));
#42659=CARTESIAN_POINT('Ctrl Pts',(76.0256912719453,66.7828276281816,45.5166754377604));
#42660=CARTESIAN_POINT('Ctrl Pts',(81.8674190268599,66.1463595995248,49.8474689158044));
#42661=CARTESIAN_POINT('Ctrl Pts',(81.3750964829256,65.5098915708677,57.0887530830819));
#42662=CARTESIAN_POINT('Ctrl Pts',(75.0227667999605,64.8734235422109,60.5996625774228));
#42663=CARTESIAN_POINT('Ctrl Pts',(68.6265085836188,64.2369555135538,57.1399752878129));
#42664=CARTESIAN_POINT('Ctrl Pts',(68.1847561090447,63.7065654896731,51.1143609292439));
#42665=CARTESIAN_POINT('Ctrl Pts',(70.9783360671663,63.2822534705684,47.7081442434712));
#42666=CARTESIAN_POINT('Ctrl Pts',(75.0206341615341,62.8579414514639,45.9570796503953));
#42667=CARTESIAN_POINT('Ctrl Pts',(80.6934236010896,62.327551427583,48.0361740738063));
#42668=CARTESIAN_POINT('Ctrl Pts',(82.2640911799573,61.6910833989261,55.1364950995558));
#42669=CARTESIAN_POINT('Ctrl Pts',(77.1440776652516,61.054615370269,60.2808161906002));
#42670=CARTESIAN_POINT('Ctrl Pts',(70.0458843870298,60.4181473416123,58.766144588061));
#42671=CARTESIAN_POINT('Ctrl Pts',(67.4853392181704,59.7816793129551,51.9598854282703));
#42672=CARTESIAN_POINT('Ctrl Pts',(71.1029800499966,59.2512892890746,47.1208929237402));
#42673=CARTESIAN_POINT('Ctrl Pts',(75.4456765806947,58.8269772699698,46.3810362246994));
#42674=CARTESIAN_POINT('Ctrl Pts',(79.6458228213659,58.4026652508653,47.7096342262889));
#42675=CARTESIAN_POINT('Ctrl Pts',(82.5654440617889,57.8722752269843,52.999150788269));
#42676=CARTESIAN_POINT('Ctrl Pts',(79.0954161603868,57.2358071983275,59.3898050329843));
#42677=CARTESIAN_POINT('Ctrl Pts',(71.8565449965068,56.5993391696705,59.9164188870352));
#42678=CARTESIAN_POINT('Ctrl Pts',(67.490639844384,55.9628711410137,54.1183631714356));
#42679=CARTESIAN_POINT('Ctrl Pts',(70.0204882082515,55.3264031123566,47.3006346224358));
#42680=CARTESIAN_POINT('Ctrl Pts',(75.9248594739311,54.7960130884758,46.0193955331134));
#42681=CARTESIAN_POINT('Ctrl Pts',(79.6887286312557,54.3717010693712,48.3084324614724));
#42682=CARTESIAN_POINT('Ctrl Pts',(81.9886294577527,53.9473890502666,52.0656731086939));
#42683=CARTESIAN_POINT('Ctrl Pts',(80.7244528662546,53.4169990263858,57.9737211105724));
#42684=CARTESIAN_POINT('Ctrl Pts',(73.9140612514626,52.7805309977289,60.5232546689272));
#42685=CARTESIAN_POINT('Ctrl Pts',(68.1034170573312,52.144062969072,56.1741177513611));
#42686=CARTESIAN_POINT('Ctrl Pts',(68.6091163227816,51.5075949404148,48.9337554585296));
#42687=CARTESIAN_POINT('Ctrl Pts',(74.9897193286527,50.8711269117581,45.4452800618159));
#42688=CARTESIAN_POINT('Ctrl Pts',(80.2876483184124,50.3407368878771,48.3496082227601));
#42689=CARTESIAN_POINT('Ctrl Pts',(81.6283745877845,49.9164248687726,52.5458987469576));
#42690=CARTESIAN_POINT('Ctrl Pts',(80.9010666018048,49.492112849668,56.890714529748));
#42691=CARTESIAN_POINT('Ctrl Pts',(76.0725453005356,48.9617228257872,60.5223196418405));
#42692=CARTESIAN_POINT('Ctrl Pts',(69.2589173778265,48.3252547971302,57.9814477751606));
#42693=CARTESIAN_POINT('Ctrl Pts',(67.7237461093988,47.6887867684733,50.8876598550767));
#42694=CARTESIAN_POINT('Ctrl Pts',(72.8532545152761,47.0523187398164,45.7528062648988));
#42695=CARTESIAN_POINT('Ctrl Pts',(79.9580834172726,46.4158507111594,47.3029551562518));
#42696=CARTESIAN_POINT('Ctrl Pts',(82.0535572989614,45.8854606872788,52.9697146233679));
#42697=CARTESIAN_POINT('Ctrl Pts',(80.3141778168881,45.4611486681739,57.0170545041042));
#42698=CARTESIAN_POINT('Ctrl Pts',(76.9160457242635,45.0368366490694,59.8204630319368));
#42699=CARTESIAN_POINT('Ctrl Pts',(70.8891803301883,44.5064466251886,59.3961198115476));
#42700=CARTESIAN_POINT('Ctrl Pts',(67.4110293127906,43.8699785965316,53.0098829844179));
#42701=CARTESIAN_POINT('Ctrl Pts',(70.9035728970707,43.2335105678747,46.6474371347127));
#42702=CARTESIAN_POINT('Ctrl Pts',(78.1434045755907,42.5970425392179,46.1341972831528));
#42703=CARTESIAN_POINT('Ctrl Pts',(82.4910561621044,41.9605745105607,51.9633894222313));
#42704=CARTESIAN_POINT('Ctrl Pts',(80.3572818064038,41.4301844866801,57.6158385061191));
#42705=CARTESIAN_POINT('Ctrl Pts',(76.3901015894628,41.0058724675753,59.5310100961249));
#42706=CARTESIAN_POINT('Ctrl Pts',(71.986247835856,40.5815604484709,59.419326571397));
#42707=CARTESIAN_POINT('Ctrl Pts',(67.7142338204333,40.0511704245899,55.1469654093431));
#42708=CARTESIAN_POINT('Ctrl Pts',(69.275871844425,39.4147023959331,48.0446529694379));
#42709=CARTESIAN_POINT('Ctrl Pts',(76.0847657125096,38.778234367276,45.5311808347832));
#42710=CARTESIAN_POINT('Ctrl Pts',(81.8873653875674,38.1417663386191,49.8910449255035));
#42711=CARTESIAN_POINT('Ctrl Pts',(81.3474677094592,37.5052983099622,57.1429457666064));
#42712=CARTESIAN_POINT('Ctrl Pts',(76.0300056776799,36.9749082860814,60.0113549402709));
#42713=CARTESIAN_POINT('Ctrl Pts',(71.7789637198702,36.5505962669768,58.8559141733789));
#42714=CARTESIAN_POINT('Ctrl Pts',(68.5272996093743,36.1262842478722,55.8838641056007));
#42715=CARTESIAN_POINT('Ctrl Pts',(68.1034461174788,35.5958942239914,49.8569642504253));
#42716=CARTESIAN_POINT('Ctrl Pts',(73.9396624076152,34.9594261953344,45.5187463297918));
#42717=CARTESIAN_POINT('Ctrl Pts',(80.7285130577238,34.3229581666775,48.0858623632235));
#42718=CARTESIAN_POINT('Ctrl Pts',(82.2505766296694,33.6864901380205,55.1824742562947));
#42719=CARTESIAN_POINT('Ctrl Pts',(77.0876823646044,33.0500221093636,60.3036145708011));
#42720=CARTESIAN_POINT('Ctrl Pts',(71.1921167813803,32.5196320854828,58.9824483810628));
#42721=CARTESIAN_POINT('Ctrl Pts',(68.7402458099335,32.0953200663781,55.3225672585752));
#42722=CARTESIAN_POINT('Ctrl Pts',(68.2341037132805,31.6710080472735,50.946470678878));
#42723=CARTESIAN_POINT('Ctrl Pts',(71.8661011659931,31.1406180233927,46.1182444891829));
#42724=CARTESIAN_POINT('Ctrl Pts',(79.1171193063283,30.5041499947358,46.6698704896195));
#42725=CARTESIAN_POINT('Ctrl Pts',(82.5593545172997,29.8676819660789,53.0596744512932));
#42726=CARTESIAN_POINT('Ctrl Pts',(79.0550629000917,29.231213937422,59.4156573061479));
#42727=CARTESIAN_POINT('Ctrl Pts',(71.7990171583499,28.5947459087649,59.8966516467535));
#42728=CARTESIAN_POINT('Ctrl Pts',(68.2142059078879,28.0643558848842,55.0332883940346));
#42729=CARTESIAN_POINT('Ctrl Pts',(68.7629354775493,27.6400438657795,50.6623277839382));
#42730=CARTESIAN_POINT('Ctrl Pts',(71.2503276753517,27.215731846675,47.0264947721512));
#42731=CARTESIAN_POINT('Ctrl Pts',(77.1584783503202,26.6853418227941,45.7627984010655));
#42732=CARTESIAN_POINT('Ctrl Pts',(82.2712616960307,26.0488737941373,50.9339684465705));
#42733=CARTESIAN_POINT('Ctrl Pts',(80.6801681651456,25.4124057654802,58.0154235336963));
#42734=CARTESIAN_POINT('Ctrl Pts',(73.866642710383,24.7759377368233,60.5163117476636));
#42735=CARTESIAN_POINT('Ctrl Pts',(68.0729453817716,24.1394697081664,56.12147205692));
#42736=CARTESIAN_POINT('Ctrl Pts',(68.5554653314807,23.6090796842856,50.0989820315547));
#42737=CARTESIAN_POINT('Ctrl Pts',(71.8359141101355,23.1847676651809,47.1587399770951));
#42738=CARTESIAN_POINT('Ctrl Pts',(76.0980073818475,22.7604556460764,46.044738731972));
#42739=CARTESIAN_POINT('Ctrl Pts',(81.3872823714418,22.2300656221955,48.9648097787581));
#42740=CARTESIAN_POINT('Ctrl Pts',(81.8565481913765,21.5935975935386,56.2215875539192));
#42741=CARTESIAN_POINT('Ctrl Pts',(76.0117562751922,20.9571295648817,60.5248076967008));
#42742=CARTESIAN_POINT('Ctrl Pts',(69.2276857397562,20.3206615362247,57.9450335920459));
#42743=CARTESIAN_POINT('Ctrl Pts',(67.7352284395576,19.6841935075678,50.8280874080433));
#42744=CARTESIAN_POINT('Ctrl Pts',(72.0487341561334,19.153803483687,46.5970962084509));
#42745=CARTESIAN_POINT('Ctrl Pts',(76.4533287195552,18.7294914645823,46.5289391655419));
#42746=CARTESIAN_POINT('Ctrl Pts',(80.4019430431638,18.3051794454777,48.481393986882));
#42747=CARTESIAN_POINT('Ctrl Pts',(82.479976533845,17.7747894215969,54.1571331492716));
#42748=CARTESIAN_POINT('Ctrl Pts',(78.0768644284893,17.13832139294,59.9386486421499));
#42749=CARTESIAN_POINT('Ctrl Pts',(70.8404208569049,16.5018533642831,59.3639367716877));
#42750=CARTESIAN_POINT('Ctrl Pts',(67.4137579998166,15.8653853356261,52.9507745892659));
#42751=CARTESIAN_POINT('Ctrl Pts',(70.3570038465839,15.3349953117452,47.6862554085638));
#42752=CARTESIAN_POINT('Ctrl Pts',(74.5788989575806,14.9106832926407,46.370762759139));
#42753=CARTESIAN_POINT('Ctrl Pts',(76.7327422243518,14.6985272830883,46.7693660572235));
#42754=CARTESIAN_POINT('Ctrl Pts',(77.6994510401983,14.5924492783122,47.2211751965707));
#42755=CARTESIAN_POINT('Ctrl Pts',(70.0990315389037,416.,55.841954369316));
#42756=CARTESIAN_POINT('Ctrl Pts',(69.6292862985721,415.893921995224,55.0273288624995));
#42757=CARTESIAN_POINT('Ctrl Pts',(69.1165406058533,415.681765985672,53.1663787797211));
#42758=CARTESIAN_POINT('Ctrl Pts',(69.9524819678234,415.257453966567,49.3601406988557));
#42759=CARTESIAN_POINT('Ctrl Pts',(74.352298526842,414.727063942686,46.3781169629522));
#42760=CARTESIAN_POINT('Ctrl Pts',(80.2420155782074,414.090595914029,48.9020647204953));
#42761=CARTESIAN_POINT('Ctrl Pts',(81.293491257306,413.454127885372,55.2122271685484));
#42762=CARTESIAN_POINT('Ctrl Pts',(76.5500783965337,412.817659856716,59.5150838971706));
#42763=CARTESIAN_POINT('Ctrl Pts',(71.4097383128725,412.287269832834,58.1195031021403));
#42764=CARTESIAN_POINT('Ctrl Pts',(69.397075484847,411.86295781373,54.8001736486049));
#42765=CARTESIAN_POINT('Ctrl Pts',(69.1240494715453,411.438645794625,50.9277902465141));
#42766=CARTESIAN_POINT('Ctrl Pts',(72.5128743250655,410.908255770745,46.8207854764477));
#42767=CARTESIAN_POINT('Ctrl Pts',(78.8743400235446,410.271787742087,47.5933144106201));
#42768=CARTESIAN_POINT('Ctrl Pts',(81.6520725540428,409.635319713431,53.3547651639986));
#42769=CARTESIAN_POINT('Ctrl Pts',(78.3155544127733,408.998851684773,58.8116972627153));
#42770=CARTESIAN_POINT('Ctrl Pts',(71.90864214512,408.362383656117,58.9480975871434));
#42771=CARTESIAN_POINT('Ctrl Pts',(68.9450950083279,407.831993632236,54.524794049794));
#42772=CARTESIAN_POINT('Ctrl Pts',(69.6010890929968,407.407681613131,50.6984892817582));
#42773=CARTESIAN_POINT('Ctrl Pts',(71.9347077043872,406.983369594027,47.5960537873647));
#42774=CARTESIAN_POINT('Ctrl Pts',(77.1859865465286,406.452979570146,46.7172645440322));
#42775=CARTESIAN_POINT('Ctrl Pts',(81.4825007141912,405.816511541489,51.4719982227287));
#42776=CARTESIAN_POINT('Ctrl Pts',(79.8016393924563,405.180043512832,57.643270644141));
#42777=CARTESIAN_POINT('Ctrl Pts',(73.704367667017,404.543575484175,59.575416161524));
#42778=CARTESIAN_POINT('Ctrl Pts',(68.7776943304863,403.907107455519,55.477194252816));
#42779=CARTESIAN_POINT('Ctrl Pts',(69.4407233960758,403.376717431636,50.194338734914));
#42780=CARTESIAN_POINT('Ctrl Pts',(72.4450042051697,402.952405412533,47.7356388492427));
#42781=CARTESIAN_POINT('Ctrl Pts',(76.2412371124112,402.528093393428,46.9235284074953));
#42782=CARTESIAN_POINT('Ctrl Pts',(80.7821829418601,401.997703369548,49.7034531632788));
#42783=CARTESIAN_POINT('Ctrl Pts',(80.9082303071252,401.36123534089,56.1106090638576));
#42784=CARTESIAN_POINT('Ctrl Pts',(75.5925088429904,400.724767312234,59.6677158495928));
#42785=CARTESIAN_POINT('Ctrl Pts',(69.7221234542071,400.088299283577,57.1283303225627));
#42786=CARTESIAN_POINT('Ctrl Pts',(68.6898157193372,399.451831254919,50.8036267423682));
#42787=CARTESIAN_POINT('Ctrl Pts',(72.6545162366563,398.921441231039,47.2498512386062));
#42788=CARTESIAN_POINT('Ctrl Pts',(76.5349782081459,398.497129211934,47.3635296330406));
#42789=CARTESIAN_POINT('Ctrl Pts',(79.9336475688305,398.072817192829,49.2396838010189));
#42790=CARTESIAN_POINT('Ctrl Pts',(81.5391758901464,397.542427168949,54.31614411719));
#42791=CARTESIAN_POINT('Ctrl Pts',(77.4329911410624,396.905959140291,59.2361828813744));
#42792=CARTESIAN_POINT('Ctrl Pts',(71.0871415122597,396.269491111636,58.436122929515));
#42793=CARTESIAN_POINT('Ctrl Pts',(68.3201615171243,395.633023082977,52.6695186301911));
#42794=CARTESIAN_POINT('Ctrl Pts',(71.6880557805561,394.996555054321,47.2174710456321));
#42795=CARTESIAN_POINT('Ctrl Pts',(77.0117036986669,394.46616503044,47.1341441224853));
#42796=CARTESIAN_POINT('Ctrl Pts',(79.8669002864431,394.041853011336,49.7644977739172));
#42797=CARTESIAN_POINT('Ctrl Pts',(81.2026403625402,393.617540992231,53.409591234385));
#42798=CARTESIAN_POINT('Ctrl Pts',(79.0860339449119,393.087150968349,58.2950950779045));
#42799=CARTESIAN_POINT('Ctrl Pts',(72.7596690106956,392.450682939694,59.3171720578613));
#42800=CARTESIAN_POINT('Ctrl Pts',(68.4931906324375,391.814214911036,54.5519789152622));
#42801=CARTESIAN_POINT('Ctrl Pts',(70.1854506547193,391.177746882379,48.3838220223643));
#42802=CARTESIAN_POINT('Ctrl Pts',(76.3032611663828,390.541278853722,46.4759621802336));
#42803=CARTESIAN_POINT('Ctrl Pts',(80.3772412432425,390.010888829841,49.9039144648412));
#42804=CARTESIAN_POINT('Ctrl Pts',(80.8081112306684,389.586576810737,53.7620563674119));
#42805=CARTESIAN_POINT('Ctrl Pts',(79.4264024191887,389.162264791632,57.3899743166933));
#42806=CARTESIAN_POINT('Ctrl Pts',(74.6248094448821,388.631874767752,59.6905993277034));
#42807=CARTESIAN_POINT('Ctrl Pts',(69.1782161333895,387.995406739095,56.3138914734408));
#42808=CARTESIAN_POINT('Ctrl Pts',(69.0817056595131,387.358938710438,49.9185346290693));
#42809=CARTESIAN_POINT('Ctrl Pts',(74.4039894636263,386.72247068178,46.3712541852796));
#42810=CARTESIAN_POINT('Ctrl Pts',(80.2739571702038,386.086002653124,48.9424433571557));
#42811=CARTESIAN_POINT('Ctrl Pts',(81.1019979235157,385.555612629243,54.201960354281));
#42812=CARTESIAN_POINT('Ctrl Pts',(78.897412769893,385.131300610139,57.3973808566349));
#42813=CARTESIAN_POINT('Ctrl Pts',(75.4752995936722,384.706988591033,59.2304245810384));
#42814=CARTESIAN_POINT('Ctrl Pts',(70.3415256590186,384.176598567153,57.8188525070491));
#42815=CARTESIAN_POINT('Ctrl Pts',(68.4435630952913,383.540130538496,51.6979642757119));
#42816=CARTESIAN_POINT('Ctrl Pts',(72.5643111612702,382.903662509839,46.8062019332478));
#42817=CARTESIAN_POINT('Ctrl Pts',(78.9086719290272,382.267194481182,47.6179838540664));
#42818=CARTESIAN_POINT('Ctrl Pts',(81.65448204411,381.630726452525,53.4083259377208));
#42819=CARTESIAN_POINT('Ctrl Pts',(78.8308391867579,381.100336428644,57.9222168919113));
#42820=CARTESIAN_POINT('Ctrl Pts',(75.0710571136364,380.67602440954,58.8891432847));
#42821=CARTESIAN_POINT('Ctrl Pts',(71.2853928743543,380.251712390435,58.0291118004746));
#42822=CARTESIAN_POINT('Ctrl Pts',(68.3350139784818,379.721322366554,53.5970203186811));
#42823=CARTESIAN_POINT('Ctrl Pts',(70.9156937160722,379.084854337897,47.7312188622881));
#42824=CARTESIAN_POINT('Ctrl Pts',(77.2345122810668,378.448386309241,46.7400400786665));
#42825=CARTESIAN_POINT('Ctrl Pts',(81.4921801522575,377.811918280583,51.5131069896837));
#42826=CARTESIAN_POINT('Ctrl Pts',(79.7683714008492,377.175450251926,57.6853041691651));
#42827=CARTESIAN_POINT('Ctrl Pts',(74.676644657417,376.645060228046,59.2417389742301));
#42828=CARTESIAN_POINT('Ctrl Pts',(71.2039784868037,376.220748208941,57.5063722827453));
#42829=CARTESIAN_POINT('Ctrl Pts',(68.9097584028537,375.796436189837,54.3746855019773));
#42830=CARTESIAN_POINT('Ctrl Pts',(69.5884755901131,375.266046165955,49.0938225505349));
#42831=CARTESIAN_POINT('Ctrl Pts',(75.3832511001032,374.629578137299,46.3573811711787));
#42832=CARTESIAN_POINT('Ctrl Pts',(80.8038861164523,373.993110108642,49.7524687190848));
#42833=CARTESIAN_POINT('Ctrl Pts',(80.8885816316862,373.356642079985,56.1479929437374));
#42834=CARTESIAN_POINT('Ctrl Pts',(75.5398292911409,372.720174051328,59.677636414875));
#42835=CARTESIAN_POINT('Ctrl Pts',(70.6749913177946,372.189784027447,57.5139538999746));
#42836=CARTESIAN_POINT('Ctrl Pts',(69.1910655822406,371.765472008342,53.9266328524801));
#42837=CARTESIAN_POINT('Ctrl Pts',(69.5124694584528,371.341159989238,50.0578336285873));
#42838=CARTESIAN_POINT('Ctrl Pts',(73.4877077677736,370.810769965357,46.5158495918775));
#42839=CARTESIAN_POINT('Ctrl Pts',(79.6571088321875,370.1743019367,48.2496388351935));
#42840=CARTESIAN_POINT('Ctrl Pts',(81.5234208748353,369.537833908044,54.367382111753));
#42841=CARTESIAN_POINT('Ctrl Pts',(77.3936427899844,368.901365879386,59.2515234291501));
#42842=CARTESIAN_POINT('Ctrl Pts',(71.0408633993679,368.26489785073,58.4090694850156));
#42843=CARTESIAN_POINT('Ctrl Pts',(68.7867101717712,367.734507826848,53.5854853654303));
#42844=CARTESIAN_POINT('Ctrl Pts',(70.0186562199422,367.310195807744,49.904015982041));
#42845=CARTESIAN_POINT('Ctrl Pts',(72.7981944809444,366.885883788639,47.1938361094012));
#42846=CARTESIAN_POINT('Ctrl Pts',(78.1220664110398,366.355493764758,47.126321635835));
#42847=CARTESIAN_POINT('Ctrl Pts',(81.643054336671,365.719025736102,52.4807757313887));
#42848=CARTESIAN_POINT('Ctrl Pts',(79.0405407724415,365.082557707444,58.3234486288234));
#42849=CARTESIAN_POINT('Ctrl Pts',(72.7199018846829,364.446089678788,59.302952324055));
#42850=CARTESIAN_POINT('Ctrl Pts',(68.4759904733059,363.809621650131,54.5012077904277));
#42851=CARTESIAN_POINT('Ctrl Pts',(69.9370688277395,363.279231626249,49.3813034383522));
#42852=CARTESIAN_POINT('Ctrl Pts',(73.2812266717887,362.854919607146,47.4096249147279));
#42853=CARTESIAN_POINT('Ctrl Pts',(77.1569110752008,362.43060758804,47.1860666637397));
#42854=CARTESIAN_POINT('Ctrl Pts',(81.2206916178702,361.90021756416,50.6261041974329));
#42855=CARTESIAN_POINT('Ctrl Pts',(80.3679639602247,361.263749535503,56.9775127164719));
#42856=CARTESIAN_POINT('Ctrl Pts',(74.5718700069468,360.627281506846,59.6821750471879));
#42857=CARTESIAN_POINT('Ctrl Pts',(69.1575163315875,359.990813478189,56.2770792017615));
#42858=CARTESIAN_POINT('Ctrl Pts',(69.1020116217968,359.354345449532,49.8689239398295));
#42859=CARTESIAN_POINT('Ctrl Pts',(73.5623855454864,358.823955425652,46.9614791866025));
#42860=CARTESIAN_POINT('Ctrl Pts',(77.3801004030129,358.399643406547,47.665724281053));
#42861=CARTESIAN_POINT('Ctrl Pts',(80.4528253805887,357.975331387442,50.0383323604923));
#42862=CARTESIAN_POINT('Ctrl Pts',(81.2652408784827,357.444941363561,55.3002855711336));
#42863=CARTESIAN_POINT('Ctrl Pts',(76.4566386365349,356.808473334904,59.5364252185682));
#42864=CARTESIAN_POINT('Ctrl Pts',(70.3070805562703,356.172005306247,57.777778336482));
#42865=CARTESIAN_POINT('Ctrl Pts',(68.4520736285264,355.53553727759,51.6565976712477));
#42866=CARTESIAN_POINT('Ctrl Pts',(72.6121732175607,354.899069248933,46.7820611760358));
#42867=CARTESIAN_POINT('Ctrl Pts',(77.886236228337,354.368679225053,47.5117391122231));
#42868=CARTESIAN_POINT('Ctrl Pts',(80.3068079108729,353.944367205948,50.5468240560329));
#42869=CARTESIAN_POINT('Ctrl Pts',(81.0709222002272,353.520055186843,54.3530081345088));
#42870=CARTESIAN_POINT('Ctrl Pts',(78.2338848228655,352.989665162963,58.858492509318));
#42871=CARTESIAN_POINT('Ctrl Pts',(71.8256481706415,352.353197134305,58.9036327676611));
#42872=CARTESIAN_POINT('Ctrl Pts',(68.3359414908884,351.716729105649,53.5434228158304));
#42873=CARTESIAN_POINT('Ctrl Pts',(70.9492443786796,351.080261076991,47.7055677769413));
#42874=CARTESIAN_POINT('Ctrl Pts',(77.2864777741945,350.443793048335,46.7531983504033));
#42875=CARTESIAN_POINT('Ctrl Pts',(80.7899114940622,349.913403024454,50.7624529822129));
#42876=CARTESIAN_POINT('Ctrl Pts',(80.6272472545832,349.48909100535,54.6411703258245));
#42877=CARTESIAN_POINT('Ctrl Pts',(78.7083308692968,349.064778986245,58.0158803567333));
#42878=CARTESIAN_POINT('Ctrl Pts',(73.6120037259175,348.534388962364,59.557185057255));
#42879=CARTESIAN_POINT('Ctrl Pts',(68.7442020401091,347.897920933707,55.3892069645249));
#42880=CARTESIAN_POINT('Ctrl Pts',(69.6243212317588,347.26145290505,49.0539647712928));
#42881=CARTESIAN_POINT('Ctrl Pts',(75.4254018924481,346.624984876393,46.3600147705323));
#42882=CARTESIAN_POINT('Ctrl Pts',(80.8344916837998,345.988516847736,49.7964783980026));
#42883=CARTESIAN_POINT('Ctrl Pts',(80.8505953206296,345.458126823855,55.1207540487439));
#42884=CARTESIAN_POINT('Ctrl Pts',(78.1844014847269,345.033814804751,57.942512067397));
#42885=CARTESIAN_POINT('Ctrl Pts',(74.5227334601851,344.609502785646,59.2321225374558));
#42886=CARTESIAN_POINT('Ctrl Pts',(69.664343426917,344.079112761766,57.0540002229753));
#42887=CARTESIAN_POINT('Ctrl Pts',(68.7222249177504,343.442644733109,50.7152347794114));
#42888=CARTESIAN_POINT('Ctrl Pts',(73.540906987327,342.806176704451,46.5092620559193));
#42889=CARTESIAN_POINT('Ctrl Pts',(79.6872056462168,342.169708675795,48.279266641831));
#42890=CARTESIAN_POINT('Ctrl Pts',(81.5176696288029,341.533240647137,54.4206782256844));
#42891=CARTESIAN_POINT('Ctrl Pts',(78.0385523165719,341.002850623257,58.4510520619348));
#42892=CARTESIAN_POINT('Ctrl Pts',(74.1752777672687,340.578538604152,58.8331746118364));
#42893=CARTESIAN_POINT('Ctrl Pts',(70.5650945300378,340.154226585048,57.4057696657705));
#42894=CARTESIAN_POINT('Ctrl Pts',(68.3252780582827,339.623836561167,52.5755116286618));
#42895=CARTESIAN_POINT('Ctrl Pts',(71.7704857081252,338.98736853251,47.1719869564409));
#42896=CARTESIAN_POINT('Ctrl Pts',(78.1665513135014,338.350900503852,47.1562322701325));
#42897=CARTESIAN_POINT('Ctrl Pts',(81.6463495765641,337.714432475197,52.522879965557));
#42898=CARTESIAN_POINT('Ctrl Pts',(79.0012508535765,337.077964446539,58.3599158040183));
#42899=CARTESIAN_POINT('Ctrl Pts',(73.7316982178695,336.547574422658,59.1214836287799));
#42900=CARTESIAN_POINT('Ctrl Pts',(70.5643676301849,336.123262403554,56.8767286678197));
#42901=CARTESIAN_POINT('Ctrl Pts',(68.7746777925706,335.698950384449,53.4317441727057));
#42902=CARTESIAN_POINT('Ctrl Pts',(70.2509566334843,335.168560360568,48.3162020395523));
#42903=CARTESIAN_POINT('Ctrl Pts',(76.3953207281506,334.532092331911,46.4956734058825));
#42904=CARTESIAN_POINT('Ctrl Pts',(81.2346643690577,333.895624303255,50.6778566352051));
#42905=CARTESIAN_POINT('Ctrl Pts',(80.3428429412503,333.259156274597,57.0114620838672));
#42906=CARTESIAN_POINT('Ctrl Pts',(74.5182936803783,332.622688245941,59.6839441776349));
#42907=CARTESIAN_POINT('Ctrl Pts',(70.0404139918865,332.09229822206,56.8035337854184));
#42908=CARTESIAN_POINT('Ctrl Pts',(69.1210358704998,331.667986202955,53.0318429502156));
#42909=CARTESIAN_POINT('Ctrl Pts',(70.0287967856483,331.24367418385,49.257339273258));
#42910=CARTESIAN_POINT('Ctrl Pts',(74.4977866088157,330.71328415997,46.3631553653794));
#42911=CARTESIAN_POINT('Ctrl Pts',(80.3305367008356,330.076816131312,49.0176912942896));
#42912=CARTESIAN_POINT('Ctrl Pts',(81.2418547574505,329.440348102656,55.3485208479978));
#42913=CARTESIAN_POINT('Ctrl Pts',(76.4154107889894,328.803880073999,59.5455843521308));
#42914=CARTESIAN_POINT('Ctrl Pts',(70.265470501402,328.167412045342,57.7439825390367));
#42915=CARTESIAN_POINT('Ctrl Pts',(68.7734481583349,327.637022021461,52.6330100425361));
#42916=CARTESIAN_POINT('Ctrl Pts',(70.5525225770171,327.212710002356,49.182531510618));
#42917=CARTESIAN_POINT('Ctrl Pts',(73.7129266627949,326.788397983251,46.9280351364722));
#42918=CARTESIAN_POINT('Ctrl Pts',(78.984799150373,326.258007959371,47.6733746610617));
#42919=CARTESIAN_POINT('Ctrl Pts',(81.6478572785503,325.621539930714,53.5022387047481));
#42920=CARTESIAN_POINT('Ctrl Pts',(78.1845991508713,324.985071902057,58.8795750880781));
#42921=CARTESIAN_POINT('Ctrl Pts',(71.7885153548133,324.3486038734,58.8835136441829));
#42922=CARTESIAN_POINT('Ctrl Pts',(68.3266868515903,323.712135844743,53.4906222074762));
#42923=CARTESIAN_POINT('Ctrl Pts',(70.5516205825161,323.181745820863,48.6534907822217));
#42924=CARTESIAN_POINT('Ctrl Pts',(74.1573917987538,322.757433801757,47.2149770274767));
#42925=CARTESIAN_POINT('Ctrl Pts',(78.0218245725355,322.333121782654,47.5852029360215));
#42926=CARTESIAN_POINT('Ctrl Pts',(81.5133347143192,321.802731758772,51.6048456392999));
#42927=CARTESIAN_POINT('Ctrl Pts',(79.7017885087686,321.166263730116,57.7518640205145));
#42928=CARTESIAN_POINT('Ctrl Pts',(73.5609687392484,320.529795701458,59.5407843643785));
#42929=CARTESIAN_POINT('Ctrl Pts',(68.7293595293914,319.893327672802,55.3496680594258));
#42930=CARTESIAN_POINT('Ctrl Pts',(69.6519568295469,319.256859644144,49.0080319254632));
#42931=CARTESIAN_POINT('Ctrl Pts',(74.5036175039259,318.726469620264,46.8149611940725));
#42932=CARTESIAN_POINT('Ctrl Pts',(78.1692388187073,318.302157601159,48.0932914577593));
#42933=CARTESIAN_POINT('Ctrl Pts',(80.8441080694396,317.877845582055,50.9068270231865));
#42934=CARTESIAN_POINT('Ctrl Pts',(80.8443976887383,317.347455558173,56.2311270192722));
#42935=CARTESIAN_POINT('Ctrl Pts',(75.4459142368694,316.710987529517,59.6842286762946));
#42936=CARTESIAN_POINT('Ctrl Pts',(69.6365665351741,316.07451950086,57.0081526834969));
#42937=CARTESIAN_POINT('Ctrl Pts',(68.7369456197939,315.438051472203,50.6756503623739));
#42938=CARTESIAN_POINT('Ctrl Pts',(73.5918912351737,314.801583443546,46.4927043065974));
#42939=CARTESIAN_POINT('Ctrl Pts',(78.6929398225512,314.271193419665,48.0183103636822));
#42940=CARTESIAN_POINT('Ctrl Pts',(80.6222376764774,313.846881400561,51.3870961504713));
#42941=CARTESIAN_POINT('Ctrl Pts',(80.7968435226311,313.422569381455,55.2652942739464));
#42942=CARTESIAN_POINT('Ctrl Pts',(77.3057707044781,312.892179357576,59.2853168000712));
#42943=CARTESIAN_POINT('Ctrl Pts',(70.9656350492383,312.255711328918,58.3524639140331));
#42944=CARTESIAN_POINT('Ctrl Pts',(68.3343700832684,311.619243300261,52.5226827760076));
#42945=CARTESIAN_POINT('Ctrl Pts',(71.8075564021643,310.982775271605,47.1517535982347));
#42946=CARTESIAN_POINT('Ctrl Pts',(78.2159016640937,310.346307242947,47.1771630008298));
#42947=CARTESIAN_POINT('Ctrl Pts',(81.0667977561599,309.815917219067,51.6738909228237));
#42948=CARTESIAN_POINT('Ctrl Pts',(80.3144061400767,309.391605199962,55.4824096299437));
#42949=CARTESIAN_POINT('Ctrl Pts',(77.9031908065171,308.967293180857,58.5249330072815));
#42950=CARTESIAN_POINT('Ctrl Pts',(72.6313994367438,308.436903156976,59.2708460623881));
#42951=CARTESIAN_POINT('Ctrl Pts',(68.456311111176,307.80043512832,54.4091414120066));
#42952=CARTESIAN_POINT('Ctrl Pts',(70.2924624355432,307.163967099663,48.28227828701));
#42953=CARTESIAN_POINT('Ctrl Pts',(76.4365765807934,306.527499071006,46.5047055575397));
#42954=CARTESIAN_POINT('Ctrl Pts',(81.2581988932575,305.891031042348,50.7260196787322));
#42955=CARTESIAN_POINT('Ctrl Pts',(80.4619885383012,305.360641018468,55.9904493347213));
#42956=CARTESIAN_POINT('Ctrl Pts',(77.3965832675933,304.936328999363,58.372506935359));
#42957=CARTESIAN_POINT('Ctrl Pts',(73.5810548415566,304.512016980259,59.0885032457832));
#42958=CARTESIAN_POINT('Ctrl Pts',(69.1117501822202,303.981626956378,56.1948055431484));
#42959=CARTESIAN_POINT('Ctrl Pts',(69.1475242377325,303.345158927721,49.7865097594955));
#42960=CARTESIAN_POINT('Ctrl Pts',(74.551368128498,302.708690899064,46.3647595285971));
#42961=CARTESIAN_POINT('Ctrl Pts',(80.3557621291498,302.072222870407,49.0515631543982));
#42962=CARTESIAN_POINT('Ctrl Pts',(81.2280414156741,301.435754841751,55.4003160618702));
#42963=CARTESIAN_POINT('Ctrl Pts',(77.1748718396303,300.905364817869,58.8528494679402));
#42964=CARTESIAN_POINT('Ctrl Pts',(73.2985174821482,300.481052798765,58.6412253160407));
#42965=CARTESIAN_POINT('Ctrl Pts',(69.9483047892701,300.05674077966,56.6798526337298));
#42966=CARTESIAN_POINT('Ctrl Pts',(68.4714694295786,299.526350755779,51.5644711374421));
#42967=CARTESIAN_POINT('Ctrl Pts',(72.700576392418,298.889882727122,46.7496825719188));
#42968=CARTESIAN_POINT('Ctrl Pts',(79.0242011636225,298.253414698465,47.7097206916977));
#42969=CARTESIAN_POINT('Ctrl Pts',(81.6446916911186,297.616946669809,53.544352885223));
#42970=CARTESIAN_POINT('Ctrl Pts',(78.1402065526217,296.980478641151,58.909622547401));
#42971=CARTESIAN_POINT('Ctrl Pts',(72.8161519838604,296.450088617271,58.8585003306135));
#42972=CARTESIAN_POINT('Ctrl Pts',(70.0282823888382,296.025776598166,56.1568913641665));
#42973=CARTESIAN_POINT('Ctrl Pts',(68.7850071190202,295.601464579061,52.4792325314445));
#42974=CARTESIAN_POINT('Ctrl Pts',(71.0242980864921,295.071074555181,47.6487308499217));
#42975=CARTESIAN_POINT('Ctrl Pts',(77.3744534912965,294.434606526524,46.7867210073652));
#42976=CARTESIAN_POINT('Ctrl Pts',(81.5192500291734,293.798138497867,51.6581237928087));
#42977=CARTESIAN_POINT('Ctrl Pts',(79.6717830599399,293.16167046921,57.7815843533094));
#42978=CARTESIAN_POINT('Ctrl Pts',(73.5077494891626,292.525202440553,59.5343606573951));
#42979=CARTESIAN_POINT('Ctrl Pts',(69.5216244297834,291.994812416672,56.0046329705635));
#42980=CARTESIAN_POINT('Ctrl Pts',(69.188310236716,291.570500397568,52.1368416712381));
#42981=CARTESIAN_POINT('Ctrl Pts',(70.6611837554908,291.146188378463,48.5449686940674));
#42982=CARTESIAN_POINT('Ctrl Pts',(75.519336798809,290.615798354582,46.3663178409258));
#42983=CARTESIAN_POINT('Ctrl Pts',(80.8789313829989,289.979330325925,49.8794760393219));
#42984=CARTESIAN_POINT('Ctrl Pts',(80.8139277700718,289.342862297268,56.2752307226039));
#42985=CARTESIAN_POINT('Ctrl Pts',(75.4037717530398,288.706394268611,59.6869920433574));
#42986=CARTESIAN_POINT('Ctrl Pts',(69.6005983433171,288.069926239955,56.9684054601267));
#42987=CARTESIAN_POINT('Ctrl Pts',(68.9056248589062,287.539536216073,51.6896572763087));
#42988=CARTESIAN_POINT('Ctrl Pts',(71.1901917605342,287.115224196969,48.5509215501885));
#42989=CARTESIAN_POINT('Ctrl Pts',(74.6574983630918,286.690912177864,46.8048709179623));
#42990=CARTESIAN_POINT('Ctrl Pts',(79.7539931571663,286.160522153983,48.3456211722762));
#42991=CARTESIAN_POINT('Ctrl Pts',(81.496797625751,285.524054125327,54.5124815743055));
#42992=CARTESIAN_POINT('Ctrl Pts',(77.2538459713296,284.887586096669,59.2986350086054));
#42993=CARTESIAN_POINT('Ctrl Pts',(70.9320055672451,284.251118068013,58.3269162510927));
#42994=CARTESIAN_POINT('Ctrl Pts',(68.3332775512137,283.614650039355,52.4690883829723));
#42995=CARTESIAN_POINT('Ctrl Pts',(71.2699962732185,283.084260015475,48.0279338393853));
#42996=CARTESIAN_POINT('Ctrl Pts',(75.0529945743877,282.65994799637,47.1562505598691));
#42997=CARTESIAN_POINT('Ctrl Pts',(78.8157359444728,282.235635977266,48.1115961875279));
#42998=CARTESIAN_POINT('Ctrl Pts',(81.6532634634593,281.705245953385,52.6167718901163));
#42999=CARTESIAN_POINT('Ctrl Pts',(78.9252945386105,281.068777924728,58.415540740389));
#43000=CARTESIAN_POINT('Ctrl Pts',(72.5834632791282,280.432309896071,59.2468527844925));
#43001=CARTESIAN_POINT('Ctrl Pts',(68.4476732525639,279.795841867414,54.3678012071275));
#43002=CARTESIAN_POINT('Ctrl Pts',(70.326780909695,279.159373838757,48.2410982563761));
#43003=CARTESIAN_POINT('Ctrl Pts',(75.4561843501935,278.628983814876,46.8137262387156));
#43004=CARTESIAN_POINT('Ctrl Pts',(78.8839251560877,278.204671795772,48.6362247583429));
#43005=CARTESIAN_POINT('Ctrl Pts',(81.0983384007498,277.780359776667,51.8248423064824));
#43006=CARTESIAN_POINT('Ctrl Pts',(80.2864953634584,277.249969752786,57.0868838698871));
#43007=CARTESIAN_POINT('Ctrl Pts',(74.4244720439219,276.613501724129,59.6761341928656));
#43008=CARTESIAN_POINT('Ctrl Pts',(69.0912915673428,275.977033695473,56.1452576101099));
#43009=CARTESIAN_POINT('Ctrl Pts',(69.1681105982651,275.340565666815,49.7496339286456));
#43010=CARTESIAN_POINT('Ctrl Pts',(74.6042813775611,274.704097638159,46.3561722901173));
#43011=CARTESIAN_POINT('Ctrl Pts',(79.412935102352,274.173707614278,48.6420025303696));
#43012=CARTESIAN_POINT('Ctrl Pts',(80.8058075434052,273.749395595173,52.2656490707197));
#43013=CARTESIAN_POINT('Ctrl Pts',(80.3868186252344,273.325083576069,56.1250993130324));
#43014=CARTESIAN_POINT('Ctrl Pts',(76.3234123534648,272.794693552187,59.5655789311586));
#43015=CARTESIAN_POINT('Ctrl Pts',(70.1997566345717,272.158225523531,57.6765645663912));
#43016=CARTESIAN_POINT('Ctrl Pts',(68.4885131854145,271.521757494873,51.5136472948276));
#43017=CARTESIAN_POINT('Ctrl Pts',(72.740299548083,270.885289466217,46.7353404645114));
#43018=CARTESIAN_POINT('Ctrl Pts',(79.0697814196283,270.24882143756,47.737934037007));
#43019=CARTESIAN_POINT('Ctrl Pts',(81.2014200278245,269.718431413679,52.6168977975042));
#43020=CARTESIAN_POINT('Ctrl Pts',(79.8769093444932,269.294119394574,56.2660866575358));
#43021=CARTESIAN_POINT('Ctrl Pts',(77.0298250182992,268.86980737547,58.9052188493705));
#43022=CARTESIAN_POINT('Ctrl Pts',(71.7059457747086,268.339417351589,58.8382835682292));
#43023=CARTESIAN_POINT('Ctrl Pts',(68.3212808918114,267.702949322932,53.396631405116));
#43024=CARTESIAN_POINT('Ctrl Pts',(71.0704926838037,267.066481294275,47.6215350456437));
#43025=CARTESIAN_POINT('Ctrl Pts',(77.413848888673,266.430013265619,46.8019403308202));
#43026=CARTESIAN_POINT('Ctrl Pts',(81.5351627289913,265.793545236961,51.7093130355808));
#43027=CARTESIAN_POINT('Ctrl Pts',(79.9452721866972,265.26315521308,56.7906926312932));
#43028=CARTESIAN_POINT('Ctrl Pts',(76.5523955207542,264.838843193976,58.677302240125));
#43029=CARTESIAN_POINT('Ctrl Pts',(72.6723019530944,264.414531174871,58.8029278451709));
#43030=CARTESIAN_POINT('Ctrl Pts',(68.6966783295341,263.88414115099,55.2613763015696));
#43031=CARTESIAN_POINT('Ctrl Pts',(69.7095077253019,263.247673122334,48.9335242766798));
#43032=CARTESIAN_POINT('Ctrl Pts',(75.5720466440224,262.611205093676,46.3760761608992));
#43033=CARTESIAN_POINT('Ctrl Pts',(80.8986950719364,261.97473706502,49.9167992457815));
#43034=CARTESIAN_POINT('Ctrl Pts',(80.7923756078113,261.338269036362,56.3243128669436));
#43035=CARTESIAN_POINT('Ctrl Pts',(76.2600105715705,260.807879012482,59.1182057980456));
#43036=CARTESIAN_POINT('Ctrl Pts',(72.4612951821995,260.383566993377,58.317787609226));
#43037=CARTESIAN_POINT('Ctrl Pts',(69.4494584547942,259.959254974273,55.8683494259096));
#43038=CARTESIAN_POINT('Ctrl Pts',(68.7701667585371,259.428864950391,50.5875603443804));
#43039=CARTESIAN_POINT('Ctrl Pts',(73.6841987474315,258.792396921735,46.4741889478306));
#43040=CARTESIAN_POINT('Ctrl Pts',(79.78739015126,258.155928893078,48.3875519888271));
#43041=CARTESIAN_POINT('Ctrl Pts',(81.4872452956088,257.519460864421,54.5536200979751));
#43042=CARTESIAN_POINT('Ctrl Pts',(77.2053896188859,256.882992835764,59.321559547837));
#43043=CARTESIAN_POINT('Ctrl Pts',(71.9514325914311,256.352602811883,58.458943708744));
#43044=CARTESIAN_POINT('Ctrl Pts',(69.608268828627,255.928290792779,55.3637068087443));
#43045=CARTESIAN_POINT('Ctrl Pts',(68.9405046437633,255.503978773674,51.5394423200026));
#43046=CARTESIAN_POINT('Ctrl Pts',(71.8904013482855,254.973588749793,47.1070298882851));
#43047=CARTESIAN_POINT('Ctrl Pts',(78.2977346304908,254.337120721136,47.2237125544275));
#43048=CARTESIAN_POINT('Ctrl Pts',(81.6509829051717,253.700652692479,52.6703288844776));
#43049=CARTESIAN_POINT('Ctrl Pts',(78.8911068809706,253.064184663823,58.4403364901449));
#43050=CARTESIAN_POINT('Ctrl Pts',(72.531846601885,252.427716635165,59.2323865748476));
#43051=CARTESIAN_POINT('Ctrl Pts',(69.1307639245367,251.897326611285,55.1359482250076));
#43052=CARTESIAN_POINT('Ctrl Pts',(69.3913142509957,251.47301459218,51.2625748355938));
#43053=CARTESIAN_POINT('Ctrl Pts',(71.3948305414538,251.048702573075,47.9373935833451));
#43054=CARTESIAN_POINT('Ctrl Pts',(76.5284508786805,250.518312549195,46.5252630067303));
#43055=CARTESIAN_POINT('Ctrl Pts',(81.2894587335241,249.881844520538,50.8148246206893));
#43056=CARTESIAN_POINT('Ctrl Pts',(80.2496547382429,249.245376491881,57.1258238355375));
#43057=CARTESIAN_POINT('Ctrl Pts',(74.3824011893066,248.608908463224,59.6724371220249));
#43058=CARTESIAN_POINT('Ctrl Pts',(69.0618070063151,247.972440434567,56.1004891697511));
#43059=CARTESIAN_POINT('Ctrl Pts',(69.1801469266377,247.442050410686,50.777504462329));
#43060=CARTESIAN_POINT('Ctrl Pts',(71.9167403237001,247.017738391581,48.0239677428365));
#43061=CARTESIAN_POINT('Ctrl Pts',(75.6098036593971,246.593426372477,46.8272258805422));
#43062=CARTESIAN_POINT('Ctrl Pts',(80.4116468937403,246.063036348596,49.1273285054245));
#43063=CARTESIAN_POINT('Ctrl Pts',(81.1934106450685,245.426568319939,55.4878615075355));
#43064=CARTESIAN_POINT('Ctrl Pts',(76.2700637597904,244.790100291282,59.5708210818689));
#43065=CARTESIAN_POINT('Ctrl Pts',(70.1704175211297,244.153632262625,57.6461862589446));
#43066=CARTESIAN_POINT('Ctrl Pts',(68.4956083292596,243.517164233968,51.4605133929858));
#43067=CARTESIAN_POINT('Ctrl Pts',(72.0753836691866,242.986774210088,47.5192725924447));
#43068=CARTESIAN_POINT('Ctrl Pts',(75.9470751017479,242.562462190983,47.234819894324));
#43069=CARTESIAN_POINT('Ctrl Pts',(79.520065189934,242.138150171878,48.7529271751713));
#43070=CARTESIAN_POINT('Ctrl Pts',(81.6372030963402,241.607760147998,53.6382007209877));
#43071=CARTESIAN_POINT('Ctrl Pts',(78.0566544293302,240.97129211934,58.9530107718744));
#43072=CARTESIAN_POINT('Ctrl Pts',(71.6622303016729,240.334824090684,58.8072592228149));
#43073=CARTESIAN_POINT('Ctrl Pts',(68.3190498381245,239.698356062027,53.3544573901267));
#43074=CARTESIAN_POINT('Ctrl Pts',(71.1106908750382,239.06188803337,47.586071571299));
#43075=CARTESIAN_POINT('Ctrl Pts',(76.3977930505111,238.531498009489,46.9578032223369));
#43076=CARTESIAN_POINT('Ctrl Pts',(79.507433526864,238.107185990384,49.2818178510052));
#43077=CARTESIAN_POINT('Ctrl Pts',(81.209566592217,237.68287397128,52.770893790888));
#43078=CARTESIAN_POINT('Ctrl Pts',(79.6045905562849,237.152483947399,57.8475287448985));
#43079=CARTESIAN_POINT('Ctrl Pts',(73.4162169892982,236.516015918742,59.5123312044275));
#43080=CARTESIAN_POINT('Ctrl Pts',(68.6840167868883,235.879547890085,55.2092875510666));
#43081=CARTESIAN_POINT('Ctrl Pts',(69.735477959311,235.243079861428,48.9002200414177));
#43082=CARTESIAN_POINT('Ctrl Pts',(75.6256505593195,234.60661183277,46.3756604014124));
#43083=CARTESIAN_POINT('Ctrl Pts',(80.0293719336459,234.076221808891,49.3682192712584));
#43084=CARTESIAN_POINT('Ctrl Pts',(80.8532214045015,233.651909789785,53.1619219396033));
#43085=CARTESIAN_POINT('Ctrl Pts',(79.8504433688653,233.227597770682,56.9123011334566));
#43086=CARTESIAN_POINT('Ctrl Pts',(75.3098000176901,232.697207746799,59.6927198950109));
#43087=CARTESIAN_POINT('Ctrl Pts',(69.5459368691264,232.060739718144,56.8917528765499));
#43088=CARTESIAN_POINT('Ctrl Pts',(68.7947633682085,231.424271689486,50.5399309481628));
#43089=CARTESIAN_POINT('Ctrl Pts',(73.7256447190361,230.78780366083,46.4660737412472));
#43090=CARTESIAN_POINT('Ctrl Pts',(79.8281335926119,230.151335632172,48.4223876685125));
#43091=CARTESIAN_POINT('Ctrl Pts',(81.1906277281917,229.620945608292,53.5694043056184));
#43092=CARTESIAN_POINT('Ctrl Pts',(79.3249956567615,229.196633589187,56.973860923079));
#43093=CARTESIAN_POINT('Ctrl Pts',(76.1086729866622,228.772321570083,59.1478380087876));
#43094=CARTESIAN_POINT('Ctrl Pts',(70.8573012407579,228.241931546201,58.2696208856052));
#43095=CARTESIAN_POINT('Ctrl Pts',(68.3422715097577,227.605463517545,52.3753728345039));
#43096=CARTESIAN_POINT('Ctrl Pts',(71.9402036438859,226.968995488888,47.087198498792));
#43097=CARTESIAN_POINT('Ctrl Pts',(78.3343475963114,226.332527460231,47.2447628702198));
#43098=CARTESIAN_POINT('Ctrl Pts',(81.6589013761616,225.696059431574,52.7233463383287));
#43099=CARTESIAN_POINT('Ctrl Pts',(79.3125390351989,225.165669407693,57.5027557511392));
#43100=CARTESIAN_POINT('Ctrl Pts',(75.6715948746436,224.741357388588,58.8497648206672));
#43101=CARTESIAN_POINT('Ctrl Pts',(71.8177424321106,224.317045369484,58.3820796919963));
#43102=CARTESIAN_POINT('Ctrl Pts',(68.4288418723472,223.786655345603,54.2755576487171));
#43103=CARTESIAN_POINT('Ctrl Pts',(70.395023167623,223.150187316946,48.1762408565892));
#43104=CARTESIAN_POINT('Ctrl Pts',(76.5790555611666,222.513719288289,46.5429470970313));
#43105=CARTESIAN_POINT('Ctrl Pts',(81.3032979875237,221.877251259633,50.8547257155437));
#43106=CARTESIAN_POINT('Ctrl Pts',(80.2208684679564,221.240783230975,57.1710441926388));
#43107=CARTESIAN_POINT('Ctrl Pts',(75.3153785508202,220.710393207095,59.2409109611796));
#43108=CARTESIAN_POINT('Ctrl Pts',(71.6832052365558,220.286081187989,57.8704308428568));
#43109=CARTESIAN_POINT('Ctrl Pts',(69.0802282421642,219.861769168886,54.9902519886439));
#43110=CARTESIAN_POINT('Ctrl Pts',(69.2143835119882,219.331379145004,49.6676414947474));
#43111=CARTESIAN_POINT('Ctrl Pts',(74.698326373318,218.694911116347,46.3519543542357));
#43112=CARTESIAN_POINT('Ctrl Pts',(80.4382692886431,218.05844308769,49.1738612228084));
#43113=CARTESIAN_POINT('Ctrl Pts',(81.177672384873,217.421975059033,55.5270645828276));
#43114=CARTESIAN_POINT('Ctrl Pts',(76.2187228071657,216.785507030377,59.5860802860795));
#43115=CARTESIAN_POINT('Ctrl Pts',(71.1576983282718,216.255117006495,57.9321749584298));
#43116=CARTESIAN_POINT('Ctrl Pts',(69.31426183066,215.830804987392,54.5157242093268));
#43117=CARTESIAN_POINT('Ctrl Pts',(69.2372749896401,215.406492968286,50.6344011155516));
#43118=CARTESIAN_POINT('Ctrl Pts',(72.829541004845,214.876102944406,46.7037054021372));
#43119=CARTESIAN_POINT('Ctrl Pts',(79.1426438599285,214.239634915749,47.7965405392687));
#43120=CARTESIAN_POINT('Ctrl Pts',(81.6284456217072,213.603166887092,53.6905654701027));
#43121=CARTESIAN_POINT('Ctrl Pts',(78.0159571360404,212.966698858435,58.9727077333983));
#43122=CARTESIAN_POINT('Ctrl Pts',(71.6194256917035,212.330230829778,58.7843319643082));
#43123=CARTESIAN_POINT('Ctrl Pts',(68.3174643030566,211.693762801121,53.3056650395866));
#43124=CARTESIAN_POINT('Ctrl Pts',(71.1496401123775,211.057294772464,47.5586365481913));
#43125=CARTESIAN_POINT('Ctrl Pts',(76.4416934236012,210.526904748583,46.9679457097492));
#43126=CARTESIAN_POINT('Ctrl Pts',(79.5342341192608,210.102592729479,49.3146003451081));
#43127=CARTESIAN_POINT('Ctrl Pts',(81.2112769892146,209.678280710374,52.8157317414015));
#43128=CARTESIAN_POINT('Ctrl Pts',(79.5696286458101,209.147890686493,57.8807452976899));
#43129=CARTESIAN_POINT('Ctrl Pts',(73.3694517075265,208.511422657837,59.5008055828234));
#43130=CARTESIAN_POINT('Ctrl Pts',(68.6683970655276,207.874954629179,55.1637564563535));
#43131=CARTESIAN_POINT('Ctrl Pts',(69.7653637905974,207.238486600523,48.8624258785963));
#43132=CARTESIAN_POINT('Ctrl Pts',(75.6735905312152,206.602018571865,46.3804373005538));
#43133=CARTESIAN_POINT('Ctrl Pts',(80.0556099260794,206.071628547985,49.4046869809193));
#43134=CARTESIAN_POINT('Ctrl Pts',(80.8520645262666,205.64731652888,53.2042368931363));
#43135=CARTESIAN_POINT('Ctrl Pts',(79.8222544701088,205.223004509775,56.947282442927));
#43136=CARTESIAN_POINT('Ctrl Pts',(75.2616679235261,204.692614485895,59.6948686777458));
#43137=CARTESIAN_POINT('Ctrl Pts',(69.5181641574838,204.056146457238,56.8523878495988));
#43138=CARTESIAN_POINT('Ctrl Pts',(68.8128385238247,203.419678428581,50.4953117049742));
#43139=CARTESIAN_POINT('Ctrl Pts',(73.7729845636653,202.783210399924,46.4571368186103));
#43140=CARTESIAN_POINT('Ctrl Pts',(79.8611997119805,202.146742371267,48.4574294283178));
#43141=CARTESIAN_POINT('Ctrl Pts',(81.1865226116244,201.616352347386,53.6141424809881));
#43142=CARTESIAN_POINT('Ctrl Pts',(79.2963758820999,201.192040328282,57.0050499361194));
#43143=CARTESIAN_POINT('Ctrl Pts',(76.064451658235,200.767728309176,59.1557646138185));
#43144=CARTESIAN_POINT('Ctrl Pts',(70.8195529427137,200.237338285297,58.2396816294403));
#43145=CARTESIAN_POINT('Ctrl Pts',(68.3471157639746,199.600870256639,52.3274410178494));
#43146=CARTESIAN_POINT('Ctrl Pts',(71.9831085027866,198.964402227983,47.0653634605732));
#43147=CARTESIAN_POINT('Ctrl Pts',(78.3759491980706,198.327934199325,47.2690575728888));
#43148=CARTESIAN_POINT('Ctrl Pts',(81.6608883801067,197.691466170669,52.7714851467922));
#43149=CARTESIAN_POINT('Ctrl Pts',(79.2801036087496,197.161076146787,57.5338411185366));
#43150=CARTESIAN_POINT('Ctrl Pts',(75.6295355167696,196.736764127683,58.8545456627842));
#43151=CARTESIAN_POINT('Ctrl Pts',(71.7791577583434,196.312452108578,58.3590671026649));
#43152=CARTESIAN_POINT('Ctrl Pts',(68.4199739824153,195.782062084697,54.2282009838377));
#43153=CARTESIAN_POINT('Ctrl Pts',(70.4301108370362,195.14559405604,48.1432289658392));
#43154=CARTESIAN_POINT('Ctrl Pts',(76.6257663738702,194.509126027384,46.5545956201064));
#43155=CARTESIAN_POINT('Ctrl Pts',(81.3187765389438,193.872657998727,50.9003474571235));
#43156=CARTESIAN_POINT('Ctrl Pts',(80.1908023736674,193.236189970069,57.208691845023));
#43157=CARTESIAN_POINT('Ctrl Pts',(75.2705069128446,192.705799946189,59.2431114453968));
#43158=CARTESIAN_POINT('Ctrl Pts',(71.6483148472814,192.281487927084,57.8464609785267));
#43159=CARTESIAN_POINT('Ctrl Pts',(69.0661887410767,191.857175907979,54.9475762519299));
#43160=CARTESIAN_POINT('Ctrl Pts',(69.2387374677117,191.326785884099,49.6260729427954));
#43161=CARTESIAN_POINT('Ctrl Pts',(74.746470817058,190.690317855442,46.3500375360377));
#43162=CARTESIAN_POINT('Ctrl Pts',(80.4658856290766,190.053849826785,49.2132870268233));
#43163=CARTESIAN_POINT('Ctrl Pts',(81.1594658110218,189.417381798128,55.571655525867));
#43164=CARTESIAN_POINT('Ctrl Pts',(76.1712915211055,188.780913769471,59.5947950818913));
#43165=CARTESIAN_POINT('Ctrl Pts',(71.122455804744,188.25052374559,57.9044020975852));
#43166=CARTESIAN_POINT('Ctrl Pts',(69.3035327663159,187.826211726486,54.4747626315898));
#43167=CARTESIAN_POINT('Ctrl Pts',(69.2549135694621,187.40189970738,50.5929403713447));
#43168=CARTESIAN_POINT('Ctrl Pts',(72.8746450227851,186.871509683501,46.6883642435143));
#43169=CARTESIAN_POINT('Ctrl Pts',(79.1811568044568,186.235041654843,47.8265398808685));
#43170=CARTESIAN_POINT('Ctrl Pts',(81.6217878086657,185.598573626186,53.738665026678));
#43171=CARTESIAN_POINT('Ctrl Pts',(77.9760801015144,184.962105597529,58.9940164661573));
#43172=CARTESIAN_POINT('Ctrl Pts',(71.5719371009017,184.325637568872,58.760591828347));
#43173=CARTESIAN_POINT('Ctrl Pts',(68.8685169582398,183.795247544992,54.1736876365801));
#43174=CARTESIAN_POINT('Ctrl Pts',(69.7441447209343,183.370935525887,50.3916003943771));
#43175=CARTESIAN_POINT('Ctrl Pts',(72.2528560934249,182.946623506783,47.4289537505847));
#43176=CARTESIAN_POINT('Ctrl Pts',(77.5460829854539,182.416233482901,46.8545674679323));
#43177=CARTESIAN_POINT('Ctrl Pts',(81.5611495397949,181.779765454245,51.8492421518375));
#43178=CARTESIAN_POINT('Ctrl Pts',(79.5270748169464,181.143297425587,57.9132708011999));
#43179=CARTESIAN_POINT('Ctrl Pts',(73.3284950085148,180.506829396931,59.4904555706305));
#43180=CARTESIAN_POINT('Ctrl Pts',(68.6464467632618,179.870361368274,55.1148460287544));
#43181=CARTESIAN_POINT('Ctrl Pts',(69.6131321617587,179.339971344393,49.8790376028731));
#43182=CARTESIAN_POINT('Ctrl Pts',(72.7542485557096,178.915659325288,47.5977450556339));
#43183=CARTESIAN_POINT('Ctrl Pts',(76.5910088428193,178.491347306184,47.0059863330989));
#43184=CARTESIAN_POINT('Ctrl Pts',(80.9640223938111,177.960957282303,50.0432421693827));
#43185=CARTESIAN_POINT('Ctrl Pts',(80.7202401717823,177.324489253646,56.4469992589398));
#43186=CARTESIAN_POINT('Ctrl Pts',(75.208166943184,176.688021224989,59.6915257515102));
#43187=CARTESIAN_POINT('Ctrl Pts',(69.4940514634066,176.051553196332,56.8177150893079));
#43188=CARTESIAN_POINT('Ctrl Pts',(68.828326029216,175.415085167675,50.4439921364254));
#43189=CARTESIAN_POINT('Ctrl Pts',(72.9914360826229,174.884695143794,47.1248529083393));
#43190=CARTESIAN_POINT('Ctrl Pts',(76.8588776947801,174.46038312469,47.4622003004928));
#43191=CARTESIAN_POINT('Ctrl Pts',(80.1436543482285,174.036071105585,49.5312943591081));
#43192=CARTESIAN_POINT('Ctrl Pts',(81.4536551141952,173.505681081704,54.6919211161372));
#43193=CARTESIAN_POINT('Ctrl Pts',(77.0704786758444,172.869213053048,59.3668862437205));
#43194=CARTESIAN_POINT('Ctrl Pts',(70.781351567379,172.23274502439,58.2020756788708));
#43195=CARTESIAN_POINT('Ctrl Pts',(68.351646798808,171.596276995734,52.2854517956076));
#43196=CARTESIAN_POINT('Ctrl Pts',(72.0284531099989,170.959808967076,47.0367729157542));
#43197=CARTESIAN_POINT('Ctrl Pts',(77.3480421827307,170.429418943196,47.260698415578));
#43198=CARTESIAN_POINT('Ctrl Pts',(80.0467424555462,170.005106924091,50.0513837657998));
#43199=CARTESIAN_POINT('Ctrl Pts',(81.1699777859826,169.580794904987,53.767463727116));
#43200=CARTESIAN_POINT('Ctrl Pts',(78.7750585603247,169.050404881106,58.5227273827689));
#43201=CARTESIAN_POINT('Ctrl Pts',(72.4002672174427,168.413936852449,59.1781432572696));
#43202=CARTESIAN_POINT('Ctrl Pts',(68.415791308239,167.777468823792,54.1747588859273));
#43203=CARTESIAN_POINT('Ctrl Pts',(70.4610652576824,167.141000795135,48.1144983378858));
#43204=CARTESIAN_POINT('Ctrl Pts',(76.6787490482889,166.504532766478,46.5627435525341));
#43205=CARTESIAN_POINT('Ctrl Pts',(80.5481907545866,165.974142742597,50.220009117647));
#43206=CARTESIAN_POINT('Ctrl Pts',(80.7557724814388,165.549830723493,54.0965820517106));
#43207=CARTESIAN_POINT('Ctrl Pts',(79.1670753196014,165.125518704388,57.6387493563994));
#43208=CARTESIAN_POINT('Ctrl Pts',(74.2407590117034,164.595128680508,59.6585459220802));
#43209=CARTESIAN_POINT('Ctrl Pts',(68.9980337649973,163.95866065185,55.9732553471886));
#43210=CARTESIAN_POINT('Ctrl Pts',(69.2706230284558,163.322192623193,49.5829816025151));
#43211=CARTESIAN_POINT('Ctrl Pts',(74.7886807951738,162.685724594536,46.3486436607436));
#43212=CARTESIAN_POINT('Ctrl Pts',(80.5005445843739,162.04925656588,49.2541809066686));
#43213=CARTESIAN_POINT('Ctrl Pts',(81.0237923101313,161.518866541998,54.5527073385821));
#43214=CARTESIAN_POINT('Ctrl Pts',(78.6385393623837,161.094554522894,57.6156269035887));
#43215=CARTESIAN_POINT('Ctrl Pts',(75.1163796021698,160.670242503789,59.2482011009735));
#43216=CARTESIAN_POINT('Ctrl Pts',(70.0725868922178,160.139852479909,57.5428197268428));
#43217=CARTESIAN_POINT('Ctrl Pts',(68.530890451871,159.503384451252,51.3226343019818));
#43218=CARTESIAN_POINT('Ctrl Pts',(72.9269747274227,158.866916422595,46.6767386422982));
#43219=CARTESIAN_POINT('Ctrl Pts',(79.2139392306464,158.230448393938,47.8531657644027));
#43220=CARTESIAN_POINT('Ctrl Pts',(81.6211399760129,157.593980365281,53.7922666395636));
#43221=CARTESIAN_POINT('Ctrl Pts',(78.5417996070232,157.0635903414,58.135748356356));
#43222=CARTESIAN_POINT('Ctrl Pts',(74.7324983674773,156.639278322295,58.8841679932114));
#43223=CARTESIAN_POINT('Ctrl Pts',(71.002752658437,156.214966303191,57.8071792131713));
#43224=CARTESIAN_POINT('Ctrl Pts',(68.3129682762291,155.68457627931,53.2122656656242));
#43225=CARTESIAN_POINT('Ctrl Pts',(71.2277399375131,155.048108250653,47.5051086854453));
#43226=CARTESIAN_POINT('Ctrl Pts',(77.5932150058283,154.411640221996,46.8801042110002));
#43227=CARTESIAN_POINT('Ctrl Pts',(81.5684408542748,153.775172193339,51.8908409724219));
#43228=CARTESIAN_POINT('Ctrl Pts',(79.4914376377215,153.138704164682,57.9533150772952));
#43229=CARTESIAN_POINT('Ctrl Pts',(74.3184020126598,152.608314140801,59.2134233877355));
#43230=CARTESIAN_POINT('Ctrl Pts',(70.9516299530984,152.184002121697,57.2806135715887));
#43231=CARTESIAN_POINT('Ctrl Pts',(68.8418931422078,151.759690102592,54.0217919325278));
#43232=CARTESIAN_POINT('Ctrl Pts',(69.8241254614745,151.229300078712,48.7888778110099));
#43233=CARTESIAN_POINT('Ctrl Pts',(75.7671119106681,150.592832050054,46.3912859569748));
#43234=CARTESIAN_POINT('Ctrl Pts',(80.982861794159,149.956364021397,50.0934281194647));
#43235=CARTESIAN_POINT('Ctrl Pts',(80.6984675924352,149.31989599274,56.4831873775621));
#43236=CARTESIAN_POINT('Ctrl Pts',(75.1550028210449,148.683427964083,59.698390786709));
#43237=CARTESIAN_POINT('Ctrl Pts',(70.4230863720779,148.153037940203,57.2576660475808));
#43238=CARTESIAN_POINT('Ctrl Pts',(69.1485793584295,147.728725921098,53.5907136673885));
#43239=CARTESIAN_POINT('Ctrl Pts',(69.6926334846929,147.304413901994,49.7468987662606));
#43240=CARTESIAN_POINT('Ctrl Pts',(73.8655835469356,146.774023878113,46.4401392784498));
#43241=CARTESIAN_POINT('Ctrl Pts',(79.9246904329767,146.137555849456,48.5269450617855));
#43242=CARTESIAN_POINT('Ctrl Pts',(81.434970490104,145.501087820799,54.7421648959878));
#43243=CARTESIAN_POINT('Ctrl Pts',(77.0303108800882,144.864619792142,59.3799312935453));
#43244=CARTESIAN_POINT('Ctrl Pts',(70.7367111994093,144.228151763485,58.1723975701266));
#43245=CARTESIAN_POINT('Ctrl Pts',(68.764577662108,143.697761739604,53.2268076312774));
#43246=CARTESIAN_POINT('Ctrl Pts',(70.206850777246,143.273449720499,49.6225384754308));
#43247=CARTESIAN_POINT('Ctrl Pts',(73.1381064817095,142.849137701395,47.0772196581726));
#43248=CARTESIAN_POINT('Ctrl Pts',(78.4570069957002,142.318747677514,47.3169441968919));
#43249=CARTESIAN_POINT('Ctrl Pts',(81.6632403479369,141.682279648857,52.8656019016743));
#43250=CARTESIAN_POINT('Ctrl Pts',(78.7280054750341,141.0458116202,58.5484092782544));
#43251=CARTESIAN_POINT('Ctrl Pts',(72.3613866346612,140.409343591543,59.1616530958568));
#43252=CARTESIAN_POINT('Ctrl Pts',(68.4015487075305,139.772875562886,54.1230800612873));
#43253=CARTESIAN_POINT('Ctrl Pts',(70.1555537992788,139.242485539006,49.0959897825756));
#43254=CARTESIAN_POINT('Ctrl Pts',(73.6078856957486,138.818173519901,47.320514532662));
#43255=CARTESIAN_POINT('Ctrl Pts',(77.490012397573,138.393861500796,47.3209112928323));
#43256=CARTESIAN_POINT('Ctrl Pts',(81.3485743749271,137.863471476916,50.9896535840151));
#43257=CARTESIAN_POINT('Ctrl Pts',(80.1308631311827,137.227003448258,57.2812920002539));
#43258=CARTESIAN_POINT('Ctrl Pts',(74.1883937223739,136.590535419602,59.6470816704889));
#43259=CARTESIAN_POINT('Ctrl Pts',(68.9794920835046,135.954067390944,55.9353102396218));
#43260=CARTESIAN_POINT('Ctrl Pts',(69.2937571436266,135.317599362288,49.534624955543));
#43261=CARTESIAN_POINT('Ctrl Pts',(73.9144292228386,134.787209338407,46.8893347883613));
#43262=CARTESIAN_POINT('Ctrl Pts',(77.6851592684559,134.362897319302,47.8126455754286));
#43263=CARTESIAN_POINT('Ctrl Pts',(80.6158946395786,133.938585300198,50.3585634984749));
#43264=CARTESIAN_POINT('Ctrl Pts',(81.1234025901064,133.408195276317,55.6586206880105));
#43265=CARTESIAN_POINT('Ctrl Pts',(76.0784316098281,132.77172724766,59.6103041826723));
#43266=CARTESIAN_POINT('Ctrl Pts',(70.0405686636907,132.135259219003,57.4998268712375));
#43267=CARTESIAN_POINT('Ctrl Pts',(68.5417731922881,131.498791190346,51.2818275488413));
#43268=CARTESIAN_POINT('Ctrl Pts',(72.9761497214014,130.862323161689,46.6553991821764));
#43269=CARTESIAN_POINT('Ctrl Pts',(78.1993353737933,130.331933137808,47.6881151028675));
#43270=CARTESIAN_POINT('Ctrl Pts',(80.4407861829379,129.907621118704,50.8577848264537));
#43271=CARTESIAN_POINT('Ctrl Pts',(80.9840546085708,129.483309099599,54.7017108538572));
#43272=CARTESIAN_POINT('Ctrl Pts',(77.8918269900061,128.952919075718,59.0360272806059));
#43273=CARTESIAN_POINT('Ctrl Pts',(71.4916583615966,128.316451047061,58.7114103344188));
#43274=CARTESIAN_POINT('Ctrl Pts',(68.3169862074485,127.679983018404,53.1588109294466));
#43275=CARTESIAN_POINT('Ctrl Pts',(71.2627145002853,127.043514989747,47.4814358085654));
#43276=CARTESIAN_POINT('Ctrl Pts',(77.644334875132,126.40704696109,46.8962383844676));
#43277=CARTESIAN_POINT('Ctrl Pts',(80.9106458936276,125.87665693721,51.1009242065776));
#43278=CARTESIAN_POINT('Ctrl Pts',(80.5244948813005,125.452344918105,54.9637981732141));
#43279=CARTESIAN_POINT('Ctrl Pts',(78.414091999895,125.028032899,58.2221885065829));
#43280=CARTESIAN_POINT('Ctrl Pts',(73.2373364704086,124.49764287512,59.4669265192302));
#43281=CARTESIAN_POINT('Ctrl Pts',(68.6180861968185,123.861174846463,55.0250731286094));
#43282=CARTESIAN_POINT('Ctrl Pts',(69.8622107451905,123.224706817806,48.7511542937376));
#43283=CARTESIAN_POINT('Ctrl Pts',(75.8090405776548,122.588238789149,46.3963467894746));
#43284=CARTESIAN_POINT('Ctrl Pts',(81.0108775362534,121.951770760492,50.1391300973867));
#43285=CARTESIAN_POINT('Ctrl Pts',(80.7198044889218,121.421380736611,55.4554678418605));
#43286=CARTESIAN_POINT('Ctrl Pts',(77.8952676648289,120.997068717506,58.1187176641229));
#43287=CARTESIAN_POINT('Ctrl Pts',(74.1653018934157,120.572756698402,59.1949440485428));
#43288=CARTESIAN_POINT('Ctrl Pts',(69.4406556577397,120.042366674521,56.7401755299422));
#43289=CARTESIAN_POINT('Ctrl Pts',(68.8657804610841,119.405898645864,50.3576170192741));
#43290=CARTESIAN_POINT('Ctrl Pts',(73.9190741955237,118.769430617207,46.4366317002641));
#43291=CARTESIAN_POINT('Ctrl Pts',(79.9530279387085,118.13296258855,48.5582597693486));
#43292=CARTESIAN_POINT('Ctrl Pts',(81.4261542452689,117.496494559893,54.7950404708605));
#43293=CARTESIAN_POINT('Ctrl Pts',(77.7203244431643,116.966104536013,58.6179969197401));
#43294=CARTESIAN_POINT('Ctrl Pts',(73.841439580255,116.541792516908,58.7766162966422));
#43295=CARTESIAN_POINT('Ctrl Pts',(70.3196135975197,116.117480497803,57.1433221915374));
#43296=CARTESIAN_POINT('Ctrl Pts',(68.3621779488011,115.587090473922,52.1918965167118));
#43297=CARTESIAN_POINT('Ctrl Pts',(72.1133696732489,114.950622445266,46.9961198394222));
#43298=CARTESIAN_POINT('Ctrl Pts',(78.4996923124141,114.314154416609,47.3493712893946));
#43299=CARTESIAN_POINT('Ctrl Pts',(81.6641011668332,113.677686387952,52.9078261142979));
#43300=CARTESIAN_POINT('Ctrl Pts',(78.6866772492128,113.041218359294,58.5825491426592));
#43301=CARTESIAN_POINT('Ctrl Pts',(73.3819666201983,112.510828335414,59.0388557003805));
#43302=CARTESIAN_POINT('Ctrl Pts',(70.3494075285618,112.086516316309,56.6151203100856));
#43303=CARTESIAN_POINT('Ctrl Pts',(68.7614344313501,111.662204297205,53.0726283441146));
#43304=CARTESIAN_POINT('Ctrl Pts',(70.5303630449218,111.131814273324,48.0507699139827));
#43305=CARTESIAN_POINT('Ctrl Pts',(76.7695181841129,110.495346244667,46.587732736418));
#43306=CARTESIAN_POINT('Ctrl Pts',(81.359538331985,109.85887821601,51.0421259027817));
#43307=CARTESIAN_POINT('Ctrl Pts',(80.1038254574957,109.222410187353,57.3137356335653));
#43308=CARTESIAN_POINT('Ctrl Pts',(74.1348045617336,108.585942158696,59.6457571128379));
#43309=CARTESIAN_POINT('Ctrl Pts',(69.8305489765598,108.055552134815,56.5118211866107));
#43310=CARTESIAN_POINT('Ctrl Pts',(69.1302854250172,107.631240115711,52.6933740094433));
#43311=CARTESIAN_POINT('Ctrl Pts',(70.2542803117838,107.206928096606,48.9775237190036));
#43312=CARTESIAN_POINT('Ctrl Pts',(74.8827889425443,106.676538072725,46.3459693518712));
#43313=CARTESIAN_POINT('Ctrl Pts',(80.5526889428833,106.040070044068,49.3325675203539));
#43314=CARTESIAN_POINT('Ctrl Pts',(81.0972727913765,105.403602015411,55.7054265232176));
#43315=CARTESIAN_POINT('Ctrl Pts',(76.0367440446578,104.767133986754,59.6170696871648));
#43316=CARTESIAN_POINT('Ctrl Pts',(70.0009775363973,104.130665958098,57.4636869316869));
#43317=CARTESIAN_POINT('Ctrl Pts',(68.8062846772482,103.600275934217,52.2751534679328));
#43318=CARTESIAN_POINT('Ctrl Pts',(70.781449457728,103.175963915112,48.9330535328036));
#43319=CARTESIAN_POINT('Ctrl Pts',(74.0666489726483,102.751651896007,46.8646309372967));
#43320=CARTESIAN_POINT('Ctrl Pts',(79.2867442551898,102.221261872127,47.912855995854));
#43321=CARTESIAN_POINT('Ctrl Pts',(81.6091085496205,101.58479384347,53.8856408335813));
#43322=CARTESIAN_POINT('Ctrl Pts',(77.8414071731253,100.948325814813,59.0542315289232));
#43323=CARTESIAN_POINT('Ctrl Pts',(71.4557480292651,100.311857786156,58.689182577611));
#43324=CARTESIAN_POINT('Ctrl Pts',(68.3107929723319,99.6753897574989,53.1055643668355));
#43325=CARTESIAN_POINT('Ctrl Pts',(70.811068570169,99.144999733618,48.404841819497));
#43326=CARTESIAN_POINT('Ctrl Pts',(74.4938206403223,98.7206877145134,47.176735522705));
#43327=CARTESIAN_POINT('Ctrl Pts',(78.330459889719,98.2963756954088,47.7692784801554));
#43328=CARTESIAN_POINT('Ctrl Pts',(81.5842679143076,97.765985671528,51.9836472195184));
#43329=CARTESIAN_POINT('Ctrl Pts',(79.4211258880999,97.129517642871,58.0159230096566));
#43330=CARTESIAN_POINT('Ctrl Pts',(73.1873326085736,96.4930496142142,59.4476090040522));
#43331=CARTESIAN_POINT('Ctrl Pts',(68.6055493474303,95.8565815855572,54.9847438272487));
#43332=CARTESIAN_POINT('Ctrl Pts',(69.8924501197539,95.2201135569002,48.7068922014112));
#43333=CARTESIAN_POINT('Ctrl Pts',(74.8625460934215,94.6897235330196,46.7973591315942));
#43334=CARTESIAN_POINT('Ctrl Pts',(78.4483177343854,94.2654115139148,48.2850249627864));
#43335=CARTESIAN_POINT('Ctrl Pts',(80.9564234790893,93.8410994948103,51.2481843341032));
#43336=CARTESIAN_POINT('Ctrl Pts',(80.6495613460078,93.3107094709293,56.5636340952688));
#43337=CARTESIAN_POINT('Ctrl Pts',(75.0608638721642,92.6742414422724,59.6995542440752));
#43338=CARTESIAN_POINT('Ctrl Pts',(69.4155699040053,92.0377734136156,56.6928019344417));
#43339=CARTESIAN_POINT('Ctrl Pts',(68.8827602162151,91.4013053849584,50.3189477413327));
#43340=CARTESIAN_POINT('Ctrl Pts',(73.9709287285413,90.7648373563017,46.423042734276));
#43341=CARTESIAN_POINT('Ctrl Pts',(78.9754721333284,90.2344473324207,48.2403803038539));
#43342=CARTESIAN_POINT('Ctrl Pts',(80.7072165422673,89.8101353133163,51.7148542479994));
#43343=CARTESIAN_POINT('Ctrl Pts',(80.6578038883262,89.3858232942115,55.596666489217));
#43344=CARTESIAN_POINT('Ctrl Pts',(76.9406356429825,88.8554332703309,59.4085991706795));
#43345=CARTESIAN_POINT('Ctrl Pts',(70.6648736271285,88.2189652416738,58.1115464523212));
#43346=CARTESIAN_POINT('Ctrl Pts',(68.3743024533118,87.5824972130169,52.1396801497238));
#43347=CARTESIAN_POINT('Ctrl Pts',(72.1515458643403,86.9460291843599,46.9780587327407));
#43348=CARTESIAN_POINT('Ctrl Pts',(78.5477530123006,86.3095611557031,47.3731141139413));
#43349=CARTESIAN_POINT('Ctrl Pts',(81.1344914826134,85.7791711318223,52.0268174369308));
#43350=CARTESIAN_POINT('Ctrl Pts',(80.1636448686008,85.3548591127175,55.78558914302));
#43351=CARTESIAN_POINT('Ctrl Pts',(77.580926274119,84.9305470936132,58.683946013413));
#43352=CARTESIAN_POINT('Ctrl Pts',(72.2748837406891,84.4001570697319,59.1244947231283));
#43353=CARTESIAN_POINT('Ctrl Pts',(68.3872132968793,83.7636890410755,54.030031733356));
#43354=CARTESIAN_POINT('Ctrl Pts',(70.5737567372417,83.1272210124182,48.0192970676245));
#43355=CARTESIAN_POINT('Ctrl Pts',(76.8101842784523,82.4907529837615,46.5991298374534));
#43356=CARTESIAN_POINT('Ctrl Pts',(81.3802552051738,81.8542849551044,51.0915664100236));
#43357=CARTESIAN_POINT('Ctrl Pts',(80.2816734014653,81.3238949312238,56.3012965904414));
#43358=CARTESIAN_POINT('Ctrl Pts',(77.0839556680519,80.8995829121189,58.5025483215824));
#43359=CARTESIAN_POINT('Ctrl Pts',(73.2334767124565,80.4752708930145,58.9972398405646));
#43360=CARTESIAN_POINT('Ctrl Pts',(68.9385484018002,79.9448808691335,55.8505334134376));
#43361=CARTESIAN_POINT('Ctrl Pts',(69.3439483205791,79.3084128404767,49.4549735833925));
#43362=CARTESIAN_POINT('Ctrl Pts',(74.9361886871511,78.6719448118197,46.3506618849799));
#43363=CARTESIAN_POINT('Ctrl Pts',(80.5759183421823,78.0354767831628,49.3678381901666));
#43364=CARTESIAN_POINT('Ctrl Pts',(81.0804944619725,77.3990087545058,55.7563386067879));
#43365=CARTESIAN_POINT('Ctrl Pts',(76.8349031968461,76.8686187306251,58.969300688992));
#43366=CARTESIAN_POINT('Ctrl Pts',(72.9772127085787,76.4443067115204,58.5344076180339));
#43367=CARTESIAN_POINT('Ctrl Pts',(69.7457281592464,76.0199946924158,56.3830323616302));
#43368=CARTESIAN_POINT('Ctrl Pts',(68.5664513403961,75.489604668535,51.1909733561184));
#43369=CARTESIAN_POINT('Ctrl Pts',(73.0662735475183,74.853136639878,46.6281743535191));
#43370=CARTESIAN_POINT('Ctrl Pts',(79.323983898762,74.2166686112211,47.9514145427363));
#43371=CARTESIAN_POINT('Ctrl Pts',(81.6035187270877,73.5802005825642,53.9275022600366));
#43372=CARTESIAN_POINT('Ctrl Pts',(77.7953551100307,72.9437325539072,59.0816680023808));
#43373=CARTESIAN_POINT('Ctrl Pts',(72.4831162429305,72.4133425300264,58.7234938114221));
#43374=CARTESIAN_POINT('Ctrl Pts',(69.8557414558012,71.9890305109219,55.8655558109758));
#43375=CARTESIAN_POINT('Ctrl Pts',(68.8266955931637,71.5647184918171,52.1222988736249));
#43376=CARTESIAN_POINT('Ctrl Pts',(71.340922056943,71.0343284679364,47.4290232775165));
#43377=CARTESIAN_POINT('Ctrl Pts',(77.7302302056465,70.3978604392794,46.9347804073151));
#43378=CARTESIAN_POINT('Ctrl Pts',(81.5870998373005,69.7613924106225,52.0371778911306));
#43379=CARTESIAN_POINT('Ctrl Pts',(79.3894558859262,69.1249243819656,58.0438628754964));
#43380=CARTESIAN_POINT('Ctrl Pts',(73.1345725628523,68.4884563533086,59.4381258523295));
#43381=CARTESIAN_POINT('Ctrl Pts',(69.3587108404486,67.9580663294278,55.6843226095527));
#43382=CARTESIAN_POINT('Ctrl Pts',(69.249079101151,67.5337543103232,51.8037442031582));
#43383=CARTESIAN_POINT('Ctrl Pts',(70.9267097640773,67.1094422912186,48.3028210041651));
#43384=CARTESIAN_POINT('Ctrl Pts',(75.9024554322703,66.5790522673377,46.4080583336293));
#43385=CARTESIAN_POINT('Ctrl Pts',(81.050455211294,65.9425842386809,50.2245531795589));
#43386=CARTESIAN_POINT('Ctrl Pts',(80.6165978913874,65.3061162100238,56.6059065833737));
#43387=CARTESIAN_POINT('Ctrl Pts',(75.0186321565642,64.669648181367,59.6998818693395));
#43388=CARTESIAN_POINT('Ctrl Pts',(69.3819545731897,64.0331801527098,56.6510459513343));
#43389=CARTESIAN_POINT('Ctrl Pts',(68.9926619294876,63.5027901288293,51.3409968207));
#43390=CARTESIAN_POINT('Ctrl Pts',(71.4544933619757,63.0784781097245,48.3392816635851));
#43391=CARTESIAN_POINT('Ctrl Pts',(75.0167527772727,62.65416609062,46.7961628267598));
#43392=CARTESIAN_POINT('Ctrl Pts',(80.0158763253887,62.1237760667393,48.6283566709993));
#43393=CARTESIAN_POINT('Ctrl Pts',(81.4000209976796,61.4873080380821,54.8854868566357));
#43394=CARTESIAN_POINT('Ctrl Pts',(76.8880290754071,60.8508400094253,59.418899735667));
#43395=CARTESIAN_POINT('Ctrl Pts',(70.6327739589726,60.2143719807683,58.0841012989217));
#43396=CARTESIAN_POINT('Ctrl Pts',(68.3763035247955,59.5779039521114,52.0861119846998));
#43397=CARTESIAN_POINT('Ctrl Pts',(71.5643353852583,59.0475139282306,47.82176873059));
#43398=CARTESIAN_POINT('Ctrl Pts',(75.3913197498731,58.623201909126,47.1697729028191));
#43399=CARTESIAN_POINT('Ctrl Pts',(79.0926822278916,58.1988898900212,48.3405947051246));
#43400=CARTESIAN_POINT('Ctrl Pts',(81.6655870483687,57.6684998661406,53.0019605261004));
#43401=CARTESIAN_POINT('Ctrl Pts',(78.6076385065898,57.0320318374835,58.6336996313561));
#43402=CARTESIAN_POINT('Ctrl Pts',(72.2284115525991,56.3955638088267,59.0977760344396));
#43403=CARTESIAN_POINT('Ctrl Pts',(68.3809746809543,55.7590957801697,53.9882620695771));
#43404=CARTESIAN_POINT('Ctrl Pts',(70.610393675563,55.1226277515128,47.9801654008882));
#43405=CARTESIAN_POINT('Ctrl Pts',(75.8135978038988,54.592237727632,46.8510784551353));
#43406=CARTESIAN_POINT('Ctrl Pts',(79.1304928053609,54.1679257085273,48.8682833122854));
#43407=CARTESIAN_POINT('Ctrl Pts',(81.1572714303364,53.7436136894227,52.1793369650948));
#43408=CARTESIAN_POINT('Ctrl Pts',(80.0432207441853,53.2132236655419,57.3857812028527));
#43409=CARTESIAN_POINT('Ctrl Pts',(74.0415897201263,52.576755636885,59.6325476982599));
#43410=CARTESIAN_POINT('Ctrl Pts',(68.9209822076985,51.9402876082281,55.7998877678607));
#43411=CARTESIAN_POINT('Ctrl Pts',(69.366627711221,51.303819579571,49.4193467623025));
#43412=CARTESIAN_POINT('Ctrl Pts',(74.9895092014814,50.6673515509142,46.3451414372926));
#43413=CARTESIAN_POINT('Ctrl Pts',(79.6582884415991,50.1369615270333,48.9045692911776));
#43414=CARTESIAN_POINT('Ctrl Pts',(80.8397982325435,49.7126495079288,52.6025339341049));
#43415=CARTESIAN_POINT('Ctrl Pts',(80.1988609091723,49.2883374888241,56.4313858813532));
#43416=CARTESIAN_POINT('Ctrl Pts',(75.94374536206,48.7579474649434,59.6317237092895));
#43417=CARTESIAN_POINT('Ctrl Pts',(69.9392623542817,48.1214794362863,57.3925902958604));
#43418=CARTESIAN_POINT('Ctrl Pts',(68.586398666995,47.4850114076294,51.1412173840883));
#43419=CARTESIAN_POINT('Ctrl Pts',(73.1067579250465,46.8485433789726,46.6161477032359));
#43420=CARTESIAN_POINT('Ctrl Pts',(79.3678606590281,46.2120753503155,47.9822103622522));
#43421=CARTESIAN_POINT('Ctrl Pts',(81.2144888369357,45.6816853264348,52.9760200206947));
#43422=CARTESIAN_POINT('Ctrl Pts',(79.6816674585669,45.2573733073301,56.5427224905476));
#43423=CARTESIAN_POINT('Ctrl Pts',(76.6870768176045,44.8330612882254,59.0132153117264));
#43424=CARTESIAN_POINT('Ctrl Pts',(71.3759252168139,44.3026712643447,58.6392645053152));
#43425=CARTESIAN_POINT('Ctrl Pts',(68.3108182107715,43.6662032356877,53.011418232064));
#43426=CARTESIAN_POINT('Ctrl Pts',(71.38860861019,43.0297352070309,47.4045376647909));
#43427=CARTESIAN_POINT('Ctrl Pts',(77.7686820139573,42.3932671783739,46.9522470491929));
#43428=CARTESIAN_POINT('Ctrl Pts',(81.6000330021679,41.7567991497169,52.0891998656953));
#43429=CARTESIAN_POINT('Ctrl Pts',(79.7196526810578,41.2264091258361,57.0703985547842));
#43430=CARTESIAN_POINT('Ctrl Pts',(76.2235906019975,40.8020971067315,58.7581360420116));
#43431=CARTESIAN_POINT('Ctrl Pts',(72.3427116734402,40.3777850876269,58.6597153718375));
#43432=CARTESIAN_POINT('Ctrl Pts',(68.5780159994796,39.8473950637461,54.8947137762651));
#43433=CARTESIAN_POINT('Ctrl Pts',(69.9542034117819,39.2109270350892,48.6358286646777));
#43434=CARTESIAN_POINT('Ctrl Pts',(75.9545145524023,38.5744590064322,46.4208411581293));
#43435=CARTESIAN_POINT('Ctrl Pts',(81.0680328638006,37.9379909777753,50.2629543679937));
#43436=CARTESIAN_POINT('Ctrl Pts',(80.5922501426276,37.3015229491183,56.6536636741718));
#43437=CARTESIAN_POINT('Ctrl Pts',(75.9062574854849,36.7711329252376,59.1814380607402));
#43438=CARTESIAN_POINT('Ctrl Pts',(72.1600433554254,36.3468209061329,58.1632103955392));
#43439=CARTESIAN_POINT('Ctrl Pts',(69.2945270519295,35.9225088870284,55.5441028756294));
#43440=CARTESIAN_POINT('Ctrl Pts',(68.9210078168386,35.3921188631475,50.232920906129));
#43441=CARTESIAN_POINT('Ctrl Pts',(74.06415063904,34.7556508344905,46.4098832991481));
#43442=CARTESIAN_POINT('Ctrl Pts',(80.046798772065,34.1191828058336,48.6721442820747));
#43443=CARTESIAN_POINT('Ctrl Pts',(81.3881113529965,33.4827147771767,54.9260058090179));
#43444=CARTESIAN_POINT('Ctrl Pts',(76.8383309368684,32.8462467485197,59.4389907192186));
#43445=CARTESIAN_POINT('Ctrl Pts',(71.6428867818201,32.315856724639,58.2747181720951));
#43446=CARTESIAN_POINT('Ctrl Pts',(69.4821850598707,31.8915447055342,55.0494622203846));
#43447=CARTESIAN_POINT('Ctrl Pts',(69.0361493130766,31.4672326864297,51.1930441929765));
#43448=CARTESIAN_POINT('Ctrl Pts',(72.23683288965,30.9368426625488,46.9381887117852));
#43449=CARTESIAN_POINT('Ctrl Pts',(78.6267643192226,30.300374633892,47.4243069712248));
#43450=CARTESIAN_POINT('Ctrl Pts',(81.6602206610601,29.663906605235,53.0552967678677));
#43451=CARTESIAN_POINT('Ctrl Pts',(78.5720773534861,29.0274385765781,58.656481846159));
#43452=CARTESIAN_POINT('Ctrl Pts',(72.1777153698012,28.390970547921,59.0803562311091));
#43453=CARTESIAN_POINT('Ctrl Pts',(69.0186144497526,27.8605805240404,54.7945363502979));
#43454=CARTESIAN_POINT('Ctrl Pts',(69.5021802408798,27.4362685049357,50.9426443760508));
#43455=CARTESIAN_POINT('Ctrl Pts',(71.6941849048853,27.0119564858311,47.7385807280143));
#43456=CARTESIAN_POINT('Ctrl Pts',(76.9007196229027,26.4815664619503,46.6249532342245));
#43457=CARTESIAN_POINT('Ctrl Pts',(81.4063399869758,25.8450984332934,51.1820266495584));
#43458=CARTESIAN_POINT('Ctrl Pts',(80.0041950242122,25.2086304046363,57.4225313004325));
#43459=CARTESIAN_POINT('Ctrl Pts',(73.9998023159127,24.5721623759795,59.6264292760001));
#43460=CARTESIAN_POINT('Ctrl Pts',(68.8941291625674,23.9356943473224,55.7534939551535));
#43461=CARTESIAN_POINT('Ctrl Pts',(69.3193479845805,23.4053043234418,50.4461981309576));
#43462=CARTESIAN_POINT('Ctrl Pts',(72.2102306645205,22.980992304337,47.855121298611));
#43463=CARTESIAN_POINT('Ctrl Pts',(75.9661837218133,22.5566802852325,46.8734120501945));
#43464=CARTESIAN_POINT('Ctrl Pts',(80.6273366580689,22.0262902613516,49.4467132607705));
#43465=CARTESIAN_POINT('Ctrl Pts',(81.0408753299635,21.3898222326947,55.8417203460487));
#43466=CARTESIAN_POINT('Ctrl Pts',(75.890175270785,20.7533542040378,59.633916297922));
#43467=CARTESIAN_POINT('Ctrl Pts',(69.9117395951546,20.1168861753808,57.3605004391449));
#43468=CARTESIAN_POINT('Ctrl Pts',(68.5965174256227,19.4804181467239,51.0887193976995));
#43469=CARTESIAN_POINT('Ctrl Pts',(72.3977774992468,18.9500281228431,47.3601749200438));
#43470=CARTESIAN_POINT('Ctrl Pts',(76.2793092635613,18.5257161037384,47.3001117920513));
#43471=CARTESIAN_POINT('Ctrl Pts',(79.7590102216015,18.1014040846339,49.0207049813434));
#43472=CARTESIAN_POINT('Ctrl Pts',(81.5902691230174,17.571014060753,54.0224279611908));
#43473=CARTESIAN_POINT('Ctrl Pts',(77.7100437690878,16.9345460320961,59.1173659193523));
#43474=CARTESIAN_POINT('Ctrl Pts',(71.3329561213306,16.2980780034392,58.6109033270751));
#43475=CARTESIAN_POINT('Ctrl Pts',(68.3132228555609,15.6616099747823,52.9593291895844));
#43476=CARTESIAN_POINT('Ctrl Pts',(70.9069467681505,15.1312199509014,48.3199922132729));
#43477=CARTESIAN_POINT('Ctrl Pts',(74.6274753532391,14.7069079317968,47.1607194514));
#43478=CARTESIAN_POINT('Ctrl Pts',(76.5255413238862,14.4947519222445,47.5119870517647));
#43479=CARTESIAN_POINT('Ctrl Pts',(77.3774496940034,14.3886739174683,47.9101420920371));
#43480=CARTESIAN_POINT('',(70.0990315389018,416.,55.8419543693127));
#43481=CARTESIAN_POINT('Ctrl Pts',(70.0990315389037,416.,55.841954369316));
#43482=CARTESIAN_POINT('Ctrl Pts',(69.6292862985721,415.893921995224,55.0273288624995));
#43483=CARTESIAN_POINT('Ctrl Pts',(69.1165406058533,415.681765985672,53.1663787797211));
#43484=CARTESIAN_POINT('Ctrl Pts',(69.9524819678234,415.257453966567,49.3601406988557));
#43485=CARTESIAN_POINT('Ctrl Pts',(74.352298526842,414.727063942686,46.3781169629522));
#43486=CARTESIAN_POINT('Ctrl Pts',(79.5853747435743,414.161555332607,48.6206713789087));
#43487=CARTESIAN_POINT('Ctrl Pts',(80.618334511065,413.808202732081,51.7724009204073));
#43488=CARTESIAN_POINT('Ctrl Pts',(80.6269259201534,413.667006141107,53.0266694084182));
#43489=CARTESIAN_POINT('Ctrl Pts',(67.799287262509,416.,49.6622531841046));
#43490=CARTESIAN_POINT('Ctrl Pts',(67.7727972152803,416.,49.8439307127705));
#43491=CARTESIAN_POINT('Ctrl Pts',(67.7532000446317,416.,50.0264066333373));
#43492=CARTESIAN_POINT('Ctrl Pts',(67.7404788167283,416.,50.2092880641438));
#43493=CARTESIAN_POINT('Ctrl Pts',(67.7278723972532,416.,50.3905189994324));
#43494=CARTESIAN_POINT('Ctrl Pts',(67.7220188772554,416.,50.5721488441017));
#43495=CARTESIAN_POINT('Ctrl Pts',(67.7229416225055,416.,50.753763833248));
#43496=CARTESIAN_POINT('Ctrl Pts',(67.7238504120265,416.,50.9326320517298));
#43497=CARTESIAN_POINT('Ctrl Pts',(67.7313325809072,416.,51.1114863999918));
#43498=CARTESIAN_POINT('Ctrl Pts',(67.7454415376628,416.,51.2898920110631));
#43499=CARTESIAN_POINT('Ctrl Pts',(67.7591628710778,416.,51.463396183982));
#43500=CARTESIAN_POINT('Ctrl Pts',(67.7791524196438,416.,51.6364762550094));
#43501=CARTESIAN_POINT('Ctrl Pts',(67.805480958599,416.,51.808688414873));
#43502=CARTESIAN_POINT('Ctrl Pts',(67.8234105205741,416.,51.9259637638168));
#43503=CARTESIAN_POINT('Ctrl Pts',(67.8442802475463,416.,52.0428357113456));
#43504=CARTESIAN_POINT('Ctrl Pts',(67.8681165251726,416.,52.1591508831993));
#43505=CARTESIAN_POINT('Ctrl Pts',(67.8875438715047,416.,52.2539515547932));
#43506=CARTESIAN_POINT('Ctrl Pts',(67.9089419096746,416.,52.3483821840596));
#43507=CARTESIAN_POINT('Ctrl Pts',(67.9323259532379,416.,52.442353961058));
#43508=CARTESIAN_POINT('Ctrl Pts',(67.9395750602858,416.,52.4714854270979));
#43509=CARTESIAN_POINT('Ctrl Pts',(67.9470155216451,416.,52.5005743522527));
#43510=CARTESIAN_POINT('Ctrl Pts',(67.9546422512565,416.,52.5295976798077));
#43511=CARTESIAN_POINT('Ctrl Pts',(67.9964865806882,416.,52.688835222149));
#43512=CARTESIAN_POINT('Ctrl Pts',(68.0439703007979,416.,52.8462431417993));
#43513=CARTESIAN_POINT('Ctrl Pts',(68.0971152503823,416.,53.0014558004715));
#43514=CARTESIAN_POINT('Ctrl Pts',(68.1180500535734,416.,53.0625970093256));
#43515=CARTESIAN_POINT('Ctrl Pts',(68.1398635694756,416.,53.1233970689567));
#43516=CARTESIAN_POINT('Ctrl Pts',(68.1625579867857,416.,53.1838315598754));
#43517=CARTESIAN_POINT('Ctrl Pts',(68.2193464906623,416.,53.3350574880378));
#43518=CARTESIAN_POINT('Ctrl Pts',(68.2816503057749,416.,53.4839978932803));
#43519=CARTESIAN_POINT('Ctrl Pts',(68.349429310753,416.,53.630304289414));
#43520=CARTESIAN_POINT('Ctrl Pts',(68.416111980046,416.,53.7742441574007));
#43521=CARTESIAN_POINT('Ctrl Pts',(68.48809477141,416.,53.9156346722019));
#43522=CARTESIAN_POINT('Ctrl Pts',(68.5653421937902,416.,54.0540943533638));
#43523=CARTESIAN_POINT('Ctrl Pts',(68.6136238378459,416.,54.1406352480104));
#43524=CARTESIAN_POINT('Ctrl Pts',(68.6639621726723,416.,54.2260301943717));
#43525=CARTESIAN_POINT('Ctrl Pts',(68.7163474154008,416.,54.3101756515064));
#43526=CARTESIAN_POINT('Ctrl Pts',(68.7407921608684,416.,54.3494407989942));
#43527=CARTESIAN_POINT('Ctrl Pts',(68.7656825950477,416.,54.3884337573348));
#43528=CARTESIAN_POINT('Ctrl Pts',(68.7910175880391,416.,54.4271433901568));
#43529=CARTESIAN_POINT('Ctrl Pts',(68.8059692190121,416.,54.4499881624151));
#43530=CARTESIAN_POINT('Ctrl Pts',(68.8210705916636,416.,54.4727264570017));
#43531=CARTESIAN_POINT('Ctrl Pts',(68.8363201371293,416.,54.4953546820925));
#43532=CARTESIAN_POINT('Ctrl Pts',(68.9295715007333,416.,54.6337268618015));
#43533=CARTESIAN_POINT('Ctrl Pts',(69.0283775975531,416.,54.768007608802));
#43534=CARTESIAN_POINT('Ctrl Pts',(69.1326128816522,416.,54.8977087194485));
#43535=CARTESIAN_POINT('Ctrl Pts',(69.2033921426718,416.,54.9857801325435));
#43536=CARTESIAN_POINT('Ctrl Pts',(69.2766745528862,416.,55.0717387231204));
#43537=CARTESIAN_POINT('Ctrl Pts',(69.3524152746615,416.,55.1554160240979));
#43538=CARTESIAN_POINT('Ctrl Pts',(69.4007152851134,416.,55.2087772070529));
#43539=CARTESIAN_POINT('Ctrl Pts',(69.4500142507147,416.,55.2612100391359));
#43540=CARTESIAN_POINT('Ctrl Pts',(69.5003120398134,416.,55.312680490538));
#43541=CARTESIAN_POINT('Ctrl Pts',(69.5475874334726,416.,55.3610580811928));
#43542=CARTESIAN_POINT('Ctrl Pts',(69.5957454872076,416.,55.4085849866432));
#43543=CARTESIAN_POINT('Ctrl Pts',(69.6447558924706,416.,55.4552025719907));
#43544=CARTESIAN_POINT('Ctrl Pts',(69.7553610612021,416.,55.5604076986479));
#43545=CARTESIAN_POINT('Ctrl Pts',(69.8703283582921,416.,55.6610034002696));
#43546=CARTESIAN_POINT('Ctrl Pts',(69.9894762648668,416.,55.7564943579827));
#43547=CARTESIAN_POINT('Ctrl Pts',(70.0256123701293,416.,55.7854555995079));
#43548=CARTESIAN_POINT('Ctrl Pts',(70.0621327420081,416.,55.8139470646645));
#43549=CARTESIAN_POINT('Ctrl Pts',(70.0990315389037,416.,55.841954369316));
#43550=CARTESIAN_POINT('Origin',(74.9879498948689,423.667006141107,53.0228109606356));
#43551=CARTESIAN_POINT('',(79.8830110631917,416.,55.8460953909508));
#43552=CARTESIAN_POINT('Ctrl Pts',(79.8830110631917,416.,55.8460953909508));
#43553=CARTESIAN_POINT('Ctrl Pts',(79.8459760618144,415.991619351292,55.9103951483955));
#43554=CARTESIAN_POINT('Ctrl Pts',(78.8362070251561,415.771082693031,57.5815756537791));
#43555=CARTESIAN_POINT('Ctrl Pts',(75.0514316659349,415.338390025218,59.6975379999433));
#43556=CARTESIAN_POINT('Ctrl Pts',(69.3998575284373,414.701921996561,56.6778047341864));
#43557=CARTESIAN_POINT('Ctrl Pts',(68.8933949361463,414.065453967904,50.30071708643));
#43558=CARTESIAN_POINT('Ctrl Pts',(73.9883328942991,413.428985939247,46.4204917324893));
#43559=CARTESIAN_POINT('Ctrl Pts',(78.9900558741506,412.898595915367,48.2517506338942));
#43560=CARTESIAN_POINT('Ctrl Pts',(80.4714786825846,412.533265221915,51.2477571262032));
#43561=CARTESIAN_POINT('Ctrl Pts',(80.6285029194401,412.380090538016,52.6086444510753));
#43562=CARTESIAN_POINT('Ctrl Pts',(80.6310716108719,412.332993858894,53.0264521482468));
#43563=CARTESIAN_POINT('Origin',(74.9879498948689,416.,53.0228109606356));
#43564=CARTESIAN_POINT('Origin',(74.9879498948689,455.,53.0228109606356));
#43565=CARTESIAN_POINT('Ctrl Pts',(78.8686068361685,455.,50.1705810192551));
#43566=CARTESIAN_POINT('Ctrl Pts',(78.7971362865198,455.,50.0496527591843));
#43567=CARTESIAN_POINT('Ctrl Pts',(78.7205501200313,455.,49.9320764112506));
#43568=CARTESIAN_POINT('Ctrl Pts',(78.6391280567385,455.,49.8181536474318));
#43569=CARTESIAN_POINT('Ctrl Pts',(78.5567895823215,455.,49.7029486747886));
#43570=CARTESIAN_POINT('Ctrl Pts',(78.4695055308971,455.,49.5914792507712));
#43571=CARTESIAN_POINT('Ctrl Pts',(78.3775130294169,455.,49.4840669138619));
#43572=CARTESIAN_POINT('Ctrl Pts',(78.3375958441137,455.,49.4374587872508));
#43573=CARTESIAN_POINT('Ctrl Pts',(78.2967914896971,455.,49.3916147355805));
#43574=CARTESIAN_POINT('Ctrl Pts',(78.2551164948957,455.,49.3465621292919));
#43575=CARTESIAN_POINT('',(79.722466405091,455.,53.9090580914827));
#43576=CARTESIAN_POINT('Origin',(74.9879498948689,455.,53.0228109606356));
#43577=CARTESIAN_POINT('Ctrl Pts',(79.5259634687995,455.,54.9172708347116));
#43578=CARTESIAN_POINT('Ctrl Pts',(79.5671055435192,455.,54.7833057439901));
#43579=CARTESIAN_POINT('Ctrl Pts',(79.6025381242703,455.,54.6476488793227));
#43580=CARTESIAN_POINT('Ctrl Pts',(79.6320742294025,455.,54.5106387216536));
#43581=CARTESIAN_POINT('Ctrl Pts',(79.6610001784902,455.,54.3764589160396));
#43582=CARTESIAN_POINT('Ctrl Pts',(79.6842707237605,455.,54.2409805184599));
#43583=CARTESIAN_POINT('Ctrl Pts',(79.7016610667469,455.,54.1045284674012));
#43584=CARTESIAN_POINT('Ctrl Pts',(79.7099385218545,455.,54.0395800228609));
#43585=CARTESIAN_POINT('Ctrl Pts',(79.7168830527446,455.,53.9744111521296));
#43586=CARTESIAN_POINT('Ctrl Pts',(79.722466405091,455.,53.9090580914828));
#43587=CARTESIAN_POINT('Ctrl Pts',(75.8078350467992,437.941398947677,48.2763523965962));
#43588=CARTESIAN_POINT('Ctrl Pts',(75.0263656302742,437.987255402119,48.1413643496868));
#43589=CARTESIAN_POINT('Ctrl Pts',(73.3961753647049,438.078968311002,48.2651239894432));
#43590=CARTESIAN_POINT('Ctrl Pts',(71.3306174890971,438.216537674327,49.5884496895898));
#43591=CARTESIAN_POINT('Ctrl Pts',(70.1396312756662,438.354107037653,51.7327415034739));
#43592=CARTESIAN_POINT('Ctrl Pts',(70.1074607270008,438.491676400978,54.1854768655665));
#43593=CARTESIAN_POINT('Ctrl Pts',(71.242010804005,438.629245764303,56.360277322365));
#43594=CARTESIAN_POINT('Ctrl Pts',(73.2719781460082,438.766815127628,57.7372832840433));
#43595=CARTESIAN_POINT('Ctrl Pts',(75.7121534069691,438.904384490953,57.9873162880474));
#43596=CARTESIAN_POINT('Ctrl Pts',(77.9792050969341,439.041953854279,57.0506108876648));
#43597=CARTESIAN_POINT('Ctrl Pts',(79.5312149397283,439.179523217604,55.1510795096557));
#43598=CARTESIAN_POINT('Ctrl Pts',(79.9971786085583,439.317092580929,52.7427964908572));
#43599=CARTESIAN_POINT('Ctrl Pts',(79.2657116989475,439.454661944254,50.4014494245561));
#43600=CARTESIAN_POINT('Ctrl Pts',(77.5116668773773,439.592231307579,48.6867258388772));
#43601=CARTESIAN_POINT('Ctrl Pts',(75.1543402086109,439.729800670904,48.0085217694175));
#43602=CARTESIAN_POINT('Ctrl Pts',(72.7572387087512,439.86737003423,48.5289585575719));
#43603=CARTESIAN_POINT('Ctrl Pts',(70.8933776271112,440.004939397555,50.1236283637003));
#43604=CARTESIAN_POINT('Ctrl Pts',(70.0083036305712,440.14250876088,52.4113333252207));
#43605=CARTESIAN_POINT('Ctrl Pts',(70.3135892642953,440.280078124205,54.8452089672548));
#43606=CARTESIAN_POINT('Ctrl Pts',(71.7362575112132,440.41764748753,56.8434494476892));
#43607=CARTESIAN_POINT('Ctrl Pts',(73.9362266197783,440.555216850856,57.9283853364634));
#43608=CARTESIAN_POINT('Ctrl Pts',(76.387604935838,440.692786214181,57.8406681161432));
#43609=CARTESIAN_POINT('Ctrl Pts',(78.5044026893045,440.830355577506,56.6012661509721));
#43610=CARTESIAN_POINT('Ctrl Pts',(79.7806099252566,440.967924940831,54.5064523046412));
#43611=CARTESIAN_POINT('Ctrl Pts',(79.9111556636527,441.105494304156,52.0569813882592));
#43612=CARTESIAN_POINT('Ctrl Pts',(78.8648335961934,441.243063667482,49.8383872182613));
#43613=CARTESIAN_POINT('Ctrl Pts',(76.8917617991304,441.380633030807,48.3810136753364));
#43614=CARTESIAN_POINT('Ctrl Pts',(74.4635932533763,441.518202394132,48.0332386425771));
#43615=CARTESIAN_POINT('Ctrl Pts',(72.1607695498123,441.655771757457,48.8781960085396));
#43616=CARTESIAN_POINT('Ctrl Pts',(70.5337692194001,441.793341120782,50.713902925461));
#43617=CARTESIAN_POINT('Ctrl Pts',(69.9715185834993,441.930910484107,53.101542802499));
#43618=CARTESIAN_POINT('Ctrl Pts',(70.6084208548284,442.068479847433,55.4703622250742));
#43619=CARTESIAN_POINT('Ctrl Pts',(72.2922277192217,442.206049210758,57.2541067144605));
#43620=CARTESIAN_POINT('Ctrl Pts',(74.6204335364492,442.343618574083,58.0263810391802));
#43621=CARTESIAN_POINT('Ctrl Pts',(77.0364923077588,442.481187937408,57.6025768702869));
#43622=CARTESIAN_POINT('Ctrl Pts',(78.9628572235115,442.618757300733,56.0840024824643));
#43623=CARTESIAN_POINT('Ctrl Pts',(79.9390403500092,442.756326664059,53.8336655158004));
#43624=CARTESIAN_POINT('Ctrl Pts',(79.7316899753536,442.893896027384,51.389497808354));
#43625=CARTESIAN_POINT('Ctrl Pts',(78.390372173343,443.031465390709,49.335765470876));
#43626=CARTESIAN_POINT('Ctrl Pts',(76.2357222805272,443.169034754034,48.1634029845338));
#43627=CARTESIAN_POINT('Ctrl Pts',(73.7827986167874,443.306604117359,48.1526577596006));
#43628=CARTESIAN_POINT('Ctrl Pts',(71.6179603605938,443.444173480684,49.3060983885513));
#43629=CARTESIAN_POINT('Ctrl Pts',(70.2587013093226,443.581742844009,51.3480006368313));
#43630=CARTESIAN_POINT('Ctrl Pts',(70.0299455657551,443.719312207335,53.7902579471445));
#43631=CARTESIAN_POINT('Ctrl Pts',(70.9863760504612,443.85688157066,56.049060879655));
#43632=CARTESIAN_POINT('Ctrl Pts',(72.8993628221321,443.994450933985,57.5844538493555));
#43633=CARTESIAN_POINT('Ctrl Pts',(75.3116159257467,444.13202029731,58.0294088179703));
#43634=CARTESIAN_POINT('Ctrl Pts',(77.6464982775643,444.269589660636,57.2775615175402));
#43635=CARTESIAN_POINT('Ctrl Pts',(79.3458678865093,444.407159023961,55.5086372986467));
#43636=CARTESIAN_POINT('Ctrl Pts',(80.0034989158186,444.544728387286,53.1454886809583));
#43637=CARTESIAN_POINT('Ctrl Pts',(79.4621879450261,444.682297750611,50.7530145655511));
#43638=CARTESIAN_POINT('Ctrl Pts',(77.8513326642527,444.819867113936,48.9031239675973));
#43639=CARTESIAN_POINT('Ctrl Pts',(75.5560000011943,444.957436477261,48.0380240162099));
#43640=CARTESIAN_POINT('Ctrl Pts',(73.1248777909117,445.095005840587,48.364512543824));
#43641=CARTESIAN_POINT('Ctrl Pts',(71.1391136830664,445.232575203912,49.8045440948628));
#43642=CARTESIAN_POINT('Ctrl Pts',(70.07339469223,445.370144567237,52.0138863029791));
#43643=CARTESIAN_POINT('Ctrl Pts',(70.1824756324979,445.507713930562,54.4644069228604));
#43644=CARTESIAN_POINT('Ctrl Pts',(71.4402812486687,445.645283293887,56.5703212116962));
#43645=CARTESIAN_POINT('Ctrl Pts',(73.5461393760615,445.782852657213,57.8282208528788));
#43646=CARTESIAN_POINT('Ctrl Pts',(75.9966551231817,445.920422020538,57.9374112055169));
#43647=CARTESIAN_POINT('Ctrl Pts',(78.206044912028,446.057991383863,56.8717908599269));
#43648=CARTESIAN_POINT('Ctrl Pts',(79.6461651233516,446.195560747188,54.8860910495501));
#43649=CARTESIAN_POINT('Ctrl Pts',(79.9727621970059,446.333130110513,52.4549834189681));
#43650=CARTESIAN_POINT('Ctrl Pts',(79.1077647300243,446.470699473838,50.159612132638));
#43651=CARTESIAN_POINT('Ctrl Pts',(77.2579460564552,446.608268837164,48.5486742583212));
#43652=CARTESIAN_POINT('Ctrl Pts',(74.8654961122459,446.745838200489,48.0072564672885));
#43653=CARTESIAN_POINT('Ctrl Pts',(72.5023181345641,446.883407563814,48.6647819845069));
#43654=CARTESIAN_POINT('Ctrl Pts',(70.7333180428463,447.020976927139,50.3640726116498));
#43655=CARTESIAN_POINT('Ctrl Pts',(69.9813664937813,447.158546290464,52.6989213921604));
#43656=CARTESIAN_POINT('Ctrl Pts',(70.4262137580673,447.29611565379,55.1111943600169));
#43657=CARTESIAN_POINT('Ctrl Pts',(71.9615213139283,447.433685017115,57.0242496830301));
#43658=CARTESIAN_POINT('Ctrl Pts',(74.2202815408413,447.57125438044,57.9807810193227));
#43659=CARTESIAN_POINT('Ctrl Pts',(76.6625490623592,447.708823743765,57.7521343195162));
#43660=CARTESIAN_POINT('Ctrl Pts',(78.7045119977084,447.84639310709,56.3929664378131));
#43661=CARTESIAN_POINT('Ctrl Pts',(79.8580492826516,447.983962470415,54.2281796833637));
#43662=CARTESIAN_POINT('Ctrl Pts',(79.8474135775007,448.121531833741,51.775255542309));
#43663=CARTESIAN_POINT('Ctrl Pts',(78.6751472945723,448.259101197066,49.6205533072187));
#43664=CARTESIAN_POINT('Ctrl Pts',(76.6214748471931,448.396670560391,48.2791438101341));
#43665=CARTESIAN_POINT('Ctrl Pts',(74.1773164001007,448.534239923716,48.0716843068553));
#43666=CARTESIAN_POINT('Ctrl Pts',(71.9269358504046,448.671809287042,49.0477669578345));
#43667=CARTESIAN_POINT('Ctrl Pts',(70.4082754544702,448.809378650367,50.9740640693451));
#43668=CARTESIAN_POINT('Ctrl Pts',(69.9843634121962,448.946948013692,53.3901039159554));
#43669=CARTESIAN_POINT('Ctrl Pts',(70.7565337848602,449.084517377017,55.7183442118813));
#43670=CARTESIAN_POINT('Ctrl Pts',(72.5402030927367,449.222086740342,57.4022307164097));
#43671=CARTESIAN_POINT('Ctrl Pts',(74.9089940761134,449.359656103667,58.0392387517333));
#43672=CARTESIAN_POINT('Ctrl Pts',(77.2966590545129,449.497225466993,57.4770947213303));
#43673=CARTESIAN_POINT('Ctrl Pts',(79.1324386130003,449.634794830318,55.8501763544067));
#43674=CARTESIAN_POINT('Ctrl Pts',(79.9774987961291,449.772364193643,53.5473903793574));
#43675=CARTESIAN_POINT('Ctrl Pts',(79.6298321782047,449.909933556968,51.1192063083334));
#43676=CARTESIAN_POINT('Ctrl Pts',(78.1725467317586,450.047502920293,49.1460694434481));
#43677=CARTESIAN_POINT('Ctrl Pts',(75.9539992808559,450.185072283618,48.0996483197667));
#43678=CARTESIAN_POINT('Ctrl Pts',(73.5045225382257,450.322641646944,48.2300846924063));
#43679=CARTESIAN_POINT('Ctrl Pts',(71.4096517130236,450.460211010268,49.5061983964745));
#43680=CARTESIAN_POINT('Ctrl Pts',(70.1701552369073,450.597780373594,51.6229408101112));
#43681=CARTESIAN_POINT('Ctrl Pts',(70.0823285658649,450.735349736919,54.0743152074334));
#43682=CARTESIAN_POINT('Ctrl Pts',(71.1671662279536,450.872919100245,56.2743327543879));
#43683=CARTESIAN_POINT('Ctrl Pts',(73.1653431859865,451.01048846357,57.6970902194464));
#43684=CARTESIAN_POINT('Ctrl Pts',(75.5992051954103,451.148057826895,58.0024845204358));
#43685=CARTESIAN_POINT('Ctrl Pts',(77.8869496712317,451.28562719022,57.1175126715371));
#43686=CARTESIAN_POINT('Ctrl Pts',(79.4817026967351,451.423196553545,55.2537227832616));
#43687=CARTESIAN_POINT('Ctrl Pts',(80.0022465081079,451.56076591687,52.8566445408086));
#43688=CARTESIAN_POINT('Ctrl Pts',(79.3241477011989,451.698335280195,50.4992875529827));
#43689=CARTESIAN_POINT('Ctrl Pts',(77.6095024167226,451.835904643521,48.7451662605903));
#43690=CARTESIAN_POINT('Ctrl Pts',(75.268188065539,451.973474006846,48.0135946175118));
#43691=CARTESIAN_POINT('Ctrl Pts',(72.8598841761585,452.111043370171,48.4794511794175));
#43692=CARTESIAN_POINT('Ctrl Pts',(70.9602837922551,452.248612733496,50.0313752567566));
#43693=CARTESIAN_POINT('Ctrl Pts',(70.0234769197435,452.386182096821,52.2983871320682));
#43694=CARTESIAN_POINT('Ctrl Pts',(70.2734025728211,452.523751460147,54.7385689140928));
#43695=CARTESIAN_POINT('Ctrl Pts',(71.6503172704237,452.661320823472,56.768607306331));
#43696=CARTESIAN_POINT('Ctrl Pts',(73.8250764135404,452.798890186797,57.9032317501341));
#43697=CARTESIAN_POINT('Ctrl Pts',(76.2778146704519,452.936459550122,57.8712159196889));
#43698=CARTESIAN_POINT('Ctrl Pts',(78.4222171738024,453.074028913447,56.6802130540946));
#43699=CARTESIAN_POINT('Ctrl Pts',(79.7456752114561,453.211598276772,54.6149264217687));
#43700=CARTESIAN_POINT('Ctrl Pts',(79.9318226886387,453.349167640098,52.1690525697788));
#43701=CARTESIAN_POINT('Ctrl Pts',(78.9361620760772,453.486737003423,49.9272653015586));
#43702=CARTESIAN_POINT('Ctrl Pts',(76.9967008584153,453.624306366748,48.4254530263665));
#43703=CARTESIAN_POINT('Ctrl Pts',(74.5770580405339,453.761875730073,48.0226157475833));
#43704=CARTESIAN_POINT('Ctrl Pts',(72.2556360896412,453.899445093398,48.8150513185195));
#43705=CARTESIAN_POINT('Ctrl Pts',(70.5873615618629,454.037014456724,50.6133284028548));
#43706=CARTESIAN_POINT('Ctrl Pts',(69.9710218005993,454.174583820049,52.9875855721569));
#43707=CARTESIAN_POINT('Ctrl Pts',(70.5539601059199,454.312153183374,55.370251255858));
#43708=CARTESIAN_POINT('Ctrl Pts',(72.1968012676347,454.449722546699,57.1917983514602));
#43709=CARTESIAN_POINT('Ctrl Pts',(74.5068799898513,454.587291910024,58.0167116789214));
#43710=CARTESIAN_POINT('Ctrl Pts',(76.9318483449357,454.724861273349,57.6479786853993));
#43711=CARTESIAN_POINT('Ctrl Pts',(78.8922444243951,454.862430636675,56.1733372178574));
#43712=CARTESIAN_POINT('Ctrl Pts',(79.5765523475053,454.954143545558,54.6885613368712));
#43713=CARTESIAN_POINT('Ctrl Pts',(79.7224664050908,455.,53.9090580914826));
#43714=CARTESIAN_POINT('Ctrl Pts',(75.8135940020368,437.960932631785,48.2430127973331));
#43715=CARTESIAN_POINT('Ctrl Pts',(75.0266354662385,438.006789086226,48.1070765808929));
#43716=CARTESIAN_POINT('Ctrl Pts',(73.3849945813404,438.09850199511,48.2317055207262));
#43717=CARTESIAN_POINT('Ctrl Pts',(71.304928020805,438.236071358435,49.5643263928294));
#43718=CARTESIAN_POINT('Ctrl Pts',(70.1055762011968,438.37364072176,51.7236799266913));
#43719=CARTESIAN_POINT('Ctrl Pts',(70.0731796833828,438.511210085085,54.1936435470669));
#43720=CARTESIAN_POINT('Ctrl Pts',(71.2156989535025,438.648779448411,56.3837200195998));
#43721=CARTESIAN_POINT('Ctrl Pts',(73.2599249889687,438.786348811736,57.7703982087559));
#43722=CARTESIAN_POINT('Ctrl Pts',(75.7172402848071,438.923918175061,58.0221874695656));
#43723=CARTESIAN_POINT('Ctrl Pts',(78.0002159723868,439.061487538386,57.0789025568467));
#43724=CARTESIAN_POINT('Ctrl Pts',(79.5631272874079,439.199056901711,55.1660286806199));
#43725=CARTESIAN_POINT('Ctrl Pts',(80.0323639316109,439.336626265037,52.7408296412398));
#43726=CARTESIAN_POINT('Ctrl Pts',(79.2957591253323,439.474195628362,50.3830367191764));
#43727=CARTESIAN_POINT('Ctrl Pts',(77.5293937176552,439.611764991687,48.6562687436809));
#43728=CARTESIAN_POINT('Ctrl Pts',(75.1555089508019,439.749334355012,47.973300901065));
#43729=CARTESIAN_POINT('Ctrl Pts',(72.741569970467,439.886903718337,48.4973932892262));
#43730=CARTESIAN_POINT('Ctrl Pts',(70.8646169423356,440.024473081663,50.1032642154267));
#43731=CARTESIAN_POINT('Ctrl Pts',(69.9733260975992,440.162042444988,52.4070382452052));
#43732=CARTESIAN_POINT('Ctrl Pts',(70.2807560881215,440.299611808313,54.8580096729639));
#43733=CARTESIAN_POINT('Ctrl Pts',(71.7134172989717,440.437181171638,56.8702859942152));
#43734=CARTESIAN_POINT('Ctrl Pts',(73.9288392103963,440.574750534963,57.9628425810889));
#43735=CARTESIAN_POINT('Ctrl Pts',(76.3974362527121,440.712319898288,57.8745092262476));
#43736=CARTESIAN_POINT('Ctrl Pts',(78.5291026051286,440.849889261614,56.6264015778208));
#43737=CARTESIAN_POINT('Ctrl Pts',(79.8142740482362,440.987458624939,54.5168735497005));
#43738=CARTESIAN_POINT('Ctrl Pts',(79.9457367529441,441.125027988264,52.0501973048284));
#43739=CARTESIAN_POINT('Ctrl Pts',(78.892065214725,441.262597351589,49.8160195076783));
#43740=CARTESIAN_POINT('Ctrl Pts',(76.9051343641921,441.400166714914,48.3484092273538));
#43741=CARTESIAN_POINT('Ctrl Pts',(74.459910119928,441.53773607824,47.9981913880117));
#43742=CARTESIAN_POINT('Ctrl Pts',(72.1409111525511,441.675305441565,48.8490838189484));
#43743=CARTESIAN_POINT('Ctrl Pts',(70.5024826092334,441.81287480489,50.6976849246948));
#43744=CARTESIAN_POINT('Ctrl Pts',(69.9362826686808,441.950444168215,53.1020958228239));
#43745=CARTESIAN_POINT('Ctrl Pts',(70.5776586052088,442.08801353154,55.4875540697372));
#43746=CARTESIAN_POINT('Ctrl Pts',(72.2732926972788,442.225582894866,57.2838277586649));
#43747=CARTESIAN_POINT('Ctrl Pts',(74.6178520648221,442.363152258191,58.0615266154141));
#43748=CARTESIAN_POINT('Ctrl Pts',(77.0508814743759,442.500721621516,57.6347456036881));
#43749=CARTESIAN_POINT('Ctrl Pts',(78.9907773697968,442.638290984841,56.1055045976158));
#43750=CARTESIAN_POINT('Ctrl Pts',(79.9738173041241,442.775860348166,53.8393610392238));
#43751=CARTESIAN_POINT('Ctrl Pts',(79.7650104797166,442.913429711491,51.3780252535568));
#43752=CARTESIAN_POINT('Ctrl Pts',(78.4142711274279,443.050999074817,49.3098672949128));
#43753=CARTESIAN_POINT('Ctrl Pts',(76.2444867584528,443.188568438142,48.1292700173134));
#43754=CARTESIAN_POINT('Ctrl Pts',(73.7743335137805,443.326137801467,48.1184493168465));
#43755=CARTESIAN_POINT('Ctrl Pts',(71.5942892173451,443.463707164792,49.2799918280372));
#43756=CARTESIAN_POINT('Ctrl Pts',(70.2254825946682,443.601276528117,51.3362366017546));
#43757=CARTESIAN_POINT('Ctrl Pts',(69.9951200478985,443.738845891443,53.795648571468));
#43758=CARTESIAN_POINT('Ctrl Pts',(70.9582685959045,443.876415254768,56.0703175614966));
#43759=CARTESIAN_POINT('Ctrl Pts',(72.8846923778225,444.013984618093,57.6164952848467));
#43760=CARTESIAN_POINT('Ctrl Pts',(75.3138893882913,444.151553981418,58.064575661625));
#43761=CARTESIAN_POINT('Ctrl Pts',(77.6651721870708,444.289123344743,57.3074473106253));
#43762=CARTESIAN_POINT('Ctrl Pts',(79.3764783379654,444.426692708068,55.5260979912513));
#43763=CARTESIAN_POINT('Ctrl Pts',(80.038728633341,444.564262071394,53.1463503815249));
#43764=CARTESIAN_POINT('Ctrl Pts',(79.493615440197,444.701831434719,50.7370712888534));
#43765=CARTESIAN_POINT('Ctrl Pts',(77.8714453509601,444.839400798044,48.8741868744816));
#43766=CARTESIAN_POINT('Ctrl Pts',(75.5599900419058,444.976970161369,48.003010374587));
#43767=CARTESIAN_POINT('Ctrl Pts',(73.1117913862783,445.114539524694,48.3317921902448));
#43768=CARTESIAN_POINT('Ctrl Pts',(71.112079072904,445.25210888802,49.7819386667991));
#43769=CARTESIAN_POINT('Ctrl Pts',(70.0388743653796,445.389678251345,52.0067995153628));
#43770=CARTESIAN_POINT('Ctrl Pts',(70.1487215010723,445.52724761467,54.4745328369565));
#43771=CARTESIAN_POINT('Ctrl Pts',(71.4153620695824,445.664816977995,56.5952392781992));
#43772=CARTESIAN_POINT('Ctrl Pts',(73.5360119548985,445.80238634132,57.8619745321622));
#43773=CARTESIAN_POINT('Ctrl Pts',(76.0037403695044,445.939955704645,57.9719318487485));
#43774=CARTESIAN_POINT('Ctrl Pts',(78.2286491330098,446.07752506797,56.8988264793647));
#43775=CARTESIAN_POINT('Ctrl Pts',(79.6788848926077,446.215094431296,54.8991789150905));
#43776=CARTESIAN_POINT('Ctrl Pts',(80.0077760167439,446.352663794621,52.4509949415729));
#43777=CARTESIAN_POINT('Ctrl Pts',(79.1367027211158,446.490233157946,50.1395007379533));
#43778=CARTESIAN_POINT('Ctrl Pts',(77.2738907363328,446.627802521271,48.5172474750277));
#43779=CARTESIAN_POINT('Ctrl Pts',(74.8646359846401,446.765371884597,47.9720267113274));
#43780=CARTESIAN_POINT('Ctrl Pts',(72.4848588086928,446.902941247922,48.6341707534847));
#43781=CARTESIAN_POINT('Ctrl Pts',(70.7034330835562,447.040510611247,50.3453973678012));
#43782=CARTESIAN_POINT('Ctrl Pts',(69.9461997516687,447.178079974572,52.6966463594655));
#43783=CARTESIAN_POINT('Ctrl Pts',(70.3941716675923,447.315649337897,55.1258633737044));
#43784=CARTESIAN_POINT('Ctrl Pts',(71.9402633771475,447.453218701222,57.0523561884764));
#43785=CARTESIAN_POINT('Ctrl Pts',(74.2148893616102,447.590788064548,58.0156062964603));
#43786=CARTESIAN_POINT('Ctrl Pts',(76.6743116142528,447.728357427873,57.785353559386));
#43787=CARTESIAN_POINT('Ctrl Pts',(78.7306175013115,447.865926791198,56.4166387466614));
#43788=CARTESIAN_POINT('Ctrl Pts',(79.892257347416,448.003496154523,54.2366463137236));
#43789=CARTESIAN_POINT('Ctrl Pts',(79.8815469360093,448.141065517849,51.7664925883836));
#43790=CARTESIAN_POINT('Ctrl Pts',(78.7010465375661,448.278634881173,49.5966555094766));
#43791=CARTESIAN_POINT('Ctrl Pts',(76.6329488896949,448.416204244499,48.2458238180386));
#43792=CARTESIAN_POINT('Ctrl Pts',(74.1716224294276,448.553773607824,48.0369070984776));
#43793=CARTESIAN_POINT('Ctrl Pts',(71.9054349818719,448.691342971149,49.0198458515363));
#43794=CARTESIAN_POINT('Ctrl Pts',(70.3761073635582,448.828912334474,50.9596734664513));
#43795=CARTESIAN_POINT('Ctrl Pts',(69.9492177207381,448.9664816978,53.3926838183768));
#43796=CARTESIAN_POINT('Ctrl Pts',(70.7268118952619,449.104051061125,55.7372779068002));
#43797=CARTESIAN_POINT('Ctrl Pts',(72.5230098745974,449.24162042445,57.4329921984057));
#43798=CARTESIAN_POINT('Ctrl Pts',(74.9084394825524,449.379189787775,58.074474641825));
#43799=CARTESIAN_POINT('Ctrl Pts',(77.3128756583575,449.5167591511,57.508382055578));
#43800=CARTESIAN_POINT('Ctrl Pts',(79.1615499159115,449.654328514426,55.8700360514686));
#43801=CARTESIAN_POINT('Ctrl Pts',(80.0125458862126,449.791897877751,53.5510750776152));
#43802=CARTESIAN_POINT('Ctrl Pts',(79.6624372232219,449.929467241076,51.1058351990302));
#43803=CARTESIAN_POINT('Ctrl Pts',(78.1949156581748,450.067036604401,49.1188388236321));
#43804=CARTESIAN_POINT('Ctrl Pts',(75.9607849082795,450.204605967726,48.06506753341));
#43805=CARTESIAN_POINT('Ctrl Pts',(73.4941027962351,450.342175331051,48.1964201041654));
#43806=CARTESIAN_POINT('Ctrl Pts',(71.3845173890182,450.479744694376,49.4814973584119));
#43807=CARTESIAN_POINT('Ctrl Pts',(70.1363145657919,450.617314057702,51.6131079822862));
#43808=CARTESIAN_POINT('Ctrl Pts',(70.0478709914357,450.754883421027,54.0817010783388));
#43809=CARTESIAN_POINT('Ctrl Pts',(71.1403286616697,450.892452784352,56.2971717683888));
#43810=CARTESIAN_POINT('Ctrl Pts',(73.1525410143319,451.030022147677,57.7299228240568));
#43811=CARTESIAN_POINT('Ctrl Pts',(75.6034987137235,451.167591511002,58.0374622451341));
#43812=CARTESIAN_POINT('Ctrl Pts',(77.9073125353553,451.305160874328,57.1462742655343));
#43813=CARTESIAN_POINT('Ctrl Pts',(79.513267265472,451.442730237653,55.2693929308367));
#43814=CARTESIAN_POINT('Ctrl Pts',(80.0374674285935,451.580299600978,52.8554773712709));
#43815=CARTESIAN_POINT('Ctrl Pts',(79.3546055879029,451.717868964303,50.4815620723939));
#43816=CARTESIAN_POINT('Ctrl Pts',(77.6279164636054,451.855438327628,48.7151196567561));
#43817=CARTESIAN_POINT('Ctrl Pts',(75.2701564864537,451.993007690953,47.9784093813513));
#43818=CARTESIAN_POINT('Ctrl Pts',(72.8449364298946,452.130577054279,48.4475381663004));
#43819=CARTESIAN_POINT('Ctrl Pts',(70.9319930630693,452.268146417604,50.0103631134411));
#43820=CARTESIAN_POINT('Ctrl Pts',(69.9886059654709,452.405715780929,52.2932987067053));
#43821=CARTESIAN_POINT('Ctrl Pts',(70.2402871213106,452.543285144254,54.750620569412));
#43822=CARTESIAN_POINT('Ctrl Pts',(71.626873405343,452.68085450758,56.7949181541772));
#43823=CARTESIAN_POINT('Ctrl Pts',(73.8169082740026,452.818423870904,57.9375123134555));
#43824=CARTESIAN_POINT('Ctrl Pts',(76.2868748095306,452.95599323423,57.905271600618));
#43825=CARTESIAN_POINT('Ctrl Pts',(78.4463398103528,453.093562597555,56.7059030118799));
#43826=CARTESIAN_POINT('Ctrl Pts',(79.779093949515,453.23113196088,54.6261095998664));
#43827=CARTESIAN_POINT('Ctrl Pts',(79.9665489451789,453.368701324205,52.1630556855262));
#43828=CARTESIAN_POINT('Ctrl Pts',(78.9638947129792,453.50627068753,49.9055218795142));
#43829=CARTESIAN_POINT('Ctrl Pts',(77.0108105259159,453.643840050856,48.3931607248264));
#43830=CARTESIAN_POINT('Ctrl Pts',(74.574171895089,453.781409414181,47.9874938767418));
#43831=CARTESIAN_POINT('Ctrl Pts',(72.2364440444356,453.918978777506,48.7854955943157));
#43832=CARTESIAN_POINT('Ctrl Pts',(70.5564513896651,454.056548140831,50.5964039565915));
#43833=CARTESIAN_POINT('Ctrl Pts',(69.935782396328,454.194117504156,52.9873381455081));
#43834=CARTESIAN_POINT('Ctrl Pts',(70.5228153185577,454.331686867482,55.3867399110692));
#43835=CARTESIAN_POINT('Ctrl Pts',(72.17719596076,454.469256230807,57.2210817354965));
#43836=CARTESIAN_POINT('Ctrl Pts',(74.5035009067655,454.606825594132,58.0517893366026));
#43837=CARTESIAN_POINT('Ctrl Pts',(76.945502481901,454.744394957457,57.6804663256868));
#43838=CARTESIAN_POINT('Ctrl Pts',(78.9196685793232,454.881964320782,56.1954668291174));
#43839=CARTESIAN_POINT('Ctrl Pts',(79.6087831496676,454.973677229666,54.7002617339708));
#43840=CARTESIAN_POINT('Ctrl Pts',(79.7557221221745,455.019533684108,53.9152831798916));
#43841=CARTESIAN_POINT('Ctrl Pts',(75.8193529572743,437.980466315892,48.20967319807));
#43842=CARTESIAN_POINT('Ctrl Pts',(75.0269053022029,438.026322770334,48.0727888120991));
#43843=CARTESIAN_POINT('Ctrl Pts',(73.3738137979759,438.118035679217,48.1982870520092));
#43844=CARTESIAN_POINT('Ctrl Pts',(71.279238552513,438.255605042543,49.5402030960689));
#43845=CARTESIAN_POINT('Ctrl Pts',(70.0715211267274,438.393174405868,51.7146183499088));
#43846=CARTESIAN_POINT('Ctrl Pts',(70.0388986397648,438.530743769193,54.2018102285672));
#43847=CARTESIAN_POINT('Ctrl Pts',(71.189387103,438.668313132518,56.4071627168346));
#43848=CARTESIAN_POINT('Ctrl Pts',(73.2478718319292,438.805882495844,57.8035131334684));
#43849=CARTESIAN_POINT('Ctrl Pts',(75.7223271626451,438.943451859169,58.0570586510839));
#43850=CARTESIAN_POINT('Ctrl Pts',(78.0212268478395,439.081021222494,57.1071942260285));
#43851=CARTESIAN_POINT('Ctrl Pts',(79.5950396350873,439.218590585819,55.1809778515842));
#43852=CARTESIAN_POINT('Ctrl Pts',(80.0675492546636,439.356159949144,52.7388627916225));
#43853=CARTESIAN_POINT('Ctrl Pts',(79.325806551717,439.493729312469,50.3646240137967));
#43854=CARTESIAN_POINT('Ctrl Pts',(77.5471205579331,439.631298675795,48.6258116484846));
#43855=CARTESIAN_POINT('Ctrl Pts',(75.1566776929928,439.76886803912,47.9380800327125));
#43856=CARTESIAN_POINT('Ctrl Pts',(72.7259012321828,439.906437402445,48.4658280208805));
#43857=CARTESIAN_POINT('Ctrl Pts',(70.8358562575599,440.04400676577,50.0829000671532));
#43858=CARTESIAN_POINT('Ctrl Pts',(69.9383485646273,440.181576129095,52.4027431651896));
#43859=CARTESIAN_POINT('Ctrl Pts',(70.2479229119477,440.319145492421,54.870810378673));
#43860=CARTESIAN_POINT('Ctrl Pts',(71.6905770867303,440.456714855746,56.8971225407413));
#43861=CARTESIAN_POINT('Ctrl Pts',(73.9214518010143,440.594284219071,57.9972998257143));
#43862=CARTESIAN_POINT('Ctrl Pts',(76.4072675695861,440.731853582396,57.908350336352));
#43863=CARTESIAN_POINT('Ctrl Pts',(78.5538025209526,440.869422945721,56.6515370046695));
#43864=CARTESIAN_POINT('Ctrl Pts',(79.8479381712158,441.006992309046,54.5272947947597));
#43865=CARTESIAN_POINT('Ctrl Pts',(79.9803178422356,441.144561672372,52.0434132213975));
#43866=CARTESIAN_POINT('Ctrl Pts',(78.9192968332566,441.282131035697,49.7936517970953));
#43867=CARTESIAN_POINT('Ctrl Pts',(76.9185069292538,441.419700399022,48.3158047793713));
#43868=CARTESIAN_POINT('Ctrl Pts',(74.4562269864796,441.557269762347,47.9631441334462));
#43869=CARTESIAN_POINT('Ctrl Pts',(72.1210527552898,441.694839125672,48.8199716293573));
#43870=CARTESIAN_POINT('Ctrl Pts',(70.4711959990666,441.832408488998,50.6814669239287));
#43871=CARTESIAN_POINT('Ctrl Pts',(69.9010467538623,441.969977852323,53.1026488431487));
#43872=CARTESIAN_POINT('Ctrl Pts',(70.5468963555892,442.107547215648,55.5047459144002));
#43873=CARTESIAN_POINT('Ctrl Pts',(72.254357675336,442.245116578973,57.3135488028693));
#43874=CARTESIAN_POINT('Ctrl Pts',(74.6152705931949,442.382685942298,58.096672191648));
#43875=CARTESIAN_POINT('Ctrl Pts',(77.065270640993,442.520255305623,57.6669143370894));
#43876=CARTESIAN_POINT('Ctrl Pts',(79.018697516082,442.657824668949,56.1270067127672));
#43877=CARTESIAN_POINT('Ctrl Pts',(80.008594258239,442.795394032274,53.8450565626472));
#43878=CARTESIAN_POINT('Ctrl Pts',(79.7983309840795,442.932963395599,51.3665526987597));
#43879=CARTESIAN_POINT('Ctrl Pts',(78.4381700815129,443.070532758924,49.2839691189496));
#43880=CARTESIAN_POINT('Ctrl Pts',(76.2532512363784,443.208102122249,48.095137050093));
#43881=CARTESIAN_POINT('Ctrl Pts',(73.7658684107736,443.345671485574,48.0842408740924));
#43882=CARTESIAN_POINT('Ctrl Pts',(71.5706180740964,443.4832408489,49.2538852675232));
#43883=CARTESIAN_POINT('Ctrl Pts',(70.1922638800138,443.620810212225,51.3244725666779));
#43884=CARTESIAN_POINT('Ctrl Pts',(69.9602945300419,443.75837957555,53.8010391957915));
#43885=CARTESIAN_POINT('Ctrl Pts',(70.9301611413476,443.895948938875,56.0915742433382));
#43886=CARTESIAN_POINT('Ctrl Pts',(72.870021933513,444.0335183022,57.648536720338));
#43887=CARTESIAN_POINT('Ctrl Pts',(75.3161628508358,444.171087665526,58.0997425052797));
#43888=CARTESIAN_POINT('Ctrl Pts',(77.6838460965772,444.308657028851,57.3373331037104));
#43889=CARTESIAN_POINT('Ctrl Pts',(79.4070887894214,444.446226392176,55.5435586838559));
#43890=CARTESIAN_POINT('Ctrl Pts',(80.0739583508635,444.583795755501,53.1472120820915));
#43891=CARTESIAN_POINT('Ctrl Pts',(79.5250429353678,444.721365118826,50.7211280121556));
#43892=CARTESIAN_POINT('Ctrl Pts',(77.8915580376675,444.858934482152,48.8452497813659));
#43893=CARTESIAN_POINT('Ctrl Pts',(75.5639800826174,444.996503845477,47.9679967329641));
#43894=CARTESIAN_POINT('Ctrl Pts',(73.098704981645,445.134073208802,48.2990718366656));
#43895=CARTESIAN_POINT('Ctrl Pts',(71.0850444627416,445.271642572127,49.7593332387354));
#43896=CARTESIAN_POINT('Ctrl Pts',(70.0043540385292,445.409211935453,51.9997127277465));
#43897=CARTESIAN_POINT('Ctrl Pts',(70.1149673696467,445.546781298777,54.4846587510525));
#43898=CARTESIAN_POINT('Ctrl Pts',(71.3904428904962,445.684350662103,56.6201573447021));
#43899=CARTESIAN_POINT('Ctrl Pts',(73.5258845337356,445.821920025428,57.8957282114455));
#43900=CARTESIAN_POINT('Ctrl Pts',(76.010825615827,445.959489388753,58.0064524919801));
#43901=CARTESIAN_POINT('Ctrl Pts',(78.2512533539917,446.097058752078,56.9258620988023));
#43902=CARTESIAN_POINT('Ctrl Pts',(79.7116046618638,446.234628115403,54.9122667806309));
#43903=CARTESIAN_POINT('Ctrl Pts',(80.0427898364819,446.372197478728,52.4470064641778));
#43904=CARTESIAN_POINT('Ctrl Pts',(79.1656407122073,446.509766842054,50.1193893432686));
#43905=CARTESIAN_POINT('Ctrl Pts',(77.2898354162105,446.647336205379,48.4858206917342));
#43906=CARTESIAN_POINT('Ctrl Pts',(74.8637758570342,446.784905568704,47.9367969553663));
#43907=CARTESIAN_POINT('Ctrl Pts',(72.4673994828215,446.922474932029,48.6035595224625));
#43908=CARTESIAN_POINT('Ctrl Pts',(70.6735481242661,447.060044295355,50.3267221239526));
#43909=CARTESIAN_POINT('Ctrl Pts',(69.9110330095561,447.19761365868,52.6943713267705));
#43910=CARTESIAN_POINT('Ctrl Pts',(70.3621295771172,447.335183022005,55.1405323873919));
#43911=CARTESIAN_POINT('Ctrl Pts',(71.9190054403667,447.47275238533,57.0804626939226));
#43912=CARTESIAN_POINT('Ctrl Pts',(74.2094971823791,447.610321748655,58.050431573598));
#43913=CARTESIAN_POINT('Ctrl Pts',(76.6860741661464,447.747891111981,57.8185727992557));
#43914=CARTESIAN_POINT('Ctrl Pts',(78.7567230049145,447.885460475306,56.4403110555097));
#43915=CARTESIAN_POINT('Ctrl Pts',(79.9264654121804,448.023029838631,54.2451129440834));
#43916=CARTESIAN_POINT('Ctrl Pts',(79.9156802945179,448.160599201956,51.7577296344582));
#43917=CARTESIAN_POINT('Ctrl Pts',(78.7269457805599,448.298168565281,49.5727577117345));
#43918=CARTESIAN_POINT('Ctrl Pts',(76.6444229321967,448.435737928606,48.2125038259431));
#43919=CARTESIAN_POINT('Ctrl Pts',(74.1659284587545,448.573307291932,48.0021298900998));
#43920=CARTESIAN_POINT('Ctrl Pts',(71.8839341133392,448.710876655257,48.9919247452381));
#43921=CARTESIAN_POINT('Ctrl Pts',(70.3439392726461,448.848446018582,50.9452828635574));
#43922=CARTESIAN_POINT('Ctrl Pts',(69.9140720292799,448.986015381907,53.3952637207982));
#43923=CARTESIAN_POINT('Ctrl Pts',(70.6970900056636,449.123584745232,55.7562116017192));
#43924=CARTESIAN_POINT('Ctrl Pts',(72.5058166564581,449.261154108558,57.4637536804017));
#43925=CARTESIAN_POINT('Ctrl Pts',(74.9078848889915,449.398723471882,58.1097105319168));
#43926=CARTESIAN_POINT('Ctrl Pts',(77.329092262202,449.536292835208,57.5396693898256));
#43927=CARTESIAN_POINT('Ctrl Pts',(79.1906612188226,449.673862198533,55.8898957485305));
#43928=CARTESIAN_POINT('Ctrl Pts',(80.0475929762962,449.811431561858,53.5547597758731));
#43929=CARTESIAN_POINT('Ctrl Pts',(79.6950422682392,449.949000925183,51.0924640897269));
#43930=CARTESIAN_POINT('Ctrl Pts',(78.217284584591,450.086570288509,49.0916082038161));
#43931=CARTESIAN_POINT('Ctrl Pts',(75.9675705357031,450.224139651834,48.0304867470534));
#43932=CARTESIAN_POINT('Ctrl Pts',(73.4836830542445,450.361709015159,48.1627555159246));
#43933=CARTESIAN_POINT('Ctrl Pts',(71.3593830650128,450.499278378484,49.4567963203493));
#43934=CARTESIAN_POINT('Ctrl Pts',(70.1024738946765,450.63684774181,51.6032751544611));
#43935=CARTESIAN_POINT('Ctrl Pts',(70.0134134170065,450.774417105134,54.0890869492442));
#43936=CARTESIAN_POINT('Ctrl Pts',(71.1134910953859,450.91198646846,56.3200107823898));
#43937=CARTESIAN_POINT('Ctrl Pts',(73.1397388426772,451.049555831785,57.7627554286672));
#43938=CARTESIAN_POINT('Ctrl Pts',(75.6077922320367,451.18712519511,58.0724399698325));
#43939=CARTESIAN_POINT('Ctrl Pts',(77.9276753994789,451.324694558435,57.1750358595316));
#43940=CARTESIAN_POINT('Ctrl Pts',(79.544831834209,451.46226392176,55.2850630784119));
#43941=CARTESIAN_POINT('Ctrl Pts',(80.072688349079,451.599833285086,52.8543102017332));
#43942=CARTESIAN_POINT('Ctrl Pts',(79.3850634746068,451.737402648411,50.4638365918052));
#43943=CARTESIAN_POINT('Ctrl Pts',(77.6463305104883,451.874972011736,48.6850730529218));
#43944=CARTESIAN_POINT('Ctrl Pts',(75.2721249073685,452.012541375061,47.9432241451907));
#43945=CARTESIAN_POINT('Ctrl Pts',(72.8299886836307,452.150110738386,48.4156251531833));
#43946=CARTESIAN_POINT('Ctrl Pts',(70.9037023338835,452.287680101711,49.9893509701255));
#43947=CARTESIAN_POINT('Ctrl Pts',(69.9537350111984,452.425249465037,52.2882102813424));
#43948=CARTESIAN_POINT('Ctrl Pts',(70.2071716698,452.562818828362,54.7626722247312));
#43949=CARTESIAN_POINT('Ctrl Pts',(71.6034295402623,452.700388191687,56.8212290020234));
#43950=CARTESIAN_POINT('Ctrl Pts',(73.8087401344649,452.837957555012,57.971792876777));
#43951=CARTESIAN_POINT('Ctrl Pts',(76.2959349486093,452.975526918338,57.9393272815472));
#43952=CARTESIAN_POINT('Ctrl Pts',(78.4704624469033,453.113096281663,56.7315929696652));
#43953=CARTESIAN_POINT('Ctrl Pts',(79.8125126875738,453.250665644988,54.637292777964));
#43954=CARTESIAN_POINT('Ctrl Pts',(80.0012752017191,453.388235008313,52.1570588012735));
#43955=CARTESIAN_POINT('Ctrl Pts',(78.9916273498813,453.525804371638,49.8837784574698));
#43956=CARTESIAN_POINT('Ctrl Pts',(77.0249201934165,453.663373734963,48.3608684232863));
#43957=CARTESIAN_POINT('Ctrl Pts',(74.5712857496441,453.800943098289,47.9523720059004));
#43958=CARTESIAN_POINT('Ctrl Pts',(72.21725199923,453.938512461614,48.7559398701119));
#43959=CARTESIAN_POINT('Ctrl Pts',(70.5255412174673,454.076081824939,50.5794795103282));
#43960=CARTESIAN_POINT('Ctrl Pts',(69.9005429920568,454.213651188264,52.9870907188594));
#43961=CARTESIAN_POINT('Ctrl Pts',(70.4916705311956,454.351220551589,55.4032285662804));
#43962=CARTESIAN_POINT('Ctrl Pts',(72.1575906538854,454.488789914914,57.2503651195328));
#43963=CARTESIAN_POINT('Ctrl Pts',(74.5001218236798,454.62635927824,58.0868669942838));
#43964=CARTESIAN_POINT('Ctrl Pts',(76.9591566188663,454.763928641565,57.7129539659744));
#43965=CARTESIAN_POINT('Ctrl Pts',(78.9470927342512,454.90149800489,56.2175964403774));
#43966=CARTESIAN_POINT('Ctrl Pts',(79.6410139518298,454.993210913773,54.7119621310705));
#43967=CARTESIAN_POINT('Ctrl Pts',(79.7889778392583,455.039067368215,53.9215082683005));
#43968=CARTESIAN_POINT('Ctrl Pts',(75.8251119125118,438.,48.1763335988069));
#43969=CARTESIAN_POINT('Ctrl Pts',(75.0271751381672,438.045856454442,48.0385010433052));
#43970=CARTESIAN_POINT('Ctrl Pts',(73.3626330146115,438.137569363325,48.1648685832922));
#43971=CARTESIAN_POINT('Ctrl Pts',(71.2535490842209,438.275138726651,49.5160797993085));
#43972=CARTESIAN_POINT('Ctrl Pts',(70.0374660522581,438.412708089975,51.7055567731262));
#43973=CARTESIAN_POINT('Ctrl Pts',(70.0046175961469,438.550277453301,54.2099769100676));
#43974=CARTESIAN_POINT('Ctrl Pts',(71.1630752524974,438.687846816626,56.4306054140694));
#43975=CARTESIAN_POINT('Ctrl Pts',(73.2358186748897,438.825416179951,57.836628058181));
#43976=CARTESIAN_POINT('Ctrl Pts',(75.7274140404831,438.962985543276,58.0919298326021));
#43977=CARTESIAN_POINT('Ctrl Pts',(78.0422377232922,439.100554906601,57.1354858952104));
#43978=CARTESIAN_POINT('Ctrl Pts',(79.6269519827668,439.238124269927,55.1959270225485));
#43979=CARTESIAN_POINT('Ctrl Pts',(80.1027345777162,439.375693633252,52.7368959420052));
#43980=CARTESIAN_POINT('Ctrl Pts',(79.3558539781017,439.513262996577,50.346211308417));
#43981=CARTESIAN_POINT('Ctrl Pts',(77.564847398211,439.650832359902,48.5953545532883));
#43982=CARTESIAN_POINT('Ctrl Pts',(75.1578464351838,439.788401723227,47.90285916436));
#43983=CARTESIAN_POINT('Ctrl Pts',(72.7102324938985,439.925971086553,48.4342627525347));
#43984=CARTESIAN_POINT('Ctrl Pts',(70.8070955727843,440.063540449878,50.0625359188796));
#43985=CARTESIAN_POINT('Ctrl Pts',(69.9033710316553,440.201109813203,52.398448085174));
#43986=CARTESIAN_POINT('Ctrl Pts',(70.2150897357739,440.338679176528,54.8836110843821));
#43987=CARTESIAN_POINT('Ctrl Pts',(71.6677368744888,440.476248539853,56.9239590872673));
#43988=CARTESIAN_POINT('Ctrl Pts',(73.9140643916323,440.613817903178,58.0317570703397));
#43989=CARTESIAN_POINT('Ctrl Pts',(76.4170988864601,440.751387266504,57.9421914464564));
#43990=CARTESIAN_POINT('Ctrl Pts',(78.5785024367767,440.888956629829,56.6766724315182));
#43991=CARTESIAN_POINT('Ctrl Pts',(79.8816022941954,441.026525993154,54.5377160398189));
#43992=CARTESIAN_POINT('Ctrl Pts',(80.014898931527,441.164095356479,52.0366291379667));
#43993=CARTESIAN_POINT('Ctrl Pts',(78.9465284517881,441.301664719805,49.7712840865122));
#43994=CARTESIAN_POINT('Ctrl Pts',(76.9318794943156,441.43923408313,48.2832003313887));
#43995=CARTESIAN_POINT('Ctrl Pts',(74.4525438530313,441.576803446455,47.9280968788807));
#43996=CARTESIAN_POINT('Ctrl Pts',(72.1011943580286,441.71437280978,48.7908594397661));
#43997=CARTESIAN_POINT('Ctrl Pts',(70.4399093888999,441.851942173105,50.6652489231625));
#43998=CARTESIAN_POINT('Ctrl Pts',(69.8658108390438,441.989511536431,53.1032018634736));
#43999=CARTESIAN_POINT('Ctrl Pts',(70.5161341059696,442.127080899755,55.5219377590632));
#44000=CARTESIAN_POINT('Ctrl Pts',(72.2354226533932,442.264650263081,57.3432698470737));
#44001=CARTESIAN_POINT('Ctrl Pts',(74.6126891215678,442.402219626406,58.1318177678819));
#44002=CARTESIAN_POINT('Ctrl Pts',(77.0796598076102,442.539788989731,57.6990830704906));
#44003=CARTESIAN_POINT('Ctrl Pts',(79.0466176623673,442.677358353056,56.1485088279186));
#44004=CARTESIAN_POINT('Ctrl Pts',(80.0433712123539,442.814927716381,53.8507520860707));
#44005=CARTESIAN_POINT('Ctrl Pts',(79.8316514884425,442.952497079707,51.3550801439626));
#44006=CARTESIAN_POINT('Ctrl Pts',(78.4620690355979,443.090066443032,49.2580709429864));
#44007=CARTESIAN_POINT('Ctrl Pts',(76.2620157143041,443.227635806357,48.0610040828726));
#44008=CARTESIAN_POINT('Ctrl Pts',(73.7574033077667,443.365205169682,48.0500324313384));
#44009=CARTESIAN_POINT('Ctrl Pts',(71.5469469308476,443.502774533007,49.2277787070091));
#44010=CARTESIAN_POINT('Ctrl Pts',(70.1590451653594,443.640343896333,51.3127085316012));
#44011=CARTESIAN_POINT('Ctrl Pts',(69.9254690121854,443.777913259658,53.806429820115));
#44012=CARTESIAN_POINT('Ctrl Pts',(70.9020536867909,443.915482622983,56.1128309251798));
#44013=CARTESIAN_POINT('Ctrl Pts',(72.8553514892035,444.053051986308,57.6805781558292));
#44014=CARTESIAN_POINT('Ctrl Pts',(75.3184363133803,444.190621349633,58.1349093489344));
#44015=CARTESIAN_POINT('Ctrl Pts',(77.7025200060835,444.328190712959,57.3672188967954));
#44016=CARTESIAN_POINT('Ctrl Pts',(79.4376992408775,444.465760076284,55.5610193764604));
#44017=CARTESIAN_POINT('Ctrl Pts',(80.1091880683859,444.603329439609,53.1480737826581));
#44018=CARTESIAN_POINT('Ctrl Pts',(79.5564704305387,444.740898802934,50.7051847354578));
#44019=CARTESIAN_POINT('Ctrl Pts',(77.9116707243749,444.878468166259,48.8163126882502));
#44020=CARTESIAN_POINT('Ctrl Pts',(75.567970123329,445.016037529584,47.9329830913412));
#44021=CARTESIAN_POINT('Ctrl Pts',(73.0856185770117,445.15360689291,48.2663514830863));
#44022=CARTESIAN_POINT('Ctrl Pts',(71.0580098525792,445.291176256235,49.7367278106718));
#44023=CARTESIAN_POINT('Ctrl Pts',(69.9698337116788,445.42874561956,51.9926259401302));
#44024=CARTESIAN_POINT('Ctrl Pts',(70.0812132382212,445.566314982885,54.4947846651486));
#44025=CARTESIAN_POINT('Ctrl Pts',(71.3655237114099,445.70388434621,56.6450754112051));
#44026=CARTESIAN_POINT('Ctrl Pts',(73.5157571125727,445.841453709536,57.9294818907289));
#44027=CARTESIAN_POINT('Ctrl Pts',(76.0179108621497,445.979023072861,58.0409731352117));
#44028=CARTESIAN_POINT('Ctrl Pts',(78.2738575749735,446.116592436186,56.95289771824));
#44029=CARTESIAN_POINT('Ctrl Pts',(79.7443244311198,446.254161799511,54.9253546461714));
#44030=CARTESIAN_POINT('Ctrl Pts',(80.0778036562199,446.391731162836,52.4430179867826));
#44031=CARTESIAN_POINT('Ctrl Pts',(79.1945787032988,446.529300526162,50.0992779485839));
#44032=CARTESIAN_POINT('Ctrl Pts',(77.3057800960881,446.666869889487,48.4543939084407));
#44033=CARTESIAN_POINT('Ctrl Pts',(74.8629157294284,446.804439252812,47.9015671994052));
#44034=CARTESIAN_POINT('Ctrl Pts',(72.4499401569502,446.942008616137,48.5729482914402));
#44035=CARTESIAN_POINT('Ctrl Pts',(70.643663164976,447.079577979463,50.308046880104));
#44036=CARTESIAN_POINT('Ctrl Pts',(69.8758662674435,447.217147342787,52.6920962940756));
#44037=CARTESIAN_POINT('Ctrl Pts',(70.3300874866422,447.354716706113,55.1552014010794));
#44038=CARTESIAN_POINT('Ctrl Pts',(71.8977475035859,447.492286069438,57.1085691993689));
#44039=CARTESIAN_POINT('Ctrl Pts',(74.204105003148,447.629855432763,58.0852568507357));
#44040=CARTESIAN_POINT('Ctrl Pts',(76.6978367180401,447.767424796088,57.8517920391255));
#44041=CARTESIAN_POINT('Ctrl Pts',(78.7828285085176,447.904994159413,56.463983364358));
#44042=CARTESIAN_POINT('Ctrl Pts',(79.9606734769448,448.042563522738,54.2535795744433));
#44043=CARTESIAN_POINT('Ctrl Pts',(79.9498136530265,448.180132886064,51.7489666805328));
#44044=CARTESIAN_POINT('Ctrl Pts',(78.7528450235537,448.317702249389,49.5488599139924));
#44045=CARTESIAN_POINT('Ctrl Pts',(76.6558969746985,448.455271612714,48.1791838338476));
#44046=CARTESIAN_POINT('Ctrl Pts',(74.1602344880813,448.592840976039,47.9673526817221));
#44047=CARTESIAN_POINT('Ctrl Pts',(71.8624332448065,448.730410339365,48.9640036389398));
#44048=CARTESIAN_POINT('Ctrl Pts',(70.311771181734,448.867979702689,50.9308922606635));
#44049=CARTESIAN_POINT('Ctrl Pts',(69.8789263378217,449.005549066015,53.3978436232196));
#44050=CARTESIAN_POINT('Ctrl Pts',(70.6673681160653,449.14311842934,55.7751452966382));
#44051=CARTESIAN_POINT('Ctrl Pts',(72.4886234383188,449.280687792665,57.4945151623977));
#44052=CARTESIAN_POINT('Ctrl Pts',(74.9073302954306,449.41825715599,58.1449464220086));
#44053=CARTESIAN_POINT('Ctrl Pts',(77.3453088660466,449.555826519316,57.5709567240733));
#44054=CARTESIAN_POINT('Ctrl Pts',(79.2197725217338,449.693395882641,55.9097554455925));
#44055=CARTESIAN_POINT('Ctrl Pts',(80.0826400663797,449.830965245966,53.5584444741309));
#44056=CARTESIAN_POINT('Ctrl Pts',(79.7276473132564,449.968534609291,51.0790929804237));
#44057=CARTESIAN_POINT('Ctrl Pts',(78.2396535110072,450.106103972616,49.0643775840001));
#44058=CARTESIAN_POINT('Ctrl Pts',(75.9743561631267,450.243673335941,47.9959059606967));
#44059=CARTESIAN_POINT('Ctrl Pts',(73.4732633122539,450.381242699267,48.1290909276837));
#44060=CARTESIAN_POINT('Ctrl Pts',(71.3342487410075,450.518812062591,49.4320952822867));
#44061=CARTESIAN_POINT('Ctrl Pts',(70.0686332235611,450.656381425917,51.5934423266361));
#44062=CARTESIAN_POINT('Ctrl Pts',(69.9789558425772,450.793950789242,54.0964728201495));
#44063=CARTESIAN_POINT('Ctrl Pts',(71.0866535291021,450.931520152567,56.3428497963907));
#44064=CARTESIAN_POINT('Ctrl Pts',(73.1269366710226,451.069089515892,57.7955880332776));
#44065=CARTESIAN_POINT('Ctrl Pts',(75.6120857503499,451.206658879218,58.1074176945308));
#44066=CARTESIAN_POINT('Ctrl Pts',(77.9480382636025,451.344228242543,57.2037974535288));
#44067=CARTESIAN_POINT('Ctrl Pts',(79.5763964029459,451.481797605868,55.300733225987));
#44068=CARTESIAN_POINT('Ctrl Pts',(80.1079092695645,451.619366969193,52.8531430321954));
#44069=CARTESIAN_POINT('Ctrl Pts',(79.4155213613108,451.756936332518,50.4461111112164));
#44070=CARTESIAN_POINT('Ctrl Pts',(77.6647445573712,451.894505695844,48.6550264490875));
#44071=CARTESIAN_POINT('Ctrl Pts',(75.2740933282832,452.032075059169,47.9080389090301));
#44072=CARTESIAN_POINT('Ctrl Pts',(72.8150409373668,452.169644422494,48.3837121400662));
#44073=CARTESIAN_POINT('Ctrl Pts',(70.8754116046977,452.307213785819,49.96833882681));
#44074=CARTESIAN_POINT('Ctrl Pts',(69.9188640569258,452.444783149145,52.2831218559795));
#44075=CARTESIAN_POINT('Ctrl Pts',(70.1740562182895,452.582352512469,54.7747238800505));
#44076=CARTESIAN_POINT('Ctrl Pts',(71.5799856751815,452.719921875795,56.8475398498696));
#44077=CARTESIAN_POINT('Ctrl Pts',(73.8005719949271,452.85749123912,58.0060734400985));
#44078=CARTESIAN_POINT('Ctrl Pts',(76.304995087688,452.995060602445,57.9733829624763));
#44079=CARTESIAN_POINT('Ctrl Pts',(78.4945850834537,453.13262996577,56.7572829274506));
#44080=CARTESIAN_POINT('Ctrl Pts',(79.8459314256328,453.270199329095,54.6484759560617));
#44081=CARTESIAN_POINT('Ctrl Pts',(80.0360014582592,453.407768692421,52.1510619170208));
#44082=CARTESIAN_POINT('Ctrl Pts',(79.0193599867834,453.545338055746,49.8620350354254));
#44083=CARTESIAN_POINT('Ctrl Pts',(77.0390298609172,453.682907419071,48.3285761217461));
#44084=CARTESIAN_POINT('Ctrl Pts',(74.5683996041992,453.820476782396,47.9172501350589));
#44085=CARTESIAN_POINT('Ctrl Pts',(72.1980599540245,453.958046145721,48.726384145908));
#44086=CARTESIAN_POINT('Ctrl Pts',(70.4946310452694,454.095615509047,50.562555064065));
#44087=CARTESIAN_POINT('Ctrl Pts',(69.8653035877856,454.233184872372,52.9868432922107));
#44088=CARTESIAN_POINT('Ctrl Pts',(70.4605257438334,454.370754235697,55.4197172214916));
#44089=CARTESIAN_POINT('Ctrl Pts',(72.1379853470107,454.508323599022,57.2796485035691));
#44090=CARTESIAN_POINT('Ctrl Pts',(74.4967427405941,454.645892962347,58.121944651965));
#44091=CARTESIAN_POINT('Ctrl Pts',(76.9728107558315,454.783462325672,57.745441606262));
#44092=CARTESIAN_POINT('Ctrl Pts',(78.9745168891792,454.921031688998,56.2397260516373));
#44093=CARTESIAN_POINT('Ctrl Pts',(79.673244753992,455.012744597881,54.7236625281701));
#44094=CARTESIAN_POINT('Ctrl Pts',(79.822233556342,455.058601052323,53.9277333567095));
#44095=CARTESIAN_POINT('',(75.8251119125118,438.,48.1763335988071));
#44096=CARTESIAN_POINT('Ctrl Pts',(75.8251119125118,438.,48.1763335988069));
#44097=CARTESIAN_POINT('Ctrl Pts',(75.0271751381672,438.045856454442,48.0385010433052));
#44098=CARTESIAN_POINT('Ctrl Pts',(73.3626330146115,438.137569363325,48.1648685832922));
#44099=CARTESIAN_POINT('Ctrl Pts',(71.2535490842209,438.275138726651,49.5160797993085));
#44100=CARTESIAN_POINT('Ctrl Pts',(70.2293979957942,438.390995793545,51.3599960179249));
#44101=CARTESIAN_POINT('Ctrl Pts',(70.0701468767135,438.460996405998,52.5964026908782));
#44102=CARTESIAN_POINT('Ctrl Pts',(70.0700845742477,438.485140564009,53.0228422002615));
#44103=CARTESIAN_POINT('Ctrl Pts',(79.722466405091,455.,53.9090580914827));
#44104=CARTESIAN_POINT('Ctrl Pts',(79.5765523475055,454.954143545558,54.6885613368713));
#44105=CARTESIAN_POINT('Ctrl Pts',(79.2343983859504,454.908287091117,55.4309492773644));
#44106=CARTESIAN_POINT('Ctrl Pts',(78.736588725263,454.862430636675,56.0479168255346));
#44107=CARTESIAN_POINT('Ctrl Pts',(78.2387790645755,454.816574182233,56.6648843737049));
#44108=CARTESIAN_POINT('Ctrl Pts',(77.5853137047556,454.770717727791,57.1564315295522));
#44109=CARTESIAN_POINT('Ctrl Pts',(76.8544196323316,454.72486127335,57.4636606063962));
#44110=CARTESIAN_POINT('Ctrl Pts',(76.1235255599076,454.679004818908,57.7708896832402));
#44111=CARTESIAN_POINT('Ctrl Pts',(75.3152027748794,454.633148364466,57.8938006810809));
#44112=CARTESIAN_POINT('Ctrl Pts',(74.5260282619959,454.587291910025,57.8177706254244));
#44113=CARTESIAN_POINT('Ctrl Pts',(73.7368537491124,454.541435455583,57.7417405697679));
#44114=CARTESIAN_POINT('Ctrl Pts',(72.9668275083734,454.495579001141,57.4667694606141));
#44115=CARTESIAN_POINT('Ctrl Pts',(72.3080075277182,454.449722546699,57.0256927234369));
#44116=CARTESIAN_POINT('Ctrl Pts',(71.6491875470629,454.403866092258,56.5846159862597));
#44117=CARTESIAN_POINT('Ctrl Pts',(71.1015738264913,454.358009637816,55.9774336210589));
#44118=CARTESIAN_POINT('Ctrl Pts',(70.7306105819854,454.312153183374,55.2767314911749));
#44119=CARTESIAN_POINT('Ctrl Pts',(70.3649209659794,454.266948626145,54.5859905711328));
#44120=CARTESIAN_POINT('Ctrl Pts',(70.170894985723,454.221744068916,53.8043699479757));
#44121=CARTESIAN_POINT('Ctrl Pts',(70.170785177935,454.176539511687,53.0227998720929));
#44122=CARTESIAN_POINT('Ctrl Pts',(74.7983630544219,438.,48.2104548970641));
#44123=CARTESIAN_POINT('Ctrl Pts',(74.9465799254592,438.,48.1896568984132));
#44124=CARTESIAN_POINT('Ctrl Pts',(75.0957540366303,438.,48.1757286123456));
#44125=CARTESIAN_POINT('Ctrl Pts',(75.2453698829481,438.,48.1687204856835));
#44126=CARTESIAN_POINT('Ctrl Pts',(75.3943109611245,438.,48.1617439657043));
#44127=CARTESIAN_POINT('Ctrl Pts',(75.5436906225955,438.,48.161625107134));
#44128=CARTESIAN_POINT('Ctrl Pts',(75.6930137380414,438.,48.1684631220341));
#44129=CARTESIAN_POINT('Ctrl Pts',(75.7370555516977,438.,48.1704799469384));
#44130=CARTESIAN_POINT('Ctrl Pts',(75.7810924905272,438.,48.1731023005458));
#44131=CARTESIAN_POINT('Ctrl Pts',(75.8251119125118,438.,48.1763335988071));
#44132=CARTESIAN_POINT('Origin',(74.9879498948689,438.,53.0228109606356));
#44133=CARTESIAN_POINT('',(70.6773963296588,438.,50.6560254819444));
#44134=CARTESIAN_POINT('Ctrl Pts',(70.6773963296589,438.,50.6560254819442));
#44135=CARTESIAN_POINT('Ctrl Pts',(70.7621366228395,438.,50.5320627139349));
#44136=CARTESIAN_POINT('Ctrl Pts',(70.8523397873687,438.,50.4122232081957));
#44137=CARTESIAN_POINT('Ctrl Pts',(70.9477495550052,438.,50.2969251560475));
#44138=CARTESIAN_POINT('Ctrl Pts',(71.0421808602021,438.,50.1828095280492));
#44139=CARTESIAN_POINT('Ctrl Pts',(71.141713099239,438.,50.0731421574764));
#44140=CARTESIAN_POINT('Ctrl Pts',(71.2461307971266,438.,49.9683670778037));
#44141=CARTESIAN_POINT('Ctrl Pts',(71.278010555787,438.,49.9363782069402));
#44142=CARTESIAN_POINT('Ctrl Pts',(71.3103459100883,438.,49.9048456707748));
#44143=CARTESIAN_POINT('Ctrl Pts',(71.3431312258736,438.,49.8737829466856));
#44144=CARTESIAN_POINT('Origin',(74.9879498948689,438.,53.0228109606356));
#44145=CARTESIAN_POINT('Origin',(74.9879498948689,433.764859435991,53.0228109606356));
#44146=CARTESIAN_POINT('Ctrl Pts',(70.6773963296586,438.,50.6560254819443));
#44147=CARTESIAN_POINT('Ctrl Pts',(70.4537513653296,438.026322786249,51.0635801320965));
#44148=CARTESIAN_POINT('Ctrl Pts',(70.1589582985954,438.072942598246,51.8409980362099));
#44149=CARTESIAN_POINT('Ctrl Pts',(70.0700718391714,438.119562410242,52.6643217470763));
#44150=CARTESIAN_POINT('Ctrl Pts',(70.0701612938333,438.139859435991,53.0228096632581));
#44151=CARTESIAN_POINT('Ctrl Pts',(71.2663265142102,437.941398947677,49.8074256843371));
#44152=CARTESIAN_POINT('Ctrl Pts',(70.7369368452775,437.987255418033,50.4201637546089));
#44153=CARTESIAN_POINT('Ctrl Pts',(69.9872801539104,438.078968358746,51.9117019039279));
#44154=CARTESIAN_POINT('Ctrl Pts',(70.0581083962177,438.216537769815,54.4154980042378));
#44155=CARTESIAN_POINT('Ctrl Pts',(71.3075510106673,438.354107180884,56.586112001967));
#44156=CARTESIAN_POINT('Ctrl Pts',(73.4367474201414,438.491676591953,57.9050989515375));
#44157=CARTESIAN_POINT('Ctrl Pts',(75.9367802424272,438.629246003022,58.0569396214243));
#44158=CARTESIAN_POINT('Ctrl Pts',(78.2099924611958,438.766815414091,57.0054284326608));
#44159=CARTESIAN_POINT('Ctrl Pts',(79.7129963873825,438.90438482516,55.0018790181383));
#44160=CARTESIAN_POINT('Ctrl Pts',(80.0864990188232,439.041954236229,52.5252494404828));
#44161=CARTESIAN_POINT('Ctrl Pts',(79.2412191183861,439.179523647298,50.1675568417403));
#44162=CARTESIAN_POINT('Ctrl Pts',(77.3792153333098,439.317093058367,48.492400302215));
#44163=CARTESIAN_POINT('Ctrl Pts',(74.9455912824701,439.454662469436,47.9002160217303));
#44164=CARTESIAN_POINT('Ctrl Pts',(72.5220927714855,439.592231880505,48.5325636389322));
#44165=CARTESIAN_POINT('Ctrl Pts',(70.6880455611049,439.729801291574,50.2382831133303));
#44166=CARTESIAN_POINT('Ctrl Pts',(69.8818697359254,439.867370702643,52.6096306023301));
#44167=CARTESIAN_POINT('Ctrl Pts',(70.2962777667704,440.004940113712,55.0797468393278));
#44168=CARTESIAN_POINT('Ctrl Pts',(71.8322073992925,440.142509524781,57.0581624818043));
#44169=CARTESIAN_POINT('Ctrl Pts',(74.1225020644475,440.28007893585,58.0719467909454));
#44170=CARTESIAN_POINT('Ctrl Pts',(76.6196778606811,440.417648346919,57.8787595222969));
#44171=CARTESIAN_POINT('Ctrl Pts',(78.7267969530214,440.555217757988,56.5247811576843));
#44172=CARTESIAN_POINT('Ctrl Pts',(79.9401626795821,440.692787169057,54.3336736996951));
#44173=CARTESIAN_POINT('Ctrl Pts',(79.969725812863,440.830356580126,51.8292108229069));
#44174=CARTESIAN_POINT('Ctrl Pts',(78.8084194282583,440.967925991195,49.6100723052293));
#44175=CARTESIAN_POINT('Ctrl Pts',(76.7338482188175,441.105495402264,48.2067325114984));
#44176=CARTESIAN_POINT('Ctrl Pts',(74.2419284313758,441.243064813333,47.9546530544782));
#44177=CARTESIAN_POINT('Ctrl Pts',(71.928341478485,441.380634224401,48.9140923131546));
#44178=CARTESIAN_POINT('Ctrl Pts',(70.346139168261,441.518203635471,50.8557009578655));
#44179=CARTESIAN_POINT('Ctrl Pts',(69.8735393357385,441.655773046539,53.3153468018811));
#44180=CARTESIAN_POINT('Ctrl Pts',(70.6235146926476,441.793342457608,55.7050633632576));
#44181=CARTESIAN_POINT('Ctrl Pts',(72.4167872452805,441.930911868677,57.4536004179581));
#44182=CARTESIAN_POINT('Ctrl Pts',(74.8246838346499,442.068481279746,58.1429786121231));
#44183=CARTESIAN_POINT('Ctrl Pts',(77.2716083886679,442.206050690815,57.608405411681));
#44184=CARTESIAN_POINT('Ctrl Pts',(79.1726353884369,442.343620101884,55.9776679632129));
#44185=CARTESIAN_POINT('Ctrl Pts',(80.0733334938275,442.481189512953,53.6405861925782));
#44186=CARTESIAN_POINT('Ctrl Pts',(79.7583951646866,442.618758924023,51.1558282308192));
#44187=CARTESIAN_POINT('Ctrl Pts',(78.3031048903914,442.756328335091,49.1173634905726));
#44188=CARTESIAN_POINT('Ctrl Pts',(76.0553427955826,442.89389774616,48.0124771412913));
#44189=CARTESIAN_POINT('Ctrl Pts',(73.5524255733744,443.031467157229,48.1052869385125));
#44190=CARTESIAN_POINT('Ctrl Pts',(71.3926635200745,443.169036568298,49.3736071476132));
#44191=CARTESIAN_POINT('Ctrl Pts',(70.0923373430908,443.306605979367,51.5142519367218));
#44192=CARTESIAN_POINT('Ctrl Pts',(69.9622837466277,443.444175390436,54.0155104882782));
#44193=CARTESIAN_POINT('Ctrl Pts',(71.0335914159785,443.581744801505,56.279469003198));
#44194=CARTESIAN_POINT('Ctrl Pts',(73.0501694171724,443.719314212574,57.7649391122166));
#44195=CARTESIAN_POINT('Ctrl Pts',(75.5299645002191,443.856883623643,58.1168263466887));
#44196=CARTESIAN_POINT('Ctrl Pts',(77.8801936047136,443.994453034712,57.2510137595351));
#44197=CARTESIAN_POINT('Ctrl Pts',(79.5390457928333,444.132022445781,55.3744696759449));
#44198=CARTESIAN_POINT('Ctrl Pts',(80.1099804457359,444.26959185685,52.9357729129582));
#44199=CARTESIAN_POINT('Ctrl Pts',(79.4565183869152,444.407161267919,50.5178821756897));
#44200=CARTESIAN_POINT('Ctrl Pts',(77.7348665714272,444.544730678988,48.6987825891046));
#44201=CARTESIAN_POINT('Ctrl Pts',(75.3565775663022,444.682300090057,47.9133211401532));
#44202=CARTESIAN_POINT('Ctrl Pts',(72.8901698933421,444.819869501126,48.3492586017812));
#44203=CARTESIAN_POINT('Ctrl Pts',(70.9252264171065,444.957438912195,49.9023862252835));
#44204=CARTESIAN_POINT('Ctrl Pts',(69.9314574033058,445.095008323264,52.2014363393299));
#44205=CARTESIAN_POINT('Ctrl Pts',(70.1464185440873,445.232577734333,54.6968320970487));
#44206=CARTESIAN_POINT('Ctrl Pts',(71.5187244149973,445.370147145402,56.7920611719599));
#44207=CARTESIAN_POINT('Ctrl Pts',(73.7203319129862,445.507716556471,57.9862691540494));
#44208=CARTESIAN_POINT('Ctrl Pts',(76.2249573788151,445.64528596754,57.9939863820444));
#44209=CARTESIAN_POINT('Ctrl Pts',(78.4338821687736,445.782855378609,56.813368089795));
#44210=CARTESIAN_POINT('Ctrl Pts',(79.8190734602514,445.920424789678,54.7266353887282));
#44211=CARTESIAN_POINT('Ctrl Pts',(80.0494079525281,446.057994200747,52.2326116716488));
#44212=CARTESIAN_POINT('Ctrl Pts',(79.0698252955847,446.195563611816,49.927481285336));
#44213=CARTESIAN_POINT('Ctrl Pts',(77.1144900013488,446.333133022885,48.3622745364359));
#44214=CARTESIAN_POINT('Ctrl Pts',(74.6508155459415,446.470702433954,47.9111465529761));
#44215=CARTESIAN_POINT('Ctrl Pts',(72.2677314314422,446.608271845023,48.6819373046774));
#44216=CARTESIAN_POINT('Ctrl Pts',(70.5349024274333,446.745841256092,50.4903929780497));
#44217=CARTESIAN_POINT('Ctrl Pts',(69.8665529539796,446.883410667161,52.9042109622857));
#44218=CARTESIAN_POINT('Ctrl Pts',(70.4224487308386,447.02098007823,55.3463797043995));
#44219=CARTESIAN_POINT('Ctrl Pts',(72.069705552325,447.158549489299,57.2331105394031));
#44220=CARTESIAN_POINT('Ctrl Pts',(74.4145546160935,447.296118900368,58.1133895564375));
#44221=CARTESIAN_POINT('Ctrl Pts',(76.8964710571215,447.433688311437,57.7767902999883));
#44222=CARTESIAN_POINT('Ctrl Pts',(78.9221647146049,447.571257722506,56.3037751996861));
#44223=CARTESIAN_POINT('Ctrl Pts',(80.0074032848607,447.708827133575,54.0464614143837));
#44224=CARTESIAN_POINT('Ctrl Pts',(79.8927657192128,447.846396544644,51.5444489227623));
#44225=CARTESIAN_POINT('Ctrl Pts',(78.605655575103,447.983965955713,49.3958317496446));
#44226=CARTESIAN_POINT('Ctrl Pts',(76.4537503277871,448.121535366782,48.1142264725559));
#44227=CARTESIAN_POINT('Ctrl Pts',(73.9514525530772,448.259104777851,48.0059946548279));
#44228=CARTESIAN_POINT('Ctrl Pts',(71.6969244713428,448.39667418892,49.0970085907417));
#44229=CARTESIAN_POINT('Ctrl Pts',(70.2291001522561,448.534243599989,51.1264666583019));
#44230=CARTESIAN_POINT('Ctrl Pts',(69.8988559234434,448.671813011058,53.6092366897432));
#44231=CARTESIAN_POINT('Ctrl Pts',(70.7851350758139,448.809382422127,55.9518244775881));
#44232=CARTESIAN_POINT('Ctrl Pts',(72.6760768504256,448.946951833196,57.594245703923));
#44233=CARTESIAN_POINT('Ctrl Pts',(75.1196607316056,449.084521244265,58.1438874921126));
#44234=CARTESIAN_POINT('Ctrl Pts',(77.5317597721941,449.222090655334,57.469360622315));
#44235=CARTESIAN_POINT('Ctrl Pts',(79.3357733243977,449.359660066403,55.7319074911046));
#44236=CARTESIAN_POINT('Ctrl Pts',(80.1004606450606,449.497229477472,53.3468578938625));
#44237=CARTESIAN_POINT('Ctrl Pts',(79.6430269164599,449.634798888541,50.8843464393459));
#44238=CARTESIAN_POINT('Ctrl Pts',(78.0728194662947,449.77236829961,48.9330246198776));
#44239=CARTESIAN_POINT('Ctrl Pts',(75.7651888161234,449.909937710679,47.9593465097831));
#44240=CARTESIAN_POINT('Ctrl Pts',(73.2717629486147,450.047507121747,48.1960651675296));
#44241=CARTESIAN_POINT('Ctrl Pts',(71.1885832974899,450.185076532817,49.586594139118));
#44242=CARTESIAN_POINT('Ctrl Pts',(70.013623916093,450.322645943885,51.7985341771286));
#44243=CARTESIAN_POINT('Ctrl Pts',(70.0277531804915,450.460215354954,54.3031316784399));
#44244=CARTESIAN_POINT('Ctrl Pts',(71.2275935581432,450.597784766023,56.5016746841243));
#44245=CARTESIAN_POINT('Ctrl Pts',(73.326328990768,450.735354177093,57.8686120870556));
#44246=CARTESIAN_POINT('Ctrl Pts',(75.8222668904432,450.872923588161,58.0771840905751));
#44247=CARTESIAN_POINT('Ctrl Pts',(78.1187653342674,451.01049299923,57.0775325626919));
#44248=CARTESIAN_POINT('Ctrl Pts',(79.6668574398354,451.148062410299,55.1086193821872));
#44249=CARTESIAN_POINT('Ctrl Pts',(80.096479252104,451.285631821368,52.6411037534401));
#44250=CARTESIAN_POINT('Ctrl Pts',(79.304931747903,451.423201232437,50.2648333925011));
#44251=CARTESIAN_POINT('Ctrl Pts',(77.4814305423453,451.560770643506,48.547844274008));
#44252=CARTESIAN_POINT('Ctrl Pts',(75.0618748081809,451.698340054575,47.9005743697575));
#44253=CARTESIAN_POINT('Ctrl Pts',(72.6246476798502,451.835909465644,48.4777504300927));
#44254=CARTESIAN_POINT('Ctrl Pts',(70.7523565534021,451.973478876713,50.1414013001772));
#44255=CARTESIAN_POINT('Ctrl Pts',(69.8925635969428,452.111048287782,52.493839259314));
#44256=CARTESIAN_POINT('Ctrl Pts',(70.2507981720304,452.248617698851,54.9727253537667));
#44257=CARTESIAN_POINT('Ctrl Pts',(71.7414260302598,452.38618710992,56.9854938121638));
#44258=CARTESIAN_POINT('Ctrl Pts',(74.0081197682281,452.523756520989,58.0510020380353));
#44259=CARTESIAN_POINT('Ctrl Pts',(76.509037174062,452.661325932058,57.9145454249311));
#44260=CARTESIAN_POINT('Ctrl Pts',(78.646345999496,452.798895343127,56.6087432716859));
#44261=CARTESIAN_POINT('Ctrl Pts',(79.9091328695011,452.936464754196,54.4457412810724));
#44262=CARTESIAN_POINT('Ctrl Pts',(79.9955346778371,453.074034165265,51.9425946677425));
#44263=CARTESIAN_POINT('Ctrl Pts',(78.884897471774,453.211603576334,49.6976685283788));
#44264=CARTESIAN_POINT('Ctrl Pts',(76.842713757919,453.349172987403,48.2476017112594));
#44265=CARTESIAN_POINT('Ctrl Pts',(74.357157626194,453.486742398472,47.9390255330312));
#44266=CARTESIAN_POINT('Ctrl Pts',(72.0223894626918,453.624311809541,48.8457040127446));
#44267=CARTESIAN_POINT('Ctrl Pts',(70.3965239417743,453.76188122061,50.7508992351417));
#44268=CARTESIAN_POINT('Ctrl Pts',(69.8682172124607,453.899450631679,53.1991852682697));
#44269=CARTESIAN_POINT('Ctrl Pts',(70.5637564965961,454.037020042748,55.6053073318474));
#44270=CARTESIAN_POINT('Ctrl Pts',(72.3168804345463,454.174589453817,57.394102321988));
#44271=CARTESIAN_POINT('Ctrl Pts',(74.708503577028,454.312158864886,58.1379492928087));
#44272=CARTESIAN_POINT('Ctrl Pts',(77.1669384806062,454.449728275955,57.6590781969942));
#44273=CARTESIAN_POINT('Ctrl Pts',(79.104460246599,454.587297687024,56.0718752075947));
#44274=CARTESIAN_POINT('Ctrl Pts',(80.0579990258397,454.724867098093,53.7559659325096));
#44275=CARTESIAN_POINT('Ctrl Pts',(79.7993737921405,454.862436509162,51.264555781545));
#44276=CARTESIAN_POINT('Ctrl Pts',(78.8603172683709,454.954149449875,49.8843949028968));
#44277=CARTESIAN_POINT('Ctrl Pts',(78.2550383520211,455.000005920231,49.3464926833852));
#44278=CARTESIAN_POINT('Ctrl Pts',(71.2919280847647,437.960932631785,49.8295447717866));
#44279=CARTESIAN_POINT('Ctrl Pts',(70.7661801618051,438.006789102141,50.4380677307123));
#44280=CARTESIAN_POINT('Ctrl Pts',(70.0216804642315,438.098502042854,51.9193453793684));
#44281=CARTESIAN_POINT('Ctrl Pts',(70.0920214691003,438.236071453923,54.4059175142311));
#44282=CARTESIAN_POINT('Ctrl Pts',(71.3328689921139,438.373640864992,56.5615995530474));
#44283=CARTESIAN_POINT('Ctrl Pts',(73.4474183600886,438.51121027606,57.8715130059215));
#44284=CARTESIAN_POINT('Ctrl Pts',(75.9302531050459,438.64877968713,58.0223091424889));
#44285=CARTESIAN_POINT('Ctrl Pts',(78.187827577312,438.786349098198,56.9780314470519));
#44286=CARTESIAN_POINT('Ctrl Pts',(79.6804921281445,438.923918509268,54.9882647306826));
#44287=CARTESIAN_POINT('Ctrl Pts',(80.0514253824632,439.061487920337,52.5286722361449));
#44288=CARTESIAN_POINT('Ctrl Pts',(79.2119602813209,439.199057331405,50.1871985363179));
#44289=CARTESIAN_POINT('Ctrl Pts',(77.3627654821092,439.336626742474,48.5235656341814));
#44290=CARTESIAN_POINT('Ctrl Pts',(74.945882673321,439.474196153543,47.9354550726326));
#44291=CARTESIAN_POINT('Ctrl Pts',(72.5390557493757,439.611765564612,48.5634526816578));
#44292=CARTESIAN_POINT('Ctrl Pts',(70.7176252076512,439.749334975681,50.2574382719404));
#44293=CARTESIAN_POINT('Ctrl Pts',(69.9169951793341,439.88690438675,52.6124729281146));
#44294=CARTESIAN_POINT('Ctrl Pts',(70.3285524390626,440.024473797819,55.0655968881807));
#44295=CARTESIAN_POINT('Ctrl Pts',(71.8539161956667,440.162043208888,57.0304027312562));
#44296=CARTESIAN_POINT('Ctrl Pts',(74.1284556017685,440.299612619957,58.0372130755806));
#44297=CARTESIAN_POINT('Ctrl Pts',(76.6084529745575,440.437182031026,57.8453547693184));
#44298=CARTESIAN_POINT('Ctrl Pts',(78.7010768983675,440.574751442095,56.5006906122666));
#44299=CARTESIAN_POINT('Ctrl Pts',(79.9060957114769,440.712320853164,54.3246560905852));
#44300=CARTESIAN_POINT('Ctrl Pts',(79.9354554758069,440.849890264234,51.8374217660934));
#44301=CARTESIAN_POINT('Ctrl Pts',(78.7821378811198,440.987459675302,49.6335490143246));
#44302=CARTESIAN_POINT('Ctrl Pts',(76.7218379387462,441.125029086371,48.2398629923665));
#44303=CARTESIAN_POINT('Ctrl Pts',(74.2470604179255,441.26259849744,47.9895176253775));
#44304=CARTESIAN_POINT('Ctrl Pts',(71.9493889550104,441.400167908509,48.9423567664812));
#44305=CARTESIAN_POINT('Ctrl Pts',(70.3780708369611,441.537737319578,50.8706088123044));
#44306=CARTESIAN_POINT('Ctrl Pts',(69.9087220851415,441.675306730647,53.313334406694));
#44307=CARTESIAN_POINT('Ctrl Pts',(70.6535382561121,441.812876141716,55.686611771813));
#44308=CARTESIAN_POINT('Ctrl Pts',(72.434474634693,441.950445552785,57.4231203942423));
#44309=CARTESIAN_POINT('Ctrl Pts',(74.8258069648359,442.088014963854,58.1077562588723));
#44310=CARTESIAN_POINT('Ctrl Pts',(77.2558987807707,442.225584374923,57.5768604626454));
#44311=CARTESIAN_POINT('Ctrl Pts',(79.1438483484939,442.363153785992,55.9573410863927));
#44312=CARTESIAN_POINT('Ctrl Pts',(80.0383504249652,442.500723197061,53.6363364298888));
#44313=CARTESIAN_POINT('Ctrl Pts',(79.7255786008758,442.63829260813,51.1686714675448));
#44314=CARTESIAN_POINT('Ctrl Pts',(78.2802994730141,442.775862019199,49.1442296128866));
#44315=CARTESIAN_POINT('Ctrl Pts',(76.0480000497264,442.913431430268,48.0469439321665));
#44316=CARTESIAN_POINT('Ctrl Pts',(73.5623007470393,443.051000841337,48.1391152777421));
#44317=CARTESIAN_POINT('Ctrl Pts',(71.4173960006007,443.188570252406,49.3987105337786));
#44318=CARTESIAN_POINT('Ctrl Pts',(70.1260149502347,443.326139663475,51.5246295263745));
#44319=CARTESIAN_POINT('Ctrl Pts',(69.9968560107494,443.463709074544,54.0086815686384));
#44320=CARTESIAN_POINT('Ctrl Pts',(71.0607940039999,443.601278485613,56.2570659945857));
#44321=CARTESIAN_POINT('Ctrl Pts',(73.0634996815609,443.738847896682,57.7323173458439));
#44322=CARTESIAN_POINT('Ctrl Pts',(75.5262359055331,443.876417307751,58.0817838985492));
#44323=CARTESIAN_POINT('Ctrl Pts',(77.8602974535386,444.01398671882,57.2219273579296));
#44324=CARTESIAN_POINT('Ctrl Pts',(79.5077381641954,444.151556129889,55.358292284962));
#44325=CARTESIAN_POINT('Ctrl Pts',(80.0747452773383,444.289125540958,52.936371659927));
#44326=CARTESIAN_POINT('Ctrl Pts',(79.4257784759072,444.426694952027,50.5351139330338));
#44327=CARTESIAN_POINT('Ctrl Pts',(77.7159701453494,444.564264363096,48.7285281882989));
#44328=CARTESIAN_POINT('Ctrl Pts',(75.3540417247156,444.701833774165,47.9484700391031));
#44329=CARTESIAN_POINT('Ctrl Pts',(72.9046008169535,444.839403185234,48.3814086256329));
#44330=CARTESIAN_POINT('Ctrl Pts',(70.9531744631929,444.976972596303,49.9238520658189));
#44331=CARTESIAN_POINT('Ctrl Pts',(69.9662417261778,445.114542007372,52.2070866908481));
#44332=CARTESIAN_POINT('Ctrl Pts',(70.1797241190449,445.252111418441,54.6853162702576));
#44333=CARTESIAN_POINT('Ctrl Pts',(71.5425897049011,445.38968082951,56.7661319697402));
#44334=CARTESIAN_POINT('Ctrl Pts',(73.7290520353306,445.527250240579,57.9521248271964));
#44335=CARTESIAN_POINT('Ctrl Pts',(76.2164478303903,445.664819651648,57.959788967295));
#44336=CARTESIAN_POINT('Ctrl Pts',(78.410177116109,445.802389062717,56.7872923142914));
#44337=CARTESIAN_POINT('Ctrl Pts',(79.785839481913,445.939958473786,54.7149145409028));
#44338=CARTESIAN_POINT('Ctrl Pts',(80.0145894708287,446.077527884854,52.2380475636723));
#44339=CARTESIAN_POINT('Ctrl Pts',(79.0417455007272,446.215097295924,49.9487744934246));
#44340=CARTESIAN_POINT('Ctrl Pts',(77.0998612329313,446.352666706993,48.3943350218429));
#44341=CARTESIAN_POINT('Ctrl Pts',(74.6531347405342,446.490236118061,47.946310411217));
#44342=CARTESIAN_POINT('Ctrl Pts',(72.2864441967577,446.627805529131,48.711798784952));
#44343=CARTESIAN_POINT('Ctrl Pts',(70.5655355671304,446.7653749402,50.5078138374498));
#44344=CARTESIAN_POINT('Ctrl Pts',(69.9017837636851,446.902944351269,52.9050268283514));
#44345=CARTESIAN_POINT('Ctrl Pts',(70.4538554553274,447.040513762338,55.3303955482807));
#44346=CARTESIAN_POINT('Ctrl Pts',(72.0897805655085,447.178083173406,57.2041472965662));
#44347=CARTESIAN_POINT('Ctrl Pts',(74.4184990828446,447.315652584475,58.0783707504614));
#44348=CARTESIAN_POINT('Ctrl Pts',(76.8833420716781,447.453221995544,57.7440870076285));
#44349=CARTESIAN_POINT('Ctrl Pts',(78.8951006976473,447.590791406614,56.2812049853304));
#44350=CARTESIAN_POINT('Ctrl Pts',(79.9728737591767,447.728360817682,54.039419578971));
#44351=CARTESIAN_POINT('Ctrl Pts',(79.8590248014627,447.865930228751,51.5546187831019));
#44352=CARTESIAN_POINT('Ctrl Pts',(78.5807688690222,448.00349963982,49.4207822496474));
#44353=CARTESIAN_POINT('Ctrl Pts',(76.4436668804944,448.141069050889,48.1479933154738));
#44354=CARTESIAN_POINT('Ctrl Pts',(73.9585827640392,448.278638461958,48.040506039639));
#44355=CARTESIAN_POINT('Ctrl Pts',(71.7195638980013,448.416207873027,49.1240147372739));
#44356=CARTESIAN_POINT('Ctrl Pts',(70.2618369488048,448.553777284096,51.1395118774135));
#44357=CARTESIAN_POINT('Ctrl Pts',(69.9338645164797,448.691346695165,53.6052025846919));
#44358=CARTESIAN_POINT('Ctrl Pts',(70.8140468299362,448.828916106234,55.9316753817396));
#44359=CARTESIAN_POINT('Ctrl Pts',(72.6919805501841,448.966485517303,57.5627981615082));
#44360=CARTESIAN_POINT('Ctrl Pts',(75.1187546742391,449.104054928372,58.1086588865485));
#44361=CARTESIAN_POINT('Ctrl Pts',(77.5142605463483,449.241624339441,57.4387721819374));
#44362=CARTESIAN_POINT('Ctrl Pts',(79.3058640356535,449.37919375051,55.7132712351298));
#44363=CARTESIAN_POINT('Ctrl Pts',(80.0652909647104,449.516763161579,53.3446287294427));
#44364=CARTESIAN_POINT('Ctrl Pts',(79.6110039870512,449.654332572648,50.8990572374897));
#44365=CARTESIAN_POINT('Ctrl Pts',(78.0515982147316,449.791901983717,48.9611588352041));
#44366=CARTESIAN_POINT('Ctrl Pts',(75.7598420802921,449.929471394786,47.9941787937435));
#44367=CARTESIAN_POINT('Ctrl Pts',(73.2835688399409,450.067040805855,48.229269030557));
#44368=CARTESIAN_POINT('Ctrl Pts',(71.2147196745641,450.204610216924,49.6102323578195));
#44369=CARTESIAN_POINT('Ctrl Pts',(70.0478430039696,450.342179627993,51.806956149275));
#44370=CARTESIAN_POINT('Ctrl Pts',(70.0618750711716,450.479749039062,54.2943241721889));
#44371=CARTESIAN_POINT('Ctrl Pts',(71.2534615781489,450.617318450131,56.4777430913874));
#44372=CARTESIAN_POINT('Ctrl Pts',(73.3377595146173,450.7548878612,57.835277139711));
#44373=CARTESIAN_POINT('Ctrl Pts',(75.8165275065125,450.892457272269,58.0424143470898));
#44374=CARTESIAN_POINT('Ctrl Pts',(78.0972280146179,451.030026683338,57.0496395626336));
#44375=CARTESIAN_POINT('Ctrl Pts',(79.6346705769054,451.167596094407,55.0942708127578));
#44376=CARTESIAN_POINT('Ctrl Pts',(80.0613369603159,451.305165505476,52.6437295709924));
#44377=CARTESIAN_POINT('Ctrl Pts',(79.2752346227003,451.442734916545,50.2838059080074));
#44378=CARTESIAN_POINT('Ctrl Pts',(77.4642775383486,451.580304327614,48.5786281990962));
#44379=CARTESIAN_POINT('Ctrl Pts',(75.0613662683072,451.717873738683,47.9358109555334));
#44380=CARTESIAN_POINT('Ctrl Pts',(72.6409051681049,451.855443149752,48.5090165405895));
#44381=CARTESIAN_POINT('Ctrl Pts',(70.7814937955892,451.993012560821,50.1612229224031));
#44382=CARTESIAN_POINT('Ctrl Pts',(69.9276154757779,452.13058197189,52.4974781300291));
#44383=CARTESIAN_POINT('Ctrl Pts',(70.28338570485,452.268151382959,54.9593116184677));
#44384=CARTESIAN_POINT('Ctrl Pts',(71.7637593244369,452.405720794028,56.9582339596125));
#44385=CARTESIAN_POINT('Ctrl Pts',(74.0148601574488,452.543290205097,58.0164124045709));
#44386=CARTESIAN_POINT('Ctrl Pts',(76.4985734007796,452.680859616166,57.8808944956963));
#44387=CARTESIAN_POINT('Ctrl Pts',(78.6211793782641,452.818429027235,56.5840751390796));
#44388=CARTESIAN_POINT('Ctrl Pts',(79.8752793598227,452.955998438304,54.4359527433117));
#44389=CARTESIAN_POINT('Ctrl Pts',(79.9610867979697,453.093567849373,51.9500256275167));
#44390=CARTESIAN_POINT('Ctrl Pts',(78.8580898214202,453.231137260442,49.7205426507378));
#44391=CARTESIAN_POINT('Ctrl Pts',(76.829954576496,453.368706671511,48.2804510471555));
#44392=CARTESIAN_POINT('Ctrl Pts',(74.3614969349096,453.50627608258,47.9739976078481));
#44393=CARTESIAN_POINT('Ctrl Pts',(72.0427899699093,453.643845493649,48.8744389188063));
#44394=CARTESIAN_POINT('Ctrl Pts',(70.4281090065325,453.781414904718,50.7665280353679));
#44395=CARTESIAN_POINT('Ctrl Pts',(69.9034365734981,453.918984315787,53.1979719646065));
#44396=CARTESIAN_POINT('Ctrl Pts',(70.5941911450941,454.056553726855,55.5875419761702));
#44397=CARTESIAN_POINT('Ctrl Pts',(72.3352550969583,454.194123137925,57.3640315940408));
#44398=CARTESIAN_POINT('Ctrl Pts',(74.710425927543,454.331692548993,58.1027615369526));
#44399=CARTESIAN_POINT('Ctrl Pts',(77.1519489117248,454.469261960063,57.627184662743));
#44400=CARTESIAN_POINT('Ctrl Pts',(79.0761421930432,454.606831371131,56.0509002658933));
#44401=CARTESIAN_POINT('Ctrl Pts',(80.023121444939,454.744400782201,53.7509224563649));
#44402=CARTESIAN_POINT('Ctrl Pts',(79.7662753305892,454.881970193269,51.2766510661603));
#44403=CARTESIAN_POINT('Ctrl Pts',(78.8336787086927,454.973683133982,49.9059845082687));
#44404=CARTESIAN_POINT('Ctrl Pts',(78.2325635911202,455.019539604339,49.3717825937627));
#44405=CARTESIAN_POINT('Ctrl Pts',(71.3175296553191,437.980466315892,49.8516638592361));
#44406=CARTESIAN_POINT('Ctrl Pts',(70.7954234783326,438.026322786249,50.4559717068158));
#44407=CARTESIAN_POINT('Ctrl Pts',(70.0560807745525,438.118035726961,51.9269888548089));
#44408=CARTESIAN_POINT('Ctrl Pts',(70.125934541983,438.25560513803,54.3963370242244));
#44409=CARTESIAN_POINT('Ctrl Pts',(71.3581869735604,438.393174549099,56.5370871041277));
#44410=CARTESIAN_POINT('Ctrl Pts',(73.4580893000358,438.530743960168,57.8379270603054));
#44411=CARTESIAN_POINT('Ctrl Pts',(75.9237259676645,438.668313371237,57.9876786635535));
#44412=CARTESIAN_POINT('Ctrl Pts',(78.1656626934283,438.805882782306,56.9506344614431));
#44413=CARTESIAN_POINT('Ctrl Pts',(79.6479878689065,438.943452193375,54.9746504432268));
#44414=CARTESIAN_POINT('Ctrl Pts',(80.0163517461031,439.081021604444,52.5320950318071));
#44415=CARTESIAN_POINT('Ctrl Pts',(79.1827014442556,439.218591015513,50.2068402308956));
#44416=CARTESIAN_POINT('Ctrl Pts',(77.3463156309085,439.356160426582,48.5547309661478));
#44417=CARTESIAN_POINT('Ctrl Pts',(74.946174064172,439.493729837651,47.9706941235349));
#44418=CARTESIAN_POINT('Ctrl Pts',(72.5560187272658,439.63129924872,48.5943417243833));
#44419=CARTESIAN_POINT('Ctrl Pts',(70.7472048541975,439.768868659789,50.2765934305506));
#44420=CARTESIAN_POINT('Ctrl Pts',(69.9521206227429,439.906438070858,52.615315253899));
#44421=CARTESIAN_POINT('Ctrl Pts',(70.3608271113549,440.044007481927,55.0514469370336));
#44422=CARTESIAN_POINT('Ctrl Pts',(71.8756249920409,440.181576892996,57.002642980708));
#44423=CARTESIAN_POINT('Ctrl Pts',(74.1344091390896,440.319146304065,58.0024793602158));
#44424=CARTESIAN_POINT('Ctrl Pts',(76.597228088434,440.456715715134,57.8119500163398));
#44425=CARTESIAN_POINT('Ctrl Pts',(78.6753568437137,440.594285126203,56.4766000668489));
#44426=CARTESIAN_POINT('Ctrl Pts',(79.8720287433716,440.731854537272,54.3156384814752));
#44427=CARTESIAN_POINT('Ctrl Pts',(79.9011851387508,440.869423948341,51.8456327092798));
#44428=CARTESIAN_POINT('Ctrl Pts',(78.7558563339814,441.00699335941,49.65702572342));
#44429=CARTESIAN_POINT('Ctrl Pts',(76.709827658675,441.144562770479,48.2729934732346));
#44430=CARTESIAN_POINT('Ctrl Pts',(74.2521924044753,441.282132181548,48.0243821962769));
#44431=CARTESIAN_POINT('Ctrl Pts',(71.9704364315359,441.419701592617,48.9706212198079));
#44432=CARTESIAN_POINT('Ctrl Pts',(70.4100025056612,441.557271003686,50.8855166667433));
#44433=CARTESIAN_POINT('Ctrl Pts',(69.9439048345445,441.694840414755,53.311322011507));
#44434=CARTESIAN_POINT('Ctrl Pts',(70.6835618195766,441.832409825824,55.6681601803684));
#44435=CARTESIAN_POINT('Ctrl Pts',(72.4521620241055,441.969979236893,57.3926403705265));
#44436=CARTESIAN_POINT('Ctrl Pts',(74.8269300950219,442.107548647962,58.0725339056214));
#44437=CARTESIAN_POINT('Ctrl Pts',(77.2401891728734,442.245118059031,57.5453155136098));
#44438=CARTESIAN_POINT('Ctrl Pts',(79.1150613085509,442.3826874701,55.9370142095725));
#44439=CARTESIAN_POINT('Ctrl Pts',(80.0033673561028,442.520256881169,53.6320866671993));
#44440=CARTESIAN_POINT('Ctrl Pts',(79.6927620370649,442.657826292238,51.1815147042704));
#44441=CARTESIAN_POINT('Ctrl Pts',(78.2574940556369,442.795395703307,49.1710957352006));
#44442=CARTESIAN_POINT('Ctrl Pts',(76.0406573038701,442.932965114376,48.0814107230417));
#44443=CARTESIAN_POINT('Ctrl Pts',(73.5721759207042,443.070534525445,48.1729436169717));
#44444=CARTESIAN_POINT('Ctrl Pts',(71.4421284811268,443.208103936514,49.4238139199439));
#44445=CARTESIAN_POINT('Ctrl Pts',(70.1596925573787,443.345673347583,51.5350071160272));
#44446=CARTESIAN_POINT('Ctrl Pts',(70.031428274871,443.483242758652,54.0018526489985));
#44447=CARTESIAN_POINT('Ctrl Pts',(71.0879965920213,443.620812169721,56.2346629859735));
#44448=CARTESIAN_POINT('Ctrl Pts',(73.0768299459495,443.75838158079,57.6996955794712));
#44449=CARTESIAN_POINT('Ctrl Pts',(75.5225073108471,443.895950991858,58.0467414504097));
#44450=CARTESIAN_POINT('Ctrl Pts',(77.8404013023635,444.033520402927,57.192840956324));
#44451=CARTESIAN_POINT('Ctrl Pts',(79.4764305355575,444.171089813996,55.3421148939791));
#44452=CARTESIAN_POINT('Ctrl Pts',(80.0395101089407,444.308659225066,52.936970406896));
#44453=CARTESIAN_POINT('Ctrl Pts',(79.3950385648993,444.446228636135,50.5523456903779));
#44454=CARTESIAN_POINT('Ctrl Pts',(77.6970737192715,444.583798047203,48.7582737874932));
#44455=CARTESIAN_POINT('Ctrl Pts',(75.3515058831289,444.721367458273,47.983618938053));
#44456=CARTESIAN_POINT('Ctrl Pts',(72.919031740565,444.858936869342,48.4135586494846));
#44457=CARTESIAN_POINT('Ctrl Pts',(70.9811225092794,444.99650628041,49.9453179063543));
#44458=CARTESIAN_POINT('Ctrl Pts',(70.0010260490498,445.13407569148,52.2127370423663));
#44459=CARTESIAN_POINT('Ctrl Pts',(70.2130296940026,445.271645102548,54.6738004434664));
#44460=CARTESIAN_POINT('Ctrl Pts',(71.5664549948049,445.409214513617,56.7402027675205));
#44461=CARTESIAN_POINT('Ctrl Pts',(73.7377721576751,445.546783924686,57.9179805003435));
#44462=CARTESIAN_POINT('Ctrl Pts',(76.2079382819655,445.684353335755,57.9255915525455));
#44463=CARTESIAN_POINT('Ctrl Pts',(78.3864720634444,445.821922746824,56.7612165387878));
#44464=CARTESIAN_POINT('Ctrl Pts',(79.7526055035746,445.959492157893,54.7031936930774));
#44465=CARTESIAN_POINT('Ctrl Pts',(79.9797709891293,446.097061568962,52.2434834556957));
#44466=CARTESIAN_POINT('Ctrl Pts',(79.0136657058697,446.234630980031,49.9700677015131));
#44467=CARTESIAN_POINT('Ctrl Pts',(77.0852324645138,446.3722003911,48.4263955072499));
#44468=CARTESIAN_POINT('Ctrl Pts',(74.6554539351268,446.509769802169,47.9814742694579));
#44469=CARTESIAN_POINT('Ctrl Pts',(72.3051569620732,446.647339213238,48.7416602652266));
#44470=CARTESIAN_POINT('Ctrl Pts',(70.5961687068276,446.784908624307,50.5252346968499));
#44471=CARTESIAN_POINT('Ctrl Pts',(69.9370145733906,446.922478035376,52.9058426944171));
#44472=CARTESIAN_POINT('Ctrl Pts',(70.4852621798161,447.060047446445,55.314411392162));
#44473=CARTESIAN_POINT('Ctrl Pts',(72.109855578692,447.197616857514,57.1751840537294));
#44474=CARTESIAN_POINT('Ctrl Pts',(74.4224435495957,447.335186268583,58.0433519444853));
#44475=CARTESIAN_POINT('Ctrl Pts',(76.8702130862349,447.472755679652,57.7113837152687));
#44476=CARTESIAN_POINT('Ctrl Pts',(78.8680366806898,447.610325090721,56.2586347709747));
#44477=CARTESIAN_POINT('Ctrl Pts',(79.9383442334927,447.74789450179,54.0323777435583));
#44478=CARTESIAN_POINT('Ctrl Pts',(79.8252838837127,447.885463912859,51.5647886434414));
#44479=CARTESIAN_POINT('Ctrl Pts',(78.5558821629415,448.023033323928,49.4457327496502));
#44480=CARTESIAN_POINT('Ctrl Pts',(76.4335834332017,448.160602734997,48.1817601583917));
#44481=CARTESIAN_POINT('Ctrl Pts',(73.9657129750013,448.298172146066,48.0750174244501));
#44482=CARTESIAN_POINT('Ctrl Pts',(71.7422033246598,448.435741557135,49.1510208838061));
#44483=CARTESIAN_POINT('Ctrl Pts',(70.2945737453536,448.573310968204,51.1525570965252));
#44484=CARTESIAN_POINT('Ctrl Pts',(69.9688731095159,448.710880379273,53.6011684796407));
#44485=CARTESIAN_POINT('Ctrl Pts',(70.8429585840585,448.848449790342,55.911526285891));
#44486=CARTESIAN_POINT('Ctrl Pts',(72.7078842499427,448.986019201411,57.5313506190933));
#44487=CARTESIAN_POINT('Ctrl Pts',(75.1178486168725,449.12358861248,58.0734302809844));
#44488=CARTESIAN_POINT('Ctrl Pts',(77.4967613205024,449.261158023549,57.4081837415597));
#44489=CARTESIAN_POINT('Ctrl Pts',(79.2759547469092,449.398727434618,55.694634979155));
#44490=CARTESIAN_POINT('Ctrl Pts',(80.0301212843603,449.536296845687,53.342399565023));
#44491=CARTESIAN_POINT('Ctrl Pts',(79.5789810576424,449.673866256756,50.9137680356334));
#44492=CARTESIAN_POINT('Ctrl Pts',(78.0303769631685,449.811435667825,48.9892930505306));
#44493=CARTESIAN_POINT('Ctrl Pts',(75.7544953444607,449.949005078894,48.0290110777038));
#44494=CARTESIAN_POINT('Ctrl Pts',(73.2953747312671,450.086574489963,48.2624728935843));
#44495=CARTESIAN_POINT('Ctrl Pts',(71.2408560516383,450.224143901032,49.633870576521));
#44496=CARTESIAN_POINT('Ctrl Pts',(70.0820620918462,450.361713312101,51.8153781214214));
#44497=CARTESIAN_POINT('Ctrl Pts',(70.0959969618516,450.49928272317,54.2855166659378));
#44498=CARTESIAN_POINT('Ctrl Pts',(71.2793295981546,450.636852134239,56.4538114986504));
#44499=CARTESIAN_POINT('Ctrl Pts',(73.3491900384668,450.774421545308,57.8019421923663));
#44500=CARTESIAN_POINT('Ctrl Pts',(75.8107881225818,450.911990956377,58.0076446036044));
#44501=CARTESIAN_POINT('Ctrl Pts',(78.0756906949682,451.049560367446,57.0217465625752));
#44502=CARTESIAN_POINT('Ctrl Pts',(79.6024837139754,451.187129778515,55.0799222433284));
#44503=CARTESIAN_POINT('Ctrl Pts',(80.0261946685277,451.324699189584,52.6463553885448));
#44504=CARTESIAN_POINT('Ctrl Pts',(79.2455374974976,451.462268600653,50.3027784235138));
#44505=CARTESIAN_POINT('Ctrl Pts',(77.4471245343519,451.599838011722,48.6094121241844));
#44506=CARTESIAN_POINT('Ctrl Pts',(75.0608577284335,451.737407422791,47.9710475413092));
#44507=CARTESIAN_POINT('Ctrl Pts',(72.6571626563595,451.874976833859,48.5402826510862));
#44508=CARTESIAN_POINT('Ctrl Pts',(70.8106310377763,452.012546244929,50.181044544629));
#44509=CARTESIAN_POINT('Ctrl Pts',(69.962667354613,452.150115655997,52.5011170007442));
#44510=CARTESIAN_POINT('Ctrl Pts',(70.3159732376696,452.287685067066,54.9458978831686));
#44511=CARTESIAN_POINT('Ctrl Pts',(71.7860926186139,452.425254478135,56.9309741070612));
#44512=CARTESIAN_POINT('Ctrl Pts',(74.0216005466695,452.562823889204,57.9818227711066));
#44513=CARTESIAN_POINT('Ctrl Pts',(76.4881096274971,452.700393300274,57.8472435664614));
#44514=CARTESIAN_POINT('Ctrl Pts',(78.5960127570322,452.837962711342,56.5594070064733));
#44515=CARTESIAN_POINT('Ctrl Pts',(79.8414258501443,452.975532122412,54.4261642055509));
#44516=CARTESIAN_POINT('Ctrl Pts',(79.9266389181023,453.113101533481,51.957456587291));
#44517=CARTESIAN_POINT('Ctrl Pts',(78.8312821710664,453.250670944549,49.7434167730967));
#44518=CARTESIAN_POINT('Ctrl Pts',(76.8171953950731,453.388240355619,48.3133003830516));
#44519=CARTESIAN_POINT('Ctrl Pts',(74.3658362436251,453.525809766687,48.0089696826649));
#44520=CARTESIAN_POINT('Ctrl Pts',(72.0631904771268,453.663379177756,48.9031738248679));
#44521=CARTESIAN_POINT('Ctrl Pts',(70.4596940712907,453.800948588825,50.7821568355942));
#44522=CARTESIAN_POINT('Ctrl Pts',(69.9386559345355,453.938517999894,53.1967586609433));
#44523=CARTESIAN_POINT('Ctrl Pts',(70.6246257935922,454.076087410963,55.5697766204929));
#44524=CARTESIAN_POINT('Ctrl Pts',(72.3536297593703,454.213656822032,57.3339608660936));
#44525=CARTESIAN_POINT('Ctrl Pts',(74.712348278058,454.351226233101,58.0675737810965));
#44526=CARTESIAN_POINT('Ctrl Pts',(77.1369593428433,454.48879564417,57.5952911284919));
#44527=CARTESIAN_POINT('Ctrl Pts',(79.0478241394874,454.626365055239,56.029925324192));
#44528=CARTESIAN_POINT('Ctrl Pts',(79.9882438640382,454.763934466308,53.7458789802202));
#44529=CARTESIAN_POINT('Ctrl Pts',(79.7331768690378,454.901503877377,51.2887463507757));
#44530=CARTESIAN_POINT('Ctrl Pts',(78.8070401490145,454.99321681809,49.9275741136407));
#44531=CARTESIAN_POINT('Ctrl Pts',(78.2100888302193,455.039073288446,49.3970725041402));
#44532=CARTESIAN_POINT('Ctrl Pts',(71.3431312258736,438.,49.8737829466856));
#44533=CARTESIAN_POINT('Ctrl Pts',(70.8246667948602,438.045856470356,50.4738756829193));
#44534=CARTESIAN_POINT('Ctrl Pts',(70.0904810848736,438.137569411069,51.9346323302495));
#44535=CARTESIAN_POINT('Ctrl Pts',(70.1598476148656,438.275138822138,54.3867565342177));
#44536=CARTESIAN_POINT('Ctrl Pts',(71.3835049550069,438.412708233207,56.5125746552081));
#44537=CARTESIAN_POINT('Ctrl Pts',(73.4687602399829,438.550277644276,57.8043411146894));
#44538=CARTESIAN_POINT('Ctrl Pts',(75.9171988302832,438.687847055345,57.9530481846181));
#44539=CARTESIAN_POINT('Ctrl Pts',(78.1434978095446,438.825416466414,56.9232374758342));
#44540=CARTESIAN_POINT('Ctrl Pts',(79.6154836096685,438.962985877483,54.9610361557711));
#44541=CARTESIAN_POINT('Ctrl Pts',(79.9812781097431,439.100555288552,52.5355178274692));
#44542=CARTESIAN_POINT('Ctrl Pts',(79.1534426071904,439.238124699621,50.2264819254732));
#44543=CARTESIAN_POINT('Ctrl Pts',(77.3298657797079,439.37569411069,48.5858962981143));
#44544=CARTESIAN_POINT('Ctrl Pts',(74.946465455023,439.513263521759,48.0059331744372));
#44545=CARTESIAN_POINT('Ctrl Pts',(72.5729817051559,439.650832932828,48.6252307671089));
#44546=CARTESIAN_POINT('Ctrl Pts',(70.7767845007438,439.788402343897,50.2957485891607));
#44547=CARTESIAN_POINT('Ctrl Pts',(69.9872460661516,439.925971754966,52.6181575796835));
#44548=CARTESIAN_POINT('Ctrl Pts',(70.3931017836471,440.063541166035,55.0372969858864));
#44549=CARTESIAN_POINT('Ctrl Pts',(71.8973337884151,440.201110577104,56.9748832301599));
#44550=CARTESIAN_POINT('Ctrl Pts',(74.1403626764107,440.338679988173,57.967745644851));
#44551=CARTESIAN_POINT('Ctrl Pts',(76.5860032023106,440.476249399242,57.7785452633612));
#44552=CARTESIAN_POINT('Ctrl Pts',(78.6496367890598,440.613818810311,56.4525095214311));
#44553=CARTESIAN_POINT('Ctrl Pts',(79.8379617752664,440.75138822138,54.3066208723653));
#44554=CARTESIAN_POINT('Ctrl Pts',(79.8669148016947,440.888957632449,51.8538436524662));
#44555=CARTESIAN_POINT('Ctrl Pts',(78.729574786843,441.026527043518,49.6805024325154));
#44556=CARTESIAN_POINT('Ctrl Pts',(76.6978173786037,441.164096454587,48.3061239541028));
#44557=CARTESIAN_POINT('Ctrl Pts',(74.257324391025,441.301665865656,48.0592467671762));
#44558=CARTESIAN_POINT('Ctrl Pts',(71.9914839080614,441.439235276725,48.9988856731345));
#44559=CARTESIAN_POINT('Ctrl Pts',(70.4419341743612,441.576804687793,50.9004245211821));
#44560=CARTESIAN_POINT('Ctrl Pts',(69.9790875839475,441.714374098863,53.3093096163199));
#44561=CARTESIAN_POINT('Ctrl Pts',(70.713585383041,441.851943509931,55.6497085889238));
#44562=CARTESIAN_POINT('Ctrl Pts',(72.4698494135181,441.989512921,57.3621603468108));
#44563=CARTESIAN_POINT('Ctrl Pts',(74.828053225208,442.127082332069,58.0373115523705));
#44564=CARTESIAN_POINT('Ctrl Pts',(77.2244795649762,442.264651743138,57.5137705645742));
#44565=CARTESIAN_POINT('Ctrl Pts',(79.0862742686079,442.402221154207,55.9166873327523));
#44566=CARTESIAN_POINT('Ctrl Pts',(79.9683842872405,442.539790565276,53.6278369045098));
#44567=CARTESIAN_POINT('Ctrl Pts',(79.6599454732541,442.677359976345,51.194357940996));
#44568=CARTESIAN_POINT('Ctrl Pts',(78.2346886382596,442.814929387414,49.1979618575147));
#44569=CARTESIAN_POINT('Ctrl Pts',(76.0333145580138,442.952498798483,48.1158775139168));
#44570=CARTESIAN_POINT('Ctrl Pts',(73.5820510943691,443.090068209552,48.2067719562013));
#44571=CARTESIAN_POINT('Ctrl Pts',(71.466860961653,443.227637620621,49.4489173061093));
#44572=CARTESIAN_POINT('Ctrl Pts',(70.1933701645227,443.36520703169,51.5453847056798));
#44573=CARTESIAN_POINT('Ctrl Pts',(70.0660005389926,443.502776442759,53.9950237293587));
#44574=CARTESIAN_POINT('Ctrl Pts',(71.1151991800427,443.640345853828,56.2122599773613));
#44575=CARTESIAN_POINT('Ctrl Pts',(73.090160210338,443.777915264897,57.6670738130985));
#44576=CARTESIAN_POINT('Ctrl Pts',(75.5187787161611,443.915484675966,58.0116990022701));
#44577=CARTESIAN_POINT('Ctrl Pts',(77.8205051511885,444.053054087035,57.1637545547184));
#44578=CARTESIAN_POINT('Ctrl Pts',(79.4451229069195,444.190623498104,55.3259375029962));
#44579=CARTESIAN_POINT('Ctrl Pts',(80.004274940543,444.328192909173,52.9375691538648));
#44580=CARTESIAN_POINT('Ctrl Pts',(79.3642986538913,444.465762320242,50.569577447722));
#44581=CARTESIAN_POINT('Ctrl Pts',(77.6781772931937,444.603331731311,48.7880193866875));
#44582=CARTESIAN_POINT('Ctrl Pts',(75.3489700415422,444.74090114238,48.0187678370029));
#44583=CARTESIAN_POINT('Ctrl Pts',(72.9334626641764,444.878470553449,48.4457086733363));
#44584=CARTESIAN_POINT('Ctrl Pts',(71.0090705553659,445.016039964518,49.9667837468897));
#44585=CARTESIAN_POINT('Ctrl Pts',(70.0358103719218,445.153609375587,52.2183873938844));
#44586=CARTESIAN_POINT('Ctrl Pts',(70.2463352689603,445.291178786656,54.6622846166753));
#44587=CARTESIAN_POINT('Ctrl Pts',(71.5903202847087,445.428748197725,56.7142735653008));
#44588=CARTESIAN_POINT('Ctrl Pts',(73.7464922800195,445.566317608794,57.8838361734905));
#44589=CARTESIAN_POINT('Ctrl Pts',(76.1994287335407,445.703887019863,57.891394137796));
#44590=CARTESIAN_POINT('Ctrl Pts',(78.3627670107798,445.841456430932,56.7351407632842));
#44591=CARTESIAN_POINT('Ctrl Pts',(79.7193715252362,445.979025842001,54.691472845252));
#44592=CARTESIAN_POINT('Ctrl Pts',(79.9449525074299,446.11659525307,52.2489193477191));
#44593=CARTESIAN_POINT('Ctrl Pts',(78.9855859110121,446.254164664139,49.9913609096016));
#44594=CARTESIAN_POINT('Ctrl Pts',(77.0706036960962,446.391734075208,48.4584559926568));
#44595=CARTESIAN_POINT('Ctrl Pts',(74.6577731297195,446.529303486277,48.0166381276987));
#44596=CARTESIAN_POINT('Ctrl Pts',(72.3238697273887,446.666872897346,48.7715217455012));
#44597=CARTESIAN_POINT('Ctrl Pts',(70.6268018465247,446.804442308415,50.54265555625));
#44598=CARTESIAN_POINT('Ctrl Pts',(69.9722453830961,446.942011719484,52.9066585604828));
#44599=CARTESIAN_POINT('Ctrl Pts',(70.5166689043049,447.079581130553,55.2984272360433));
#44600=CARTESIAN_POINT('Ctrl Pts',(72.1299305918756,447.217150541622,57.1462208108926));
#44601=CARTESIAN_POINT('Ctrl Pts',(74.4263880163468,447.354719952691,58.0083331385092));
#44602=CARTESIAN_POINT('Ctrl Pts',(76.8570841007916,447.49228936376,57.6786804229088));
#44603=CARTESIAN_POINT('Ctrl Pts',(78.8409726637322,447.629858774829,56.236064556619));
#44604=CARTESIAN_POINT('Ctrl Pts',(79.9038147078087,447.767428185898,54.0253359081455));
#44605=CARTESIAN_POINT('Ctrl Pts',(79.7915429659626,447.904997596967,51.5749585037809));
#44606=CARTESIAN_POINT('Ctrl Pts',(78.5309954568607,448.042567008036,49.4706832496531));
#44607=CARTESIAN_POINT('Ctrl Pts',(76.423499985909,448.180136419105,48.2155270013095));
#44608=CARTESIAN_POINT('Ctrl Pts',(73.9728431859633,448.317705830174,48.1095288092612));
#44609=CARTESIAN_POINT('Ctrl Pts',(71.7648427513183,448.455275241243,49.1780270303383));
#44610=CARTESIAN_POINT('Ctrl Pts',(70.3273105419023,448.592844652312,51.1656023156368));
#44611=CARTESIAN_POINT('Ctrl Pts',(70.0038817025521,448.730414063381,53.5971343745895));
#44612=CARTESIAN_POINT('Ctrl Pts',(70.8718703381808,448.86798347445,55.8913771900424));
#44613=CARTESIAN_POINT('Ctrl Pts',(72.7237879497012,449.005552885519,57.4999030766785));
#44614=CARTESIAN_POINT('Ctrl Pts',(75.116942559506,449.143122296588,58.0382016754203));
#44615=CARTESIAN_POINT('Ctrl Pts',(77.4792620946565,449.280691707657,57.377595301182));
#44616=CARTESIAN_POINT('Ctrl Pts',(79.246045458165,449.418261118726,55.6759987231803));
#44617=CARTESIAN_POINT('Ctrl Pts',(79.9949516040101,449.555830529795,53.3401704006032));
#44618=CARTESIAN_POINT('Ctrl Pts',(79.5469581282337,449.693399940864,50.9284788337772));
#44619=CARTESIAN_POINT('Ctrl Pts',(78.0091557116053,449.830969351933,49.0174272658571));
#44620=CARTESIAN_POINT('Ctrl Pts',(75.7491486086294,449.968538763002,48.0638433616641));
#44621=CARTESIAN_POINT('Ctrl Pts',(73.3071806225934,450.10610817407,48.2956767566116));
#44622=CARTESIAN_POINT('Ctrl Pts',(71.2669924287125,450.24367758514,49.6575087952225));
#44623=CARTESIAN_POINT('Ctrl Pts',(70.1162811797229,450.381246996208,51.8238000935677));
#44624=CARTESIAN_POINT('Ctrl Pts',(70.1301188525317,450.518816407277,54.2767091596868));
#44625=CARTESIAN_POINT('Ctrl Pts',(71.3051976181603,450.656385818346,56.4298799059135));
#44626=CARTESIAN_POINT('Ctrl Pts',(73.3606205623162,450.793955229416,57.7686072450216));
#44627=CARTESIAN_POINT('Ctrl Pts',(75.8050487386511,450.931524640484,57.972874860119));
#44628=CARTESIAN_POINT('Ctrl Pts',(78.0541533753186,451.069094051554,56.9938535625169));
#44629=CARTESIAN_POINT('Ctrl Pts',(79.5702968510455,451.206663462622,55.065573673899));
#44630=CARTESIAN_POINT('Ctrl Pts',(79.9910523767396,451.344232873691,52.6489812060971));
#44631=CARTESIAN_POINT('Ctrl Pts',(79.2158403722948,451.48180228476,50.3217509390201));
#44632=CARTESIAN_POINT('Ctrl Pts',(77.4299715303552,451.619371695829,48.6401960492725));
#44633=CARTESIAN_POINT('Ctrl Pts',(75.0603491885598,451.756941106898,48.0062841270851));
#44634=CARTESIAN_POINT('Ctrl Pts',(72.6734201446142,451.894510517967,48.571548761583));
#44635=CARTESIAN_POINT('Ctrl Pts',(70.8397682799635,452.032079929036,50.2008661668549));
#44636=CARTESIAN_POINT('Ctrl Pts',(69.997719233448,452.169649340105,52.5047558714594));
#44637=CARTESIAN_POINT('Ctrl Pts',(70.3485607704892,452.307218751174,54.9324841478696));
#44638=CARTESIAN_POINT('Ctrl Pts',(71.808425912791,452.444788162243,56.9037142545098));
#44639=CARTESIAN_POINT('Ctrl Pts',(74.0283409358903,452.582357573312,57.9472331376422));
#44640=CARTESIAN_POINT('Ctrl Pts',(76.4776458542147,452.719926984381,57.8135926372266));
#44641=CARTESIAN_POINT('Ctrl Pts',(78.5708461358004,452.85749639545,56.5347388738669));
#44642=CARTESIAN_POINT('Ctrl Pts',(79.8075723404659,452.995065806519,54.4163756677902));
#44643=CARTESIAN_POINT('Ctrl Pts',(79.8921910382349,453.132635217588,51.9648875470652));
#44644=CARTESIAN_POINT('Ctrl Pts',(78.8044745207126,453.270204628657,49.7662908954556));
#44645=CARTESIAN_POINT('Ctrl Pts',(76.8044362136501,453.407774039726,48.3461497189478));
#44646=CARTESIAN_POINT('Ctrl Pts',(74.3701755523407,453.545343450795,48.0439417574817));
#44647=CARTESIAN_POINT('Ctrl Pts',(72.0835909843443,453.682912861864,48.9319087309295));
#44648=CARTESIAN_POINT('Ctrl Pts',(70.4912791360489,453.820482272933,50.7977856358205));
#44649=CARTESIAN_POINT('Ctrl Pts',(69.9738752955729,453.958051684002,53.19554535728));
#44650=CARTESIAN_POINT('Ctrl Pts',(70.6550604420902,454.095621095071,55.5520112648156));
#44651=CARTESIAN_POINT('Ctrl Pts',(72.3720044217823,454.23319050614,57.3038901381464));
#44652=CARTESIAN_POINT('Ctrl Pts',(74.714270628573,454.370759917209,58.0323860252404));
#44653=CARTESIAN_POINT('Ctrl Pts',(77.1219697739619,454.508329328278,57.5633975942407));
#44654=CARTESIAN_POINT('Ctrl Pts',(79.0195060859316,454.645898739347,56.0089503824907));
#44655=CARTESIAN_POINT('Ctrl Pts',(79.9533662831374,454.783468150416,53.7408355040756));
#44656=CARTESIAN_POINT('Ctrl Pts',(79.7000784074864,454.921037561485,51.3008416353911));
#44657=CARTESIAN_POINT('Ctrl Pts',(78.7804015893363,455.012750502198,49.9491637190126));
#44658=CARTESIAN_POINT('Ctrl Pts',(78.1876140693184,455.058606972554,49.4223624145177));
#44659=CARTESIAN_POINT('Origin',(74.9879498948689,416.,53.0228109606356));
#44660=CARTESIAN_POINT('Origin',(74.9879498948689,416.,53.0228109606356));
#44661=CARTESIAN_POINT('Ctrl Pts',(79.8830110631999,416.,55.8460953909448));
#44662=CARTESIAN_POINT('Ctrl Pts',(79.9838735321605,416.,55.7696158752547));
#44663=CARTESIAN_POINT('Ctrl Pts',(80.0818868713731,416.,55.68934340634));
#44664=CARTESIAN_POINT('Ctrl Pts',(80.1769367937531,416.,55.6056077868176));
#44665=CARTESIAN_POINT('Ctrl Pts',(80.2608081582141,416.,55.5317200814152));
#44666=CARTESIAN_POINT('Ctrl Pts',(80.3423725986366,416.,55.455135757001));
#44667=CARTESIAN_POINT('Ctrl Pts',(80.4215638414298,416.,55.376071154289));
#44668=CARTESIAN_POINT('Ctrl Pts',(80.4575782080312,416.,55.3401143807011));
#44669=CARTESIAN_POINT('Ctrl Pts',(80.4930951080665,416.,55.3036512767701));
#44670=CARTESIAN_POINT('Ctrl Pts',(80.5281101864556,416.,55.2667013119425));
#44671=CARTESIAN_POINT('Ctrl Pts',(80.57650767122,416.,55.2156294468473));
#44672=CARTESIAN_POINT('Ctrl Pts',(80.6239470702437,416.,55.1636271224708));
#44673=CARTESIAN_POINT('Ctrl Pts',(80.6704271942508,416.,55.1107322929466));
#44674=CARTESIAN_POINT('Ctrl Pts',(80.7785625890765,416.,54.9876731704287));
#44675=CARTESIAN_POINT('Ctrl Pts',(80.8814898413737,416.,54.8598021724764));
#44676=CARTESIAN_POINT('Ctrl Pts',(80.9790755347001,416.,54.7276983390789));
#44677=CARTESIAN_POINT('Ctrl Pts',(81.0522648046949,416.,54.6286204640308));
#44678=CARTESIAN_POINT('Ctrl Pts',(81.1224501122421,416.,54.5271604110985));
#44679=CARTESIAN_POINT('Ctrl Pts',(81.1895813378797,416.,54.4235414927863));
#44680=CARTESIAN_POINT('Ctrl Pts',(81.2246388416095,416.,54.3694292584168));
#44681=CARTESIAN_POINT('Ctrl Pts',(81.2588635076428,416.,54.3147279697757));
#44682=CARTESIAN_POINT('Ctrl Pts',(81.2922484633112,416.,54.2594675418588));
#44683=CARTESIAN_POINT('Ctrl Pts',(81.3126684070658,416.,54.2256674421632));
#44684=CARTESIAN_POINT('Ctrl Pts',(81.3327776128819,416.,54.1916520339595));
#44685=CARTESIAN_POINT('Ctrl Pts',(81.3525561249044,416.,54.1574603450589));
#44686=CARTESIAN_POINT('Ctrl Pts',(81.4319376986157,416.,54.0202311101349));
#44687=CARTESIAN_POINT('Ctrl Pts',(81.5060371326813,416.,53.8800954269512));
#44688=CARTESIAN_POINT('Ctrl Pts',(81.5748188145443,416.,53.7375264352072));
#44689=CARTESIAN_POINT('Ctrl Pts',(81.6218375223006,416.,53.6400672051279));
#44690=CARTESIAN_POINT('Ctrl Pts',(81.6663714865911,416.,53.541469744288));
#44691=CARTESIAN_POINT('Ctrl Pts',(81.7084103241663,416.,53.4418712821641));
#44692=CARTESIAN_POINT('Ctrl Pts',(81.7726557132268,416.,53.2896610328314));
#44693=CARTESIAN_POINT('Ctrl Pts',(81.8310745560022,416.,53.1351152483158));
#44694=CARTESIAN_POINT('Ctrl Pts',(81.8837208336072,416.,52.9786103674316));
#44695=CARTESIAN_POINT('Ctrl Pts',(81.9370199527937,416.,52.8201647435625));
#44696=CARTESIAN_POINT('Ctrl Pts',(81.9844030717354,416.,52.6597108152884));
#44697=CARTESIAN_POINT('Ctrl Pts',(82.0259096346253,416.,52.4975874466145));
#44698=CARTESIAN_POINT('Ctrl Pts',(82.0553577168838,416.,52.3825641354963));
#44699=CARTESIAN_POINT('Ctrl Pts',(82.0818474251191,416.,52.2666993851232));
#44700=CARTESIAN_POINT('Ctrl Pts',(82.1053853897379,416.,52.1501002183919));
#44701=CARTESIAN_POINT('Ctrl Pts',(82.1113952199384,416.,52.1203295391966));
#44702=CARTESIAN_POINT('Ctrl Pts',(82.1172128280547,416.,52.0905092581177));
#44703=CARTESIAN_POINT('Ctrl Pts',(82.1228344363168,416.,52.0606624486299));
#44704=CARTESIAN_POINT('Ctrl Pts',(82.1554961379767,416.,51.8872516484573));
#44705=CARTESIAN_POINT('Ctrl Pts',(82.1815754911756,416.,51.7127917293179));
#44706=CARTESIAN_POINT('Ctrl Pts',(82.201164328218,416.,51.5377077735356));
#44707=CARTESIAN_POINT('Ctrl Pts',(82.22123206082,416.,51.3583434753921));
#44708=CARTESIAN_POINT('Ctrl Pts',(82.2344886373556,416.,51.178323981131));
#44709=CARTESIAN_POINT('Ctrl Pts',(82.2410141947413,416.,50.998054756671));
#44710=CARTESIAN_POINT('Ctrl Pts',(82.2476113248581,416.,50.8158083278175));
#44711=CARTESIAN_POINT('Ctrl Pts',(82.247329519956,416.,50.6333061826993));
#44712=CARTESIAN_POINT('Ctrl Pts',(82.2402241682398,416.,50.4509211223708));
#44713=CARTESIAN_POINT('Ctrl Pts',(82.2330496544919,416.,50.2667607633897));
#44714=CARTESIAN_POINT('Ctrl Pts',(82.2189186386138,416.,50.0827192120228));
#44715=CARTESIAN_POINT('Ctrl Pts',(82.1978521894802,416.,49.8991414119943));
#44716=CARTESIAN_POINT('Ctrl Pts',(82.1889738216336,416.,49.8217733075366));
#44717=CARTESIAN_POINT('Ctrl Pts',(82.1788631247121,416.,49.7444871533955));
#44718=CARTESIAN_POINT('Ctrl Pts',(82.1675194498641,416.,49.6673071229107));
#44719=CARTESIAN_POINT('Ctrl Pts',(80.1006187634621,416.611326082532,50.6333111614898));
#44720=CARTESIAN_POINT('Ctrl Pts',(80.4987738037364,416.505248077756,51.4852195316062));
#44721=CARTESIAN_POINT('Ctrl Pts',(80.8500414041054,416.293092068204,53.3832855022525));
#44722=CARTESIAN_POINT('Ctrl Pts',(79.6907686422404,415.868780049099,57.1038140873438));
#44723=CARTESIAN_POINT('Ctrl Pts',(75.0514316659349,415.338390025218,59.6975379999433));
#44724=CARTESIAN_POINT('Ctrl Pts',(69.3998575284373,414.701921996561,56.6778047341864));
#44725=CARTESIAN_POINT('Ctrl Pts',(68.8933949361463,414.065453967904,50.30071708643));
#44726=CARTESIAN_POINT('Ctrl Pts',(73.9883328942991,413.428985939247,46.4204917324893));
#44727=CARTESIAN_POINT('Ctrl Pts',(78.9900558741506,412.898595915367,48.2517506338942));
#44728=CARTESIAN_POINT('Ctrl Pts',(80.7106490634504,412.474283896262,51.7314515919306));
#44729=CARTESIAN_POINT('Ctrl Pts',(80.6505859354663,412.049971877158,55.6129833562453));
#44730=CARTESIAN_POINT('Ctrl Pts',(76.922041457819,411.519581853277,59.4142434298776));
#44731=CARTESIAN_POINT('Ctrl Pts',(70.6502604163708,410.88311382462,58.0990212603595));
#44732=CARTESIAN_POINT('Ctrl Pts',(68.3768445575805,410.246645795963,52.120585584734));
#44733=CARTESIAN_POINT('Ctrl Pts',(72.1690405094426,409.610177767306,46.9698855255472));
#44734=CARTESIAN_POINT('Ctrl Pts',(78.5640475947216,408.973709738649,47.3834241974277));
#44735=CARTESIAN_POINT('Ctrl Pts',(81.1373488053079,408.443319714768,52.0445771336779));
#44736=CARTESIAN_POINT('Ctrl Pts',(80.1556395568995,408.019007695663,55.8005301909727));
#44737=CARTESIAN_POINT('Ctrl Pts',(77.5645627245594,407.594695676559,58.6914128709184));
#44738=CARTESIAN_POINT('Ctrl Pts',(72.2572669003642,407.064305652677,59.1166316929431));
#44739=CARTESIAN_POINT('Ctrl Pts',(68.3843315795067,406.427837624022,54.0109585396062));
#44740=CARTESIAN_POINT('Ctrl Pts',(70.5882295550609,405.791369595364,48.0065658313019));
#44741=CARTESIAN_POINT('Ctrl Pts',(76.8287342059321,405.154901566707,46.6044208685245));
#44742=CARTESIAN_POINT('Ctrl Pts',(81.3858076212758,404.51843353805,51.1100412325878));
#44743=CARTESIAN_POINT('Ctrl Pts',(80.2721801274972,403.988043514169,56.3165759506076));
#44744=CARTESIAN_POINT('Ctrl Pts',(77.0681164794659,403.563731495065,58.5085806146201));
#44745=CARTESIAN_POINT('Ctrl Pts',(73.2162245052195,403.13941947596,58.9921464057559));
#44746=CARTESIAN_POINT('Ctrl Pts',(68.9304046244017,402.609029452079,55.8330454857165));
#44747=CARTESIAN_POINT('Ctrl Pts',(69.3542790093376,401.972561423423,49.4386835020307));
#44748=CARTESIAN_POINT('Ctrl Pts',(74.9554640876222,401.336093394765,46.3505401944445));
#44749=CARTESIAN_POINT('Ctrl Pts',(80.5864538842716,400.699625366109,49.3839965362696));
#44750=CARTESIAN_POINT('Ctrl Pts',(81.0725721437252,400.063157337451,55.7739279658411));
#44751=CARTESIAN_POINT('Ctrl Pts',(76.817716662541,399.53276731357,58.9746115424238));
#44752=CARTESIAN_POINT('Ctrl Pts',(72.9612986351318,399.108455294466,58.5285757956383));
#44753=CARTESIAN_POINT('Ctrl Pts',(69.7360426834167,398.684143275361,56.3678740736957));
#44754=CARTESIAN_POINT('Ctrl Pts',(68.5717701362819,398.153753251481,51.1724299186502));
#44755=CARTESIAN_POINT('Ctrl Pts',(73.0847550464725,397.517285222823,46.622649502512));
#44756=CARTESIAN_POINT('Ctrl Pts',(79.3386165734188,396.880817194168,47.96396208343));
#44757=CARTESIAN_POINT('Ctrl Pts',(81.6008775563583,396.244349165509,53.9466102164501));
#44758=CARTESIAN_POINT('Ctrl Pts',(77.7778399493888,395.607881136854,59.0897530386598));
#44759=CARTESIAN_POINT('Ctrl Pts',(72.4666579798875,395.077491112972,58.7162338035805));
#44760=CARTESIAN_POINT('Ctrl Pts',(69.8475504599716,394.653179093868,55.8507175000904));
#44761=CARTESIAN_POINT('Ctrl Pts',(68.8293227947622,394.228867074763,52.1045033700332));
#44762=CARTESIAN_POINT('Ctrl Pts',(71.3570971813203,393.698477050882,47.4185107128847));
#44763=CARTESIAN_POINT('Ctrl Pts',(77.7478064874976,393.062009022225,46.942727991698));
#44764=CARTESIAN_POINT('Ctrl Pts',(81.5899196973729,392.425540993568,52.0562463030878));
#44765=CARTESIAN_POINT('Ctrl Pts',(79.3749321908379,391.789072964911,58.056557443713));
#44766=CARTESIAN_POINT('Ctrl Pts',(73.1160470792531,391.152604936255,59.4327448560289));
#44767=CARTESIAN_POINT('Ctrl Pts',(69.3510454836729,390.622214912373,55.6680491820767));
#44768=CARTESIAN_POINT('Ctrl Pts',(69.2526248134902,390.197902893269,51.7871702535196));
#44769=CARTESIAN_POINT('Ctrl Pts',(70.9403623007099,389.773590874164,48.2911081744554));
#44770=CARTESIAN_POINT('Ctrl Pts',(75.9215609897948,389.243200850283,46.4107278533347));
#44771=CARTESIAN_POINT('Ctrl Pts',(81.0585138063054,388.606732821626,50.2420788415338));
#44772=CARTESIAN_POINT('Ctrl Pts',(80.6062231907216,387.97026479297,56.6221522453024));
#44773=CARTESIAN_POINT('Ctrl Pts',(74.9993426234548,387.333796764312,59.6999426447327));
#44774=CARTESIAN_POINT('Ctrl Pts',(69.3714963501972,386.697328735656,56.6348356387029));
#44775=CARTESIAN_POINT('Ctrl Pts',(68.9975455437743,386.166938711775,51.323684037913));
#44776=CARTESIAN_POINT('Ctrl Pts',(71.4680383649468,385.742626692671,48.3290933969452));
#44777=CARTESIAN_POINT('Ctrl Pts',(75.0347408347962,385.318314673565,46.7962720185687));
#44778=CARTESIAN_POINT('Ctrl Pts',(80.0285504932429,384.787924649685,48.6429001964653));
#44779=CARTESIAN_POINT('Ctrl Pts',(81.3946131522726,384.151456621028,54.9040029304442));
#44780=CARTESIAN_POINT('Ctrl Pts',(76.8695434714302,383.514988592372,59.4243621885054));
#44781=CARTESIAN_POINT('Ctrl Pts',(70.6181705596548,382.878520563713,58.0714985012323));
#44782=CARTESIAN_POINT('Ctrl Pts',(68.3790371462131,382.242052535058,52.0670154934588));
#44783=CARTESIAN_POINT('Ctrl Pts',(71.5793749741399,381.711662511176,47.8118999463395));
#44784=CARTESIAN_POINT('Ctrl Pts',(75.4082269213871,381.287350492072,47.1709626229601));
#44785=CARTESIAN_POINT('Ctrl Pts',(79.1061915643167,380.863038472967,48.3524724138965));
#44786=CARTESIAN_POINT('Ctrl Pts',(81.6656194182121,380.332648449087,53.0212516540086));
#44787=CARTESIAN_POINT('Ctrl Pts',(78.5914140932141,379.696180420429,58.6441331442757));
#44788=CARTESIAN_POINT('Ctrl Pts',(72.2108730876569,379.059712391772,59.0897786478119));
#44789=CARTESIAN_POINT('Ctrl Pts',(68.3782131572467,378.423244363116,53.9691711353926));
#44790=CARTESIAN_POINT('Ctrl Pts',(70.6249796526406,377.786776334458,47.9675401113284));
#44791=CARTESIAN_POINT('Ctrl Pts',(75.8314238903965,377.256386310578,46.8534894251665));
#44792=CARTESIAN_POINT('Ctrl Pts',(79.1424775432099,376.832074291473,48.8802680501344));
#44793=CARTESIAN_POINT('Ctrl Pts',(81.1596824003675,376.407762272369,52.1971630515926));
#44794=CARTESIAN_POINT('Ctrl Pts',(80.0305954546256,375.877372248488,57.4003671799305));
#44795=CARTESIAN_POINT('Ctrl Pts',(74.0224987859417,375.240904219831,59.6297861745523));
#44796=CARTESIAN_POINT('Ctrl Pts',(68.9129848210706,374.604436191174,55.7823493029185));
#44797=CARTESIAN_POINT('Ctrl Pts',(69.3770612241408,373.967968162517,49.4031223489269));
#44798=CARTESIAN_POINT('Ctrl Pts',(75.0088003293896,373.331500133859,46.3451738071356));
#44799=CARTESIAN_POINT('Ctrl Pts',(79.6701661503711,372.80111010998,48.9180786276028));
#44800=CARTESIAN_POINT('Ctrl Pts',(80.8409879526845,372.376798090874,52.6194411056188));
#44801=CARTESIAN_POINT('Ctrl Pts',(80.1889921249218,371.95248607177,56.446425470235));
#44802=CARTESIAN_POINT('Ctrl Pts',(75.9246488708189,371.422096047889,59.6344573307068));
#44803=CARTESIAN_POINT('Ctrl Pts',(69.926659556592,370.785628019232,57.377986896543));
#44804=CARTESIAN_POINT('Ctrl Pts',(68.5918611198335,370.149159990575,51.1227317801111));
#44805=CARTESIAN_POINT('Ctrl Pts',(73.125273998855,369.512691961918,46.610739857829));
#44806=CARTESIAN_POINT('Ctrl Pts',(79.3824041844943,368.876223933261,47.9948845301062));
#44807=CARTESIAN_POINT('Ctrl Pts',(81.2145980287447,368.345833909381,52.9940080782184));
#44808=CARTESIAN_POINT('Ctrl Pts',(79.6714791919269,367.921521890276,56.5562674935186));
#44809=CARTESIAN_POINT('Ctrl Pts',(76.6697640348178,367.497209871172,59.0180989260132));
#44810=CARTESIAN_POINT('Ctrl Pts',(71.359714904182,366.96681984729,58.6288062823227));
#44811=CARTESIAN_POINT('Ctrl Pts',(68.3108789861652,366.330351818634,52.9921286989546));
#44812=CARTESIAN_POINT('Ctrl Pts',(71.4048542721186,365.693883789976,47.3941629641248));
#44813=CARTESIAN_POINT('Ctrl Pts',(77.7862076759328,365.05741576132,46.9603056442045));
#44814=CARTESIAN_POINT('Ctrl Pts',(81.602702521873,364.420947732662,52.10830542322));
#44815=CARTESIAN_POINT('Ctrl Pts',(79.7079398513482,363.890557708783,57.0840510914171));
#44816=CARTESIAN_POINT('Ctrl Pts',(76.2070166523586,363.466245689677,58.7616817543507));
#44817=CARTESIAN_POINT('Ctrl Pts',(72.3264382459639,363.041933670573,58.6520500150618));
#44818=CARTESIAN_POINT('Ctrl Pts',(68.572635003179,362.511543646692,54.8761882926657));
#44819=CARTESIAN_POINT('Ctrl Pts',(69.9668979799986,361.875075618035,48.6213049695892));
#44820=CARTESIAN_POINT('Ctrl Pts',(75.9735829643599,361.238607589378,46.4236610182017));
#44821=CARTESIAN_POINT('Ctrl Pts',(81.0759804481833,360.602139560721,50.2805306498451));
#44822=CARTESIAN_POINT('Ctrl Pts',(80.5817375779959,359.965671532064,56.6698387985494));
#44823=CARTESIAN_POINT('Ctrl Pts',(75.8884619818927,359.435281508183,59.184065262339));
#44824=CARTESIAN_POINT('Ctrl Pts',(72.1452050445395,359.010969489079,58.1550193997093));
#44825=CARTESIAN_POINT('Ctrl Pts',(69.2872670440879,358.586657469974,55.5276446125861));
#44826=CARTESIAN_POINT('Ctrl Pts',(68.9290928531176,358.056267446094,50.2154057454868));
#44827=CARTESIAN_POINT('Ctrl Pts',(74.0832585954538,357.419799417435,46.4072421284185));
#44828=CARTESIAN_POINT('Ctrl Pts',(80.0593463127588,356.78333138878,48.6867769567317));
#44829=CARTESIAN_POINT('Ctrl Pts',(81.3825865019895,356.146863360122,54.9444873079725));
#44830=CARTESIAN_POINT('Ctrl Pts',(76.8197874993998,355.510395331466,59.4443095151045));
#44831=CARTESIAN_POINT('Ctrl Pts',(71.6277284938853,354.980005307585,58.2650326962652));
#44832=CARTESIAN_POINT('Ctrl Pts',(69.4763532374749,354.55569328848,55.0335481469374));
#44833=CARTESIAN_POINT('Ctrl Pts',(69.0414601665085,354.131381269376,51.175857658671));
#44834=CARTESIAN_POINT('Ctrl Pts',(72.2544222487035,353.600991245494,46.9302663935378));
#44835=CARTESIAN_POINT('Ctrl Pts',(78.6429226653259,352.964523216838,47.4348425133144));
#44836=CARTESIAN_POINT('Ctrl Pts',(81.6600989705247,352.32805518818,53.0745721683392));
#44837=CARTESIAN_POINT('Ctrl Pts',(78.5557872721241,351.691587159524,58.6668125349179));
#44838=CARTESIAN_POINT('Ctrl Pts',(72.1602274420798,351.055119130866,59.0722124537102));
#44839=CARTESIAN_POINT('Ctrl Pts',(69.0135210149437,350.524729106987,54.7772841430609));
#44840=CARTESIAN_POINT('Ctrl Pts',(69.5082125339175,350.100417087881,50.9268051874641));
#44841=CARTESIAN_POINT('Ctrl Pts',(71.7094642650518,349.676105068777,47.7290874540463));
#44842=CARTESIAN_POINT('Ctrl Pts',(76.9191944454673,349.145715044897,46.6305056503264));
#44843=CARTESIAN_POINT('Ctrl Pts',(81.4116310180472,348.509247016239,51.2005765770387));
#44844=CARTESIAN_POINT('Ctrl Pts',(79.9914637878894,347.872778987582,57.437004118252));
#44845=CARTESIAN_POINT('Ctrl Pts',(73.9807291221626,347.236310958925,59.6235475586274));
#44846=CARTESIAN_POINT('Ctrl Pts',(68.8862661323819,346.599842930268,55.7358771148282));
#44847=CARTESIAN_POINT('Ctrl Pts',(69.326814842086,346.069452906387,50.4298345813976));
#44848=CARTESIAN_POINT('Ctrl Pts',(72.2251717124735,345.645140887283,47.8471159869094));
#44849=CARTESIAN_POINT('Ctrl Pts',(75.9839434185608,345.220828868178,46.8762693728891));
#44850=CARTESIAN_POINT('Ctrl Pts',(80.6376467415555,344.690438844298,49.4630078431919));
#44851=CARTESIAN_POINT('Ctrl Pts',(81.0327021227699,344.05397081564,55.8592149911513));
#44852=CARTESIAN_POINT('Ctrl Pts',(75.8710807057947,343.417502786984,59.6364584021908));
#44853=CARTESIAN_POINT('Ctrl Pts',(69.8992144031925,342.781034758326,57.3458872283867));
#44854=CARTESIAN_POINT('Ctrl Pts',(68.6021616848208,342.14456672967,51.0701252125357));
#44855=CARTESIAN_POINT('Ctrl Pts',(72.4140943662755,341.614176705789,47.3529569671835));
#44856=CARTESIAN_POINT('Ctrl Pts',(76.2959066074933,341.189864686684,47.3035443132344));
#44857=CARTESIAN_POINT('Ctrl Pts',(79.7703805516423,340.765552667579,49.0352887221662));
#44858=CARTESIAN_POINT('Ctrl Pts',(81.5877181212305,340.2351626437,54.0398321269494));
#44859=CARTESIAN_POINT('Ctrl Pts',(77.6918131141847,339.598694615041,59.1280006392838));
#44860=CARTESIAN_POINT('Ctrl Pts',(71.3179589210744,338.962226586385,58.5951909515068));
#44861=CARTESIAN_POINT('Ctrl Pts',(68.3112066114293,338.325758557728,52.9498969833543));
#44862=CARTESIAN_POINT('Ctrl Pts',(71.4471267602236,337.689290529071,47.3611995095039));
#44863=CARTESIAN_POINT('Ctrl Pts',(76.762576521389,337.158900505191,47.0543373764116));
#44864=CARTESIAN_POINT('Ctrl Pts',(79.7257358927106,336.734588486085,49.5624431211091));
#44865=CARTESIAN_POINT('Ctrl Pts',(81.2134017239108,336.310276466981,53.1482147620699));
#44866=CARTESIAN_POINT('Ctrl Pts',(79.3038686541036,335.7798864431,58.1183107357417));
#44867=CARTESIAN_POINT('Ctrl Pts',(73.0260170282693,335.143418414444,59.4052115080782));
#44868=CARTESIAN_POINT('Ctrl Pts',(68.5631518514559,334.506950385786,54.8234282469443));
#44869=CARTESIAN_POINT('Ctrl Pts',(69.9948378458387,333.87048235713,48.5896349674149));
#44870=CARTESIAN_POINT('Ctrl Pts',(76.0271136359725,333.234014328472,46.4264929411948));
#44871=CARTESIAN_POINT('Ctrl Pts',(80.2414823753424,332.703624304592,49.6803009657747));
#44872=CARTESIAN_POINT('Ctrl Pts',(80.8340253328005,332.279312285487,53.5169402151704));
#44873=CARTESIAN_POINT('Ctrl Pts',(79.605919036016,331.855000266382,57.199692285326));
#44874=CARTESIAN_POINT('Ctrl Pts',(74.9051964886825,331.324610242502,59.6999678831728));
#44875=CARTESIAN_POINT('Ctrl Pts',(69.3215782779007,330.688142213844,56.5550128262509));
#44876=CARTESIAN_POINT('Ctrl Pts',(68.9565293265754,330.051674185188,50.1693536823915));
#44877=CARTESIAN_POINT('Ctrl Pts',(74.1251200219098,329.415206156531,46.4016523058858));
#44878=CARTESIAN_POINT('Ctrl Pts',(80.0979048596417,328.778738127874,48.7240166003043));
#44879=CARTESIAN_POINT('Ctrl Pts',(81.1461299182097,328.248348103993,53.9441118828436));
#44880=CARTESIAN_POINT('Ctrl Pts',(79.0777073227094,327.824036084888,57.2293113977682));
#44881=CARTESIAN_POINT('Ctrl Pts',(75.7356073875843,327.399724065784,59.2044761782546));
#44882=CARTESIAN_POINT('Ctrl Pts',(70.5470739238278,326.869334041903,58.0097833191163));
#44883=CARTESIAN_POINT('Ctrl Pts',(68.3936911683374,326.232866013246,51.97401681086));
#44884=CARTESIAN_POINT('Ctrl Pts',(72.3053343322745,325.596397984589,46.9134880641335));
#44885=CARTESIAN_POINT('Ctrl Pts',(78.6781933351392,324.959929955932,47.4580719126135));
#44886=CARTESIAN_POINT('Ctrl Pts',(81.6647915036336,324.323461927275,53.1279719129468));
#44887=CARTESIAN_POINT('Ctrl Pts',(79.0332371365105,323.793071903394,57.7564805437124));
#44888=CARTESIAN_POINT('Ctrl Pts',(75.3173868460731,323.36875988429,58.8804754304867));
#44889=CARTESIAN_POINT('Ctrl Pts',(71.4989396689043,322.944447865185,58.1802118789516));
#44890=CARTESIAN_POINT('Ctrl Pts',(68.3650037426683,322.414057841304,53.8759562937844));
#44891=CARTESIAN_POINT('Ctrl Pts',(70.6970252219288,321.777589812648,47.9069353980174));
#44892=CARTESIAN_POINT('Ctrl Pts',(76.9686349527099,321.14112178399,46.6512225235155));
#44893=CARTESIAN_POINT('Ctrl Pts',(81.423028119083,320.504653755334,51.2412426713785));
#44894=CARTESIAN_POINT('Ctrl Pts',(79.9599909415306,319.868185726676,57.4803978105727));
#44895=CARTESIAN_POINT('Ctrl Pts',(74.9381325114026,319.337795702796,59.2493264241543));
#44896=CARTESIAN_POINT('Ctrl Pts',(71.3956405454282,318.913483683691,57.6613533269502));
#44897=CARTESIAN_POINT('Ctrl Pts',(68.9719051551272,318.489171664587,54.6287942353181));
#44898=CARTESIAN_POINT('Ctrl Pts',(69.4282117128379,317.958781640705,49.3240836063029));
#44899=CARTESIAN_POINT('Ctrl Pts',(75.1029347411933,317.322313612049,46.3466596886709));
#44900=CARTESIAN_POINT('Ctrl Pts',(80.6613895661029,316.685845583392,49.511068543079));
#44901=CARTESIAN_POINT('Ctrl Pts',(81.014641016088,316.049377554735,55.8973911822435));
#44902=CARTESIAN_POINT('Ctrl Pts',(75.8188643388059,315.412909526078,59.6485829067018));
#44903=CARTESIAN_POINT('Ctrl Pts',(70.8674386639765,314.882519502197,57.6911472579929));
#44904=CARTESIAN_POINT('Ctrl Pts',(69.2341445588646,314.458207483093,54.1693212752611));
#44905=CARTESIAN_POINT('Ctrl Pts',(69.3927639357589,314.033895463987,50.2904364123513));
#44906=CARTESIAN_POINT('Ctrl Pts',(73.2157203846311,313.503505440107,46.5846066102391));
#44907=CARTESIAN_POINT('Ctrl Pts',(79.452501086146,312.86703741145,48.0577329167871));
#44908=CARTESIAN_POINT('Ctrl Pts',(81.5741291552425,312.230569382793,54.0916866599676));
#44909=CARTESIAN_POINT('Ctrl Pts',(77.6531438362427,311.594101354136,59.1449803944151));
#44910=CARTESIAN_POINT('Ctrl Pts',(71.2705853255733,310.95763332548,58.5701051977721));
#44911=CARTESIAN_POINT('Ctrl Pts',(68.8158168069635,310.427243301598,53.8454589621013));
#44912=CARTESIAN_POINT('Ctrl Pts',(69.8920431913756,310.002931282494,50.1154931906856));
#44913=CARTESIAN_POINT('Ctrl Pts',(72.5552930136327,309.578619263389,47.2909563665877));
#44914=CARTESIAN_POINT('Ctrl Pts',(77.8716307581055,309.048229239508,46.9998833192451));
#44915=CARTESIAN_POINT('Ctrl Pts',(81.6144140660285,308.411761210852,52.2017202778367));
#44916=CARTESIAN_POINT('Ctrl Pts',(79.2596065617769,307.775293182194,58.1485501103052));
#44917=CARTESIAN_POINT('Ctrl Pts',(72.985687726908,307.138825153538,59.39267465869));
#44918=CARTESIAN_POINT('Ctrl Pts',(68.5438343362777,306.50235712488,54.7734243851087));
#44919=CARTESIAN_POINT('Ctrl Pts',(69.7885723489147,305.971967101,49.5966688556199));
#44920=CARTESIAN_POINT('Ctrl Pts',(73.0469626822795,305.547655081895,47.4862659742077));
#44921=CARTESIAN_POINT('Ctrl Pts',(76.909836648915,305.123343062791,47.1001149618732));
#44922=CARTESIAN_POINT('Ctrl Pts',(81.1145224710317,304.59295303891,50.3664259803601));
#44923=CARTESIAN_POINT('Ctrl Pts',(80.5293250469464,303.956485010253,56.7480463552083));
#44924=CARTESIAN_POINT('Ctrl Pts',(74.8519499260711,303.320016981596,59.6937746480561));
#44925=CARTESIAN_POINT('Ctrl Pts',(69.2993505210926,302.683548952939,56.5191024939194));
#44926=CARTESIAN_POINT('Ctrl Pts',(68.9747335748927,302.047080924282,50.1189338655102));
#44927=CARTESIAN_POINT('Ctrl Pts',(73.3090500016354,301.516690900401,47.0267062469374));
#44928=CARTESIAN_POINT('Ctrl Pts',(77.1529760290398,301.092378881297,47.569974672562));
#44929=CARTESIAN_POINT('Ctrl Pts',(80.3226457526307,300.668066862192,49.8114254817008));
#44930=CARTESIAN_POINT('Ctrl Pts',(81.355361673332,300.137676838312,55.0346111340902));
#44931=CARTESIAN_POINT('Ctrl Pts',(76.728933306676,299.501208809654,59.4689876632131));
#44932=CARTESIAN_POINT('Ctrl Pts',(70.5109339842768,298.864740780998,57.9701921918225));
#44933=CARTESIAN_POINT('Ctrl Pts',(68.40045667283,298.22827275234,51.9323292456896));
#44934=CARTESIAN_POINT('Ctrl Pts',(72.3521401674818,297.591804723684,46.8873582654032));
#44935=CARTESIAN_POINT('Ctrl Pts',(77.6521973570184,297.061414699802,47.3948662159206));
#44936=CARTESIAN_POINT('Ctrl Pts',(80.1981152800705,296.637102680698,50.3256015870383));
#44937=CARTESIAN_POINT('Ctrl Pts',(81.1214260671454,296.212790661593,54.0963316326538));
#44938=CARTESIAN_POINT('Ctrl Pts',(78.4761358999726,295.682400637713,58.717003711871));
#44939=CARTESIAN_POINT('Ctrl Pts',(72.0754506158946,295.045932609055,59.0312687720055));
#44940=CARTESIAN_POINT('Ctrl Pts',(68.3636791850171,294.409464580399,53.8223671331437));
#44941=CARTESIAN_POINT('Ctrl Pts',(70.7294688552404,293.772996551742,47.8798977243302));
#44942=CARTESIAN_POINT('Ctrl Pts',(77.0211072714768,293.136528523085,46.6621864805733));
#44943=CARTESIAN_POINT('Ctrl Pts',(80.6898495626673,292.606138499204,50.5207484579202));
#44944=CARTESIAN_POINT('Ctrl Pts',(80.6902463228452,292.181826480099,54.4028751597447));
#44945=CARTESIAN_POINT('Ctrl Pts',(78.9147710729384,291.757514460995,57.8552070562179));
#44946=CARTESIAN_POINT('Ctrl Pts',(73.8876807942301,291.227124437114,59.6092121479762));
#44947=CARTESIAN_POINT('Ctrl Pts',(68.849107759653,290.590656408457,55.6493742208554));
#44948=CARTESIAN_POINT('Ctrl Pts',(69.4623515772426,289.9541883798,49.2827553804812));
#44949=CARTESIAN_POINT('Ctrl Pts',(75.145158953817,289.317720351143,46.3475205075674));
#44950=CARTESIAN_POINT('Ctrl Pts',(80.6938166586057,288.681252322486,49.5537538597928));
#44951=CARTESIAN_POINT('Ctrl Pts',(80.9335411973356,288.150862298606,54.8726543737833));
#44952=CARTESIAN_POINT('Ctrl Pts',(78.3882223800832,287.726550279501,57.8039100782516));
#44953=CARTESIAN_POINT('Ctrl Pts',(74.7839532242394,287.302238260396,59.246183193397));
#44954=CARTESIAN_POINT('Ctrl Pts',(69.8383632853863,286.771848236515,57.2740496561053));
#44955=CARTESIAN_POINT('Ctrl Pts',(68.6308295619551,286.135380207858,50.9804499754289));
#44956=CARTESIAN_POINT('Ctrl Pts',(73.268595959504,285.498912179202,46.5757903654038));
#44957=CARTESIAN_POINT('Ctrl Pts',(79.4838157937093,284.862444150545,48.086070422519));
#44958=CARTESIAN_POINT('Ctrl Pts',(81.5706215770567,284.225976121887,54.1451773085559));
#44959=CARTESIAN_POINT('Ctrl Pts',(78.2638620892544,283.695586098007,58.3181273708052));
#44960=CARTESIAN_POINT('Ctrl Pts',(74.4200471881275,283.271274078902,58.8621814970761));
#44961=CARTESIAN_POINT('Ctrl Pts',(70.7530948079326,282.846962059797,57.5876744834349));
#44962=CARTESIAN_POINT('Ctrl Pts',(68.3123700687952,282.316572035917,52.8557580344726));
#44963=CARTESIAN_POINT('Ctrl Pts',(71.5275734779309,281.68010400726,47.3122932630761));
#44964=CARTESIAN_POINT('Ctrl Pts',(77.9173327360281,281.043635978603,47.0278990613398));
#44965=CARTESIAN_POINT('Ctrl Pts',(81.6194748985279,280.407167949946,52.2436489448233));
#44966=CARTESIAN_POINT('Ctrl Pts',(79.221883044505,279.770699921289,58.1866353940218));
#44967=CARTESIAN_POINT('Ctrl Pts',(73.9889689229884,279.240309897408,59.1688677132986));
#44968=CARTESIAN_POINT('Ctrl Pts',(70.7301472839238,278.815997878304,57.0591309024144));
#44969=CARTESIAN_POINT('Ctrl Pts',(68.7973374677702,278.391685859198,53.6923588428567));
#44970=CARTESIAN_POINT('Ctrl Pts',(70.0574457782005,277.861295835319,48.5193232177926));
#44971=CARTESIAN_POINT('Ctrl Pts',(76.1199198830696,277.224827806661,46.4423200012274));
#44972=CARTESIAN_POINT('Ctrl Pts',(81.1306566444992,276.588359778005,50.4175458496641));
#44973=CARTESIAN_POINT('Ctrl Pts',(80.5056521700667,275.951891749347,56.7830209179806));
#44974=CARTESIAN_POINT('Ctrl Pts',(74.7984951898932,275.315423720691,59.6977925792757));
#44975=CARTESIAN_POINT('Ctrl Pts',(70.2035816423413,274.78503369681,57.008008197077));
#44976=CARTESIAN_POINT('Ctrl Pts',(69.1265928622935,274.360721677705,53.2782624880387));
#44977=CARTESIAN_POINT('Ctrl Pts',(69.8750124991416,273.936409658601,49.4689612484914));
#44978=CARTESIAN_POINT('Ctrl Pts',(74.2184942159277,273.406019634719,46.389620879493));
#44979=CARTESIAN_POINT('Ctrl Pts',(80.1575950910935,272.769551606063,48.796821624848));
#44980=CARTESIAN_POINT('Ctrl Pts',(81.3340222132102,272.133083577406,55.0837861280693));
#44981=CARTESIAN_POINT('Ctrl Pts',(76.6881265535354,271.496615548749,59.4798704036303));
#44982=CARTESIAN_POINT('Ctrl Pts',(70.4679411286712,270.860147520092,57.9381739632954));
#44983=CARTESIAN_POINT('Ctrl Pts',(68.7625597545307,270.329757496211,52.8943812533468));
#44984=CARTESIAN_POINT('Ctrl Pts',(70.3951339519087,269.905445477106,49.3722214931296));
#44985=CARTESIAN_POINT('Ctrl Pts',(73.4580535169106,269.481133458002,46.9869685453763));
#44986=CARTESIAN_POINT('Ctrl Pts',(78.7565799488251,268.950743434121,47.5102162711232));
#44987=CARTESIAN_POINT('Ctrl Pts',(81.6621171947612,268.314275405464,53.2220800603177));
#44988=CARTESIAN_POINT('Ctrl Pts',(78.4277792530005,267.677807376808,58.7401378270421));
#44989=CARTESIAN_POINT('Ctrl Pts',(72.0375055083273,267.04133934815,59.0127270905129));
#44990=CARTESIAN_POINT('Ctrl Pts',(68.3522149334259,266.404871319494,53.7700018438139));
#44991=CARTESIAN_POINT('Ctrl Pts',(70.3720114990969,265.874481295612,48.8436855359119));
#44992=CARTESIAN_POINT('Ctrl Pts',(73.9141788037828,265.450169276508,47.2549883740677));
#44993=CARTESIAN_POINT('Ctrl Pts',(77.7907517378467,265.025857257403,47.4625701009125));
#44994=CARTESIAN_POINT('Ctrl Pts',(81.4480173029673,264.495467233522,51.3320118072031));
#44995=CARTESIAN_POINT('Ctrl Pts',(79.8962625176273,263.858999204865,57.5496955978126));
#44996=CARTESIAN_POINT('Ctrl Pts',(73.83600196959,263.222531176209,59.5949695472677));
#44997=CARTESIAN_POINT('Ctrl Pts',(68.8326175982397,262.586063147551,55.6104936380737));
#44998=CARTESIAN_POINT('Ctrl Pts',(69.4880334727284,261.949595118895,49.2357022951904));
#44999=CARTESIAN_POINT('Ctrl Pts',(74.2432971283764,261.419205095013,46.8407830695233));
#45000=CARTESIAN_POINT('Ctrl Pts',(77.959377089695,260.994893075909,47.9640183999525));
#45001=CARTESIAN_POINT('Ctrl Pts',(80.7500624399219,260.570581056804,50.6627186727628));
#45002=CARTESIAN_POINT('Ctrl Pts',(80.973987939756,260.040191032924,55.982307745494));
#45003=CARTESIAN_POINT('Ctrl Pts',(75.7253090599096,259.403723004267,59.6591140566951));
#45004=CARTESIAN_POINT('Ctrl Pts',(69.8086851766418,258.76725497561,57.2294092881355));
#45005=CARTESIAN_POINT('Ctrl Pts',(68.64387461178,258.130786946953,50.9402821796723));
#45006=CARTESIAN_POINT('Ctrl Pts',(73.3188397393547,257.494318918296,46.5571057413125));
#45007=CARTESIAN_POINT('Ctrl Pts',(78.4794664963865,256.963928894415,47.8671065072692));
#45008=CARTESIAN_POINT('Ctrl Pts',(80.5485605550081,256.539616875311,51.1518831607137));
#45009=CARTESIAN_POINT('Ctrl Pts',(80.8859079471689,256.115304856205,55.0193247728702));
#45010=CARTESIAN_POINT('Ctrl Pts',(77.5667687190911,255.584914832326,59.1824348262834));
#45011=CARTESIAN_POINT('Ctrl Pts',(71.193045766207,254.948446803668,58.5167093921053));
#45012=CARTESIAN_POINT('Ctrl Pts',(68.3192351039939,254.311978775012,52.8025939123332));
#45013=CARTESIAN_POINT('Ctrl Pts',(71.5637615965536,253.675510746354,47.2905206837289));
#45014=CARTESIAN_POINT('Ctrl Pts',(77.9675186861103,253.039042717698,47.0467384616874));
#45015=CARTESIAN_POINT('Ctrl Pts',(81.0047745224026,252.508652693817,51.4197520126738));
#45016=CARTESIAN_POINT('Ctrl Pts',(80.4130157998748,252.084340674712,55.2565122997844));
#45017=CARTESIAN_POINT('Ctrl Pts',(78.1317232526417,251.660028655607,58.3976286937398));
#45018=CARTESIAN_POINT('Ctrl Pts',(72.8959148267621,251.129638631727,59.3643140922468));
#45019=CARTESIAN_POINT('Ctrl Pts',(68.5203052848772,250.493170603069,54.6822658470019));
#45020=CARTESIAN_POINT('Ctrl Pts',(70.0974900542959,249.856702574413,48.4836860385676));
#45021=CARTESIAN_POINT('Ctrl Pts',(76.1615187036544,249.220234545756,46.4496113157072));
#45022=CARTESIAN_POINT('Ctrl Pts',(81.1561933875673,248.583766517099,50.4646778700389));
#45023=CARTESIAN_POINT('Ctrl Pts',(80.5818071049249,248.053376493218,55.7579047620688));
#45024=CARTESIAN_POINT('Ctrl Pts',(77.6191604611375,247.629064474113,58.2666161345652));
#45025=CARTESIAN_POINT('Ctrl Pts',(73.8370732189359,247.204752455009,59.1422438972669));
#45026=CARTESIAN_POINT('Ctrl Pts',(69.2501690271641,246.674362431128,56.4388237546138));
#45027=CARTESIAN_POINT('Ctrl Pts',(69.0167443893414,246.037894402471,50.0346807540015));
#45028=CARTESIAN_POINT('Ctrl Pts',(74.2720958288138,245.401426373814,46.3889730468402));
#45029=CARTESIAN_POINT('Ctrl Pts',(80.1842209746279,244.764958345157,48.8296040510377));
#45030=CARTESIAN_POINT('Ctrl Pts',(81.3223966119943,244.1284903165,55.1361158327074));
#45031=CARTESIAN_POINT('Ctrl Pts',(77.4178204841707,243.598100292619,58.7558472860377));
#45032=CARTESIAN_POINT('Ctrl Pts',(73.5359982239256,243.173788273515,58.7072280891914));
#45033=CARTESIAN_POINT('Ctrl Pts',(70.1063587579266,242.74947625441,56.8883050507697));
#45034=CARTESIAN_POINT('Ctrl Pts',(68.415965773611,242.21908623053,51.8394693344116));
#45035=CARTESIAN_POINT('Ctrl Pts',(72.4391053296256,241.582618201872,46.8512950444875));
#45036=CARTESIAN_POINT('Ctrl Pts',(78.7974738286708,240.946150173216,47.5448752264207));
#45037=CARTESIAN_POINT('Ctrl Pts',(81.6607233194671,240.309682144558,53.2642900384335));
#45038=CARTESIAN_POINT('Ctrl Pts',(78.3846879127202,239.673214115902,58.7720233877865));
#45039=CARTESIAN_POINT('Ctrl Pts',(73.0631846035857,239.14282409202,58.9445721144314));
#45040=CARTESIAN_POINT('Ctrl Pts',(70.1642998769843,238.718512072917,56.3624460082323));
#45041=CARTESIAN_POINT('Ctrl Pts',(68.7676494101067,238.294200053811,52.740253942672));
#45042=CARTESIAN_POINT('Ctrl Pts',(70.8020690104725,237.763810029931,47.8199584818442));
#45043=CARTESIAN_POINT('Ctrl Pts',(77.1104133983672,237.127342001273,46.6919843165582));
#45044=CARTESIAN_POINT('Ctrl Pts',(81.4561652353981,236.490873972617,51.3849944816189));
#45045=CARTESIAN_POINT('Ctrl Pts',(79.8675318896678,235.854405943959,57.5806500184647));
#45046=CARTESIAN_POINT('Ctrl Pts',(73.7825598716915,235.217937915303,59.5907868730799));
#45047=CARTESIAN_POINT('Ctrl Pts',(69.6516937528243,234.687547891422,56.2316030971915));
#45048=CARTESIAN_POINT('Ctrl Pts',(69.1562151927476,234.263235872318,52.3812253387187));
#45049=CARTESIAN_POINT('Ctrl Pts',(70.4769197368907,233.838923853213,48.7306572468295));
#45050=CARTESIAN_POINT('Ctrl Pts',(75.2392757088466,233.308533829332,46.3498724752568));
#45051=CARTESIAN_POINT('Ctrl Pts',(80.7417032823629,232.672065800675,49.634811657659));
#45052=CARTESIAN_POINT('Ctrl Pts',(80.9453973953874,232.035597772018,56.027652352275));
#45053=CARTESIAN_POINT('Ctrl Pts',(75.683319836815,231.399129743361,59.6636450923455));
#45054=CARTESIAN_POINT('Ctrl Pts',(69.7710792277636,230.762661714704,57.1912079111794));
#45055=CARTESIAN_POINT('Ctrl Pts',(68.8549962387284,230.232271690823,51.9463092001141));
#45056=CARTESIAN_POINT('Ctrl Pts',(71.0057109233227,229.807959671719,48.71438496963));
#45057=CARTESIAN_POINT('Ctrl Pts',(74.3966183648981,229.383647652614,46.8242382530895));
#45058=CARTESIAN_POINT('Ctrl Pts',(79.5533314475779,228.853257628733,48.1495611239604));
#45059=CARTESIAN_POINT('Ctrl Pts',(81.553624002664,228.216789600076,54.2377763246406));
#45060=CARTESIAN_POINT('Ctrl Pts',(77.5154492131354,227.58032157142,59.1979222716756));
#45061=CARTESIAN_POINT('Ctrl Pts',(71.1583728874286,226.943853542763,58.492596811605));
#45062=CARTESIAN_POINT('Ctrl Pts',(68.3158924128625,226.307385514106,52.7490927066299));
#45063=CARTESIAN_POINT('Ctrl Pts',(71.0634780017905,225.776995490225,48.1885067791575));
#45064=CARTESIAN_POINT('Ctrl Pts',(74.8065245107504,225.35268347112,47.1586958035716));
#45065=CARTESIAN_POINT('Ctrl Pts',(78.6060725394363,224.928371452016,47.955152209226));
#45066=CARTESIAN_POINT('Ctrl Pts',(81.6303263902578,224.397981428135,52.3371676064709));
#45067=CARTESIAN_POINT('Ctrl Pts',(79.1483302191681,223.761513399478,58.2454016254753));
#45068=CARTESIAN_POINT('Ctrl Pts',(72.8470130986032,223.125045370821,59.3423554510688));
#45069=CARTESIAN_POINT('Ctrl Pts',(68.5099388049065,222.488577342164,54.6413249332986));
#45070=CARTESIAN_POINT('Ctrl Pts',(70.1300482334095,221.852109313507,48.4411008882662));
#45071=CARTESIAN_POINT('Ctrl Pts',(75.1949720228243,221.321719289626,46.7995385915325));
#45072=CARTESIAN_POINT('Ctrl Pts',(78.6962367276934,220.897407270522,48.4764536776389));
#45073=CARTESIAN_POINT('Ctrl Pts',(81.0426295882978,220.473095251417,51.5692452983744));
#45074=CARTESIAN_POINT('Ctrl Pts',(80.4525183097322,219.942705227537,56.8607430811448));
#45075=CARTESIAN_POINT('Ctrl Pts',(74.7044349299368,219.306237198879,59.6939299756169));
#45076=CARTESIAN_POINT('Ctrl Pts',(69.2276352050903,218.669769170223,56.3901794069435));
#45077=CARTESIAN_POINT('Ctrl Pts',(69.0357866029293,218.033301141565,49.9969717623945));
#45078=CARTESIAN_POINT('Ctrl Pts',(74.3245562273971,217.396833112908,46.3781728935986));
#45079=CARTESIAN_POINT('Ctrl Pts',(79.2251026994422,216.866443089028,48.4600028300045));
#45080=CARTESIAN_POINT('Ctrl Pts',(80.7687641568812,216.442131069923,52.0219549838932));
#45081=CARTESIAN_POINT('Ctrl Pts',(80.5126174062247,216.017819050818,55.895581808213));
#45082=CARTESIAN_POINT('Ctrl Pts',(76.5965009308421,215.487429026938,59.503735860729));
#45083=CARTESIAN_POINT('Ctrl Pts',(70.4003730145984,214.85096099828,57.873534909508));
#45084=CARTESIAN_POINT('Ctrl Pts',(68.429181621647,214.214492969624,51.7880485052417));
#45085=CARTESIAN_POINT('Ctrl Pts',(72.4813418470979,213.578024940966,46.8351607156745));
#45086=CARTESIAN_POINT('Ctrl Pts',(78.8381545815176,212.94155691231,47.5713888109593));
#45087=CARTESIAN_POINT('Ctrl Pts',(81.6581187360802,212.305088883653,53.3130386131624));
#45088=CARTESIAN_POINT('Ctrl Pts',(78.3435294198688,211.668620854996,58.7960171796599));
#45089=CARTESIAN_POINT('Ctrl Pts',(73.0203157428126,211.138230831115,58.9307022339566));
#45090=CARTESIAN_POINT('Ctrl Pts',(70.1404093382657,210.713918812011,56.3274859477036));
#45091=CARTESIAN_POINT('Ctrl Pts',(68.7697904747173,210.289606792905,52.6954344925807));
#45092=CARTESIAN_POINT('Ctrl Pts',(70.8397506710645,209.759216769025,47.7898625183533));
#45093=CARTESIAN_POINT('Ctrl Pts',(77.1560180005676,209.122748740368,46.7074779213906));
#45094=CARTESIAN_POINT('Ctrl Pts',(81.4678228126991,208.486280711711,51.4316973420522));
#45095=CARTESIAN_POINT('Ctrl Pts',(79.8345150471389,207.849812683054,57.6157420369948));
#45096=CARTESIAN_POINT('Ctrl Pts',(73.7352061577403,207.213344654398,59.5819163913665));
#45097=CARTESIAN_POINT('Ctrl Pts',(69.6286797739237,206.682954630516,56.1930196438724));
#45098=CARTESIAN_POINT('Ctrl Pts',(69.1609966055946,206.258642611412,52.3391654795781));
#45099=CARTESIAN_POINT('Ctrl Pts',(70.5080046768267,205.834330592307,48.6982221958113));
#45100=CARTESIAN_POINT('Ctrl Pts',(75.2874147618561,205.303940568427,46.3518592644304));
#45101=CARTESIAN_POINT('Ctrl Pts',(80.7659978619589,204.667472539769,49.6764133674932));
#45102=CARTESIAN_POINT('Ctrl Pts',(80.9235624218643,204.031004511113,56.0705571543901));
#45103=CARTESIAN_POINT('Ctrl Pts',(75.6353879853842,203.394536482455,59.668489377038));
#45104=CARTESIAN_POINT('Ctrl Pts',(69.7411399911392,202.758068453799,57.153459596108));
#45105=CARTESIAN_POINT('Ctrl Pts',(68.8629228367167,202.227678429917,51.902087877635));
#45106=CARTESIAN_POINT('Ctrl Pts',(71.0368999365241,201.803366410813,48.6857651951434));
#45107=CARTESIAN_POINT('Ctrl Pts',(74.4413565467986,201.379054391709,46.8201331300155));
#45108=CARTESIAN_POINT('Ctrl Pts',(79.5883731887436,200.848664367828,48.1826272613378));
#45109=CARTESIAN_POINT('Ctrl Pts',(81.5446871133722,200.212196339171,54.2851161372355));
#45110=CARTESIAN_POINT('Ctrl Pts',(77.4708299078219,199.575728310514,59.2159974868797));
#45111=CARTESIAN_POINT('Ctrl Pts',(71.1190079787084,198.939260281857,58.4648239866103));
#45112=CARTESIAN_POINT('Ctrl Pts',(68.3180409606457,198.3027922532,52.7009608376928));
#45113=CARTESIAN_POINT('Ctrl Pts',(71.098459721967,197.77240222932,48.1603174867096));
#45114=CARTESIAN_POINT('Ctrl Pts',(74.8488389159196,197.348090210214,47.1575394509773));
#45115=CARTESIAN_POINT('Ctrl Pts',(78.6425415842146,196.92377819111,47.9813889218711));
#45116=CARTESIAN_POINT('Ctrl Pts',(81.6351004541037,196.393388167229,52.3851102961616));
#45117=CARTESIAN_POINT('Ctrl Pts',(79.11054081409,195.756920138572,58.2752828961914));
#45118=CARTESIAN_POINT('Ctrl Pts',(72.8014733044529,195.120452109916,59.3267440686173));
#45119=CARTESIAN_POINT('Ctrl Pts',(68.498429651078,194.483984081258,54.5945438662197));
#45120=CARTESIAN_POINT('Ctrl Pts',(70.1632321105985,193.847516052601,48.4061702992275));
#45121=CARTESIAN_POINT('Ctrl Pts',(75.2398670646046,193.317126028721,46.8011942632874));
#45122=CARTESIAN_POINT('Ctrl Pts',(78.7289430044913,192.892814009616,48.5033273286335));
#45123=CARTESIAN_POINT('Ctrl Pts',(81.0529576331648,192.468501990511,51.6129678049825));
#45124=CARTESIAN_POINT('Ctrl Pts',(80.4246892842127,191.938111966631,56.9000699804562));
#45125=CARTESIAN_POINT('Ctrl Pts',(74.65630346539,191.301643937974,59.6917110173807));
#45126=CARTESIAN_POINT('Ctrl Pts',(69.2035016326957,190.665175909317,56.3485305538422));
#45127=CARTESIAN_POINT('Ctrl Pts',(69.0577500836245,190.02870788066,49.9541064261852));
#45128=CARTESIAN_POINT('Ctrl Pts',(74.3725601345045,189.392239852003,46.3735577591653));
#45129=CARTESIAN_POINT('Ctrl Pts',(79.2578336803251,188.861849828122,48.4906956655628));
#45130=CARTESIAN_POINT('Ctrl Pts',(80.7759409611788,188.437537809017,52.0636857537459));
#45131=CARTESIAN_POINT('Ctrl Pts',(80.4914882630651,188.013225789913,55.9353771863079));
#45132=CARTESIAN_POINT('Ctrl Pts',(76.5502474625308,187.482835766032,59.515152526242));
#45133=CARTESIAN_POINT('Ctrl Pts',(70.3645745965685,186.846367737375,57.8403433343832));
#45134=CARTESIAN_POINT('Ctrl Pts',(68.4399397736334,186.209899708718,51.7406970957261));
#45135=CARTESIAN_POINT('Ctrl Pts',(72.5228993479575,185.573431680061,46.8173502104404));
#45136=CARTESIAN_POINT('Ctrl Pts',(78.8834323500699,184.936963651404,47.5991139617571));
#45137=CARTESIAN_POINT('Ctrl Pts',(81.1835349749613,184.406573627523,52.4009571960959));
#45138=CARTESIAN_POINT('Ctrl Pts',(79.9867931126735,183.982261608419,56.094020531795));
#45139=CARTESIAN_POINT('Ctrl Pts',(77.2332563931867,183.557949589314,58.8306139288627));
#45140=CARTESIAN_POINT('Ctrl Pts',(71.9102716857639,183.027559565433,58.9489538491949));
#45141=CARTESIAN_POINT('Ctrl Pts',(68.3383237334809,182.391091536777,53.6283596662101));
#45142=CARTESIAN_POINT('Ctrl Pts',(70.8849370199572,181.754623508119,47.761106117269));
#45143=CARTESIAN_POINT('Ctrl Pts',(77.1959362348037,181.118155479463,46.7213021219764));
#45144=CARTESIAN_POINT('Ctrl Pts',(81.4854978487712,180.481687450805,51.482309976812));
#45145=CARTESIAN_POINT('Ctrl Pts',(80.073367272166,179.951297426925,56.6159303140414));
#45146=CARTESIAN_POINT('Ctrl Pts',(76.7481860199208,179.52698540782,58.6194466045056));
#45147=CARTESIAN_POINT('Ctrl Pts',(72.8748126305075,179.102673388715,58.8799969309715));
#45148=CARTESIAN_POINT('Ctrl Pts',(68.7783742806616,178.572283364835,55.4789142536309));
#45149=CARTESIAN_POINT('Ctrl Pts',(69.5704243653522,177.935815336178,49.1196539745438));
#45150=CARTESIAN_POINT('Ctrl Pts',(75.340431971015,177.299347307521,46.3597779503322));
#45151=CARTESIAN_POINT('Ctrl Pts',(80.7870483010708,176.662879278864,49.7130262250032));
#45152=CARTESIAN_POINT('Ctrl Pts',(80.9037309672252,176.026411250207,56.1203595072083));
#45153=CARTESIAN_POINT('Ctrl Pts',(76.4713185355127,175.496021226327,59.0702562117385));
#45154=CARTESIAN_POINT('Ctrl Pts',(72.6470540467699,175.071709207221,58.4024920268817));
#45155=CARTESIAN_POINT('Ctrl Pts',(69.551817146766,174.647397188117,56.0593282640832));
#45156=CARTESIAN_POINT('Ctrl Pts',(68.6892013076634,174.117007164236,50.8053712366301));
#45157=CARTESIAN_POINT('Ctrl Pts',(73.4571407575176,173.480539135579,46.5235155598984));
#45158=CARTESIAN_POINT('Ctrl Pts',(79.6232088666685,172.844071106923,48.2233707042361));
#45159=CARTESIAN_POINT('Ctrl Pts',(81.5365719076763,172.207603078265,54.3265621080611));
#45160=CARTESIAN_POINT('Ctrl Pts',(77.4232005111353,171.571135049609,59.2405940969629));
#45161=CARTESIAN_POINT('Ctrl Pts',(72.1424114296051,171.040745025728,58.5613024007155));
#45162=CARTESIAN_POINT('Ctrl Pts',(69.692973246283,170.616433006623,55.5494656733147));
#45163=CARTESIAN_POINT('Ctrl Pts',(68.8925550574566,170.192120987518,51.7507502839452));
#45164=CARTESIAN_POINT('Ctrl Pts',(71.6864479885501,169.661730963638,47.2183852476993));
#45165=CARTESIAN_POINT('Ctrl Pts',(78.0939616097122,169.025262934981,47.1120657835623));
#45166=CARTESIAN_POINT('Ctrl Pts',(81.6346846946041,168.388794906324,52.43871421147));
#45167=CARTESIAN_POINT('Ctrl Pts',(79.0772365788344,167.752326877667,58.301253130195));
#45168=CARTESIAN_POINT('Ctrl Pts',(72.7493845539464,167.11585884901,59.3140825259745));
#45169=CARTESIAN_POINT('Ctrl Pts',(69.207833010338,166.585468825129,55.3384589024206));
#45170=CARTESIAN_POINT('Ctrl Pts',(69.3334586153764,166.161156806024,51.4583653347606));
#45171=CARTESIAN_POINT('Ctrl Pts',(71.2200682242025,165.73684478692,48.0654886688141));
#45172=CARTESIAN_POINT('Ctrl Pts',(76.3014478199115,165.206454763039,46.4755981265107));
#45173=CARTESIAN_POINT('Ctrl Pts',(81.20882052468,164.569986734382,50.5969119668202));
#45174=CARTESIAN_POINT('Ctrl Pts',(80.3892258098679,163.933518705725,56.940268171691));
#45175=CARTESIAN_POINT('Ctrl Pts',(74.6141294504006,163.297050677068,59.6894799636937));
#45176=CARTESIAN_POINT('Ctrl Pts',(69.1724772872813,162.660582648411,56.3048150808067));
#45177=CARTESIAN_POINT('Ctrl Pts',(69.1055420061302,162.13019262453,50.980935837216));
#45178=CARTESIAN_POINT('Ctrl Pts',(71.7446741979597,161.705880605426,48.1338515110173));
#45179=CARTESIAN_POINT('Ctrl Pts',(75.3938630579889,161.281568586321,46.8093408276792));
#45180=CARTESIAN_POINT('Ctrl Pts',(80.27282681849,160.751178562441,48.9409794358665));
#45181=CARTESIAN_POINT('Ctrl Pts',(81.2754203909972,160.114710533783,55.2704613074101));
#45182=CARTESIAN_POINT('Ctrl Pts',(76.4971135606888,159.478242505127,59.5222476700871));
#45183=CARTESIAN_POINT('Ctrl Pts',(70.334196289122,158.841774476469,57.8110042209413));
#45184=CARTESIAN_POINT('Ctrl Pts',(68.4451819243434,158.205306447813,51.6873485020516));
#45185=CARTESIAN_POINT('Ctrl Pts',(71.8856615424623,157.674916423932,47.6239422302756));
#45186=CARTESIAN_POINT('Ctrl Pts',(75.7451117847744,157.250604404827,47.2049533120979));
#45187=CARTESIAN_POINT('Ctrl Pts',(79.3687583251269,156.826292385722,48.5978257531446));
#45188=CARTESIAN_POINT('Ctrl Pts',(81.6545885653878,156.295902361842,53.4064794779313));
#45189=CARTESIAN_POINT('Ctrl Pts',(78.2611269268695,155.659434333185,58.8426502572334));
#45190=CARTESIAN_POINT('Ctrl Pts',(71.8655032454052,155.022966304528,58.9194692881673));
#45191=CARTESIAN_POINT('Ctrl Pts',(68.33462666264,154.386498275871,53.5862888115946));
#45192=CARTESIAN_POINT('Ctrl Pts',(70.9238769856076,153.750030247214,47.7242654920534));
#45193=CARTESIAN_POINT('Ctrl Pts',(76.1859185490112,153.219640223333,46.9124224547526));
#45194=CARTESIAN_POINT('Ctrl Pts',(79.3745360971544,152.795328204228,49.1268356994087));
#45195=CARTESIAN_POINT('Ctrl Pts',(81.1970346167882,152.371016185124,52.5545765052998));
#45196=CARTESIAN_POINT('Ctrl Pts',(79.7696625991367,151.840626161243,57.6839799458007));
#45197=CARTESIAN_POINT('Ctrl Pts',(73.642959648389,151.204158132586,59.5630876029432));
#45198=CARTESIAN_POINT('Ctrl Pts',(68.7639080710162,150.567690103929,55.4272975763874));
#45199=CARTESIAN_POINT('Ctrl Pts',(69.5952201151085,149.931222075272,49.0854663169038));
#45200=CARTESIAN_POINT('Ctrl Pts',(75.3939889653761,149.294754046615,46.3574973920444));
#45201=CARTESIAN_POINT('Ctrl Pts',(79.8991646679696,148.764364022735,49.1950249110227));
#45202=CARTESIAN_POINT('Ctrl Pts',(80.8545102956352,148.34005200363,52.957766281106));
#45203=CARTESIAN_POINT('Ctrl Pts',(79.9828270161261,147.915739984525,56.740764582277));
#45204=CARTESIAN_POINT('Ctrl Pts',(75.5416724725442,147.385349960645,59.6774833042897));
#45205=CARTESIAN_POINT('Ctrl Pts',(69.6838446044191,146.748881931988,57.0787552882691));
#45206=CARTESIAN_POINT('Ctrl Pts',(68.712125846895,146.112413903331,50.7569148841861));
#45207=CARTESIAN_POINT('Ctrl Pts',(73.4982792811873,145.475945874674,46.5139632297563));
#45208=CARTESIAN_POINT('Ctrl Pts',(79.6651396832196,144.839477846017,48.2567676983297));
#45209=CARTESIAN_POINT('Ctrl Pts',(81.2058899375428,144.309087822136,53.3532624924015));
#45210=CARTESIAN_POINT('Ctrl Pts',(79.4598393053229,143.884775803031,56.8205690949624));
#45211=CARTESIAN_POINT('Ctrl Pts',(76.3211035792066,143.460463783927,59.1051359965959));
#45212=CARTESIAN_POINT('Ctrl Pts',(71.0423553953876,142.930073760046,58.4101625121945));
#45213=CARTESIAN_POINT('Ctrl Pts',(68.3237688121462,142.293605731389,52.6069891024768));
#45214=CARTESIAN_POINT('Ctrl Pts',(71.7355301328902,141.657137702732,47.1968330854384));
#45215=CARTESIAN_POINT('Ctrl Pts',(78.131284816172,141.020669674075,47.1318294725001));
#45216=CARTESIAN_POINT('Ctrl Pts',(81.6444430145778,140.384201645418,52.4914240566834));
#45217=CARTESIAN_POINT('Ctrl Pts',(79.4657921614448,139.853811621537,57.3495771000057));
#45218=CARTESIAN_POINT('Ctrl Pts',(75.8739191842768,139.429499602433,58.8224506187867));
#45219=CARTESIAN_POINT('Ctrl Pts',(72.0061278849508,139.005187583328,58.4891364257266));
#45220=CARTESIAN_POINT('Ctrl Pts',(68.476400198112,138.474797559447,54.5030113663535));
#45221=CARTESIAN_POINT('Ctrl Pts',(70.2291765021866,137.83832953079,48.3389777955731));
#45222=CARTESIAN_POINT('Ctrl Pts',(76.3526370626844,137.201861502133,46.4915108263287));
#45223=CARTESIAN_POINT('Ctrl Pts',(81.2240398481348,136.565393473476,50.6363073641968));
#45224=CARTESIAN_POINT('Ctrl Pts',(80.3620300055901,135.928925444819,56.9864627690029));
#45225=CARTESIAN_POINT('Ctrl Pts',(75.5315283240709,135.398535420939,59.2257537364833));
#45226=CARTESIAN_POINT('Ctrl Pts',(71.853869491347,134.974223401834,57.9824784666719));
#45227=CARTESIAN_POINT('Ctrl Pts',(69.1522605248948,134.549911382729,55.1946088716546));
#45228=CARTESIAN_POINT('Ctrl Pts',(69.1011383080979,134.019521358849,49.8705543028932));
#45229=CARTESIAN_POINT('Ctrl Pts',(74.4664079702696,133.383053330192,46.3660691643869));
#45230=CARTESIAN_POINT('Ctrl Pts',(80.3010401637996,132.746585301535,48.9865596918726));
#45231=CARTESIAN_POINT('Ctrl Pts',(81.2610782835899,132.110117272878,55.3101844630753));
#45232=CARTESIAN_POINT('Ctrl Pts',(76.4462897180739,131.473649244221,59.5392914259234));
#45233=CARTESIAN_POINT('Ctrl Pts',(71.3309082217835,130.94325922034,58.0624560662408));
#45234=CARTESIAN_POINT('Ctrl Pts',(69.3695355394668,130.518947201236,54.7122433733663));
#45235=CARTESIAN_POINT('Ctrl Pts',(69.1579113875603,130.094635182131,50.8358890158844));
#45236=CARTESIAN_POINT('Ctrl Pts',(72.6104447936233,129.56424515825,46.7827194398347));
#45237=CARTESIAN_POINT('Ctrl Pts',(78.9591977010965,128.927777129593,47.6549987263476));
#45238=CARTESIAN_POINT('Ctrl Pts',(81.6460013269083,128.291309100936,53.4593927269945));
#45239=CARTESIAN_POINT('Ctrl Pts',(78.2242510960193,127.654841072279,58.8632366177664));
#45240=CARTESIAN_POINT('Ctrl Pts',(71.8159553123667,127.018373043623,58.8990106732897));
#45241=CARTESIAN_POINT('Ctrl Pts',(68.9222576097237,126.487983019741,54.4297060139589));
#45242=CARTESIAN_POINT('Ctrl Pts',(69.6382539201413,126.063671000637,50.6141775879205));
#45243=CARTESIAN_POINT('Ctrl Pts',(72.0203115207733,125.639358981532,47.5487723172087));
#45244=CARTESIAN_POINT('Ctrl Pts',(77.2847411767612,125.108968957652,46.7525619622429));
#45245=CARTESIAN_POINT('Ctrl Pts',(81.5060552979621,124.472500928994,51.5741842746995));
#45246=CARTESIAN_POINT('Ctrl Pts',(79.728482568503,123.836032900338,57.7182984199529));
#45247=CARTESIAN_POINT('Ctrl Pts',(73.6016194435095,123.19956487168,59.5544497443309));
#45248=CARTESIAN_POINT('Ctrl Pts',(68.7399147931205,122.563096843024,55.3793614187719));
#45249=CARTESIAN_POINT('Ctrl Pts',(69.4858278482179,122.032706819143,50.107570048997));
#45250=CARTESIAN_POINT('Ctrl Pts',(72.5283512255512,121.608394800038,47.6963547154323));
#45251=CARTESIAN_POINT('Ctrl Pts',(76.33686993267,121.184082780934,46.9439630993421));
#45252=CARTESIAN_POINT('Ctrl Pts',(80.833597854669,120.653692757053,49.7948591914003));
#45253=CARTESIAN_POINT('Ctrl Pts',(80.8590072572753,120.017224728396,56.2032044533298));
#45254=CARTESIAN_POINT('Ctrl Pts',(75.4880780795087,119.380756699739,59.6763907722353));
#45255=CARTESIAN_POINT('Ctrl Pts',(69.6582969414783,118.744288671082,57.0451258062755));
#45256=CARTESIAN_POINT('Ctrl Pts',(68.7254440554294,118.107820642425,50.7049901510374));
#45257=CARTESIAN_POINT('Ctrl Pts',(72.7454665815478,117.577430618544,47.2139173328772));
#45258=CARTESIAN_POINT('Ctrl Pts',(76.6236647050234,117.153118599439,47.3885231790242));
#45259=CARTESIAN_POINT('Ctrl Pts',(79.9924504918158,116.728806580335,49.3178210329446));
#45260=CARTESIAN_POINT('Ctrl Pts',(81.5180565489095,116.198416556454,54.4188696203192));
#45261=CARTESIAN_POINT('Ctrl Pts',(77.3351104931415,115.561948527797,59.2738152357066));
#45262=CARTESIAN_POINT('Ctrl Pts',(71.002608172017,114.92548049914,58.3741943203373));
#45263=CARTESIAN_POINT('Ctrl Pts',(68.326532179209,114.289012470483,52.5648466186468));
#45264=CARTESIAN_POINT('Ctrl Pts',(71.7796338362221,113.652544441826,47.1663631667719));
#45265=CARTESIAN_POINT('Ctrl Pts',(77.1039338323076,113.122154417946,47.1666527860612));
#45266=CARTESIAN_POINT('Ctrl Pts',(79.9174693977396,112.697842398841,49.8415220367884));
#45267=CARTESIAN_POINT('Ctrl Pts',(81.1957996614328,112.273530379737,53.5071433515677));
#45268=CARTESIAN_POINT('Ctrl Pts',(79.0027289300506,111.743140355855,58.3588040259504));
#45269=CARTESIAN_POINT('Ctrl Pts',(72.6610927960897,111.106672327199,59.2814013261173));
#45270=CARTESIAN_POINT('Ctrl Pts',(68.4699764911283,110.470204298542,54.4497921162674));
#45271=CARTESIAN_POINT('Ctrl Pts',(70.2588968349819,109.833736269885,48.3089723467443));
#45272=CARTESIAN_POINT('Ctrl Pts',(76.4059152161931,109.197268241228,46.4974261411829));
#45273=CARTESIAN_POINT('Ctrl Pts',(80.4255579194777,108.666878217347,49.9889362829594));
#45274=CARTESIAN_POINT('Ctrl Pts',(80.7957838280293,108.242566198242,53.8533690567407));
#45275=CARTESIAN_POINT('Ctrl Pts',(79.3572700732904,107.818254179138,57.4591402729806));
#45276=CARTESIAN_POINT('Ctrl Pts',(74.52013864804,107.287864155257,59.6840740039152));
#45277=CARTESIAN_POINT('Ctrl Pts',(69.1272472113271,106.6513961266,56.2222455007014));
#45278=CARTESIAN_POINT('Ctrl Pts',(69.1311857674209,106.014928097943,49.8261617046435));
#45279=CARTESIAN_POINT('Ctrl Pts',(74.5085221507447,105.378460069286,46.362903576955));
#45280=CARTESIAN_POINT('Ctrl Pts',(80.3373861944358,104.741992040629,49.0259617051221));
#45281=CARTESIAN_POINT('Ctrl Pts',(81.0827257190345,104.211602016748,54.2978341926989));
#45282=CARTESIAN_POINT('Ctrl Pts',(78.8282293448942,103.787289997644,57.4582382784806));
#45283=CARTESIAN_POINT('Ctrl Pts',(75.3777508129794,103.362977978539,59.2373126971688));
#45284=CARTESIAN_POINT('Ctrl Pts',(70.2667783164759,102.832587954658,57.7452903541108));
#45285=CARTESIAN_POINT('Ctrl Pts',(68.4651765033714,102.196119926002,51.5953500665264));
#45286=CARTESIAN_POINT('Ctrl Pts',(72.6622400074956,101.559651897344,46.7689060980581));
#45287=CARTESIAN_POINT('Ctrl Pts',(78.9930695612056,100.923183868688,47.6802241546619));
#45288=CARTESIAN_POINT('Ctrl Pts',(81.647605490126,100.286715840031,53.5129742466773));
#45289=CARTESIAN_POINT('Ctrl Pts',(78.7534215822551,99.7563258161497,57.9819640698496));
#45290=CARTESIAN_POINT('Ctrl Pts',(74.9789179052989,99.3320137970452,58.8897249850046));
#45291=CARTESIAN_POINT('Ctrl Pts',(71.2072270700948,98.9077017779404,57.9703468636246));
#45292=CARTESIAN_POINT('Ctrl Pts',(68.3268166778703,98.3773117540599,53.4924671751376));
#45293=CARTESIAN_POINT('Ctrl Pts',(70.9992987716281,97.7408437254027,47.6679179142612));
#45294=CARTESIAN_POINT('Ctrl Pts',(77.3329042202886,97.1043756967459,46.7760964864426));
#45295=CARTESIAN_POINT('Ctrl Pts',(81.5150874496195,96.4679076680889,51.6154401273427));
#45296=CARTESIAN_POINT('Ctrl Pts',(79.6945588159604,95.8314396394319,57.7598042220118));
#45297=CARTESIAN_POINT('Ctrl Pts',(74.57901668281,95.3010496155514,59.2360830629346));
#45298=CARTESIAN_POINT('Ctrl Pts',(71.1340321876925,94.8767375964465,57.4463932253265));
#45299=CARTESIAN_POINT('Ctrl Pts',(68.8892772267267,94.452425577342,54.2790626376455));
#45300=CARTESIAN_POINT('Ctrl Pts',(69.6508450514793,93.9220355534612,49.0095100019376));
#45301=CARTESIAN_POINT('Ctrl Pts',(75.4878808899357,93.285567524804,46.3644112789393));
#45302=CARTESIAN_POINT('Ctrl Pts',(80.8545285853664,92.6490994961474,49.8442095419927));
#45303=CARTESIAN_POINT('Ctrl Pts',(80.8387738990692,92.0126314674903,56.240275147369));
#45304=CARTESIAN_POINT('Ctrl Pts',(75.4352492268543,91.3761634388334,59.6854827972209));
#45305=CARTESIAN_POINT('Ctrl Pts',(70.6049911897418,90.8457734149526,57.4456663254745));
#45306=CARTESIAN_POINT('Ctrl Pts',(69.1775862436694,90.4214613958479,53.8354830882459));
#45307=CARTESIAN_POINT('Ctrl Pts',(69.5597087935644,89.9971493767433,49.9722085389421));
#45308=CARTESIAN_POINT('Ctrl Pts',(73.5900826298085,89.4667593528626,46.493091226704));
#45309=CARTESIAN_POINT('Ctrl Pts',(79.7314942136654,88.8302913242055,48.3235552092793));
#45310=CARTESIAN_POINT('Ctrl Pts',(81.5014987995875,88.1938232955488,54.4698538681659));
#45311=CARTESIAN_POINT('Ctrl Pts',(77.2955260761042,87.5573552668916,59.2885359377501));
#45312=CARTESIAN_POINT('Ctrl Pts',(70.9567606325384,86.9208872382348,58.3464174285945));
#45313=CARTESIAN_POINT('Ctrl Pts',(68.7786383180496,86.3904972143539,53.4880273953303));
#45314=CARTESIAN_POINT('Ctrl Pts',(70.0682487881018,85.9661851952494,49.8263593707863));
#45315=CARTESIAN_POINT('Ctrl Pts',(72.8900068067502,85.5418731761447,47.1601655348787));
#45316=CARTESIAN_POINT('Ctrl Pts',(78.2142824574917,85.0114831522641,47.1762691716988));
#45317=CARTESIAN_POINT('Ctrl Pts',(81.6507460849712,84.3750151236068,52.5853589630448));
#45318=CARTESIAN_POINT('Ctrl Pts',(78.9567960842213,83.7385470949501,58.3864396237387));
#45319=CARTESIAN_POINT('Ctrl Pts',(72.6215538909905,83.102079066293,59.2665588153995));
#45320=CARTESIAN_POINT('Ctrl Pts',(68.4535757982522,82.4656110376363,54.3987571295987));
#45321=CARTESIAN_POINT('Ctrl Pts',(69.9948804987645,81.9352210137553,49.3024299862164));
#45322=CARTESIAN_POINT('Ctrl Pts',(73.3695905296702,81.5109089946509,47.3835136009241));
#45323=CARTESIAN_POINT('Ctrl Pts',(77.2483078732814,81.0865969755459,47.2208493614383));
#45324=CARTESIAN_POINT('Ctrl Pts',(81.2575625050972,80.5562069516654,50.724283081299));
#45325=CARTESIAN_POINT('Ctrl Pts',(80.3051930785702,79.9197389230083,57.0615164768155));
#45326=CARTESIAN_POINT('Ctrl Pts',(74.4673380396858,79.2832708943515,59.6748193646171));
#45327=CARTESIAN_POINT('Ctrl Pts',(69.107128087849,78.6468028656945,56.1851126848734));
#45328=CARTESIAN_POINT('Ctrl Pts',(69.1522683461807,78.0103348370375,49.7768760326491));
#45329=CARTESIAN_POINT('Ctrl Pts',(73.6577527209851,77.4799448131567,46.9398386552797));
#45330=CARTESIAN_POINT('Ctrl Pts',(77.4639367994623,77.0556327940522,47.7039529446272));
#45331=CARTESIAN_POINT('Ctrl Pts',(80.4990217432763,76.6313207749475,50.1245246271578));
#45332=CARTESIAN_POINT('Ctrl Pts',(81.2286996794729,76.1009307510668,55.3985876379329));
#45333=CARTESIAN_POINT('Ctrl Pts',(76.3541631842683,75.4644627224097,59.5586872269757));
#45334=CARTESIAN_POINT('Ctrl Pts',(70.2329825190307,74.8279946937529,57.7036802992425));
#45335=CARTESIAN_POINT('Ctrl Pts',(68.4743356369337,74.1915266650958,51.554122218981));
#45336=CARTESIAN_POINT('Ctrl Pts',(72.7104752843599,73.555058636439,46.7455199770257));
#45337=CARTESIAN_POINT('Ctrl Pts',(77.9724284950027,73.0246686125582,47.5579354749106));
#45338=CARTESIAN_POINT('Ctrl Pts',(80.3450365744471,72.6003565934535,50.630660452482));
#45339=CARTESIAN_POINT('Ctrl Pts',(81.0492816689046,72.176044574349,54.4483753100075));
#45340=CARTESIAN_POINT('Ctrl Pts',(78.1418369156852,71.6456545504681,58.908749233702));
#45341=CARTESIAN_POINT('Ctrl Pts',(71.7336816537533,71.0091865218112,58.8532445239228));
#45342=CARTESIAN_POINT('Ctrl Pts',(68.3285858083172,70.3727184931542,53.4388908485694));
#45343=CARTESIAN_POINT('Ctrl Pts',(71.0332481390232,69.7362504644973,47.6427968952868));
#45344=CARTESIAN_POINT('Ctrl Pts',(77.3846566580606,69.0997824358403,46.7900692376301));
#45345=CARTESIAN_POINT('Ctrl Pts',(80.8246941917609,68.5693924119597,50.8538497802933));
#45346=CARTESIAN_POINT('Ctrl Pts',(80.6011359407797,68.1450803928549,54.7295341837058));
#45347=CARTESIAN_POINT('Ctrl Pts',(78.6294574171612,67.7207683737503,58.0736920277588));
#45348=CARTESIAN_POINT('Ctrl Pts',(73.5095530650882,67.1903783498695,59.534770382201));
#45349=CARTESIAN_POINT('Ctrl Pts',(68.7078085314535,66.5539103212125,55.2908589708327));
#45350=CARTESIAN_POINT('Ctrl Pts',(69.6873122266739,65.9174422925556,48.9702200830722));
#45351=CARTESIAN_POINT('Ctrl Pts',(75.5299851241042,65.2809742638987,46.3677065188326));
#45352=CARTESIAN_POINT('Ctrl Pts',(80.8844392196639,64.6445062352417,49.8886944444544));
#45353=CARTESIAN_POINT('Ctrl Pts',(80.8169247461073,64.1141162113609,55.2125663745499));
#45354=CARTESIAN_POINT('Ctrl Pts',(78.1067448734721,63.6898041922563,57.9921046355568));
#45355=CARTESIAN_POINT('Ctrl Pts',(74.4252754900851,63.2654921731517,59.2240506837341));
#45356=CARTESIAN_POINT('Ctrl Pts',(69.6016913704958,62.7351021492708,56.9698974561461));
#45357=CARTESIAN_POINT('Ctrl Pts',(68.7592374263501,62.0986341206141,50.6171180655309));
#45358=CARTESIAN_POINT('Ctrl Pts',(73.6433787437401,61.4621660919569,46.4873399806718));
#45359=CARTESIAN_POINT('Ctrl Pts',(79.7611220203028,60.8256980633001,48.3536520233085));
#45360=CARTESIAN_POINT('Ctrl Pts',(81.4949112636297,60.1892300346431,54.5230530877197));
#45361=CARTESIAN_POINT('Ctrl Pts',(77.9529272269266,59.6588400107624,58.4982913970464));
#45362=CARTESIAN_POINT('Ctrl Pts',(74.0841280030346,59.2345279916577,58.8196952732654));
#45363=CARTESIAN_POINT('Ctrl Pts',(70.4968069555375,58.8102159725532,57.3357695377179));
#45364=CARTESIAN_POINT('Ctrl Pts',(68.3331244406284,58.2798259486722,52.4709315643751));
#45365=CARTESIAN_POINT('Ctrl Pts',(71.8627679117568,57.6433579200153,47.1221792238239));
#45366=CARTESIAN_POINT('Ctrl Pts',(78.2582921364095,57.0068898913583,47.2068747390464));
#45367=CARTESIAN_POINT('Ctrl Pts',(81.6533796843252,56.3704218627016,52.6275097553897));
#45368=CARTESIAN_POINT('Ctrl Pts',(78.9169383049789,55.7339538340444,58.4222852653844));
#45369=CARTESIAN_POINT('Ctrl Pts',(73.6360753535378,55.2035638101638,59.1010024526532));
#45370=CARTESIAN_POINT('Ctrl Pts',(70.5043885727656,54.779251791059,56.8067823687086));
#45371=CARTESIAN_POINT('Ctrl Pts',(68.7690218812751,54.3549397719544,53.334116198098));
#45372=CARTESIAN_POINT('Ctrl Pts',(70.325456686331,53.8245497480737,48.2423894546636));
#45373=CARTESIAN_POINT('Ctrl Pts',(76.4976538658095,53.1880817194167,46.5185807032441));
#45374=CARTESIAN_POINT('Ctrl Pts',(81.2707207768341,52.5516136907598,50.7762485744269));
#45375=CARTESIAN_POINT('Ctrl Pts',(80.2795419932234,51.9151456621028,57.0950671394231));
#45376=CARTESIAN_POINT('Ctrl Pts',(74.4137405368346,51.2786776334458,59.6757468770239));
#45377=CARTESIAN_POINT('Ctrl Pts',(69.9816490550362,50.7482876095651,56.7253679811584));
#45378=CARTESIAN_POINT('Ctrl Pts',(69.1216175708044,50.3239755904604,52.9397037418783));
#45379=CARTESIAN_POINT('Ctrl Pts',(70.0885439635866,49.8996635713559,49.1799216687548));
#45380=CARTESIAN_POINT('Ctrl Pts',(74.6024349177723,49.369273547475,46.3562788113952));
#45381=CARTESIAN_POINT('Ctrl Pts',(80.3927770014313,48.7328055188181,49.1020889264681));
#45382=CARTESIAN_POINT('Ctrl Pts',(81.2045589222609,48.0963374901611,55.4464496942236));
#45383=CARTESIAN_POINT('Ctrl Pts',(76.3127965798036,47.4598694615042,59.5671977602111));
#45384=CARTESIAN_POINT('Ctrl Pts',(70.1919083484634,46.8234014328472,57.6692351964939));
#45385=CARTESIAN_POINT('Ctrl Pts',(68.7803362744653,46.2930114089665,52.535461261843));
#45386=CARTESIAN_POINT('Ctrl Pts',(70.6133799988629,45.8686993898619,49.113348085619));
#45387=CARTESIAN_POINT('Ctrl Pts',(73.808800501213,45.4443873707573,46.9087629319908));
#45388=CARTESIAN_POINT('Ctrl Pts',(79.0683174983399,44.9139973468763,47.7368036852939));
#45389=CARTESIAN_POINT('Ctrl Pts',(81.6395066702259,44.2775293182195,53.6067713918667));
#45390=CARTESIAN_POINT('Ctrl Pts',(78.0922262264452,43.6410612895625,58.9290551959863));
#45391=CARTESIAN_POINT('Ctrl Pts',(71.6968693820735,43.0045932609057,58.8325447221204));
#45392=CARTESIAN_POINT('Ctrl Pts',(68.3201615278016,42.3681252322486,53.3859514106338));
#45393=CARTESIAN_POINT('Ctrl Pts',(70.6207865388037,41.8377352083679,48.584358436323));
#45394=CARTESIAN_POINT('Ctrl Pts',(74.2487044880827,41.4134231892631,47.2026496248374));
#45395=CARTESIAN_POINT('Ctrl Pts',(78.1068463906541,40.9891111701586,47.6335196122566));
#45396=CARTESIAN_POINT('Ctrl Pts',(81.5347986752688,40.4587211462778,51.7074996891105));
#45397=CARTESIAN_POINT('Ctrl Pts',(79.6269388331483,39.8222531176209,57.8253102007773));
#45398=CARTESIAN_POINT('Ctrl Pts',(73.4587819402533,39.185785088964,59.5175702230695));
#45399=CARTESIAN_POINT('Ctrl Pts',(68.6935887976469,38.5493170603069,55.2510918448196));
#45400=CARTESIAN_POINT('Ctrl Pts',(69.715665777593,37.91284903165,48.9247269106014));
#45401=CARTESIAN_POINT('Ctrl Pts',(74.601169621109,37.3824590077692,46.808120492965));
#45402=CARTESIAN_POINT('Ctrl Pts',(78.2462630815789,36.9581469886647,48.1438605690558));
#45403=CARTESIAN_POINT('Ctrl Pts',(80.8766167330158,36.5338349695599,50.9990571568275));
#45404=CARTESIAN_POINT('Ctrl Pts',(80.793289809878,36.0034449456793,56.3227050749385));
#45405=CARTESIAN_POINT('Ctrl Pts',(75.3412422253247,35.3669769170222,59.6905993383795));
#45406=CARTESIAN_POINT('Ctrl Pts',(69.574637925996,34.7305088883653,56.9236193432539));
#45407=CARTESIAN_POINT('Ctrl Pts',(68.7745779741261,34.0940408597084,50.5777697144526));
#45408=CARTESIAN_POINT('Ctrl Pts',(73.6946167383032,33.4575728310515,46.4715849653604));
#45409=CARTESIAN_POINT('Ctrl Pts',(78.7710770544774,32.9271828071706,48.0771132866675));
#45410=CARTESIAN_POINT('Ctrl Pts',(80.6472312224613,32.5028707880661,51.4757826473492));
#45411=CARTESIAN_POINT('Ctrl Pts',(80.7609096169022,32.0785587689613,55.3562446188384));
#45412=CARTESIAN_POINT('Ctrl Pts',(77.2071341131469,31.5481687450806,59.3209451361635));
#45413=CARTESIAN_POINT('Ctrl Pts',(70.8824305329507,30.9117007164236,58.2886374013044));
#45414=CARTESIAN_POINT('Ctrl Pts',(68.3430450059106,30.2752326877667,52.4182520125253));
#45415=CARTESIAN_POINT('Ctrl Pts',(71.9001517916369,29.6387646591098,47.1025305483846));
#45416=CARTESIAN_POINT('Ctrl Pts',(78.3073076922158,29.0022966304529,47.2285779136388));
#45417=CARTESIAN_POINT('Ctrl Pts',(81.0872324480072,28.471906606572,51.7695237430829));
#45418=CARTESIAN_POINT('Ctrl Pts',(80.275122006266,28.0475945874674,55.565756650326));
#45419=CARTESIAN_POINT('Ctrl Pts',(77.8164221205999,27.6232825683628,58.5700374594237));
#45420=CARTESIAN_POINT('Ctrl Pts',(72.5335666026989,27.092892544482,59.2330665250225));
#45421=CARTESIAN_POINT('Ctrl Pts',(68.4353446939828,26.4564245158251,54.3063931884985));
#45422=CARTESIAN_POINT('Ctrl Pts',(70.3674902113553,25.8199564871681,48.2091214630561));
#45423=CARTESIAN_POINT('Ctrl Pts',(76.5387626327649,25.1834884585111,46.5282601413106));
#45424=CARTESIAN_POINT('Ctrl Pts',(81.2934963114684,24.5470204298542,50.8247743089652));
#45425=CARTESIAN_POINT('Ctrl Pts',(80.414707068145,24.0166304059735,56.0760531511082));
#45426=CARTESIAN_POINT('Ctrl Pts',(77.3122715737554,23.5923183868688,58.4096717625035));
#45427=CARTESIAN_POINT('Ctrl Pts',(73.4859668057208,23.1680063677642,59.0656658471794));
#45428=CARTESIAN_POINT('Ctrl Pts',(69.0626632683662,22.6376163438834,56.1021187103944));
#45429=CARTESIAN_POINT('Ctrl Pts',(69.1990635927837,22.0011483152264,49.695206442741));
#45430=CARTESIAN_POINT('Ctrl Pts',(74.6559956914946,21.3646802865695,46.3586883014623));
#45431=CARTESIAN_POINT('Ctrl Pts',(80.4174464448778,20.7282122579125,49.1364208319506));
#45432=CARTESIAN_POINT('Ctrl Pts',(81.1899753790609,20.0917442292556,55.4978865304285));
#45433=CARTESIAN_POINT('Ctrl Pts',(77.0829706090005,19.5613542053749,58.8867113839554));
#45434=CARTESIAN_POINT('Ctrl Pts',(73.2105872069091,19.1370421862702,58.6136853706606));
#45435=CARTESIAN_POINT('Ctrl Pts',(69.8912577533702,18.7127301671655,56.6010225426405));
#45436=CARTESIAN_POINT('Ctrl Pts',(68.4956769583314,18.1823401432847,51.4606824589819));
#45437=CARTESIAN_POINT('Ctrl Pts',(72.7985336869453,17.5458721146278,46.717269598202));
#45438=CARTESIAN_POINT('Ctrl Pts',(79.1086961350004,16.9094040859709,47.76874527729));
#45439=CARTESIAN_POINT('Ctrl Pts',(81.6326438925532,16.272936057314,53.6584623286513));
#45440=CARTESIAN_POINT('Ctrl Pts',(78.6506201566575,15.7425460334332,58.0582788876747));
#45441=CARTESIAN_POINT('Ctrl Pts',(74.8443820757933,15.3182340143285,58.8942202496515));
#45442=CARTESIAN_POINT('Ctrl Pts',(72.983431993014,15.1060780047762,58.3814745569358));
#45443=CARTESIAN_POINT('Ctrl Pts',(72.1688064861966,15.,57.9117293166054));
#45444=CARTESIAN_POINT('Ctrl Pts',(80.7895856589294,416.407550721688,50.3113098152966));
#45445=CARTESIAN_POINT('Ctrl Pts',(81.2413947982782,416.301472716912,51.2780186311425));
#45446=CARTESIAN_POINT('Ctrl Pts',(81.6399980963661,416.08931670736,53.431861897913));
#45447=CARTESIAN_POINT('Ctrl Pts',(80.3245054469483,415.665004688255,57.6537570089119));
#45448=CARTESIAN_POINT('Ctrl Pts',(75.0599862662509,415.134614664374,60.5970028556877));
#45449=CARTESIAN_POINT('Ctrl Pts',(68.6468240838236,414.498146635717,57.1703399986101));
#45450=CARTESIAN_POINT('Ctrl Pts',(68.0721122133495,413.86167860706,49.9338964270263));
#45451=CARTESIAN_POINT('Ctrl Pts',(73.8536277062205,413.225210578404,45.5307843216615));
#45452=CARTESIAN_POINT('Ctrl Pts',(79.5293668686138,412.694820554522,47.608817812333));
#45453=CARTESIAN_POINT('Ctrl Pts',(81.4818216899602,412.270508535419,51.5574321359389));
#45454=CARTESIAN_POINT('Ctrl Pts',(81.4136646470584,411.846196516312,55.9620266993605));
#45455=CARTESIAN_POINT('Ctrl Pts',(77.182673447473,411.315806492434,60.2755324159434));
#45456=CARTESIAN_POINT('Ctrl Pts',(70.0657272634679,410.679338463775,58.7830751157563));
#45457=CARTESIAN_POINT('Ctrl Pts',(67.485953158802,410.04287043512,51.9990045803245));
#45458=CARTESIAN_POINT('Ctrl Pts',(71.7891733015741,409.406402406461,46.1542126641332));
#45459=CARTESIAN_POINT('Ctrl Pts',(79.045951076736,408.769934377805,46.623478484056));
#45460=CARTESIAN_POINT('Ctrl Pts',(81.9660221235307,408.239544353924,51.9127534736459));
#45461=CARTESIAN_POINT('Ctrl Pts',(80.8520208784144,407.815232334819,56.1748467453594));
#45462=CARTESIAN_POINT('Ctrl Pts',(77.9117788239603,407.390920315716,59.4552955240192));
#45463=CARTESIAN_POINT('Ctrl Pts',(71.8892887985956,406.860530291833,59.9378154737378));
#45464=CARTESIAN_POINT('Ctrl Pts',(67.4944491078429,406.224062263178,54.1441181451339));
#45465=CARTESIAN_POINT('Ctrl Pts',(69.9953373217988,405.58759423452,47.3305926903669));
#45466=CARTESIAN_POINT('Ctrl Pts',(77.0767924089223,404.951126205863,45.7394991594704));
#45467=CARTESIAN_POINT('Ctrl Pts',(82.2479624544353,404.314658177207,50.8522825051723));
#45468=CARTESIAN_POINT('Ctrl Pts',(80.9842660833594,403.784268153325,56.7604331801431));
#45469=CARTESIAN_POINT('Ctrl Pts',(77.3484330715765,403.359956134221,59.2478253779512));
#45470=CARTESIAN_POINT('Ctrl Pts',(72.9774724614809,402.935644115116,59.7965549476201));
#45471=CARTESIAN_POINT('Ctrl Pts',(68.1141092087561,402.405254091235,56.2117436971656));
#45472=CARTESIAN_POINT('Ctrl Pts',(68.5951035493501,401.768786062579,48.9556979554233));
#45473=CARTESIAN_POINT('Ctrl Pts',(74.951086404199,401.132318033922,45.4514063382047));
#45474=CARTESIAN_POINT('Ctrl Pts',(81.3408903658783,400.495850005264,48.8936415491659));
#45475=CARTESIAN_POINT('Ctrl Pts',(81.8925163663265,399.859381976608,56.1446596895001));
#45476=CARTESIAN_POINT('Ctrl Pts',(77.0642901766376,399.328991952727,59.7766571422207));
#45477=CARTESIAN_POINT('Ctrl Pts',(72.6881935969392,398.904679933622,59.2705150455746));
#45478=CARTESIAN_POINT('Ctrl Pts',(69.028312474448,398.480367914518,56.8186440741339));
#45479=CARTESIAN_POINT('Ctrl Pts',(67.7071462846999,397.949977890636,50.9230784909119));
#45480=CARTESIAN_POINT('Ctrl Pts',(72.8282865991981,397.31350986198,45.7601842258385));
#45481=CARTESIAN_POINT('Ctrl Pts',(79.9248984922716,396.677041833323,47.2822477977728));
#45482=CARTESIAN_POINT('Ctrl Pts',(82.4920145257144,396.040573804666,54.0710984478771));
#45483=CARTESIAN_POINT('Ctrl Pts',(78.1537966050903,395.404105776009,59.9073147380206));
#45484=CARTESIAN_POINT('Ctrl Pts',(72.1268967499142,394.873715752128,59.4834612461347));
#45485=CARTESIAN_POINT('Ctrl Pts',(69.1548466821309,394.449403733024,56.2317971356439));
#45486=CARTESIAN_POINT('Ctrl Pts',(67.9994059152317,394.025091713919,51.9807551778361));
#45487=CARTESIAN_POINT('Ctrl Pts',(70.8678150888879,393.494701690038,46.6632931460518));
#45488=CARTESIAN_POINT('Ctrl Pts',(78.1197159299898,392.858233661381,46.1233954679321));
#45489=CARTESIAN_POINT('Ctrl Pts',(82.4795800207196,392.221765632725,51.9259951429827));
#45490=CARTESIAN_POINT('Ctrl Pts',(79.9661078860758,391.585297604067,58.7348890110715));
#45491=CARTESIAN_POINT('Ctrl Pts',(72.8637954461731,390.948829575411,60.2965270350745));
#45492=CARTESIAN_POINT('Ctrl Pts',(68.5914342841124,390.418439551529,56.0245130196589));
#45493=CARTESIAN_POINT('Ctrl Pts',(68.4797507593773,389.994127532425,51.6206592660523));
#45494=CARTESIAN_POINT('Ctrl Pts',(70.3949223493767,389.56981551332,47.6534790491081));
#45495=CARTESIAN_POINT('Ctrl Pts',(76.0473714332612,389.03942548944,45.5197046933984));
#45496=CARTESIAN_POINT('Ctrl Pts',(81.8765635723464,388.402957460782,49.8673562799026));
#45497=CARTESIAN_POINT('Ctrl Pts',(81.3633237207986,387.766489432126,57.1071879584235));
#45498=CARTESIAN_POINT('Ctrl Pts',(75.0008778710985,387.130021403469,60.5997315427138));
#45499=CARTESIAN_POINT('Ctrl Pts',(68.6146410439638,386.493553374812,57.1215805253265));
#45500=CARTESIAN_POINT('Ctrl Pts',(68.1902978235643,385.963163350931,51.094715131252));
#45501=CARTESIAN_POINT('Ctrl Pts',(70.9937063513919,385.538851331826,47.6965830386227));
#45502=CARTESIAN_POINT('Ctrl Pts',(75.0410462321251,385.114539312722,45.9572035565431));
#45503=CARTESIAN_POINT('Ctrl Pts',(80.7078056992447,384.584149288842,48.0526774382226));
#45504=CARTESIAN_POINT('Ctrl Pts',(82.2579545906091,383.947681260183,55.1575063402167));
#45505=CARTESIAN_POINT('Ctrl Pts',(77.1231010004394,383.311213231528,60.2870147461023));
#45506=CARTESIAN_POINT('Ctrl Pts',(70.0293130803531,382.674745202869,58.7518434776859));
#45507=CARTESIAN_POINT('Ctrl Pts',(67.4884412136621,382.038277174214,51.9382155549809));
#45508=CARTESIAN_POINT('Ctrl Pts',(71.1200463257472,381.507887150331,47.1096942537058));
#45509=CARTESIAN_POINT('Ctrl Pts',(75.4648621085364,381.083575131228,46.3823862677193));
#45510=CARTESIAN_POINT('Ctrl Pts',(79.661152632736,380.659263112123,47.7231125370846));
#45511=CARTESIAN_POINT('Ctrl Pts',(82.5654807936886,380.128873088243,53.0210415268397));
#45512=CARTESIAN_POINT('Ctrl Pts',(79.077005396985,379.492405059585,59.4016445327163));
#45513=CARTESIAN_POINT('Ctrl Pts',(71.8366431041545,378.855937030929,59.9073437981783));
#45514=CARTESIAN_POINT('Ctrl Pts',(67.4875061865788,378.219469002271,54.096699604054));
#45515=CARTESIAN_POINT('Ctrl Pts',(70.037039744923,377.583000973615,47.2863079892577));
#45516=CARTESIAN_POINT('Ctrl Pts',(75.9450877467993,377.052610949733,46.0221313977504));
#45517=CARTESIAN_POINT('Ctrl Pts',(79.7023283940244,376.62829893063,48.3220322242411));
#45518=CARTESIAN_POINT('Ctrl Pts',(81.9913653223898,376.203986911524,52.0859013815623));
#45519=CARTESIAN_POINT('Ctrl Pts',(80.7101262330765,375.673596887645,57.9902726472438));
#45520=CARTESIAN_POINT('Ctrl Pts',(73.8923976840809,375.037128858986,60.5201210111223));
#45521=CARTESIAN_POINT('Ctrl Pts',(68.0943419684742,374.40066083033,56.1542158590086));
#45522=CARTESIAN_POINT('Ctrl Pts',(68.6209558225136,373.764192801673,48.915344695128));
#45523=CARTESIAN_POINT('Ctrl Pts',(75.0116100672234,373.127724773017,45.4453167937154));
#45524=CARTESIAN_POINT('Ctrl Pts',(80.3011266292082,372.597334749135,48.3649380341302));
#45525=CARTESIAN_POINT('Ctrl Pts',(81.6297246308043,372.173022730031,52.5650842747992));
#45526=CARTESIAN_POINT('Ctrl Pts',(80.8898679317703,371.748710710926,56.9077808054986));
#45527=CARTESIAN_POINT('Ctrl Pts',(76.0508754272462,371.218320687045,60.5254216373323));
#45528=CARTESIAN_POINT('Ctrl Pts',(69.2446162674512,370.581852658388,57.9648764684838));
#45529=CARTESIAN_POINT('Ctrl Pts',(67.729944664901,369.945384629731,50.8666831902644));
#45530=CARTESIAN_POINT('Ctrl Pts',(72.8742657559371,369.308916601074,45.7466696755505));
#45531=CARTESIAN_POINT('Ctrl Pts',(79.9745867816891,368.672448572417,47.3173372544069));
#45532=CARTESIAN_POINT('Ctrl Pts',(82.0536812051091,368.142058548537,52.990126693959));
#45533=CARTESIAN_POINT('Ctrl Pts',(80.3026166120396,367.717746529432,57.0324247883297));
#45534=CARTESIAN_POINT('Ctrl Pts',(76.8963999262717,367.293434510327,59.8260047464567));
#45535=CARTESIAN_POINT('Ctrl Pts',(70.8707855677016,366.763044486447,59.3842522718924));
#45536=CARTESIAN_POINT('Ctrl Pts',(67.4110982780816,366.126576457789,52.9879940555559));
#45537=CARTESIAN_POINT('Ctrl Pts',(70.9220077724125,365.490108429133,46.6356643725854));
#45538=CARTESIAN_POINT('Ctrl Pts',(78.1632919396892,364.853640400476,46.1433418286396));
#45539=CARTESIAN_POINT('Ctrl Pts',(82.4940854177424,364.217172371819,51.9850695835472));
#45540=CARTESIAN_POINT('Ctrl Pts',(80.3439905932449,363.686782347938,57.6313308148986));
#45541=CARTESIAN_POINT('Ctrl Pts',(76.3712941874098,363.262470328833,59.5350336173121));
#45542=CARTESIAN_POINT('Ctrl Pts',(71.9677814533701,362.838158309729,59.4106282556724));
#45543=CARTESIAN_POINT('Ctrl Pts',(67.7081276982914,362.307768285848,55.1259434908579));
#45544=CARTESIAN_POINT('Ctrl Pts',(69.29027709203,361.671300257191,48.0281721076772));
#45545=CARTESIAN_POINT('Ctrl Pts',(76.106403722641,361.034832228534,45.534380690175));
#45546=CARTESIAN_POINT('Ctrl Pts',(81.8963839629881,360.398364199878,49.9109897308505));
#45547=CARTESIAN_POINT('Ctrl Pts',(81.3355385052593,359.76189617122,57.1613005989825));
#45548=CARTESIAN_POINT('Ctrl Pts',(76.0098121089718,359.231506147339,60.0143361751496));
#45549=CARTESIAN_POINT('Ctrl Pts',(71.7621258456939,358.807194128235,58.8466193851635));
#45550=CARTESIAN_POINT('Ctrl Pts',(68.5190612661091,358.382882109129,55.8651879796984));
#45551=CARTESIAN_POINT('Ctrl Pts',(68.1126206673736,357.85249208525,49.8370888027861));
#45552=CARTESIAN_POINT('Ctrl Pts',(73.9613452910871,357.216024056592,45.5157492433467));
#45553=CARTESIAN_POINT('Ctrl Pts',(80.7427514648477,356.579556027936,48.1024668902907));
#45554=CARTESIAN_POINT('Ctrl Pts',(82.2443072674208,355.943087999278,55.2034462629049));
#45555=CARTESIAN_POINT('Ctrl Pts',(77.0666400728443,355.306619970621,60.3096501105997));
#45556=CARTESIAN_POINT('Ctrl Pts',(71.1749158110719,354.776229946741,58.9714577215049));
#45557=CARTESIAN_POINT('Ctrl Pts',(68.7336281098145,354.351917927636,55.3045086555177));
#45558=CARTESIAN_POINT('Ctrl Pts',(68.2401302403252,353.927605908532,50.9269681422087));
#45559=CARTESIAN_POINT('Ctrl Pts',(71.8860608107843,353.397215884651,46.1092545846811));
#45560=CARTESIAN_POINT('Ctrl Pts',(79.1354550994434,352.760747855994,46.6818257676457));
#45561=CARTESIAN_POINT('Ctrl Pts',(82.5592164281373,352.124279827337,53.0815473430482));
#45562=CARTESIAN_POINT('Ctrl Pts',(79.0365776194958,351.48781179868,59.4273801254641));
#45563=CARTESIAN_POINT('Ctrl Pts',(71.7791726134526,350.851343770023,59.8874104399738));
#45564=CARTESIAN_POINT('Ctrl Pts',(68.2084260981037,350.320953746142,55.0137113345597));
#45565=CARTESIAN_POINT('Ctrl Pts',(68.7697806630927,349.896641727037,50.6443541569855));
#45566=CARTESIAN_POINT('Ctrl Pts',(71.2676660331981,349.472329707933,47.0157222149629));
#45567=CARTESIAN_POINT('Ctrl Pts',(77.1794427808517,348.941939684052,45.769099042993));
#45568=CARTESIAN_POINT('Ctrl Pts',(82.2772657295171,348.305471655395,50.9550181029155));
#45569=CARTESIAN_POINT('Ctrl Pts',(80.6657213081576,347.669003626738,58.0318466621302));
#45570=CARTESIAN_POINT('Ctrl Pts',(73.8449992740799,347.032535598081,60.5130416992796));
#45571=CARTESIAN_POINT('Ctrl Pts',(68.0640227548013,346.396067569424,56.101481227569));
#45572=CARTESIAN_POINT('Ctrl Pts',(68.5639383988084,345.865677545544,50.0804133824217));
#45573=CARTESIAN_POINT('Ctrl Pts',(71.8528685658973,345.441365526439,47.1496558952068));
#45574=CARTESIAN_POINT('Ctrl Pts',(76.118160318495,345.017053507335,46.047981098329));
#45575=CARTESIAN_POINT('Ctrl Pts',(81.3989818087853,344.486663483453,48.9833001669616));
#45576=CARTESIAN_POINT('Ctrl Pts',(81.8472735889369,343.850195454797,56.2414397214105));
#45577=CARTESIAN_POINT('Ctrl Pts',(75.9900885877292,343.213727426139,60.5276923668058));
#45578=CARTESIAN_POINT('Ctrl Pts',(69.2134726930078,342.577259397483,57.9284511517702));
#45579=CARTESIAN_POINT('Ctrl Pts',(67.7416333010628,341.940791368825,50.806987529991));
#45580=CARTESIAN_POINT('Ctrl Pts',(72.0672498319467,341.410401344945,46.5889055873615));
#45581=CARTESIAN_POINT('Ctrl Pts',(76.4721626684415,340.98608932584,46.5328342422951));
#45582=CARTESIAN_POINT('Ctrl Pts',(80.4148456024942,340.561777306736,48.4979429859479));
#45583=CARTESIAN_POINT('Ctrl Pts',(82.4770817672208,340.031387282855,54.1768826447122));
#45584=CARTESIAN_POINT('Ctrl Pts',(78.0561770688721,339.394919254198,59.9507164629067));
#45585=CARTESIAN_POINT('Ctrl Pts',(70.8234026819354,338.75845122554,59.3461070466697));
#45586=CARTESIAN_POINT('Ctrl Pts',(67.4114700530779,338.121983196884,52.9400713291086));
#45587=CARTESIAN_POINT('Ctrl Pts',(70.9699767657366,337.485515168227,46.5982588683077));
#45588=CARTESIAN_POINT('Ctrl Pts',(77.001719526524,336.955125144347,46.2500449761636));
#45589=CARTESIAN_POINT('Ctrl Pts',(80.364184772194,336.530813125241,49.0961350247236));
#45590=CARTESIAN_POINT('Ctrl Pts',(82.0523236900641,336.106501106137,53.1651137770432));
#45591=CARTESIAN_POINT('Ctrl Pts',(79.8854680545447,335.576111082256,58.8049639791148));
#45592=CARTESIAN_POINT('Ctrl Pts',(72.7616332336275,334.939643053599,60.2652833812645));
#45593=CARTESIAN_POINT('Ctrl Pts',(67.6973666273895,334.303175024943,55.0660736702146));
#45594=CARTESIAN_POINT('Ctrl Pts',(69.3219820447791,333.666706996285,47.9922343573584));
#45595=CARTESIAN_POINT('Ctrl Pts',(76.1671480162545,333.030238967629,45.5375942340481));
#45596=CARTESIAN_POINT('Ctrl Pts',(80.9494316003633,332.499848943748,49.2298750153747));
#45597=CARTESIAN_POINT('Ctrl Pts',(81.6218237505459,332.075536924643,53.5835274922297));
#45598=CARTESIAN_POINT('Ctrl Pts',(80.2282217793196,331.651224905538,57.7625554460304));
#45599=CARTESIAN_POINT('Ctrl Pts',(74.8940449044853,331.120834881658,60.5997601822053));
#45600=CARTESIAN_POINT('Ctrl Pts',(68.5579961719892,330.484366853,57.0310010461126));
#45601=CARTESIAN_POINT('Ctrl Pts',(68.1437543921941,329.847898824344,49.7848309110412));
#45602=CARTESIAN_POINT('Ctrl Pts',(74.0088478294097,329.211430795687,45.5094061542176));
#45603=CARTESIAN_POINT('Ctrl Pts',(80.7865060381157,328.57496276703,48.1447248290591));
#45604=CARTESIAN_POINT('Ctrl Pts',(81.9759865511057,328.044572743149,54.0682634468287));
#45605=CARTESIAN_POINT('Ctrl Pts',(79.6288299458803,327.620260724044,57.7961659352798));
#45606=CARTESIAN_POINT('Ctrl Pts',(75.8363593186907,327.19594870494,60.0374976007762));
#45607=CARTESIAN_POINT('Ctrl Pts',(69.9486356894012,326.665558681059,58.6818117551253));
#45608=CARTESIAN_POINT('Ctrl Pts',(67.5050699649132,326.029090652403,51.832684667524));
#45609=CARTESIAN_POINT('Ctrl Pts',(71.9438336438113,325.392622623745,46.0902152612994));
#45610=CARTESIAN_POINT('Ctrl Pts',(79.1754787318497,324.756154595088,46.708185486457));
#45611=CARTESIAN_POINT('Ctrl Pts',(82.564541311991,324.119686566431,53.1421430663524));
#45612=CARTESIAN_POINT('Ctrl Pts',(79.5783670997,323.58929654255,58.3943747083155));
#45613=CARTESIAN_POINT('Ctrl Pts',(75.3617807153705,323.164984523446,59.6698355490872));
#45614=CARTESIAN_POINT('Ctrl Pts',(71.028771816179,322.740672504341,58.8752067222889));
#45615=CARTESIAN_POINT('Ctrl Pts',(67.472516713564,322.210282480461,53.9909234286913));
#45616=CARTESIAN_POINT('Ctrl Pts',(70.1187939445722,321.573814451803,47.2175363787246));
#45617=CARTESIAN_POINT('Ctrl Pts',(77.2355457326337,320.937346423146,45.7926076557161));
#45618=CARTESIAN_POINT('Ctrl Pts',(82.290198667416,320.30087839449,51.0011642299913));
#45619=CARTESIAN_POINT('Ctrl Pts',(80.6300072817412,319.664410365832,58.081087949562));
#45620=CARTESIAN_POINT('Ctrl Pts',(74.9314192802274,319.134020341952,60.088391722286));
#45621=CARTESIAN_POINT('Ctrl Pts',(70.9115524333953,318.709708322847,58.2864284522404));
#45622=CARTESIAN_POINT('Ctrl Pts',(68.161202218195,318.285396303743,54.8452114020383));
#45623=CARTESIAN_POINT('Ctrl Pts',(68.6789991873789,317.755006279862,48.8256549444831));
#45624=CARTESIAN_POINT('Ctrl Pts',(75.1184297311182,317.118538251205,45.4470029078914));
#45625=CARTESIAN_POINT('Ctrl Pts',(81.4259241403883,316.482070222548,49.0378373729645));
#45626=CARTESIAN_POINT('Ctrl Pts',(81.8267786253167,315.845602193891,56.284760413845));
#45627=CARTESIAN_POINT('Ctrl Pts',(75.9308357102248,315.209134165234,60.5414507307445));
#45628=CARTESIAN_POINT('Ctrl Pts',(70.3121717567199,314.678744141353,58.3202373180855));
#45629=CARTESIAN_POINT('Ctrl Pts',(68.458780164777,314.254432122249,54.3238213362628));
#45630=CARTESIAN_POINT('Ctrl Pts',(68.6387745812983,313.830120103144,49.9222303622086));
#45631=CARTESIAN_POINT('Ctrl Pts',(72.9769004072191,313.299730079263,45.7170147951457));
#45632=CARTESIAN_POINT('Ctrl Pts',(80.0541297174874,312.663262050606,47.3886548885531));
#45633=CARTESIAN_POINT('Ctrl Pts',(82.4616615956628,312.026794021949,54.2357249286578));
#45634=CARTESIAN_POINT('Ctrl Pts',(78.0122968427819,311.390325993293,59.9699843555021));
#45635=CARTESIAN_POINT('Ctrl Pts',(70.7696451723068,310.753857964635,59.3176408170394));
#45636=CARTESIAN_POINT('Ctrl Pts',(67.9840799037379,310.223467940755,53.9563163741867));
#45637=CARTESIAN_POINT('Ctrl Pts',(69.2053351116376,309.79915592165,49.7237123518345));
#45638=CARTESIAN_POINT('Ctrl Pts',(72.227475957166,309.374843902546,46.5185499842403));
#45639=CARTESIAN_POINT('Ctrl Pts',(78.2602263630497,308.844453878664,46.1882528645145));
#45640=CARTESIAN_POINT('Ctrl Pts',(82.5073751721094,308.207985850008,52.0910727250313));
#45641=CARTESIAN_POINT('Ctrl Pts',(79.8352413443009,307.57151782135,58.8392783150243));
#45642=CARTESIAN_POINT('Ctrl Pts',(72.7158692846742,306.935049792694,60.2510571061724));
#45643=CARTESIAN_POINT('Ctrl Pts',(67.6754459456847,306.298581764036,55.0093314479775));
#45644=CARTESIAN_POINT('Ctrl Pts',(69.0879208695682,305.768191740156,49.1349729096867));
#45645=CARTESIAN_POINT('Ctrl Pts',(72.785401456947,305.343879721051,46.7401788895649));
#45646=CARTESIAN_POINT('Ctrl Pts',(77.168823957582,304.919567701947,46.3019914025474));
#45647=CARTESIAN_POINT('Ctrl Pts',(81.9401197854956,304.389177678066,50.0084600412286));
#45648=CARTESIAN_POINT('Ctrl Pts',(81.2760630292531,303.752709649409,57.2500471557014));
#45649=CARTESIAN_POINT('Ctrl Pts',(74.8336230054931,303.116241620752,60.5927323665434));
#45650=CARTESIAN_POINT('Ctrl Pts',(68.5327730738057,302.479773592095,56.9902515523144));
#45651=CARTESIAN_POINT('Ctrl Pts',(68.1644117867583,301.843305563438,49.7276166809875));
#45652=CARTESIAN_POINT('Ctrl Pts',(73.0828068247428,301.312915539558,46.2186903641038));
#45653=CARTESIAN_POINT('Ctrl Pts',(77.4447280224918,300.888603520453,46.835167904231));
#45654=CARTESIAN_POINT('Ctrl Pts',(81.0415322946407,300.464291501348,49.37866945145));
#45655=CARTESIAN_POINT('Ctrl Pts',(82.2134137079766,299.933901477468,55.3057148874212));
#45656=CARTESIAN_POINT('Ctrl Pts',(76.9635426598555,299.29743344881,60.3376538069737));
#45657=CARTESIAN_POINT('Ctrl Pts',(69.9076256472494,298.660965420154,58.6368854542147));
#45658=CARTESIAN_POINT('Ctrl Pts',(67.5127471671405,298.024497391496,51.7853794194773));
#45659=CARTESIAN_POINT('Ctrl Pts',(71.9969468835859,297.38802936284,46.0605642945113));
#45660=CARTESIAN_POINT('Ctrl Pts',(78.0112228190499,296.857639338958,46.6364623923447));
#45661=CARTESIAN_POINT('Ctrl Pts',(80.9002204941133,296.433327319855,49.9621342833063));
#45662=CARTESIAN_POINT('Ctrl Pts',(81.9479536881278,296.009015300749,54.2409958429987));
#45663=CARTESIAN_POINT('Ctrl Pts',(78.9461926833289,295.478625276869,59.4843349048045));
#45664=CARTESIAN_POINT('Ctrl Pts',(71.6829715334687,294.842157248211,59.8409493187482));
#45665=CARTESIAN_POINT('Ctrl Pts',(67.4710136627625,294.205689219555,53.9301127642556));
#45666=CARTESIAN_POINT('Ctrl Pts',(70.1556095780848,293.569221190898,47.1868551946558));
#45667=CARTESIAN_POINT('Ctrl Pts',(77.2950890531586,292.932753162241,45.8050490805407));
#45668=CARTESIAN_POINT('Ctrl Pts',(81.4582193150135,292.402363138361,50.1835785220108));
#45669=CARTESIAN_POINT('Ctrl Pts',(81.4586695413219,291.978051119255,54.5888481948173));
#45670=CARTESIAN_POINT('Ctrl Pts',(79.4439369285092,291.553739100151,58.5064052897073));
#45671=CARTESIAN_POINT('Ctrl Pts',(73.739412051243,291.02334907627,60.4967744945643));
#45672=CARTESIAN_POINT('Ctrl Pts',(68.0218570386755,290.386881047614,56.0033214804261));
#45673=CARTESIAN_POINT('Ctrl Pts',(68.7177396306583,289.750413018956,48.7787574592059));
#45674=CARTESIAN_POINT('Ctrl Pts',(75.1663439435118,289.113944990299,45.4479797279876));
#45675=CARTESIAN_POINT('Ctrl Pts',(81.4627210041053,288.477476961642,49.0862748263596));
#45676=CARTESIAN_POINT('Ctrl Pts',(81.7347500545205,287.947086937761,55.1219333523798));
#45677=CARTESIAN_POINT('Ctrl Pts',(78.8464322188351,287.522774918657,58.4481956951477));
#45678=CARTESIAN_POINT('Ctrl Pts',(74.7564632857218,287.098462899552,60.0848249198105));
#45679=CARTESIAN_POINT('Ctrl Pts',(69.1444214732981,286.568072875672,57.8469329781387));
#45680=CARTESIAN_POINT('Ctrl Pts',(67.7741643695786,285.931604847014,50.7052279449051));
#45681=CARTESIAN_POINT('Ctrl Pts',(73.0369013253525,285.295136818358,45.7070105013696));
#45682=CARTESIAN_POINT('Ctrl Pts',(80.0896642948305,284.6586687897,47.4208110658734));
#45683=CARTESIAN_POINT('Ctrl Pts',(82.4576813474655,284.022200761044,54.2964238058723));
#45684=CARTESIAN_POINT('Ctrl Pts',(78.7053135331846,283.491810737163,59.0317072644775));
#45685=CARTESIAN_POINT('Ctrl Pts',(74.3435184367344,283.067498718059,59.6490763837532));
#45686=CARTESIAN_POINT('Ctrl Pts',(70.1824192885522,282.643186698953,58.2028208835556));
#45687=CARTESIAN_POINT('Ctrl Pts',(67.4127902942353,282.112796675073,52.8332465167339));
#45688=CARTESIAN_POINT('Ctrl Pts',(71.0612642256814,281.476328646415,46.542762172618));
#45689=CARTESIAN_POINT('Ctrl Pts',(78.3120869932642,280.839860617759,46.2200439183594));
#45690=CARTESIAN_POINT('Ctrl Pts',(82.5131179862013,280.203392589102,52.1386515650035));
#45691=CARTESIAN_POINT('Ctrl Pts',(79.7924343265619,279.566924560445,58.882495849696));
#45692=CARTESIAN_POINT('Ctrl Pts',(73.8543494440967,279.036534536564,59.9970906530344));
#45693=CARTESIAN_POINT('Ctrl Pts',(70.1563794296432,278.61222251746,57.6030524609712));
#45694=CARTESIAN_POINT('Ctrl Pts',(67.9631103479317,278.187910498355,53.7825849728147));
#45695=CARTESIAN_POINT('Ctrl Pts',(69.3930268217517,277.657520474474,47.9124476213647));
#45696=CARTESIAN_POINT('Ctrl Pts',(76.2724605362172,277.021052445817,45.5555540980418));
#45697=CARTESIAN_POINT('Ctrl Pts',(81.9584281485478,276.384584417161,50.0664686605292));
#45698=CARTESIAN_POINT('Ctrl Pts',(81.2492000712417,275.748116388503,57.2897347786293));
#45699=CARTESIAN_POINT('Ctrl Pts',(74.7729648801304,275.111648359847,60.5972917413162));
#45700=CARTESIAN_POINT('Ctrl Pts',(69.5588554872861,274.581258335966,57.5450406234622));
#45701=CARTESIAN_POINT('Ctrl Pts',(68.3367351457568,274.156946316861,53.3126863183886));
#45702=CARTESIAN_POINT('Ctrl Pts',(69.1860094178192,273.732634297757,48.990055834104));
#45703=CARTESIAN_POINT('Ctrl Pts',(74.1148048310027,273.202244273876,45.4957534113066));
#45704=CARTESIAN_POINT('Ctrl Pts',(80.8542399341408,272.565776245219,48.2273408257238));
#45705=CARTESIAN_POINT('Ctrl Pts',(82.1891986104981,271.929308216562,55.361516546222));
#45706=CARTESIAN_POINT('Ctrl Pts',(76.917236919249,271.292840187905,60.3500030706631));
#45707=CARTESIAN_POINT('Ctrl Pts',(69.8588392120054,270.656372159248,58.6005525516741));
#45708=CARTESIAN_POINT('Ctrl Pts',(67.9236461013498,270.125982135367,52.8770744769839));
#45709=CARTESIAN_POINT('Ctrl Pts',(69.7762207730987,269.701670116262,48.8802797388908));
#45710=CARTESIAN_POINT('Ctrl Pts',(73.2518895769041,269.277358097158,46.1735977370467));
#45711=CARTESIAN_POINT('Ctrl Pts',(79.2644284747478,268.746968073277,46.7673566518502));
#45712=CARTESIAN_POINT('Ctrl Pts',(82.5615066218131,268.11050004462,53.2489329265036));
#45713=CARTESIAN_POINT('Ctrl Pts',(78.891319649359,267.474032015963,59.5105864993037));
#45714=CARTESIAN_POINT('Ctrl Pts',(71.6399130646353,266.837563987306,59.8199090195935));
#45715=CARTESIAN_POINT('Ctrl Pts',(67.4580045253141,266.201095958649,53.8706908961121));
#45716=CARTESIAN_POINT('Ctrl Pts',(69.7499824125412,265.670705934768,48.2805199674685));
#45717=CARTESIAN_POINT('Ctrl Pts',(73.7694808477695,265.246393915664,46.4777350601514));
#45718=CARTESIAN_POINT('Ctrl Pts',(78.1684483448451,264.822081896559,46.7132898362162));
#45719=CARTESIAN_POINT('Ctrl Pts',(82.3185553137515,264.291691872679,51.1041651240854));
#45720=CARTESIAN_POINT('Ctrl Pts',(80.5576910193728,263.655223844021,58.1597240848477));
#45721=CARTESIAN_POINT('Ctrl Pts',(73.6807691535739,263.018755815364,60.4806126065627));
#45722=CARTESIAN_POINT('Ctrl Pts',(68.0031447158811,262.382287786708,55.959201474732));
#45723=CARTESIAN_POINT('Ctrl Pts',(68.746882336194,261.74581975805,48.7253636507177));
#45724=CARTESIAN_POINT('Ctrl Pts',(74.1429501045604,261.21542973417,46.0077127742825));
#45725=CARTESIAN_POINT('Ctrl Pts',(78.3597971094831,260.791117715065,47.2823117033291));
#45726=CARTESIAN_POINT('Ctrl Pts',(81.5265462869171,260.36680569596,50.3446801886808));
#45727=CARTESIAN_POINT('Ctrl Pts',(81.7806472705137,259.83641567208,56.3811200614141));
#45728=CARTESIAN_POINT('Ctrl Pts',(75.8246732213346,259.199947643423,60.5534010248098));
#45729=CARTESIAN_POINT('Ctrl Pts',(69.1107440375934,258.563479614766,57.7962770170366));
#45730=CARTESIAN_POINT('Ctrl Pts',(67.7889673285718,257.927011586109,50.6596472655351));
#45731=CARTESIAN_POINT('Ctrl Pts',(73.0939157961889,257.290543557452,45.6858079971291));
#45732=CARTESIAN_POINT('Ctrl Pts',(78.9499721002604,256.760153533571,47.1723402741198));
#45733=CARTESIAN_POINT('Ctrl Pts',(81.2978906528269,256.335841514467,50.8997629176322));
#45734=CARTESIAN_POINT('Ctrl Pts',(81.6806978999942,255.911529495362,55.2883685850816));
#45735=CARTESIAN_POINT('Ctrl Pts',(77.9142820912556,255.381139471482,60.0124860267495));
#45736=CARTESIAN_POINT('Ctrl Pts',(70.6816566300579,254.744671442824,59.2570495634751));
#45737=CARTESIAN_POINT('Ctrl Pts',(67.4205804396085,254.108203414168,52.7729181676277));
#45738=CARTESIAN_POINT('Ctrl Pts',(71.1023289393623,253.47173538551,46.5180555901532));
#45739=CARTESIAN_POINT('Ctrl Pts',(78.3690358413775,252.835267356853,46.2414220560095));
#45740=CARTESIAN_POINT('Ctrl Pts',(81.8155825545176,252.304877332973,51.2037289188641));
#45741=CARTESIAN_POINT('Ctrl Pts',(81.1440803202529,251.880565313868,55.557518744089));
#45742=CARTESIAN_POINT('Ctrl Pts',(78.555368089813,251.456253294763,59.1219219312753));
#45743=CARTESIAN_POINT('Ctrl Pts',(72.613998875791,250.925863270883,60.218874760553));
#45744=CARTESIAN_POINT('Ctrl Pts',(67.6487461946136,250.289395242226,54.9058886769958));
#45745=CARTESIAN_POINT('Ctrl Pts',(69.4384673363466,249.652927213568,47.8720080899112));
#45746=CARTESIAN_POINT('Ctrl Pts',(76.3196650807418,249.016459184912,45.5638279667278));
#45747=CARTESIAN_POINT('Ctrl Pts',(81.9874061413906,248.379991156254,50.1199520411405));
#45748=CARTESIAN_POINT('Ctrl Pts',(81.3356174014151,247.849601132374,56.1264772500639));
#45749=CARTESIAN_POINT('Ctrl Pts',(77.9737339767994,247.425289113269,58.9732545388849));
#45750=CARTESIAN_POINT('Ctrl Pts',(73.6819847610538,247.000977094165,59.9668790967541));
#45751=CARTESIAN_POINT('Ctrl Pts',(68.4769640391432,246.470587070284,56.8991547070032));
#45752=CARTESIAN_POINT('Ctrl Pts',(68.2120838441216,245.834119041627,49.6320098897938));
#45753=CARTESIAN_POINT('Ctrl Pts',(74.1756296257088,245.19765101297,45.4950182787986));
#45754=CARTESIAN_POINT('Ctrl Pts',(80.8844538365335,244.561182984313,48.2645409067584));
#45755=CARTESIAN_POINT('Ctrl Pts',(82.176006380466,243.924714955656,55.4208980343947));
#45756=CARTESIAN_POINT('Ctrl Pts',(77.7452620688528,243.394324931776,59.5284129147206));
#45757=CARTESIAN_POINT('Ctrl Pts',(73.3403378631987,242.970012912671,59.4732419504946));
#45758=CARTESIAN_POINT('Ctrl Pts',(69.4485311580947,242.545700893566,57.4092066642255));
#45759=CARTESIAN_POINT('Ctrl Pts',(67.5303462247113,242.015310869685,51.6800060037207));
#45760=CARTESIAN_POINT('Ctrl Pts',(72.0956311926795,241.378842841029,46.0196413093522));
#45761=CARTESIAN_POINT('Ctrl Pts',(79.310833082975,240.742374812371,46.80668613705));
#45762=CARTESIAN_POINT('Ctrl Pts',(82.5599249123451,240.105906783714,53.2968309861926));
#45763=CARTESIAN_POINT('Ctrl Pts',(78.8424214579609,239.469438755058,59.5467688561755));
#45764=CARTESIAN_POINT('Ctrl Pts',(72.8038093924522,238.939048731177,59.7425696970413));
#45765=CARTESIAN_POINT('Ctrl Pts',(69.514280236937,238.514736712072,56.8124845399393));
#45766=CARTESIAN_POINT('Ctrl Pts',(67.9294216226235,238.090424692967,52.7021774631518));
#45767=CARTESIAN_POINT('Ctrl Pts',(70.2379930979051,237.560034669087,47.1188387316663));
#45768=CARTESIAN_POINT('Ctrl Pts',(77.3964297879165,236.92356664043,45.8388623775458));
#45769=CARTESIAN_POINT('Ctrl Pts',(82.3278012354823,236.287098611773,51.1642875741535));
#45770=CARTESIAN_POINT('Ctrl Pts',(80.5250887439314,235.650630583116,58.1948498241683));
#45771=CARTESIAN_POINT('Ctrl Pts',(73.6201253695851,235.014162554459,60.4758662885864));
#45772=CARTESIAN_POINT('Ctrl Pts',(68.9325969518973,234.483772530578,56.6640096569224));
#45773=CARTESIAN_POINT('Ctrl Pts',(68.3703492866676,234.059460511474,52.2947673134723));
#45774=CARTESIAN_POINT('Ctrl Pts',(69.8690277487388,233.635148492369,48.1522603478558));
#45775=CARTESIAN_POINT('Ctrl Pts',(75.2731435712621,233.104758468489,45.4506486393164));
#45776=CARTESIAN_POINT('Ctrl Pts',(81.5170606760362,232.468290439831,49.1782557136697));
#45777=CARTESIAN_POINT('Ctrl Pts',(81.74820395588,231.831822411175,56.4325751622959));
#45778=CARTESIAN_POINT('Ctrl Pts',(75.777025664907,231.195354382517,60.5585426483244));
#45779=CARTESIAN_POINT('Ctrl Pts',(69.0680704313891,230.558886353861,57.7529277447718));
#45780=CARTESIAN_POINT('Ctrl Pts',(68.0285390303481,230.028496329979,51.8012432678224));
#45781=CARTESIAN_POINT('Ctrl Pts',(70.4690771432479,229.604184310875,48.1337952706548));
#45782=CARTESIAN_POINT('Ctrl Pts',(74.3169324202657,229.17987229177,45.9889384313317));
#45783=CARTESIAN_POINT('Ctrl Pts',(80.1685476557545,228.64948226789,47.4928575710618));
#45784=CARTESIAN_POINT('Ctrl Pts',(82.438393234342,228.013014239233,54.4015011690346));
#45785=CARTESIAN_POINT('Ctrl Pts',(77.8560469329069,227.376546210576,60.0300605107207));
#45786=CARTESIAN_POINT('Ctrl Pts',(70.6423113450935,226.740078181919,59.2296876487903));
#45787=CARTESIAN_POINT('Ctrl Pts',(67.4167872981172,226.103610153262,52.7122073106552));
#45788=CARTESIAN_POINT('Ctrl Pts',(70.5346287283472,225.573220129381,47.5370514181189));
#45789=CARTESIAN_POINT('Ctrl Pts',(74.7820762065753,225.148908110276,46.3684664110055));
#45790=CARTESIAN_POINT('Ctrl Pts',(79.0936391685144,224.724596091172,47.2722507331135));
#45791=CARTESIAN_POINT('Ctrl Pts',(82.5254317902303,224.194206067291,52.2447725022218));
#45792=CARTESIAN_POINT('Ctrl Pts',(79.7089697578622,223.557738038634,58.94918123044));
#45793=CARTESIAN_POINT('Ctrl Pts',(72.5585073072376,222.921270009977,60.1939570431606));
#45794=CARTESIAN_POINT('Ctrl Pts',(67.6369827609765,222.28480198132,54.8594306967786));
#45795=CARTESIAN_POINT('Ctrl Pts',(69.4754129514866,221.648333952663,47.8236843010338));
#45796=CARTESIAN_POINT('Ctrl Pts',(75.2228696622896,221.117943928782,45.9609103224261));
#45797=CARTESIAN_POINT('Ctrl Pts',(79.1959535942427,220.693631909678,47.8638011191713));
#45798=CARTESIAN_POINT('Ctrl Pts',(81.8585388479515,220.269319890573,51.3733674413462));
#45799=CARTESIAN_POINT('Ctrl Pts',(81.1889060619244,219.738929866692,57.3779305317796));
#45800=CARTESIAN_POINT('Ctrl Pts',(74.6662293605485,219.102461838036,60.5929086255491));
#45801=CARTESIAN_POINT('Ctrl Pts',(68.4513936313183,218.465993809378,56.8439552027099));
#45802=CARTESIAN_POINT('Ctrl Pts',(68.2336921254748,217.829525780721,49.5892193551519));
#45803=CARTESIAN_POINT('Ctrl Pts',(74.2351594197245,217.193057752065,45.4827627314684));
#45804=CARTESIAN_POINT('Ctrl Pts',(79.7960878518984,216.662667728184,47.8451334079548));
#45805=CARTESIAN_POINT('Ctrl Pts',(81.5477681874052,216.238355709079,51.8870828353502));
#45806=CARTESIAN_POINT('Ctrl Pts',(81.257103920335,215.814043689975,56.2827072143604));
#45807=CARTESIAN_POINT('Ctrl Pts',(76.8132641208564,215.283653666094,60.3770845603876));
#45808=CARTESIAN_POINT('Ctrl Pts',(69.7821658351079,214.647185637437,58.5272029458524));
#45809=CARTESIAN_POINT('Ctrl Pts',(67.5453429981363,214.01071760878,51.6216558681655));
#45810=CARTESIAN_POINT('Ctrl Pts',(72.1435593680832,213.374249580123,46.0013327700207));
#45811=CARTESIAN_POINT('Ctrl Pts',(79.3569958438914,212.737781551466,46.8367726073938));
#45812=CARTESIAN_POINT('Ctrl Pts',(82.5569693436358,212.101313522809,53.3521487628495));
#45813=CARTESIAN_POINT('Ctrl Pts',(78.7957165783259,211.464845494152,59.5739959746584));
#45814=CARTESIAN_POINT('Ctrl Pts',(72.7551636611878,210.934455470271,59.7268307558592));
#45815=CARTESIAN_POINT('Ctrl Pts',(69.4871702856738,210.510143451167,56.772813373531));
#45816=CARTESIAN_POINT('Ctrl Pts',(67.9318512102494,210.085831432062,52.6513182873948));
#45817=CARTESIAN_POINT('Ctrl Pts',(70.2807526184919,209.555441408181,47.0846871324468));
#45818=CARTESIAN_POINT('Ctrl Pts',(77.4481799203683,208.918973379524,45.8564438509837));
#45819=CARTESIAN_POINT('Ctrl Pts',(82.3410297505945,208.282505350868,51.2172839626031));
#45820=CARTESIAN_POINT('Ctrl Pts',(80.4876226573618,207.64603732221,58.2346707308159));
#45821=CARTESIAN_POINT('Ctrl Pts',(73.5663904206805,207.009569293554,60.4658004491442));
#45822=CARTESIAN_POINT('Ctrl Pts',(68.906481682848,206.479179269673,56.6202268209065));
#45823=CARTESIAN_POINT('Ctrl Pts',(68.3757750274088,206.054867250568,52.2470396023114));
#45824=CARTESIAN_POINT('Ctrl Pts',(69.9043015957043,205.630555231463,48.1154544531592));
#45825=CARTESIAN_POINT('Ctrl Pts',(75.3277696890035,205.100165207583,45.4529031618409));
#45826=CARTESIAN_POINT('Ctrl Pts',(81.5446291154323,204.463697178925,49.2254635367899));
#45827=CARTESIAN_POINT('Ctrl Pts',(81.7234265711998,203.827229150269,56.4812616782425));
#45828=CARTESIAN_POINT('Ctrl Pts',(75.7226346705662,203.190761121611,60.5640397333196));
#45829=CARTESIAN_POINT('Ctrl Pts',(69.0340966790468,202.554293092955,57.7100925875615));
#45830=CARTESIAN_POINT('Ctrl Pts',(68.0375337913152,202.023903069074,51.7510628214405));
#45831=CARTESIAN_POINT('Ctrl Pts',(70.5044690880589,201.599591049969,48.1013187869457));
#45832=CARTESIAN_POINT('Ctrl Pts',(74.3676993763908,201.175279030865,45.9842801150092));
#45833=CARTESIAN_POINT('Ctrl Pts',(80.2083115098209,200.644889006984,47.5303795952959));
#45834=CARTESIAN_POINT('Ctrl Pts',(82.4282520384488,200.008420978327,54.4552203432806));
#45835=CARTESIAN_POINT('Ctrl Pts',(77.8054148727975,199.37195294967,60.0505714840824));
#45836=CARTESIAN_POINT('Ctrl Pts',(70.5976417472473,198.735484921013,59.1981722467762));
#45837=CARTESIAN_POINT('Ctrl Pts',(67.419225377324,198.099016892356,52.6575893450889));
#45838=CARTESIAN_POINT('Ctrl Pts',(70.5743244731881,197.568626868476,47.5050634268305));
#45839=CARTESIAN_POINT('Ctrl Pts',(74.8300927655731,197.144314849371,46.3671542320359));
#45840=CARTESIAN_POINT('Ctrl Pts',(79.1350226650609,196.720002830266,47.3020230211936));
#45841=CARTESIAN_POINT('Ctrl Pts',(82.5308491916423,196.189612806385,52.2991757953517));
#45842=CARTESIAN_POINT('Ctrl Pts',(79.6660879734873,195.553144777728,58.9830892055735));
#45843=CARTESIAN_POINT('Ctrl Pts',(72.5068307161614,194.916676749071,60.1762419207686));
#45844=CARTESIAN_POINT('Ctrl Pts',(67.6239226704089,194.280208720415,54.8063455628062));
#45845=CARTESIAN_POINT('Ctrl Pts',(69.5130685817726,193.643740691757,47.7840465775991));
#45846=CARTESIAN_POINT('Ctrl Pts',(75.2738146162295,193.113350667877,45.9627891072083));
#45847=CARTESIAN_POINT('Ctrl Pts',(79.2330672642372,192.689038648772,47.8942961773743));
#45848=CARTESIAN_POINT('Ctrl Pts',(81.8702586670936,192.264726629668,51.4229818530266));
#45849=CARTESIAN_POINT('Ctrl Pts',(81.1573268859826,191.734336605787,57.4225569981905));
#45850=CARTESIAN_POINT('Ctrl Pts',(74.6116118538668,191.09786857713,60.590390647602));
#45851=CARTESIAN_POINT('Ctrl Pts',(68.4240078959387,190.461400548473,56.7966938834467));
#45852=CARTESIAN_POINT('Ctrl Pts',(68.2586153345421,189.824932519816,49.5405776234103));
#45853=CARTESIAN_POINT('Ctrl Pts',(74.2896321797345,189.188464491159,45.4775256762879));
#45854=CARTESIAN_POINT('Ctrl Pts',(79.8332295550212,188.658074467278,47.8799623118115));
#45855=CARTESIAN_POINT('Ctrl Pts',(81.555912114883,188.233762448174,51.934437110204));
#45856=CARTESIAN_POINT('Ctrl Pts',(81.2331274814595,187.809450429069,56.3278652902565));
#45857=CARTESIAN_POINT('Ctrl Pts',(76.7607776831728,187.279060405188,60.3900396992102));
#45858=CARTESIAN_POINT('Ctrl Pts',(69.7415433368246,186.642592376531,58.4895385802815));
#45859=CARTESIAN_POINT('Ctrl Pts',(67.5575508842565,186.006124347874,51.567923534235));
#45860=CARTESIAN_POINT('Ctrl Pts',(72.190717024769,185.369656319217,45.9811221780975));
#45861=CARTESIAN_POINT('Ctrl Pts',(79.4083750996385,184.73318829056,46.8682339107886));
#45862=CARTESIAN_POINT('Ctrl Pts',(82.0184321936041,184.20279826668,52.3171581728088));
#45863=CARTESIAN_POINT('Ctrl Pts',(80.6604212276972,183.778486247575,56.5078869053));
#45864=CARTESIAN_POINT('Ctrl Pts',(77.5358267115987,183.35417422847,59.6132548710689));
#45865=CARTESIAN_POINT('Ctrl Pts',(71.4955336193098,182.82378420459,59.7475419003588));
#45866=CARTESIAN_POINT('Ctrl Pts',(67.4422413917183,182.187316175932,53.7099614719295));
#45867=CARTESIAN_POINT('Ctrl Pts',(70.3320281351587,181.550848147276,47.052055610777));
#45868=CARTESIAN_POINT('Ctrl Pts',(77.493477408106,180.914380118619,45.8721309566008));
#45869=CARTESIAN_POINT('Ctrl Pts',(82.3610866179652,180.277912089962,51.2747169940557));
#45870=CARTESIAN_POINT('Ctrl Pts',(80.7586618438728,179.747522066081,57.1001275796167));
#45871=CARTESIAN_POINT('Ctrl Pts',(76.985389807126,179.323210046977,59.3736313138467));
#45872=CARTESIAN_POINT('Ctrl Pts',(72.590053015099,178.898898027871,59.6692925685079));
#45873=CARTESIAN_POINT('Ctrl Pts',(67.9415917424124,178.368508003991,55.8098908735143));
#45874=CARTESIAN_POINT('Ctrl Pts',(68.8403759618455,177.732039975334,48.5936770297519));
#45875=CARTESIAN_POINT('Ctrl Pts',(75.3879313276058,177.095571946677,45.4618889445139));
#45876=CARTESIAN_POINT('Ctrl Pts',(81.5685162443548,176.45910391802,49.2670102258116));
#45877=CARTESIAN_POINT('Ctrl Pts',(81.7009226931967,175.822635889363,56.5377752367517));
#45878=CARTESIAN_POINT('Ctrl Pts',(76.6712125465343,175.292245865482,59.8851905810956));
#45879=CARTESIAN_POINT('Ctrl Pts',(72.3316024134768,174.867933846378,59.1274406316263));
#45880=CARTESIAN_POINT('Ctrl Pts',(68.8192612940262,174.443621827273,56.4685196186083));
#45881=CARTESIAN_POINT('Ctrl Pts',(67.8404021049406,173.913231803392,50.5065561555424));
#45882=CARTESIAN_POINT('Ctrl Pts',(73.2508538169764,173.276763774735,45.6476913103612));
#45883=CARTESIAN_POINT('Ctrl Pts',(80.247841532224,172.640295746078,47.5766134941744));
#45884=CARTESIAN_POINT('Ctrl Pts',(82.4190432536031,172.003827717421,54.5022514405018));
#45885=CARTESIAN_POINT('Ctrl Pts',(77.751367091034,171.367359688765,60.0784826546278));
#45886=CARTESIAN_POINT('Ctrl Pts',(71.758955772151,170.836969664884,59.307651783222));
#45887=CARTESIAN_POINT('Ctrl Pts',(68.9794391377946,170.412657645779,55.8899495767404));
#45888=CARTESIAN_POINT('Ctrl Pts',(68.0711591552949,169.988345626674,51.5793314579269));
#45889=CARTESIAN_POINT('Ctrl Pts',(71.2415481569305,169.457955602794,46.4361994136081));
#45890=CARTESIAN_POINT('Ctrl Pts',(78.5125178087286,168.821487574137,46.3155526787233));
#45891=CARTESIAN_POINT('Ctrl Pts',(82.530377405723,168.18501954548,52.360003202747));
#45892=CARTESIAN_POINT('Ctrl Pts',(79.6282957660669,167.548551516823,59.0125591052029));
#45893=CARTESIAN_POINT('Ctrl Pts',(72.4477226523281,166.912083488166,60.1618741491581));
#45894=CARTESIAN_POINT('Ctrl Pts',(68.4289229561712,166.381693464285,55.650508208652));
#45895=CARTESIAN_POINT('Ctrl Pts',(68.5714774657263,165.957381445181,51.2475456486637));
#45896=CARTESIAN_POINT('Ctrl Pts',(70.7123205480204,165.533069426076,47.3974557809012));
#45897=CARTESIAN_POINT('Ctrl Pts',(76.4784505969129,165.002679402195,45.5933166769935));
#45898=CARTESIAN_POINT('Ctrl Pts',(82.0471251430861,164.366211373538,50.2700055816363));
#45899=CARTESIAN_POINT('Ctrl Pts',(81.1170844673234,163.729743344881,57.4681721690361));
#45900=CARTESIAN_POINT('Ctrl Pts',(74.5637546035804,163.093275316224,60.5878589442599));
#45901=CARTESIAN_POINT('Ctrl Pts',(68.3888028090185,162.456807287567,56.7470874531606));
#45902=CARTESIAN_POINT('Ctrl Pts',(68.3128475435835,161.926417263686,50.7057792798719));
#45903=CARTESIAN_POINT('Ctrl Pts',(71.3076207439878,161.502105244582,47.475030980949));
#45904=CARTESIAN_POINT('Ctrl Pts',(75.4485626168732,161.077793225477,45.9720334765473));
#45905=CARTESIAN_POINT('Ctrl Pts',(80.9849999203633,160.547403201597,48.3909248820298));
#45906=CARTESIAN_POINT('Ctrl Pts',(82.1226997942578,159.910935172939,55.5733474753437));
#45907=CARTESIAN_POINT('Ctrl Pts',(76.700483626755,159.274467144283,60.3980909619345));
#45908=CARTESIAN_POINT('Ctrl Pts',(69.7070713458812,158.637999115625,58.4562458218015));
#45909=CARTESIAN_POINT('Ctrl Pts',(67.5634994504208,158.001531086969,51.5073858547998));
#45910=CARTESIAN_POINT('Ctrl Pts',(71.4676070918562,157.471141063088,46.8964079573167));
#45911=CARTESIAN_POINT('Ctrl Pts',(75.8471444980346,157.046829043983,46.4209574333503));
#45912=CARTESIAN_POINT('Ctrl Pts',(79.9591020499818,156.622517024879,48.0015289071645));
#45913=CARTESIAN_POINT('Ctrl Pts',(82.5529634584382,156.092127000998,53.4581814195306));
#45914=CARTESIAN_POINT('Ctrl Pts',(78.7022097890694,155.455658972341,59.6269131765332));
#45915=CARTESIAN_POINT('Ctrl Pts',(71.4447323271936,154.819190943684,59.714084094242));
#45916=CARTESIAN_POINT('Ctrl Pts',(67.438046115442,154.182722915027,53.6622212835787));
#45917=CARTESIAN_POINT('Ctrl Pts',(70.3762155259669,153.54625488637,47.0102504608026));
#45918=CARTESIAN_POINT('Ctrl Pts',(76.3473529711757,153.015864862489,46.0890060538096));
#45919=CARTESIAN_POINT('Ctrl Pts',(79.9656584160781,152.591552843385,48.6018265408803));
#45920=CARTESIAN_POINT('Ctrl Pts',(82.0337510039629,152.16724082428,52.4914787285174));
#45921=CARTESIAN_POINT('Ctrl Pts',(80.4140309010038,151.636850800399,58.3121041618417));
#45922=CARTESIAN_POINT('Ctrl Pts',(73.4617130669307,151.000382771742,60.4444343534476));
#45923=CARTESIAN_POINT('Ctrl Pts',(67.9251761126493,150.363914743085,55.7513184980263));
#45924=CARTESIAN_POINT('Ctrl Pts',(68.8685131074888,149.727446714428,48.5548823527737));
#45925=CARTESIAN_POINT('Ctrl Pts',(75.4487054911373,149.090978685771,45.4593010654896));
#45926=CARTESIAN_POINT('Ctrl Pts',(80.5609842542104,148.560588661891,48.6792047124364));
#45927=CARTESIAN_POINT('Ctrl Pts',(81.6450692014175,148.136276642786,52.9490010682467));
#45928=CARTESIAN_POINT('Ctrl Pts',(80.6559206726707,147.711964623682,57.2417841143524));
#45929=CARTESIAN_POINT('Ctrl Pts',(75.6162903551188,147.1815745998,60.5742456534258));
#45930=CARTESIAN_POINT('Ctrl Pts',(68.9690803493656,146.545106571144,57.6253213662624));
#45931=CARTESIAN_POINT('Ctrl Pts',(67.8664158817172,145.908638542487,50.4515699801105));
#45932=CARTESIAN_POINT('Ctrl Pts',(73.2975360364468,145.27217051383,45.6368517387779));
#45933=CARTESIAN_POINT('Ctrl Pts',(80.2954228114288,144.635702485173,47.6145109603169));
#45934=CARTESIAN_POINT('Ctrl Pts',(82.0437996394039,144.105312461292,53.3977930833325));
#45935=CARTESIAN_POINT('Ctrl Pts',(80.0624568115943,143.681000442187,57.3323428277813));
#45936=CARTESIAN_POINT('Ctrl Pts',(76.5007551034253,143.256688423083,59.92477065414));
#45937=CARTESIAN_POINT('Ctrl Pts',(70.5106597070975,142.726298399202,59.1361447669926));
#45938=CARTESIAN_POINT('Ctrl Pts',(67.4257250957628,142.089830370545,52.550954279558));
#45939=CARTESIAN_POINT('Ctrl Pts',(71.297244453972,141.453362341888,46.4117429509309));
#45940=CARTESIAN_POINT('Ctrl Pts',(78.5548705710514,140.816894313231,46.3379796591357));
#45941=CARTESIAN_POINT('Ctrl Pts',(82.5414507256682,140.180426284574,52.4198160580224));
#45942=CARTESIAN_POINT('Ctrl Pts',(80.0692118555573,139.650036260693,57.9326382586836));
#45943=CARTESIAN_POINT('Ctrl Pts',(75.9933095704882,139.225724241589,59.6039914994505));
#45944=CARTESIAN_POINT('Ctrl Pts',(71.6043070931456,138.801412222484,59.2257609523848));
#45945=CARTESIAN_POINT('Ctrl Pts',(67.5989245988587,138.271022198604,54.7024784361751));
#45946=CARTESIAN_POINT('Ctrl Pts',(69.5878994285397,137.634554169946,47.7077994271777));
#45947=CARTESIAN_POINT('Ctrl Pts',(76.5365379382289,136.99808614129,45.6113737213163));
#45948=CARTESIAN_POINT('Ctrl Pts',(82.0643953738658,136.361618112632,50.3147097766925));
#45949=CARTESIAN_POINT('Ctrl Pts',(81.0862238434915,135.725150083976,57.5205918024526));
#45950=CARTESIAN_POINT('Ctrl Pts',(75.6047792136601,135.194760060095,60.0616424546605));
#45951=CARTESIAN_POINT('Ctrl Pts',(71.4315308456683,134.77044804099,58.6508273881453));
#45952=CARTESIAN_POINT('Ctrl Pts',(68.3658617004297,134.346136021886,55.4872734080804));
#45953=CARTESIAN_POINT('Ctrl Pts',(68.3078504172972,133.815745998005,49.4457662833621));
#45954=CARTESIAN_POINT('Ctrl Pts',(74.3961266495209,133.179277969348,45.4690279424416));
#45955=CARTESIAN_POINT('Ctrl Pts',(81.0170152058,132.542809940691,48.442647387472));
#45956=CARTESIAN_POINT('Ctrl Pts',(82.1064249903531,131.906341912034,55.6184235963466));
#45957=CARTESIAN_POINT('Ctrl Pts',(76.6428109257527,131.269873883377,60.4174314797647));
#45958=CARTESIAN_POINT('Ctrl Pts',(70.8380969889688,130.739483859496,58.7415825130923));
#45959=CARTESIAN_POINT('Ctrl Pts',(68.6124160006545,130.315171840392,54.9399058788808));
#45960=CARTESIAN_POINT('Ctrl Pts',(68.3722740552658,129.890859821287,50.5411864130682));
#45961=CARTESIAN_POINT('Ctrl Pts',(72.2900598145347,129.360469797406,45.941824675668));
#45962=CARTESIAN_POINT('Ctrl Pts',(79.4943503469096,128.724001768749,46.9316495274165));
#45963=CARTESIAN_POINT('Ctrl Pts',(82.5432190311814,128.087533740092,53.5182250887076));
#45964=CARTESIAN_POINT('Ctrl Pts',(78.6603646892618,127.451065711435,59.6502736891323));
#45965=CARTESIAN_POINT('Ctrl Pts',(71.3885074732591,126.814597682778,59.6908685418939));
#45966=CARTESIAN_POINT('Ctrl Pts',(68.1048643284523,126.284207658898,54.6192946890791));
#45967=CARTESIAN_POINT('Ctrl Pts',(68.9173460103732,125.859895639793,50.28959786258));
#45968=CARTESIAN_POINT('Ctrl Pts',(71.6204020703455,125.435583620688,46.8111083873192));
#45969=CARTESIAN_POINT('Ctrl Pts',(77.5942494198532,124.905193596808,45.9076032729058));
#45970=CARTESIAN_POINT('Ctrl Pts',(82.3844143232222,124.268725568151,51.3789719783156));
#45971=CARTESIAN_POINT('Ctrl Pts',(80.3673015812238,123.632257539494,58.3510472837465));
#45972=CARTESIAN_POINT('Ctrl Pts',(73.4148019883362,122.995789510837,60.4346324846513));
#45973=CARTESIAN_POINT('Ctrl Pts',(67.8979495774062,122.35932148218,55.6969226172128));
#45974=CARTESIAN_POINT('Ctrl Pts',(68.7443794887827,121.828931458299,49.7147215129271));
#45975=CARTESIAN_POINT('Ctrl Pts',(72.19690357994,121.404619439194,46.978578517243));
#45976=CARTESIAN_POINT('Ctrl Pts',(76.5186460802307,120.98030742009,46.1247970147295));
#45977=CARTESIAN_POINT('Ctrl Pts',(81.6213386668304,120.449917396209,49.3598707408833));
#45978=CARTESIAN_POINT('Ctrl Pts',(81.6501721592166,119.813449367552,56.6317841026972));
#45979=CARTESIAN_POINT('Ctrl Pts',(75.5554737531873,119.176981338895,60.5730058952479));
#45980=CARTESIAN_POINT('Ctrl Pts',(68.9400899651232,118.540513310238,57.5871600828947));
#45981=CARTESIAN_POINT('Ctrl Pts',(67.8815288094136,117.904045281581,50.3926480360889));
#45982=CARTESIAN_POINT('Ctrl Pts',(72.4432767065111,117.3736552577,46.431129416883));
#45983=CARTESIAN_POINT('Ctrl Pts',(76.8440883983223,116.949343238596,46.6292645880943));
#45984=CARTESIAN_POINT('Ctrl Pts',(80.6668409771502,116.525031219491,48.8185484467835));
#45985=CARTESIAN_POINT('Ctrl Pts',(82.3980328243406,115.99464119561,54.6069980177146));
#45986=CARTESIAN_POINT('Ctrl Pts',(77.6514063441161,115.358173166953,60.1161805677161));
#45987=CARTESIAN_POINT('Ctrl Pts',(70.4655562751022,114.721705138296,59.095329616704));
#45988=CARTESIAN_POINT('Ctrl Pts',(67.4288608453278,114.085237109639,52.5031328094692));
#45989=CARTESIAN_POINT('Ctrl Pts',(71.3472914312269,113.448769080983,46.3771670035329));
#45990=CARTESIAN_POINT('Ctrl Pts',(77.3890770562702,112.918379057102,46.3774956509925));
#45991=CARTESIAN_POINT('Ctrl Pts',(80.5817556707862,112.494067037997,49.4128217219879));
#45992=CARTESIAN_POINT('Ctrl Pts',(82.0323496299757,112.069755018893,53.5724104346394));
#45993=CARTESIAN_POINT('Ctrl Pts',(79.5437477049679,111.539364995012,59.0778653754993));
#45994=CARTESIAN_POINT('Ctrl Pts',(72.3475329797288,110.902896966355,60.1247889353924));
#45995=CARTESIAN_POINT('Ctrl Pts',(67.5916352536787,110.266428937698,54.6420875302564));
#45996=CARTESIAN_POINT('Ctrl Pts',(69.6216247782731,109.629960909041,47.6737505400865));
#45997=CARTESIAN_POINT('Ctrl Pts',(76.5969956852068,108.993492880384,45.6180861650704));
#45998=CARTESIAN_POINT('Ctrl Pts',(81.1583125757584,108.463102856503,49.5801010402264));
#45999=CARTESIAN_POINT('Ctrl Pts',(81.5784289429698,108.038790837399,53.9652924078702));
#46000=CARTESIAN_POINT('Ctrl Pts',(79.9460656780891,107.614478818294,58.0569658142309));
#46001=CARTESIAN_POINT('Ctrl Pts',(74.4570979014776,107.084088794413,60.5817244946414));
#46002=CARTESIAN_POINT('Ctrl Pts',(68.3374776727713,106.447620765756,56.6533910606747));
#46003=CARTESIAN_POINT('Ctrl Pts',(68.3419469760824,105.811152737099,49.3953914806349));
#46004=CARTESIAN_POINT('Ctrl Pts',(74.4439160021854,105.174684708442,45.4654357705778));
#46005=CARTESIAN_POINT('Ctrl Pts',(81.0582591112123,104.538216679785,48.487359089935));
#46006=CARTESIAN_POINT('Ctrl Pts',(81.904038204952,104.007826655905,54.4696522431987));
#46007=CARTESIAN_POINT('Ctrl Pts',(79.3457331141397,103.5835146368,58.0559422698385));
#46008=CARTESIAN_POINT('Ctrl Pts',(75.4302791372836,103.159202617695,60.0747590638976));
#46009=CARTESIAN_POINT('Ctrl Pts',(69.6305683429886,102.628812593814,58.3816765645705));
#46010=CARTESIAN_POINT('Ctrl Pts',(67.586188434933,101.992344565158,51.4029900045114));
#46011=CARTESIAN_POINT('Ctrl Pts',(72.3488347856765,101.355876536501,45.9261498921585));
#46012=CARTESIAN_POINT('Ctrl Pts',(79.5327866704922,100.719408507844,46.9602742537252));
#46013=CARTESIAN_POINT('Ctrl Pts',(82.5450393663006,100.082940479187,53.5790270825144));
#46014=CARTESIAN_POINT('Ctrl Pts',(79.2608444968025,99.552550455306,58.6502436728556));
#46015=CARTESIAN_POINT('Ctrl Pts',(74.9777007832863,99.1282384362012,59.6803315439721));
#46016=CARTESIAN_POINT('Ctrl Pts',(70.6977489610756,98.7039264170968,58.6370609690939));
#46017=CARTESIAN_POINT('Ctrl Pts',(67.4291836821179,98.1735363932157,53.5557565436354));
#46018=CARTESIAN_POINT('Ctrl Pts',(70.4618009105109,97.537068364559,46.9463096637473));
#46019=CARTESIAN_POINT('Ctrl Pts',(77.6489027609979,96.900600335902,45.9343092342729));
#46020=CARTESIAN_POINT('Ctrl Pts',(82.3946636187328,96.2641323072451,51.4257873376363));
#46021=CARTESIAN_POINT('Ctrl Pts',(80.3288063723495,95.6276642785881,58.3981462748664));
#46022=CARTESIAN_POINT('Ctrl Pts',(74.5239101517951,95.0972742547074,60.0733637280889));
#46023=CARTESIAN_POINT('Ctrl Pts',(70.6146905705551,94.6729622356027,58.0425010152246));
#46024=CARTESIAN_POINT('Ctrl Pts',(68.0674396145845,94.248650216498,54.4483510934541));
#46025=CARTESIAN_POINT('Ctrl Pts',(68.9316338822774,93.7182601926173,48.4686904078737));
#46026=CARTESIAN_POINT('Ctrl Pts',(75.555249990983,93.0817921639603,45.467146645657));
#46027=CARTESIAN_POINT('Ctrl Pts',(81.6450899558155,92.4453241353034,49.4158713867934));
#46028=CARTESIAN_POINT('Ctrl Pts',(81.627212218408,91.8088561066465,56.6738503248336));
#46029=CARTESIAN_POINT('Ctrl Pts',(75.4955258534093,91.1723880779895,60.5833231324249));
#46030=CARTESIAN_POINT('Ctrl Pts',(70.0143577007266,90.6419980541087,58.0416761606747));
#46031=CARTESIAN_POINT('Ctrl Pts',(68.3946002320209,90.217686035004,53.9449961834947));
#46032=CARTESIAN_POINT('Ctrl Pts',(68.8282163938946,89.7933740158995,49.5611191189533));
#46033=CARTESIAN_POINT('Ctrl Pts',(73.4017105105445,89.2629839920186,45.6131670913877));
#46034=CARTESIAN_POINT('Ctrl Pts',(80.3707190660536,88.6265159633618,47.6902985425126));
#46035=CARTESIAN_POINT('Ctrl Pts',(82.3792438057071,87.9900479347048,54.6648527396444));
#46036=CARTESIAN_POINT('Ctrl Pts',(77.6064876577145,87.3535799060478,60.1328849844586));
#46037=CARTESIAN_POINT('Ctrl Pts',(70.4135304679223,86.7171118773909,59.0638095999201));
#46038=CARTESIAN_POINT('Ctrl Pts',(67.9418913606345,86.1867218535102,53.5507184733093));
#46039=CARTESIAN_POINT('Ctrl Pts',(69.4052856106959,85.7624098344054,49.3956157836349));
#46040=CARTESIAN_POINT('Ctrl Pts',(72.6072947099124,85.3380978153011,46.3701341985994));
#46041=CARTESIAN_POINT('Ctrl Pts',(78.649052708911,84.8077077914199,46.3884079099854));
#46042=CARTESIAN_POINT('Ctrl Pts',(82.5486031776573,84.1712397627633,52.5264093317599));
#46043=CARTESIAN_POINT('Ctrl Pts',(79.4916250958263,83.5347717341059,59.1092250580077));
#46044=CARTESIAN_POINT('Ctrl Pts',(72.3026659383084,82.8983037054495,60.1079462954285));
#46045=CARTESIAN_POINT('Ctrl Pts',(67.5730244559151,82.2618356767921,54.5841752321032));
#46046=CARTESIAN_POINT('Ctrl Pts',(69.3220304454764,81.7314456529117,48.8010833518486));
#46047=CARTESIAN_POINT('Ctrl Pts',(73.1515056005973,81.3071336338068,46.6235799352798));
#46048=CARTESIAN_POINT('Ctrl Pts',(77.552906480988,80.8828216147023,46.4389955834307));
#46049=CARTESIAN_POINT('Ctrl Pts',(82.1024354368033,80.3524315908214,50.4145408198967));
#46050=CARTESIAN_POINT('Ctrl Pts',(81.0217277540724,79.7159635621645,57.6057595077474));
#46051=CARTESIAN_POINT('Ctrl Pts',(74.3971820521111,79.0794955335075,60.5712227297676));
#46052=CARTESIAN_POINT('Ctrl Pts',(68.3146473605973,78.4430275048508,56.6112543454159));
#46053=CARTESIAN_POINT('Ctrl Pts',(68.3658705756886,77.8065594761935,49.3394642292037));
#46054=CARTESIAN_POINT('Ctrl Pts',(73.4784996066541,77.276169452313,46.1201167737832));
#46055=CARTESIAN_POINT('Ctrl Pts',(77.7975928712179,76.8518574332082,46.9872006594904));
#46056=CARTESIAN_POINT('Ctrl Pts',(81.2416761493576,76.4275454141037,49.7339608357872));
#46057=CARTESIAN_POINT('Ctrl Pts',(82.0696831491612,75.8971553902228,55.7187397001453));
#46058=CARTESIAN_POINT('Ctrl Pts',(76.5382697150696,75.2606873615659,60.4394409968975));
#46059=CARTESIAN_POINT('Ctrl Pts',(69.5922183320309,74.6242193329089,58.3344592718662));
#46060=CARTESIAN_POINT('Ctrl Pts',(67.5965818240238,73.987751304252,51.3562064241657));
#46061=CARTESIAN_POINT('Ctrl Pts',(72.4035700940913,73.351283275595,45.8996123322947));
#46062=CARTESIAN_POINT('Ctrl Pts',(78.3746072804039,72.8208932517143,46.8215063428315));
#46063=CARTESIAN_POINT('Ctrl Pts',(81.066940431951,72.3965812326096,50.3083019052256));
#46064=CARTESIAN_POINT('Ctrl Pts',(81.8660873416523,71.9722692135051,54.6404797997228));
#46065=CARTESIAN_POINT('Ctrl Pts',(78.5668446377229,71.4418791896242,59.7019194395446));
#46066=CARTESIAN_POINT('Ctrl Pts',(71.2951468796985,70.8054111609673,59.6389350926965));
#46067=CARTESIAN_POINT('Ctrl Pts',(67.4311912149224,70.1689431323103,53.4949604427505));
#46068=CARTESIAN_POINT('Ctrl Pts',(70.5003251860134,69.5324751036535,46.9178034166469));
#46069=CARTESIAN_POINT('Ctrl Pts',(77.7076291916687,68.8960070749964,45.9501649086956));
#46070=CARTESIAN_POINT('Ctrl Pts',(81.6112351748017,68.3656170511157,50.5615675126155));
#46071=CARTESIAN_POINT('Ctrl Pts',(81.357550929335,67.941305032011,54.9595267434923));
#46072=CARTESIAN_POINT('Ctrl Pts',(79.1201753175234,67.5169930129064,58.75433259683));
#46073=CARTESIAN_POINT('Ctrl Pts',(73.3103290393843,66.9866029890256,60.4123011946575));
#46074=CARTESIAN_POINT('Ctrl Pts',(67.8615167786614,66.3501349603686,55.5964938626097));
#46075=CARTESIAN_POINT('Ctrl Pts',(68.9730152573013,65.7136669317118,48.4241059052754));
#46076=CARTESIAN_POINT('Ctrl Pts',(75.6030280570083,65.0771989030548,45.4708859415329));
#46077=CARTESIAN_POINT('Ctrl Pts',(81.6790312514728,64.4407308743978,49.4663509323529));
#46078=CARTESIAN_POINT('Ctrl Pts',(81.6024187435134,63.9103408505171,55.507650806603));
#46079=CARTESIAN_POINT('Ctrl Pts',(78.5270237042011,63.4860288314123,58.6617507487461));
#46080=CARTESIAN_POINT('Ctrl Pts',(74.3494512879322,63.0617168123079,60.0597099039725));
#46081=CARTESIAN_POINT('Ctrl Pts',(68.8758564085409,62.5313267884269,57.5017942010431));
#46082=CARTESIAN_POINT('Ctrl Pts',(67.9198760668561,61.8948587597702,50.2929345895428));
#46083=CARTESIAN_POINT('Ctrl Pts',(73.4621886382343,61.2583907311131,45.6066408258451));
#46084=CARTESIAN_POINT('Ctrl Pts',(80.4043394211003,60.6219227024562,47.7244511068863));
#46085=CARTESIAN_POINT('Ctrl Pts',(82.3717685544846,59.9854546737992,54.7252209157801));
#46086=CARTESIAN_POINT('Ctrl Pts',(78.3524780838452,59.4550646499186,59.2361496183445));
#46087=CARTESIAN_POINT('Ctrl Pts',(73.9623318572474,59.0307526308137,59.6008648523837));
#46088=CARTESIAN_POINT('Ctrl Pts',(69.8915949053257,58.6064406117094,57.9169700334852));
#46089=CARTESIAN_POINT('Ctrl Pts',(67.4363414588,58.0760505878283,52.3965620630253));
#46090=CARTESIAN_POINT('Ctrl Pts',(71.4416283887399,57.4395825591715,46.3270289738281));
#46091=CARTESIAN_POINT('Ctrl Pts',(78.6989929913225,56.8031145305145,46.4231377856464));
#46092=CARTESIAN_POINT('Ctrl Pts',(82.5515916724324,56.1666465018575,52.5742402299928));
#46093=CARTESIAN_POINT('Ctrl Pts',(79.4463962098037,55.5301784732007,59.1499011436104));
#46094=CARTESIAN_POINT('Ctrl Pts',(73.4539010665363,54.9997884493199,59.9200800870426));
#46095=CARTESIAN_POINT('Ctrl Pts',(69.9001981970296,54.5754764302151,57.3166982464142));
#46096=CARTESIAN_POINT('Ctrl Pts',(67.9309790436144,54.1511644111106,53.3760666956756));
#46097=CARTESIAN_POINT('Ctrl Pts',(69.6971540221891,53.6207743872298,47.5981951505438));
#46098=CARTESIAN_POINT('Ctrl Pts',(76.7010967416689,52.9843063585729,45.6420914482174));
#46099=CARTESIAN_POINT('Ctrl Pts',(82.117366875131,52.3478383299159,50.4735090165814));
#46100=CARTESIAN_POINT('Ctrl Pts',(80.9926200105515,51.7113703012591,57.6438313502813));
#46101=CARTESIAN_POINT('Ctrl Pts',(74.3363619212952,51.0749022726018,60.572275230778));
#46102=CARTESIAN_POINT('Ctrl Pts',(69.3070159747315,50.5445122487213,57.2243127165354));
#46103=CARTESIAN_POINT('Ctrl Pts',(68.3310893999085,50.1202002296165,52.9285044790314));
#46104=CARTESIAN_POINT('Ctrl Pts',(69.4283156990817,49.695888210512,48.6620662055701));
#46105=CARTESIAN_POINT('Ctrl Pts',(74.5504841531635,49.1654981866311,45.4579182728111));
#46106=CARTESIAN_POINT('Ctrl Pts',(81.1211142061001,48.5290301579743,48.5737449720119));
#46107=CARTESIAN_POINT('Ctrl Pts',(82.0422892607611,47.8925621293172,55.7730514939763));
#46108=CARTESIAN_POINT('Ctrl Pts',(76.4913286793663,47.2560941006604,60.4490983823568));
#46109=CARTESIAN_POINT('Ctrl Pts',(69.545609137681,46.6196260720033,58.2953724573005));
#46110=CARTESIAN_POINT('Ctrl Pts',(67.9438181282235,46.0892360481227,52.4697875760198));
#46111=CARTESIAN_POINT('Ctrl Pts',(70.023876958922,45.664924029018,48.5865213794158));
#46112=CARTESIAN_POINT('Ctrl Pts',(73.6499021023712,45.2406120099134,46.0848533854706));
#46113=CARTESIAN_POINT('Ctrl Pts',(79.6181747788305,44.7102219860325,47.0244782608427));
#46114=CARTESIAN_POINT('Ctrl Pts',(82.5358491753481,44.0737539573756,53.6854640308254));
#46115=CARTESIAN_POINT('Ctrl Pts',(78.5105485707623,43.4372859287187,59.7249617683243));
#46116=CARTESIAN_POINT('Ctrl Pts',(71.2533739040916,42.8008179000617,59.6154458518454));
#46117=CARTESIAN_POINT('Ctrl Pts',(67.4216317053234,42.1643498714049,53.4348870555725));
#46118=CARTESIAN_POINT('Ctrl Pts',(70.0322815804837,41.6339598475239,47.9862467778226));
#46119=CARTESIAN_POINT('Ctrl Pts',(74.1490861427561,41.2096478284193,46.4183433085664));
#46120=CARTESIAN_POINT('Ctrl Pts',(78.527138901517,40.7853358093147,46.9072759566463));
#46121=CARTESIAN_POINT('Ctrl Pts',(82.4170310660717,40.254945785434,51.5302525513445));
#46122=CARTESIAN_POINT('Ctrl Pts',(80.2520741370471,39.618477756777,58.4724796297019));
#46123=CARTESIAN_POINT('Ctrl Pts',(73.2527161602415,38.9820097281201,60.3927831971243));
#46124=CARTESIAN_POINT('Ctrl Pts',(67.8453808390323,38.3455416994631,55.5513678459556));
#46125=CARTESIAN_POINT('Ctrl Pts',(69.0051896420068,37.7090736708062,48.372482218467));
#46126=CARTESIAN_POINT('Ctrl Pts',(74.5490483491708,37.1786836469254,45.970648693432));
#46127=CARTESIAN_POINT('Ctrl Pts',(78.6853429395574,36.7543716278208,47.4863888276205));
#46128=CARTESIAN_POINT('Ctrl Pts',(81.6701546315565,36.3300596087161,50.7263425705272));
#46129=CARTESIAN_POINT('Ctrl Pts',(81.5755988389129,35.7996695848354,56.7673882456549));
#46130=CARTESIAN_POINT('Ctrl Pts',(75.3888507691892,35.1632015561783,60.5891291622963));
#46131=CARTESIAN_POINT('Ctrl Pts',(68.8451573284352,34.5267335275214,57.4492797977542));
#46132=CARTESIAN_POINT('Ctrl Pts',(67.9372838577583,33.8902654988645,50.2482837805935));
#46133=CARTESIAN_POINT('Ctrl Pts',(73.5203313009761,33.2537974702075,45.5887627150886));
#46134=CARTESIAN_POINT('Ctrl Pts',(79.2808791639645,32.7234074463268,47.4106468950583));
#46135=CARTESIAN_POINT('Ctrl Pts',(81.4098578636657,32.2990954272222,51.2673100625624));
#46136=CARTESIAN_POINT('Ctrl Pts',(81.5388551947532,31.8747834081175,55.6706906713012));
#46137=CARTESIAN_POINT('Ctrl Pts',(77.506184276696,31.3443933842367,60.1696615427363));
#46138=CARTESIAN_POINT('Ctrl Pts',(70.3291838819809,30.7079253555798,58.9982433210564));
#46139=CARTESIAN_POINT('Ctrl Pts',(67.4475988877123,30.0714573269228,52.3367835833502));
#46140=CARTESIAN_POINT('Ctrl Pts',(71.484050000639,29.4349892982659,46.3047325057651));
#46141=CARTESIAN_POINT('Ctrl Pts',(78.7546137265724,28.798521269609,46.4477656105936));
#46142=CARTESIAN_POINT('Ctrl Pts',(81.9091522462999,28.2681312457281,51.6006347683443));
#46143=CARTESIAN_POINT('Ctrl Pts',(80.9876044002968,27.8438192266235,55.9084358736837));
#46144=CARTESIAN_POINT('Ctrl Pts',(78.1975779862256,27.4195072075189,59.3175639504902));
#46145=CARTESIAN_POINT('Ctrl Pts',(72.2028217646185,26.8891171836381,60.0699406911801));
#46146=CARTESIAN_POINT('Ctrl Pts',(67.5523365863765,26.2526491549812,54.4793646218784));
#46147=CARTESIAN_POINT('Ctrl Pts',(69.7448518505325,25.6161811263242,47.5604440708494));
#46148=CARTESIAN_POINT('Ctrl Pts',(76.7477451945052,24.9797130976673,45.6530752563823));
#46149=CARTESIAN_POINT('Ctrl Pts',(82.1432115679278,24.3432450690103,50.5285739238167));
#46150=CARTESIAN_POINT('Ctrl Pts',(81.1459994984225,23.8128550451296,56.4874982978904));
#46151=CARTESIAN_POINT('Ctrl Pts',(77.6254897250416,23.3885430260249,59.1355878854457));
#46152=CARTESIAN_POINT('Ctrl Pts',(73.2835643711842,22.9642310069203,59.8799816336974));
#46153=CARTESIAN_POINT('Ctrl Pts',(68.2641906043349,22.4338409830396,56.5170763685288));
#46154=CARTESIAN_POINT('Ctrl Pts',(68.4189717999724,21.7973729543825,49.2467891067138));
#46155=CARTESIAN_POINT('Ctrl Pts',(74.6112626053506,21.1609049257256,45.4606524580492));
#46156=CARTESIAN_POINT('Ctrl Pts',(81.1491080247995,20.5244368970687,48.6127033352101));
#46157=CARTESIAN_POINT('Ctrl Pts',(82.0257404859492,19.8879688684117,55.8314197936231));
#46158=CARTESIAN_POINT('Ctrl Pts',(77.3652888960716,19.357578844531,59.67691183969));
#46159=CARTESIAN_POINT('Ctrl Pts',(72.9710754988905,18.9332668254264,59.3670937145644));
#46160=CARTESIAN_POINT('Ctrl Pts',(69.2044438305179,18.5089548063216,57.0832108846456));
#46161=CARTESIAN_POINT('Ctrl Pts',(67.6207990335978,17.9785647824409,51.2501750211296));
#46162=CARTESIAN_POINT('Ctrl Pts',(72.5034949652097,17.3420967537839,45.867555022826));
#46163=CARTESIAN_POINT('Ctrl Pts',(79.6639947113501,16.705628725127,47.0607241995588));
#46164=CARTESIAN_POINT('Ctrl Pts',(82.5280615917182,16.0691606964701,53.7441206728326));
#46165=CARTESIAN_POINT('Ctrl Pts',(79.1441898800705,15.5387706725893,58.7368424313125));
#46166=CARTESIAN_POINT('Ctrl Pts',(74.8250353359302,15.1144586534846,59.6854325760972));
#46167=CARTESIAN_POINT('Ctrl Pts',(72.7133095752997,14.9023026439323,59.1035909146895));
#46168=CARTESIAN_POINT('Ctrl Pts',(71.7889077421008,14.7962246391561,58.5705443090233));
#46169=CARTESIAN_POINT('Ctrl Pts',(81.4785525543966,416.203775360844,49.9893084691035));
#46170=CARTESIAN_POINT('Ctrl Pts',(81.9840157928199,416.097697356068,51.0708177306788));
#46171=CARTESIAN_POINT('Ctrl Pts',(82.4299547886268,415.885541346517,53.4804382935736));
#46172=CARTESIAN_POINT('Ctrl Pts',(80.9582422516561,415.461229327411,58.2036999304802));
#46173=CARTESIAN_POINT('Ctrl Pts',(75.0685408665669,414.930839303531,61.496467711432));
#46174=CARTESIAN_POINT('Ctrl Pts',(67.8937906392098,414.294371274873,57.6628752630338));
#46175=CARTESIAN_POINT('Ctrl Pts',(67.2508294905527,413.657903246217,49.5670757676227));
#46176=CARTESIAN_POINT('Ctrl Pts',(73.718922518142,413.021435217559,44.6410769108337));
#46177=CARTESIAN_POINT('Ctrl Pts',(80.0686778630768,412.49104519368,46.965884990772));
#46178=CARTESIAN_POINT('Ctrl Pts',(82.25299431647,412.066733174574,51.3834126799471));
#46179=CARTESIAN_POINT('Ctrl Pts',(82.1767433586505,411.642421155469,56.3110700424759));
#46180=CARTESIAN_POINT('Ctrl Pts',(77.4433054371268,411.11203113159,61.1368214020091));
#46181=CARTESIAN_POINT('Ctrl Pts',(69.4811941105652,410.475563102931,59.4671289711532));
#46182=CARTESIAN_POINT('Ctrl Pts',(66.5950617600235,409.839095074275,51.877423575915));
#46183=CARTESIAN_POINT('Ctrl Pts',(71.4093060937056,409.202627045618,45.3385398027193));
#46184=CARTESIAN_POINT('Ctrl Pts',(79.5278545587503,408.566159016961,45.8635327706843));
#46185=CARTESIAN_POINT('Ctrl Pts',(82.7946954417536,408.035768993081,51.780929813614));
#46186=CARTESIAN_POINT('Ctrl Pts',(81.5484021999293,407.611456973975,56.5491632997459));
#46187=CARTESIAN_POINT('Ctrl Pts',(78.2589949233612,407.187144954872,60.2191781771201));
#46188=CARTESIAN_POINT('Ctrl Pts',(71.5213106968269,406.656754930989,60.7589992545326));
#46189=CARTESIAN_POINT('Ctrl Pts',(66.6045666361791,406.020286902334,54.2772777506614));
#46190=CARTESIAN_POINT('Ctrl Pts',(69.4024450885366,405.383818873676,46.6546195494321));
#46191=CARTESIAN_POINT('Ctrl Pts',(77.3248506119125,404.74735084502,44.8745774504162));
#46192=CARTESIAN_POINT('Ctrl Pts',(83.1101172875948,404.110882816362,50.594523777757));
#46193=CARTESIAN_POINT('Ctrl Pts',(81.6963520392216,403.580492792482,57.2042904096785));
#46194=CARTESIAN_POINT('Ctrl Pts',(77.628749663687,403.156180773377,59.9870701412823));
#46195=CARTESIAN_POINT('Ctrl Pts',(72.7387204177423,402.731868754272,60.6009634894842));
#46196=CARTESIAN_POINT('Ctrl Pts',(67.2978137931106,402.201478730392,56.5904419086148));
#46197=CARTESIAN_POINT('Ctrl Pts',(67.8359280893625,401.565010701735,48.4727124088158));
#46198=CARTESIAN_POINT('Ctrl Pts',(74.9467087207757,400.928542673078,44.5522724819652));
#46199=CARTESIAN_POINT('Ctrl Pts',(82.0953268474851,400.292074644421,48.4032865620621));
#46200=CARTESIAN_POINT('Ctrl Pts',(82.7124605889277,399.655606615763,56.5153914131592));
#46201=CARTESIAN_POINT('Ctrl Pts',(77.3108636907342,399.125216591883,60.5787027420174));
#46202=CARTESIAN_POINT('Ctrl Pts',(72.4150885587465,398.700904572778,60.012454295511));
#46203=CARTESIAN_POINT('Ctrl Pts',(68.3205822654791,398.276592553674,57.269414074572));
#46204=CARTESIAN_POINT('Ctrl Pts',(66.842522433118,397.746202529794,50.6737270631735));
#46205=CARTESIAN_POINT('Ctrl Pts',(72.5718181519236,397.109734501135,44.8977189491651));
#46206=CARTESIAN_POINT('Ctrl Pts',(80.5111804111243,396.47326647248,46.6005335121155));
#46207=CARTESIAN_POINT('Ctrl Pts',(83.3831514950707,395.836798443821,54.1955866793042));
#46208=CARTESIAN_POINT('Ctrl Pts',(78.5297532607916,395.200330415166,60.7248764373814));
#46209=CARTESIAN_POINT('Ctrl Pts',(71.7871355199413,394.669940391284,60.250688688689));
#46210=CARTESIAN_POINT('Ctrl Pts',(68.4621429042898,394.24562837218,56.6128767711974));
#46211=CARTESIAN_POINT('Ctrl Pts',(67.1694890357017,393.821316353075,51.857006985639));
#46212=CARTESIAN_POINT('Ctrl Pts',(70.378532996455,393.290926329195,45.908075579219));
#46213=CARTESIAN_POINT('Ctrl Pts',(78.4916253724822,392.654458300537,45.3040629441663));
#46214=CARTESIAN_POINT('Ctrl Pts',(83.369240344066,392.017990271881,51.7957439828776));
#46215=CARTESIAN_POINT('Ctrl Pts',(80.5572835813138,391.381522243223,59.4132205784301));
#46216=CARTESIAN_POINT('Ctrl Pts',(72.611543813093,390.745054214568,61.16030921412));
#46217=CARTESIAN_POINT('Ctrl Pts',(67.831823084552,390.214664190685,56.3809768572411));
#46218=CARTESIAN_POINT('Ctrl Pts',(67.7068767052643,389.790352171582,51.4541482785849));
#46219=CARTESIAN_POINT('Ctrl Pts',(69.8494823980434,389.366040152476,47.0158499237608));
#46220=CARTESIAN_POINT('Ctrl Pts',(76.1731818767277,388.835650128596,44.628681533462));
#46221=CARTESIAN_POINT('Ctrl Pts',(82.6946133383874,388.199182099939,49.4926337182714));
#46222=CARTESIAN_POINT('Ctrl Pts',(82.1204242508757,387.562714071282,57.5922236715447));
#46223=CARTESIAN_POINT('Ctrl Pts',(75.0024131187421,386.926246042624,61.4995204406948));
#46224=CARTESIAN_POINT('Ctrl Pts',(67.8577857377302,386.289778013968,57.6083254119501));
#46225=CARTESIAN_POINT('Ctrl Pts',(67.3830501033545,385.759387990087,50.8657462245909));
#46226=CARTESIAN_POINT('Ctrl Pts',(70.5193743378369,385.335075970983,47.0640726803003));
#46227=CARTESIAN_POINT('Ctrl Pts',(75.0473516294541,384.910763951878,45.1181350945174));
#46228=CARTESIAN_POINT('Ctrl Pts',(81.3870609052464,384.380373927997,47.4624546799801));
#46229=CARTESIAN_POINT('Ctrl Pts',(83.1212960289457,383.74390589934,55.4110097499891));
#46230=CARTESIAN_POINT('Ctrl Pts',(77.3766585294485,383.107437870683,61.1496673036992));
#46231=CARTESIAN_POINT('Ctrl Pts',(69.4404556010515,382.470969842026,59.4321884541394));
#46232=CARTESIAN_POINT('Ctrl Pts',(66.5978452811112,381.834501813369,51.8094156165031));
#46233=CARTESIAN_POINT('Ctrl Pts',(70.6607176773544,381.304111789489,46.407488561072));
#46234=CARTESIAN_POINT('Ctrl Pts',(75.5214972956857,380.879799770384,45.5938099124785));
#46235=CARTESIAN_POINT('Ctrl Pts',(80.2161137011552,380.455487751279,47.0937526602727));
#46236=CARTESIAN_POINT('Ctrl Pts',(83.4653421691651,379.925097727398,53.0208313996709));
#46237=CARTESIAN_POINT('Ctrl Pts',(79.562596700756,379.288629698742,60.1591559211569));
#46238=CARTESIAN_POINT('Ctrl Pts',(71.4624131206521,378.652161670085,60.7249089485447));
#46239=CARTESIAN_POINT('Ctrl Pts',(66.5967992159111,378.015693641428,54.2242280727153));
#46240=CARTESIAN_POINT('Ctrl Pts',(69.4490998372052,377.37922561277,46.6050758671872));
#46241=CARTESIAN_POINT('Ctrl Pts',(76.0587516032023,376.84883558889,45.1907733703342));
#46242=CARTESIAN_POINT('Ctrl Pts',(80.2621792448387,376.424523569785,47.7637963983479));
#46243=CARTESIAN_POINT('Ctrl Pts',(82.8230482444123,376.000211550681,51.9746397115319));
#46244=CARTESIAN_POINT('Ctrl Pts',(81.3896570115272,375.4698215268,58.5801781145572));
#46245=CARTESIAN_POINT('Ctrl Pts',(73.7622965822203,374.833353498143,61.4104558476921));
#46246=CARTESIAN_POINT('Ctrl Pts',(67.2756991158776,374.196885469486,56.526082415099));
#46247=CARTESIAN_POINT('Ctrl Pts',(67.8648504208867,373.560417440829,48.4275670413289));
#46248=CARTESIAN_POINT('Ctrl Pts',(75.0144198050572,372.923949412172,44.5454597802954));
#46249=CARTESIAN_POINT('Ctrl Pts',(80.9320871080452,372.393559388292,47.8117974406574));
#46250=CARTESIAN_POINT('Ctrl Pts',(82.4184613089243,371.969247369187,52.5107274439798));
#46251=CARTESIAN_POINT('Ctrl Pts',(81.5907437386188,371.544935350082,57.3691361407621));
#46252=CARTESIAN_POINT('Ctrl Pts',(76.1771019836737,371.014545326201,61.4163859439578));
#46253=CARTESIAN_POINT('Ctrl Pts',(68.56257297831,370.378077297545,58.5517660404247));
#46254=CARTESIAN_POINT('Ctrl Pts',(66.8680282099687,369.741609268887,50.6106346004175));
#46255=CARTESIAN_POINT('Ctrl Pts',(72.6232575130191,369.105141240231,44.8825994932723));
#46256=CARTESIAN_POINT('Ctrl Pts',(80.5667693788841,368.468673211573,46.6397899787074));
#46257=CARTESIAN_POINT('Ctrl Pts',(82.8927643814735,367.938283187694,52.9862453096999));
#46258=CARTESIAN_POINT('Ctrl Pts',(80.9337540321524,367.513971168588,57.5085820831407));
#46259=CARTESIAN_POINT('Ctrl Pts',(77.1230358177255,367.089659149484,60.6339105669001));
#46260=CARTESIAN_POINT('Ctrl Pts',(70.3818562312212,366.559269125603,60.139698261462));
#46261=CARTESIAN_POINT('Ctrl Pts',(66.5113175699981,365.922801096946,52.9838594121572));
#46262=CARTESIAN_POINT('Ctrl Pts',(70.4391612727063,365.286333068289,45.8771657810459));
#46263=CARTESIAN_POINT('Ctrl Pts',(78.5403762034458,364.649865039632,45.3263780130745));
#46264=CARTESIAN_POINT('Ctrl Pts',(83.3854683136115,364.013397010975,51.8618337438747));
#46265=CARTESIAN_POINT('Ctrl Pts',(80.9800413351421,363.483006987094,58.17861053838));
#46266=CARTESIAN_POINT('Ctrl Pts',(76.5355717224607,363.058694967989,60.3083854802736));
#46267=CARTESIAN_POINT('Ctrl Pts',(71.6091246607767,362.634382948885,60.169206496283));
#46268=CARTESIAN_POINT('Ctrl Pts',(66.8436203934035,362.103992925004,55.3756986890502));
#46269=CARTESIAN_POINT('Ctrl Pts',(68.6136562040615,361.467524896347,47.4350392457652));
#46270=CARTESIAN_POINT('Ctrl Pts',(76.2392244809221,360.83105686769,44.6451003621484));
#46271=CARTESIAN_POINT('Ctrl Pts',(82.7167874777929,360.194588839034,49.5414488118559));
#46272=CARTESIAN_POINT('Ctrl Pts',(82.0893394325227,359.558120810376,57.6527623994156));
#46273=CARTESIAN_POINT('Ctrl Pts',(76.1311622360508,359.027730786496,60.8446070879602));
#46274=CARTESIAN_POINT('Ctrl Pts',(71.3790466468484,358.603418767391,59.5382193706177));
#46275=CARTESIAN_POINT('Ctrl Pts',(67.7508554881302,358.179106748286,56.2027313468106));
#46276=CARTESIAN_POINT('Ctrl Pts',(67.2961484816295,357.648716724406,49.4587718600854));
#46277=CARTESIAN_POINT('Ctrl Pts',(73.8394319867204,357.012248695747,44.6242563582749));
#46278=CARTESIAN_POINT('Ctrl Pts',(81.4261566169365,356.375780667092,47.5181568238498));
#46279=CARTESIAN_POINT('Ctrl Pts',(83.1060280328521,355.739312638434,55.4624052178373));
#46280=CARTESIAN_POINT('Ctrl Pts',(77.3134926462889,355.102844609778,61.174990706095));
#46281=CARTESIAN_POINT('Ctrl Pts',(70.7221031282585,354.572454585897,59.6778827467444));
#46282=CARTESIAN_POINT('Ctrl Pts',(67.990902982154,354.148142566792,55.575469164098));
#46283=CARTESIAN_POINT('Ctrl Pts',(67.4388003141422,353.723830547688,50.6780786257463));
#46284=CARTESIAN_POINT('Ctrl Pts',(71.5176993728649,353.193440523807,45.2882427758245));
#46285=CARTESIAN_POINT('Ctrl Pts',(79.6279875335611,352.556972495149,45.928809021977));
#46286=CARTESIAN_POINT('Ctrl Pts',(83.4583338857497,351.920504466493,53.0885225177573));
#46287=CARTESIAN_POINT('Ctrl Pts',(79.5173679668675,351.284036437836,60.1879477160104));
#46288=CARTESIAN_POINT('Ctrl Pts',(71.3981177848255,350.647568409179,60.7026084262373));
#46289=CARTESIAN_POINT('Ctrl Pts',(67.4033311812638,350.117178385299,55.2501385260585));
#46290=CARTESIAN_POINT('Ctrl Pts',(68.0313487922679,349.692866366194,50.3619031265067));
#46291=CARTESIAN_POINT('Ctrl Pts',(70.8258678013444,349.268554347089,46.3023569758795));
#46292=CARTESIAN_POINT('Ctrl Pts',(77.439691116236,348.738164323209,44.9076924356594));
#46293=CARTESIAN_POINT('Ctrl Pts',(83.142900440987,348.101696294551,50.7094596287924));
#46294=CARTESIAN_POINT('Ctrl Pts',(81.339978828426,347.465228265895,58.6266892060083));
#46295=CARTESIAN_POINT('Ctrl Pts',(73.7092694259971,346.828760237237,61.4025358399319));
#46296=CARTESIAN_POINT('Ctrl Pts',(67.2417793772208,346.192292208581,56.4670853403098));
#46297=CARTESIAN_POINT('Ctrl Pts',(67.8010619555309,345.6619021847,49.7309921834458));
#46298=CARTESIAN_POINT('Ctrl Pts',(71.4805654193212,345.237590165595,46.4521958035041));
#46299=CARTESIAN_POINT('Ctrl Pts',(76.2523772184292,344.81327814649,45.2196928237691));
#46300=CARTESIAN_POINT('Ctrl Pts',(82.1603168760152,344.28288812261,48.5035924907313));
#46301=CARTESIAN_POINT('Ctrl Pts',(82.6618450551038,343.646420093953,56.6236644516698));
#46302=CARTESIAN_POINT('Ctrl Pts',(76.1090964696637,343.009952065296,61.4189263314207));
#46303=CARTESIAN_POINT('Ctrl Pts',(68.527730982823,342.373484036639,58.5110150751538));
#46304=CARTESIAN_POINT('Ctrl Pts',(66.8811049173047,341.737016007982,50.5438498474461));
#46305=CARTESIAN_POINT('Ctrl Pts',(71.720405297618,341.206625984101,45.8248542075397));
#46306=CARTESIAN_POINT('Ctrl Pts',(76.6484187293896,340.782313964996,45.7621241713557));
#46307=CARTESIAN_POINT('Ctrl Pts',(81.0593106533463,340.358001945892,47.9605972497298));
#46308=CARTESIAN_POINT('Ctrl Pts',(83.3664454132111,339.827611922011,54.3139331624748));
#46309=CARTESIAN_POINT('Ctrl Pts',(78.4205410235596,339.191143893355,60.7734322865299));
#46310=CARTESIAN_POINT('Ctrl Pts',(70.3288464427964,338.554675864696,60.0970231418323));
#46311=CARTESIAN_POINT('Ctrl Pts',(66.5117334947267,337.918207836041,52.9302456748633));
#46312=CARTESIAN_POINT('Ctrl Pts',(70.4928267712495,337.281739807383,45.8353182271111));
#46313=CARTESIAN_POINT('Ctrl Pts',(77.2408625316589,336.751349783503,45.4457525759158));
#46314=CARTESIAN_POINT('Ctrl Pts',(81.0026336516775,336.327037764398,48.6298269283381));
#46315=CARTESIAN_POINT('Ctrl Pts',(82.8912456562173,335.902725745293,53.1820127920165));
#46316=CARTESIAN_POINT('Ctrl Pts',(80.4670674549858,335.372335721413,59.4916172224879));
#46317=CARTESIAN_POINT('Ctrl Pts',(72.4972494389857,334.735867692755,61.1253552544506));
#46318=CARTESIAN_POINT('Ctrl Pts',(66.8315814033232,334.099399664099,55.3087190934851));
#46319=CARTESIAN_POINT('Ctrl Pts',(68.6491262437196,333.462931635441,47.394833747302));
#46320=CARTESIAN_POINT('Ctrl Pts',(76.3071823965364,332.826463606785,44.6486955269013));
#46321=CARTESIAN_POINT('Ctrl Pts',(81.6573808253843,332.296073582904,48.7794490649748));
#46322=CARTESIAN_POINT('Ctrl Pts',(82.4096221682912,331.871761563799,53.650114769289));
#46323=CARTESIAN_POINT('Ctrl Pts',(80.8505245226236,331.447449544695,58.3254186067349));
#46324=CARTESIAN_POINT('Ctrl Pts',(74.882893320288,330.917059520814,61.4995524812376));
#46325=CARTESIAN_POINT('Ctrl Pts',(67.7944140660781,330.280591492156,57.5069892659745));
#46326=CARTESIAN_POINT('Ctrl Pts',(67.3309794578124,329.6441234635,49.4003081396909));
#46327=CARTESIAN_POINT('Ctrl Pts',(73.8925756369099,329.007655434842,44.6171600025495));
#46328=CARTESIAN_POINT('Ctrl Pts',(81.4751072165895,328.371187406186,47.5654330578139));
#46329=CARTESIAN_POINT('Ctrl Pts',(82.8058431840019,327.840797382305,54.1924150108138));
#46330=CARTESIAN_POINT('Ctrl Pts',(80.1799525690512,327.4164853632,58.3630204727915));
#46331=CARTESIAN_POINT('Ctrl Pts',(75.9371112497972,326.992173344096,60.8705190232977));
#46332=CARTESIAN_POINT('Ctrl Pts',(69.3501974549747,326.461783320215,59.3538401911343));
#46333=CARTESIAN_POINT('Ctrl Pts',(66.6164487614888,325.825315291559,51.691352524188));
#46334=CARTESIAN_POINT('Ctrl Pts',(71.5823329553481,325.188847262901,45.2669424584653));
#46335=CARTESIAN_POINT('Ctrl Pts',(79.6727641285602,324.552379234245,45.9582990603005));
#46336=CARTESIAN_POINT('Ctrl Pts',(83.4642911203485,323.915911205587,53.1563142197581));
#46337=CARTESIAN_POINT('Ctrl Pts',(80.1234970628893,323.385521181707,59.0322688729184));
#46338=CARTESIAN_POINT('Ctrl Pts',(75.4061745846681,322.961209162602,60.4591956676878));
#46339=CARTESIAN_POINT('Ctrl Pts',(70.5586039634535,322.536897143498,59.570201565626));
#46340=CARTESIAN_POINT('Ctrl Pts',(66.5800296844598,322.006507119616,54.1058905635982));
#46341=CARTESIAN_POINT('Ctrl Pts',(69.5405626672157,321.37003909096,46.5281373594319));
#46342=CARTESIAN_POINT('Ctrl Pts',(77.5024565125574,320.733571062303,44.9339927879165));
#46343=CARTESIAN_POINT('Ctrl Pts',(83.1573692157493,320.097103033646,50.7610857886042));
#46344=CARTESIAN_POINT('Ctrl Pts',(81.3000236219517,319.460635004989,58.6817780885513));
#46345=CARTESIAN_POINT('Ctrl Pts',(74.9247060490522,318.930244981108,60.9274570204177));
#46346=CARTESIAN_POINT('Ctrl Pts',(70.4274643213623,318.505932962003,58.9115035775307));
#46347=CARTESIAN_POINT('Ctrl Pts',(67.3504992812629,318.081620942899,55.0616285687585));
#46348=CARTESIAN_POINT('Ctrl Pts',(67.9297866619199,317.551230919018,48.3272262826633));
#46349=CARTESIAN_POINT('Ctrl Pts',(75.1339247210432,316.914762890361,44.5473461271119));
#46350=CARTESIAN_POINT('Ctrl Pts',(82.1904587146737,316.278294861704,48.56460620285));
#46351=CARTESIAN_POINT('Ctrl Pts',(82.6389162345453,315.641826833047,56.6721296454466));
#46352=CARTESIAN_POINT('Ctrl Pts',(76.0428070816436,315.00535880439,61.4343185547872));
#46353=CARTESIAN_POINT('Ctrl Pts',(69.7569048494634,314.47496878051,58.9493273781782));
#46354=CARTESIAN_POINT('Ctrl Pts',(67.6834157706895,314.050656761404,54.4783213972643));
#46355=CARTESIAN_POINT('Ctrl Pts',(67.8847852268376,313.6263447423,49.554024312066));
#46356=CARTESIAN_POINT('Ctrl Pts',(72.7380804298073,313.095954718419,44.8494229800522));
#46357=CARTESIAN_POINT('Ctrl Pts',(80.6557583488287,312.459486689763,46.7195768603191));
#46358=CARTESIAN_POINT('Ctrl Pts',(83.3491940360832,311.823018661106,54.3797631973481));
#46359=CARTESIAN_POINT('Ctrl Pts',(78.371449849321,311.186550632448,60.794988316589));
#46360=CARTESIAN_POINT('Ctrl Pts',(70.2687050190405,310.550082603792,60.0651764363069));
#46361=CARTESIAN_POINT('Ctrl Pts',(67.1523430005122,310.01969257991,54.0671737862719));
#46362=CARTESIAN_POINT('Ctrl Pts',(68.5186270318996,309.595380560807,49.3319315129835));
#46363=CARTESIAN_POINT('Ctrl Pts',(71.8996589006993,309.171068541701,45.7461436018928));
#46364=CARTESIAN_POINT('Ctrl Pts',(78.6488219679938,308.640678517821,45.3766224097839));
#46365=CARTESIAN_POINT('Ctrl Pts',(83.4003362781905,308.004210489164,51.980425172226));
#46366=CARTESIAN_POINT('Ctrl Pts',(80.4108761268251,307.367742460507,59.5300065197432));
#46367=CARTESIAN_POINT('Ctrl Pts',(72.4460508424404,306.73127443185,61.1094395536548));
#46368=CARTESIAN_POINT('Ctrl Pts',(66.8070575550918,306.094806403193,55.2452385108463));
#46369=CARTESIAN_POINT('Ctrl Pts',(68.3872693902216,305.564416379312,48.6732769637535));
#46370=CARTESIAN_POINT('Ctrl Pts',(72.5238402316145,305.140104360207,45.9940918049221));
#46371=CARTESIAN_POINT('Ctrl Pts',(77.4278112662491,304.715792341103,45.5038678432214));
#46372=CARTESIAN_POINT('Ctrl Pts',(82.7657170999594,304.185402317222,49.6504941020972));
#46373=CARTESIAN_POINT('Ctrl Pts',(82.0228010115598,303.548934288565,57.7520479561944));
#46374=CARTESIAN_POINT('Ctrl Pts',(74.8152960849149,302.912466259908,61.4916900850307));
#46375=CARTESIAN_POINT('Ctrl Pts',(67.766195626519,302.275998231251,57.4614006107094));
#46376=CARTESIAN_POINT('Ctrl Pts',(67.3540899986238,301.639530202594,49.3362994964648));
#46377=CARTESIAN_POINT('Ctrl Pts',(72.8565636478503,301.109140178714,45.4106744812704));
#46378=CARTESIAN_POINT('Ctrl Pts',(77.7364800159439,300.684828159609,46.1003611359));
#46379=CARTESIAN_POINT('Ctrl Pts',(81.7604188366507,300.260516140504,48.9459134211992));
#46380=CARTESIAN_POINT('Ctrl Pts',(83.0714657426214,299.730126116623,55.5768186407524));
#46381=CARTESIAN_POINT('Ctrl Pts',(77.1981520130348,299.093658087967,61.2063199507342));
#46382=CARTESIAN_POINT('Ctrl Pts',(69.304317310222,298.45719005931,59.3035787166069));
#46383=CARTESIAN_POINT('Ctrl Pts',(66.625037661451,297.820722030652,51.6384295932651));
#46384=CARTESIAN_POINT('Ctrl Pts',(71.6417535996899,297.184254001996,45.2337703236194));
#46385=CARTESIAN_POINT('Ctrl Pts',(78.3702482810813,296.653863978115,45.8780585687687));
#46386=CARTESIAN_POINT('Ctrl Pts',(81.6023257081562,296.22955195901,49.5986669795743));
#46387=CARTESIAN_POINT('Ctrl Pts',(82.7744813091102,295.805239939906,54.3856600533435));
#46388=CARTESIAN_POINT('Ctrl Pts',(79.4162494666852,295.274849916025,60.2516660977382));
#46389=CARTESIAN_POINT('Ctrl Pts',(71.2904924510428,294.638381887368,60.6506298654907));
#46390=CARTESIAN_POINT('Ctrl Pts',(66.5783481405078,294.001913858711,54.0378583953677));
#46391=CARTESIAN_POINT('Ctrl Pts',(69.5817503009291,293.365445830054,46.4938126649812));
#46392=CARTESIAN_POINT('Ctrl Pts',(77.5690708348405,292.728977801397,44.9479116805083));
#46393=CARTESIAN_POINT('Ctrl Pts',(82.2265890673596,292.198587777516,49.8464085861014));
#46394=CARTESIAN_POINT('Ctrl Pts',(82.2270927597987,291.774275758412,54.7748212298901));
#46395=CARTESIAN_POINT('Ctrl Pts',(79.9731027840799,291.349963739307,59.1576035231967));
#46396=CARTESIAN_POINT('Ctrl Pts',(73.5911433082559,290.819573715426,61.3843368411525));
#46397=CARTESIAN_POINT('Ctrl Pts',(67.1946063176981,290.183105686769,56.3572687399966));
#46398=CARTESIAN_POINT('Ctrl Pts',(67.9731276840741,289.546637658112,48.2747595379305));
#46399=CARTESIAN_POINT('Ctrl Pts',(75.1875289332066,288.910169629455,44.548438948408));
#46400=CARTESIAN_POINT('Ctrl Pts',(82.2316253496051,288.273701600798,48.6187957929263));
#46401=CARTESIAN_POINT('Ctrl Pts',(82.5359589117053,287.743311576918,55.3712123309765));
#46402=CARTESIAN_POINT('Ctrl Pts',(79.3046420575872,287.318999557813,59.0924813120438));
#46403=CARTESIAN_POINT('Ctrl Pts',(74.7289733472039,286.894687538709,60.9234666462241));
#46404=CARTESIAN_POINT('Ctrl Pts',(68.4504796612101,286.364297514828,58.4198163001721));
#46405=CARTESIAN_POINT('Ctrl Pts',(66.917499177202,285.72782948617,50.4300059143811));
#46406=CARTESIAN_POINT('Ctrl Pts',(72.8052066912012,285.091361457514,44.8382306373356));
#46407=CARTESIAN_POINT('Ctrl Pts',(80.6955127959515,284.454893428857,46.7555517092276));
#46408=CARTESIAN_POINT('Ctrl Pts',(83.3447411178743,283.8184254002,54.4476703031889));
#46409=CARTESIAN_POINT('Ctrl Pts',(79.1467649771149,283.288035376319,59.7452871581497));
#46410=CARTESIAN_POINT('Ctrl Pts',(74.2669896853412,282.863723357215,60.4359712704303));
#46411=CARTESIAN_POINT('Ctrl Pts',(69.6117437691718,282.43941133811,58.8179672836763));
#46412=CARTESIAN_POINT('Ctrl Pts',(66.5132105196755,281.909021314229,52.810734998995));
#46413=CARTESIAN_POINT('Ctrl Pts',(70.5949549734316,281.272553285572,45.77323108216));
#46414=CARTESIAN_POINT('Ctrl Pts',(78.7068412505005,280.636085256915,45.4121887753791));
#46415=CARTESIAN_POINT('Ctrl Pts',(83.4067610738744,279.999617228258,52.0336541851837));
#46416=CARTESIAN_POINT('Ctrl Pts',(80.362985608619,279.363149199602,59.5783563053703));
#46417=CARTESIAN_POINT('Ctrl Pts',(73.7197299652048,278.83275917572,60.8253135927701));
#46418=CARTESIAN_POINT('Ctrl Pts',(69.5826115753629,278.408447156616,58.146974019528));
#46419=CARTESIAN_POINT('Ctrl Pts',(67.1288832280929,277.984135137511,53.8728111027727));
#46420=CARTESIAN_POINT('Ctrl Pts',(68.7286078653029,277.453745113631,47.3055720249368));
#46421=CARTESIAN_POINT('Ctrl Pts',(76.4250011893648,276.817277084973,44.6687881948561));
#46422=CARTESIAN_POINT('Ctrl Pts',(82.7861996525964,276.180809056317,49.7153914713944));
#46423=CARTESIAN_POINT('Ctrl Pts',(81.9927479724166,275.54434102766,57.7964486392779));
#46424=CARTESIAN_POINT('Ctrl Pts',(74.7474345703678,274.907872999002,61.4967909033568));
#46425=CARTESIAN_POINT('Ctrl Pts',(68.9141293322307,274.377482975122,58.0820730498474));
#46426=CARTESIAN_POINT('Ctrl Pts',(67.5468774292204,273.953170956017,53.3471101487385));
#46427=CARTESIAN_POINT('Ctrl Pts',(68.4970063364964,273.528858936913,48.5111504197167));
#46428=CARTESIAN_POINT('Ctrl Pts',(74.0111154460782,272.998468913031,44.6018859431201));
#46429=CARTESIAN_POINT('Ctrl Pts',(81.5508847771878,272.362000884375,47.6578600265996));
#46430=CARTESIAN_POINT('Ctrl Pts',(83.0443750077863,271.725532855717,55.6392469643748));
#46431=CARTESIAN_POINT('Ctrl Pts',(77.1463472849624,271.089064827061,61.2201357376961));
#46432=CARTESIAN_POINT('Ctrl Pts',(69.24973729534,270.452596798404,59.2629311400528));
#46433=CARTESIAN_POINT('Ctrl Pts',(67.0847324481688,269.922206774523,52.8597677006208));
#46434=CARTESIAN_POINT('Ctrl Pts',(69.1573075942886,269.497894755419,48.3883379846521));
#46435=CARTESIAN_POINT('Ctrl Pts',(73.0457256368976,269.073582736314,45.3602269287172));
#46436=CARTESIAN_POINT('Ctrl Pts',(79.7722770006702,268.543192712434,46.0244970325772));
#46437=CARTESIAN_POINT('Ctrl Pts',(83.4608960488652,267.906724683776,53.2757857926896));
#46438=CARTESIAN_POINT('Ctrl Pts',(79.3548600457172,267.27025665512,60.2810351715653));
#46439=CARTESIAN_POINT('Ctrl Pts',(71.2423206209435,266.633788626462,60.6270909486741));
#46440=CARTESIAN_POINT('Ctrl Pts',(66.5637941172022,265.997320597805,53.9713799484104));
#46441=CARTESIAN_POINT('Ctrl Pts',(69.1279533259856,265.466930573925,47.717354399025));
#46442=CARTESIAN_POINT('Ctrl Pts',(73.6247828917563,265.04261855482,45.7004817462351));
#46443=CARTESIAN_POINT('Ctrl Pts',(78.5461449518434,264.618306535716,45.9640095715196));
#46444=CARTESIAN_POINT('Ctrl Pts',(83.189093324536,264.087916511834,50.876318440968));
#46445=CARTESIAN_POINT('Ctrl Pts',(81.219119521118,263.451448483178,58.7697525718826));
#46446=CARTESIAN_POINT('Ctrl Pts',(73.5255363375579,262.81498045452,61.3662556658578));
#46447=CARTESIAN_POINT('Ctrl Pts',(67.1736718335224,262.178512425864,56.3079093113901));
#46448=CARTESIAN_POINT('Ctrl Pts',(68.0057311996598,261.542044397207,48.2150250062452));
#46449=CARTESIAN_POINT('Ctrl Pts',(74.0426030807442,261.011654373326,45.1746424790414));
#46450=CARTESIAN_POINT('Ctrl Pts',(78.7602171292713,260.587342354221,46.6006050067058));
#46451=CARTESIAN_POINT('Ctrl Pts',(82.3030301339121,260.163030335117,50.0266417045987));
#46452=CARTESIAN_POINT('Ctrl Pts',(82.5873066012716,259.632640311236,56.7799323773343));
#46453=CARTESIAN_POINT('Ctrl Pts',(75.9240373827595,258.996172282579,61.4476879929244));
#46454=CARTESIAN_POINT('Ctrl Pts',(68.4128028985451,258.359704253922,58.3631447459379));
#46455=CARTESIAN_POINT('Ctrl Pts',(66.9340600453635,257.723236225265,50.3790123513977));
#46456=CARTESIAN_POINT('Ctrl Pts',(72.8689918530231,257.086768196608,44.814510252946));
#46457=CARTESIAN_POINT('Ctrl Pts',(79.4204777041344,256.556378172727,46.4775740409702));
#46458=CARTESIAN_POINT('Ctrl Pts',(82.0472207506454,256.132066153623,50.6476426745507));
#46459=CARTESIAN_POINT('Ctrl Pts',(82.4754878528197,255.707754134518,55.5574123972929));
#46460=CARTESIAN_POINT('Ctrl Pts',(78.26179546342,255.177364110638,60.8425372272155));
#46461=CARTESIAN_POINT('Ctrl Pts',(70.1702674939088,254.540896081981,59.997389734845));
#46462=CARTESIAN_POINT('Ctrl Pts',(66.5219257752229,253.904428053323,52.7432424229221));
#46463=CARTESIAN_POINT('Ctrl Pts',(70.6408962821711,253.267960024667,45.7455904965778));
#46464=CARTESIAN_POINT('Ctrl Pts',(78.7705529966446,252.631491996009,45.4361056503313));
#46465=CARTESIAN_POINT('Ctrl Pts',(82.6263905866329,252.101101972129,50.9877058250546));
#46466=CARTESIAN_POINT('Ctrl Pts',(81.8751448406308,251.676789953024,55.8585251883935));
#46467=CARTESIAN_POINT('Ctrl Pts',(78.9790129269844,251.252477933919,59.8462151688108));
#46468=CARTESIAN_POINT('Ctrl Pts',(72.3320829248196,250.722087910039,61.0734354288592));
#46469=CARTESIAN_POINT('Ctrl Pts',(66.7771871043503,250.085619881382,55.1295115069896));
#46470=CARTESIAN_POINT('Ctrl Pts',(68.7794446183971,249.449151852725,47.2603301412549));
#46471=CARTESIAN_POINT('Ctrl Pts',(76.4778114578293,248.812683824068,44.6780446177483));
#46472=CARTESIAN_POINT('Ctrl Pts',(82.818618895214,248.176215795411,49.7752262122422));
#46473=CARTESIAN_POINT('Ctrl Pts',(82.0894276979053,247.64582577153,56.495049738059));
#46474=CARTESIAN_POINT('Ctrl Pts',(78.3283074924612,247.221513752426,59.6798929432045));
#46475=CARTESIAN_POINT('Ctrl Pts',(73.5268963031717,246.797201733321,60.7915142962413));
#46476=CARTESIAN_POINT('Ctrl Pts',(67.7037590511224,246.26681170944,57.3594856593927));
#46477=CARTESIAN_POINT('Ctrl Pts',(67.4074232989018,245.630343680783,49.2293390255862));
#46478=CARTESIAN_POINT('Ctrl Pts',(74.0791634226038,244.993875652126,44.601063510757));
#46479=CARTESIAN_POINT('Ctrl Pts',(81.5846866984392,244.357407623469,47.6994777624791));
#46480=CARTESIAN_POINT('Ctrl Pts',(83.0296161489375,243.720939594812,55.705680236082));
#46481=CARTESIAN_POINT('Ctrl Pts',(78.0727036535351,243.190549570932,60.3009785434037));
#46482=CARTESIAN_POINT('Ctrl Pts',(73.1446775024716,242.766237551827,60.2392558117977));
#46483=CARTESIAN_POINT('Ctrl Pts',(68.7907035582628,242.341925532722,57.9301082776814));
#46484=CARTESIAN_POINT('Ctrl Pts',(66.6447266758118,241.811535508841,51.5205426730296));
#46485=CARTESIAN_POINT('Ctrl Pts',(71.7521570557332,241.175067480185,45.1879875742171));
#46486=CARTESIAN_POINT('Ctrl Pts',(79.8241923372792,240.538599451528,46.0684970476793));
#46487=CARTESIAN_POINT('Ctrl Pts',(83.4591265052232,239.902131422871,53.3293719339515));
#46488=CARTESIAN_POINT('Ctrl Pts',(79.3001550032014,239.265663394214,60.3215143245647));
#46489=CARTESIAN_POINT('Ctrl Pts',(72.544434181319,238.735273370333,60.540567279651));
#46490=CARTESIAN_POINT('Ctrl Pts',(68.8642605968896,238.310961351228,57.2625230716464));
#46491=CARTESIAN_POINT('Ctrl Pts',(67.0911938351403,237.886649332124,52.6641009836316));
#46492=CARTESIAN_POINT('Ctrl Pts',(69.6739171853377,237.356259308243,46.4177189814885));
#46493=CARTESIAN_POINT('Ctrl Pts',(77.6824461774659,236.719791279586,44.9857404385333));
#46494=CARTESIAN_POINT('Ctrl Pts',(83.1994372355666,236.083323250929,50.943580666688));
#46495=CARTESIAN_POINT('Ctrl Pts',(81.1826455981949,235.446855222272,58.8090496298719));
#46496=CARTESIAN_POINT('Ctrl Pts',(73.4576908674786,234.810387193615,61.360945704093));
#46497=CARTESIAN_POINT('Ctrl Pts',(68.2135001509705,234.279997169734,57.0964162166533));
#46498=CARTESIAN_POINT('Ctrl Pts',(67.5844833805876,233.85568515063,52.2083092882258));
#46499=CARTESIAN_POINT('Ctrl Pts',(69.2611357605872,233.431373131525,47.5738634488822));
#46500=CARTESIAN_POINT('Ctrl Pts',(75.3070114336774,232.900983107644,44.5514248033759));
#46501=CARTESIAN_POINT('Ctrl Pts',(82.2924180697097,232.264515078987,48.7216997696805));
#46502=CARTESIAN_POINT('Ctrl Pts',(82.5510105163721,231.628047050331,56.8374979723166));
#46503=CARTESIAN_POINT('Ctrl Pts',(75.8707314929994,230.991579021673,61.4534402043034));
#46504=CARTESIAN_POINT('Ctrl Pts',(68.3650616350141,230.355110993017,58.3146475783642));
#46505=CARTESIAN_POINT('Ctrl Pts',(67.2020818219682,229.824720969136,51.6561773355309));
#46506=CARTESIAN_POINT('Ctrl Pts',(69.9324433631728,229.400408950031,47.5532055716795));
#46507=CARTESIAN_POINT('Ctrl Pts',(74.2372464756337,228.976096930926,45.153638609574));
#46508=CARTESIAN_POINT('Ctrl Pts',(80.7837638639308,228.445706907046,46.8361540181632));
#46509=CARTESIAN_POINT('Ctrl Pts',(83.3231624660204,227.809238878389,54.5652260134286));
#46510=CARTESIAN_POINT('Ctrl Pts',(78.1966446526784,227.172770849732,60.8621987497656));
#46511=CARTESIAN_POINT('Ctrl Pts',(70.1262498027585,226.536302821075,59.9667784859756));
#46512=CARTESIAN_POINT('Ctrl Pts',(66.5176821833719,225.899834792418,52.6753219146804));
#46513=CARTESIAN_POINT('Ctrl Pts',(70.0057794549039,225.369444768537,46.8855960570804));
#46514=CARTESIAN_POINT('Ctrl Pts',(74.7576279024003,224.945132749433,45.5782370184392));
#46515=CARTESIAN_POINT('Ctrl Pts',(79.5812057975926,224.520820730328,46.5893492570011));
#46516=CARTESIAN_POINT('Ctrl Pts',(83.4205371902028,223.990430706447,52.1523773979725));
#46517=CARTESIAN_POINT('Ctrl Pts',(80.2696092965562,223.35396267779,59.6529608354047));
#46518=CARTESIAN_POINT('Ctrl Pts',(72.2700015158721,222.717494649133,61.0455586352526));
#46519=CARTESIAN_POINT('Ctrl Pts',(66.7640267170464,222.081026620477,55.0775364602583));
#46520=CARTESIAN_POINT('Ctrl Pts',(68.8207776695637,221.444558591819,47.2062677138015));
#46521=CARTESIAN_POINT('Ctrl Pts',(75.2507673017546,220.914168567939,45.1222820533196));
#46522=CARTESIAN_POINT('Ctrl Pts',(79.6956704607921,220.489856548834,47.2511485607036));
#46523=CARTESIAN_POINT('Ctrl Pts',(82.6744481076051,220.065544529729,51.177489584318));
#46524=CARTESIAN_POINT('Ctrl Pts',(81.9252938141166,219.535154505848,57.8951179824144));
#46525=CARTESIAN_POINT('Ctrl Pts',(74.6280237911603,218.898686477192,61.4918872754814));
#46526=CARTESIAN_POINT('Ctrl Pts',(67.6751520575461,218.262218448535,57.2977309984761));
#46527=CARTESIAN_POINT('Ctrl Pts',(67.4315976480203,217.625750419878,49.1814669479095));
#46528=CARTESIAN_POINT('Ctrl Pts',(74.1457626120518,216.989282391221,44.5873525693379));
#46529=CARTESIAN_POINT('Ctrl Pts',(80.3670730043547,216.45889236734,47.2302639859052));
#46530=CARTESIAN_POINT('Ctrl Pts',(82.326772217929,216.034580348235,51.7522106868073));
#46531=CARTESIAN_POINT('Ctrl Pts',(82.0015904344453,215.61026832913,56.6698326205076));
#46532=CARTESIAN_POINT('Ctrl Pts',(77.0300273108705,215.07987830525,61.2504332600464));
#46533=CARTESIAN_POINT('Ctrl Pts',(69.1639586556176,214.443410276593,59.1808709821966));
#46534=CARTESIAN_POINT('Ctrl Pts',(66.6615043746255,213.806942247936,51.4552632310895));
#46535=CARTESIAN_POINT('Ctrl Pts',(71.8057768890687,213.170474219279,45.1675048243668));
#46536=CARTESIAN_POINT('Ctrl Pts',(79.875837106265,212.534006190622,46.1021564038283));
#46537=CARTESIAN_POINT('Ctrl Pts',(83.4558199511915,211.897538161965,53.3912589125365));
#46538=CARTESIAN_POINT('Ctrl Pts',(79.2479037367829,211.261070133308,60.3519747696568));
#46539=CARTESIAN_POINT('Ctrl Pts',(72.4900115795629,210.730680109427,60.5229592777618));
#46540=CARTESIAN_POINT('Ctrl Pts',(68.8339312330819,210.306368090323,57.2181407993583));
#46541=CARTESIAN_POINT('Ctrl Pts',(67.0939119457814,209.882056071218,52.6072020822089));
#46542=CARTESIAN_POINT('Ctrl Pts',(69.7217545659192,209.351666047338,46.3795117465403));
#46543=CARTESIAN_POINT('Ctrl Pts',(77.7403418401691,208.71519801868,45.0054097805767));
#46544=CARTESIAN_POINT('Ctrl Pts',(83.2142366884898,208.078729990024,51.0028705831539));
#46545=CARTESIAN_POINT('Ctrl Pts',(81.1407302675849,207.442261961366,58.8535994246372));
#46546=CARTESIAN_POINT('Ctrl Pts',(73.3975746836202,206.80579393271,61.3496845069219));
#46547=CARTESIAN_POINT('Ctrl Pts',(68.1842835917728,206.275403908829,57.0474339979407));
#46548=CARTESIAN_POINT('Ctrl Pts',(67.5905534492229,205.851091889724,52.1549137250446));
#46549=CARTESIAN_POINT('Ctrl Pts',(69.3005985145823,205.42677987062,47.5326867105072));
#46550=CARTESIAN_POINT('Ctrl Pts',(75.3681246161506,204.896389846739,44.5539470592515));
#46551=CARTESIAN_POINT('Ctrl Pts',(82.323260368906,204.259921818082,48.7745137060865));
#46552=CARTESIAN_POINT('Ctrl Pts',(82.523290720535,203.623453789425,56.8919662020949));
#46553=CARTESIAN_POINT('Ctrl Pts',(75.8098813557484,202.986985760768,61.4595900896012));
#46554=CARTESIAN_POINT('Ctrl Pts',(68.3270533669542,202.350517732111,58.2667255790149));
#46555=CARTESIAN_POINT('Ctrl Pts',(67.2121447459138,201.82012770823,51.6000377652461));
#46556=CARTESIAN_POINT('Ctrl Pts',(69.9720382395937,201.395815689125,47.516872378748));
#46557=CARTESIAN_POINT('Ctrl Pts',(74.294042205983,200.971503670021,45.1484271000031));
#46558=CARTESIAN_POINT('Ctrl Pts',(80.8282498308984,200.44111364614,46.8781319292539));
#46559=CARTESIAN_POINT('Ctrl Pts',(83.3118169635253,199.804645617483,54.6253245493258));
#46560=CARTESIAN_POINT('Ctrl Pts',(78.1399998377731,199.168177588826,60.8851454812851));
#46561=CARTESIAN_POINT('Ctrl Pts',(70.0762755157864,198.531709560169,59.9315205069422));
#46562=CARTESIAN_POINT('Ctrl Pts',(66.5204097940023,197.895241531512,52.614217852485));
#46563=CARTESIAN_POINT('Ctrl Pts',(70.0501892244093,197.364851507632,46.8498093669514));
#46564=CARTESIAN_POINT('Ctrl Pts',(74.8113466152267,196.940539488527,45.5767690130946));
#46565=CARTESIAN_POINT('Ctrl Pts',(79.6275037459071,196.516227469422,46.622657120516));
#46566=CARTESIAN_POINT('Ctrl Pts',(83.426597929181,195.985837445542,52.2132412945418));
#46567=CARTESIAN_POINT('Ctrl Pts',(80.2216351328844,195.349369416884,59.6908955149556));
#46568=CARTESIAN_POINT('Ctrl Pts',(72.21218812787,194.712901388228,61.02573977292));
#46569=CARTESIAN_POINT('Ctrl Pts',(66.7494156897398,194.076433359571,55.0181472593925));
#46570=CARTESIAN_POINT('Ctrl Pts',(68.8629050529468,193.439965330914,47.1619228559709));
#46571=CARTESIAN_POINT('Ctrl Pts',(75.3077621678543,192.909575307033,45.1243839511291));
#46572=CARTESIAN_POINT('Ctrl Pts',(79.7371915239832,192.485263287928,47.2852650261152));
#46573=CARTESIAN_POINT('Ctrl Pts',(82.6875597010222,192.060951268824,51.2329959010707));
#46574=CARTESIAN_POINT('Ctrl Pts',(81.8899644877527,191.530561244943,57.9450440159248));
#46575=CARTESIAN_POINT('Ctrl Pts',(74.5669202423437,190.894093216286,61.4890702778233));
#46576=CARTESIAN_POINT('Ctrl Pts',(67.6445141591816,190.257625187629,57.2448572130513));
#46577=CARTESIAN_POINT('Ctrl Pts',(67.4594805854599,189.621157158972,49.1270488206354));
#46578=CARTESIAN_POINT('Ctrl Pts',(74.2067042249644,188.984689130315,44.5814935934104));
#46579=CARTESIAN_POINT('Ctrl Pts',(80.4086254297172,188.454299106434,47.2692289580603));
#46580=CARTESIAN_POINT('Ctrl Pts',(82.3358832685874,188.02998708733,51.805188466662));
#46581=CARTESIAN_POINT('Ctrl Pts',(81.9747666998536,187.605675068225,56.7203533942049));
#46582=CARTESIAN_POINT('Ctrl Pts',(76.9713079038153,187.075285044344,61.2649268721786));
#46583=CARTESIAN_POINT('Ctrl Pts',(69.1185120770804,186.438817015687,59.1387338261796));
#46584=CARTESIAN_POINT('Ctrl Pts',(66.6751619948799,185.80234898703,51.3951499727439));
#46585=CARTESIAN_POINT('Ctrl Pts',(71.8585347015804,185.165880958374,45.1448941457544));
#46586=CARTESIAN_POINT('Ctrl Pts',(79.933317849207,184.529412929716,46.1373538598204));
#46587=CARTESIAN_POINT('Ctrl Pts',(82.853329412247,183.999022905836,52.2333591495215));
#46588=CARTESIAN_POINT('Ctrl Pts',(81.3340493427206,183.574710886731,56.9217532788052));
#46589=CARTESIAN_POINT('Ctrl Pts',(77.8383970300113,183.150398867627,60.3958958132751));
#46590=CARTESIAN_POINT('Ctrl Pts',(71.0807955528553,182.620008843746,60.5461299515229));
#46591=CARTESIAN_POINT('Ctrl Pts',(66.5461590499559,181.983540815089,53.7915632776489));
#46592=CARTESIAN_POINT('Ctrl Pts',(69.77911925036,181.347072786432,46.343005104285));
#46593=CARTESIAN_POINT('Ctrl Pts',(77.7910185814084,180.710604757775,45.0229597912255));
#46594=CARTESIAN_POINT('Ctrl Pts',(83.236675387159,180.074136729118,51.0671240112991));
#46595=CARTESIAN_POINT('Ctrl Pts',(81.4439564155797,179.543746705237,57.584324845192));
#46596=CARTESIAN_POINT('Ctrl Pts',(77.2225935943312,179.119434686133,60.1278160231877));
#46597=CARTESIAN_POINT('Ctrl Pts',(72.3052933996905,178.695122667028,60.4585882060443));
#46598=CARTESIAN_POINT('Ctrl Pts',(67.1048092041633,178.164732643147,56.1408674933977));
#46599=CARTESIAN_POINT('Ctrl Pts',(68.1103275583388,177.52826461449,48.0677000849601));
#46600=CARTESIAN_POINT('Ctrl Pts',(75.4354306841967,176.891796585833,44.5639999386958));
#46601=CARTESIAN_POINT('Ctrl Pts',(82.3499841876386,176.255328557176,48.8209942266199));
#46602=CARTESIAN_POINT('Ctrl Pts',(82.4981144191685,175.618860528519,56.9551909662954));
#46603=CARTESIAN_POINT('Ctrl Pts',(76.8711065575554,175.088470504638,60.7001249504526));
#46604=CARTESIAN_POINT('Ctrl Pts',(72.0161507801839,174.664158485534,59.8523892363709));
#46605=CARTESIAN_POINT('Ctrl Pts',(68.0867054412862,174.239846466429,56.8777109731333));
#46606=CARTESIAN_POINT('Ctrl Pts',(66.9916029022179,173.709456442548,50.2077410744549));
#46607=CARTESIAN_POINT('Ctrl Pts',(73.0445668764352,173.072988413891,44.771867060824));
#46608=CARTESIAN_POINT('Ctrl Pts',(80.8724741977796,172.436520385235,46.9298562841126));
#46609=CARTESIAN_POINT('Ctrl Pts',(83.3015145995298,171.800052356578,54.6779407729424));
#46610=CARTESIAN_POINT('Ctrl Pts',(78.0795336709331,171.16358432792,60.9163712122925));
#46611=CARTESIAN_POINT('Ctrl Pts',(71.3755001146967,170.63319430404,60.0540011657286));
#46612=CARTESIAN_POINT('Ctrl Pts',(68.2659050293063,170.208882284935,56.2304334801661));
#46613=CARTESIAN_POINT('Ctrl Pts',(67.2497632531332,169.78457026583,51.4079126319087));
#46614=CARTESIAN_POINT('Ctrl Pts',(70.7966483253109,169.25418024195,45.6540135795167));
#46615=CARTESIAN_POINT('Ctrl Pts',(78.931074007745,168.617712213293,45.5190395738844));
#46616=CARTESIAN_POINT('Ctrl Pts',(83.4260701168421,167.981244184636,52.2812921940239));
#46617=CARTESIAN_POINT('Ctrl Pts',(80.1793549532992,167.344776155979,59.7238650802109));
#46618=CARTESIAN_POINT('Ctrl Pts',(72.1460607507099,166.708308127322,61.0096657723415));
#46619=CARTESIAN_POINT('Ctrl Pts',(67.6500129020043,166.177918103441,55.9625575148834));
#46620=CARTESIAN_POINT('Ctrl Pts',(67.8094963160762,165.753606084337,51.0367259625668));
#46621=CARTESIAN_POINT('Ctrl Pts',(70.2045728718383,165.329294065232,46.7294228929882));
#46622=CARTESIAN_POINT('Ctrl Pts',(76.6554533739143,164.798904041351,44.7110352274765));
#46623=CARTESIAN_POINT('Ctrl Pts',(82.8854297614923,164.162436012694,49.9430991964524));
#46624=CARTESIAN_POINT('Ctrl Pts',(81.8449431247788,163.525967984037,57.9960761663812));
#46625=CARTESIAN_POINT('Ctrl Pts',(74.5133797567601,162.88949995538,61.4862379248261));
#46626=CARTESIAN_POINT('Ctrl Pts',(67.6051283307556,162.253031926723,57.1893598255144));
#46627=CARTESIAN_POINT('Ctrl Pts',(67.5201530810369,161.722641902843,50.430622722528));
#46628=CARTESIAN_POINT('Ctrl Pts',(70.8705672900159,161.298329883738,46.8162104508805));
#46629=CARTESIAN_POINT('Ctrl Pts',(75.5032621757575,160.874017864633,45.1347261254156));
#46630=CARTESIAN_POINT('Ctrl Pts',(81.6971730222364,160.343627840753,47.840870328193));
#46631=CARTESIAN_POINT('Ctrl Pts',(82.9699791975185,159.707159812095,55.8762336432774));
#46632=CARTESIAN_POINT('Ctrl Pts',(76.9038536928211,159.070691783439,61.2739342537818));
#46633=CARTESIAN_POINT('Ctrl Pts',(69.0799464026406,158.434223754781,59.1014874226617));
#46634=CARTESIAN_POINT('Ctrl Pts',(66.6818169764982,157.797755726125,51.3274232075481));
#46635=CARTESIAN_POINT('Ctrl Pts',(71.0495526412501,157.267365702244,46.1688736843576));
#46636=CARTESIAN_POINT('Ctrl Pts',(75.9491772112947,156.84305368314,45.6369615546028));
#46637=CARTESIAN_POINT('Ctrl Pts',(80.5494457748369,156.418741664034,47.4052320611843));
#46638=CARTESIAN_POINT('Ctrl Pts',(83.4513383514884,155.888351640154,53.5098833611299));
#46639=CARTESIAN_POINT('Ctrl Pts',(79.1432926512695,155.251883611497,60.411176095833));
#46640=CARTESIAN_POINT('Ctrl Pts',(71.0239614089819,154.61541558284,60.5086989003167));
#46641=CARTESIAN_POINT('Ctrl Pts',(66.5414655682442,153.978947554183,53.7381537555628));
#46642=CARTESIAN_POINT('Ctrl Pts',(69.8285540663259,153.342479525526,46.2962354295517));
#46643=CARTESIAN_POINT('Ctrl Pts',(76.5087873933404,152.812089501645,45.2655896528667));
#46644=CARTESIAN_POINT('Ctrl Pts',(80.5567807350017,152.387777482541,48.0768173823518));
#46645=CARTESIAN_POINT('Ctrl Pts',(82.8704673911375,151.963465463436,52.4283809517351));
#46646=CARTESIAN_POINT('Ctrl Pts',(81.0583992028712,151.433075439555,58.9402283778824));
#46647=CARTESIAN_POINT('Ctrl Pts',(73.2804664854723,150.796607410899,61.3257811039523));
#46648=CARTESIAN_POINT('Ctrl Pts',(67.0864441542822,150.160139382241,56.0753394196649));
#46649=CARTESIAN_POINT('Ctrl Pts',(68.1418060998694,149.523671353585,48.0242983886437));
#46650=CARTESIAN_POINT('Ctrl Pts',(75.5034220168983,148.887203324927,44.5611047389346));
#46651=CARTESIAN_POINT('Ctrl Pts',(81.2228038404513,148.356813301047,48.1633845138502));
#46652=CARTESIAN_POINT('Ctrl Pts',(82.4356281071999,147.932501281942,52.9402358553873));
#46653=CARTESIAN_POINT('Ctrl Pts',(81.3290143292153,147.508189262838,57.7428036464279));
#46654=CARTESIAN_POINT('Ctrl Pts',(75.6909082376934,146.977799238957,61.4710080025618));
#46655=CARTESIAN_POINT('Ctrl Pts',(68.2543160943122,146.3413312103,58.1718874442559));
#46656=CARTESIAN_POINT('Ctrl Pts',(67.0207059165395,145.704863181643,50.1462250760347));
#46657=CARTESIAN_POINT('Ctrl Pts',(73.0967927917064,145.068395152986,44.7597402477996));
#46658=CARTESIAN_POINT('Ctrl Pts',(80.925705939638,144.431927124329,46.9722542223041));
#46659=CARTESIAN_POINT('Ctrl Pts',(82.881709341265,143.901537100448,53.4423236742635));
#46660=CARTESIAN_POINT('Ctrl Pts',(80.6650743178658,143.477225081343,57.8441165606002));
#46661=CARTESIAN_POINT('Ctrl Pts',(76.680406627644,143.052913062239,60.7444053116841));
#46662=CARTESIAN_POINT('Ctrl Pts',(69.9789640188073,142.522523038358,59.8621270217908));
#46663=CARTESIAN_POINT('Ctrl Pts',(66.5276813793795,141.886055009701,52.4949194566393));
#46664=CARTESIAN_POINT('Ctrl Pts',(70.8589587750538,141.249586981044,45.6266528164233));
#46665=CARTESIAN_POINT('Ctrl Pts',(78.9784563259308,140.613118952387,45.5441298457715));
#46666=CARTESIAN_POINT('Ctrl Pts',(83.4384584367587,139.97665092373,52.3482080593613));
#46667=CARTESIAN_POINT('Ctrl Pts',(80.6726315496697,139.44626089985,58.5156994173616));
#46668=CARTESIAN_POINT('Ctrl Pts',(76.1126999566996,139.021948880745,60.3855323801142));
#46669=CARTESIAN_POINT('Ctrl Pts',(71.2024863013405,138.59763686164,59.9623854790432));
#46670=CARTESIAN_POINT('Ctrl Pts',(66.7214489996053,138.06724683776,54.9019455059963));
#46671=CARTESIAN_POINT('Ctrl Pts',(68.9466223548929,137.430778809102,47.0766210587825));
#46672=CARTESIAN_POINT('Ctrl Pts',(76.7204388137733,136.794310780446,44.7312366163038));
#46673=CARTESIAN_POINT('Ctrl Pts',(82.9047508995969,136.157842751789,49.9931121891882));
#46674=CARTESIAN_POINT('Ctrl Pts',(81.8104176813927,135.521374723132,58.0547208359023));
#46675=CARTESIAN_POINT('Ctrl Pts',(75.6780301032495,134.990984699251,60.8975311728376));
#46676=CARTESIAN_POINT('Ctrl Pts',(71.0091921999896,134.566672680146,59.3191763096188));
#46677=CARTESIAN_POINT('Ctrl Pts',(67.5794628759647,134.142360661042,55.7799379445062));
#46678=CARTESIAN_POINT('Ctrl Pts',(67.5145625264963,133.611970637161,49.0209782638311));
#46679=CARTESIAN_POINT('Ctrl Pts',(74.3258453287723,132.975502608504,44.5719867204963));
#46680=CARTESIAN_POINT('Ctrl Pts',(81.7329902478001,132.339034579847,47.8987350830714));
#46681=CARTESIAN_POINT('Ctrl Pts',(82.9517716971165,131.70256655119,55.9266627296179));
#46682=CARTESIAN_POINT('Ctrl Pts',(76.8393321334314,131.066098522533,61.2955715336061));
#46683=CARTESIAN_POINT('Ctrl Pts',(70.345285756154,130.535708498652,59.4207089599438));
#46684=CARTESIAN_POINT('Ctrl Pts',(67.8552964618423,130.111396479548,55.1675683843954));
#46685=CARTESIAN_POINT('Ctrl Pts',(67.5866367229714,129.687084460443,50.2464838102518));
#46686=CARTESIAN_POINT('Ctrl Pts',(71.9696748354462,129.156694436562,45.1009299115017));
#46687=CARTESIAN_POINT('Ctrl Pts',(80.0295029927227,128.520226407905,46.208300328485));
#46688=CARTESIAN_POINT('Ctrl Pts',(83.4404367354544,127.883758379248,53.5770574504209));
#46689=CARTESIAN_POINT('Ctrl Pts',(79.0964782825046,127.247290350591,60.4373107604981));
#46690=CARTESIAN_POINT('Ctrl Pts',(70.9610596341513,126.610822321935,60.4827264104982));
#46691=CARTESIAN_POINT('Ctrl Pts',(67.2874710471809,126.080432298054,54.8088833641994));
#46692=CARTESIAN_POINT('Ctrl Pts',(68.1964381006051,125.656120278949,49.9650181372395));
#46693=CARTESIAN_POINT('Ctrl Pts',(71.2204926199176,125.231808259844,46.0734444574296));
#46694=CARTESIAN_POINT('Ctrl Pts',(77.9037576629453,124.701418235964,45.0626445835687));
#46695=CARTESIAN_POINT('Ctrl Pts',(83.2627733484823,124.064950207307,51.1837596819317));
#46696=CARTESIAN_POINT('Ctrl Pts',(81.0061205939446,123.42848217865,58.9837961475401));
#46697=CARTESIAN_POINT('Ctrl Pts',(73.2279845331631,122.792014149993,61.3148152249716));
#46698=CARTESIAN_POINT('Ctrl Pts',(67.0559843616916,122.155546121336,56.0144838156537));
#46699=CARTESIAN_POINT('Ctrl Pts',(68.0029311293476,121.625156097455,49.3218729768572));
#46700=CARTESIAN_POINT('Ctrl Pts',(71.8654559343288,121.200844078351,46.2608023190536));
#46701=CARTESIAN_POINT('Ctrl Pts',(76.7004222277914,120.776532059246,45.3056309301169));
#46702=CARTESIAN_POINT('Ctrl Pts',(82.409079478992,120.246142035365,48.9248822903661));
#46703=CARTESIAN_POINT('Ctrl Pts',(82.4413370611576,119.609674006708,57.0603637520646));
#46704=CARTESIAN_POINT('Ctrl Pts',(75.6228694268662,118.973205978051,61.4696210182606));
#46705=CARTESIAN_POINT('Ctrl Pts',(68.221882988768,118.336737949394,58.1291943595137));
#46706=CARTESIAN_POINT('Ctrl Pts',(67.0376135633978,117.700269920737,50.0803059211407));
#46707=CARTESIAN_POINT('Ctrl Pts',(72.1410868314743,117.169879896856,45.6483415008885));
#46708=CARTESIAN_POINT('Ctrl Pts',(77.0645120916213,116.745567877752,45.8700059971645));
#46709=CARTESIAN_POINT('Ctrl Pts',(81.3412314624846,116.321255858647,48.3192758606224));
#46710=CARTESIAN_POINT('Ctrl Pts',(83.2780090997717,115.790865834766,54.7951264151101));
#46711=CARTESIAN_POINT('Ctrl Pts',(77.9677021950907,115.15439780611,60.9585458997256));
#46712=CARTESIAN_POINT('Ctrl Pts',(69.9285043781874,114.517929777452,59.8164649130708));
#46713=CARTESIAN_POINT('Ctrl Pts',(66.5311895114466,113.881461748796,52.4414190002914));
#46714=CARTESIAN_POINT('Ctrl Pts',(70.9149490262317,113.244993720139,45.5879708402938));
#46715=CARTESIAN_POINT('Ctrl Pts',(77.6742202802328,112.714603696258,45.5883385159239));
#46716=CARTESIAN_POINT('Ctrl Pts',(81.2460419438328,112.290291677153,48.9841214071873));
#46717=CARTESIAN_POINT('Ctrl Pts',(82.8688995985184,111.865979658049,53.6376775177111));
#46718=CARTESIAN_POINT('Ctrl Pts',(80.0847664798852,111.335589634168,59.7969267250482));
#46719=CARTESIAN_POINT('Ctrl Pts',(72.0339731633678,110.699121605511,60.9681765446677));
#46720=CARTESIAN_POINT('Ctrl Pts',(66.7132940162291,110.062653576854,54.8343829442452));
#46721=CARTESIAN_POINT('Ctrl Pts',(68.9843527215643,109.426185548197,47.0385287334289));
#46722=CARTESIAN_POINT('Ctrl Pts',(76.7880761542206,108.78971751954,44.7387461889578));
#46723=CARTESIAN_POINT('Ctrl Pts',(81.8910672320391,108.259327495659,49.1712657974936));
#46724=CARTESIAN_POINT('Ctrl Pts',(82.3610740579104,107.835015476555,54.0772157589995));
#46725=CARTESIAN_POINT('Ctrl Pts',(80.5348612828878,107.41070345745,58.6547913554813));
#46726=CARTESIAN_POINT('Ctrl Pts',(74.3940571549151,106.880313433569,61.4793749853676));
#46727=CARTESIAN_POINT('Ctrl Pts',(67.5477081342156,106.243845404912,57.0845366206481));
#46728=CARTESIAN_POINT('Ctrl Pts',(67.5527081847441,105.607377376255,48.9646212566263));
#46729=CARTESIAN_POINT('Ctrl Pts',(74.3793098536259,104.970909347599,44.5679679642004));
#46730=CARTESIAN_POINT('Ctrl Pts',(81.7791320279888,104.334441318941,47.948756474748));
#46731=CARTESIAN_POINT('Ctrl Pts',(82.7253506908695,103.804051295061,54.6414702936983));
#46732=CARTESIAN_POINT('Ctrl Pts',(79.8632368833852,103.379739275956,58.6536462611964));
#46733=CARTESIAN_POINT('Ctrl Pts',(75.482807461588,102.955427256852,60.9122054306265));
#46734=CARTESIAN_POINT('Ctrl Pts',(68.9943583695012,102.425037232971,59.0180627750301));
#46735=CARTESIAN_POINT('Ctrl Pts',(66.7072003664947,101.788569204314,51.2106299424965));
#46736=CARTESIAN_POINT('Ctrl Pts',(72.0354295638575,101.152101175657,45.0833936862588));
#46737=CARTESIAN_POINT('Ctrl Pts',(80.0725037797786,100.515633147,46.2403243527888));
#46738=CARTESIAN_POINT('Ctrl Pts',(83.4424732424755,99.8791651183427,53.6450799183514));
#46739=CARTESIAN_POINT('Ctrl Pts',(79.7682674113498,99.3487750944621,59.3185232758616));
#46740=CARTESIAN_POINT('Ctrl Pts',(74.9764836612738,98.9244630753574,60.4709381029394));
#46741=CARTESIAN_POINT('Ctrl Pts',(70.1882708520563,98.5001510562529,59.3037750745634));
#46742=CARTESIAN_POINT('Ctrl Pts',(66.5315506863656,97.969761032372,53.6190459121331));
#46743=CARTESIAN_POINT('Ctrl Pts',(69.9243030493936,97.3332930037152,46.2247014132335));
#46744=CARTESIAN_POINT('Ctrl Pts',(77.9649013017072,96.696824975058,45.0925219821032));
#46745=CARTESIAN_POINT('Ctrl Pts',(83.274239787846,96.0603569464012,51.2361345479301));
#46746=CARTESIAN_POINT('Ctrl Pts',(80.9630539287384,95.4238889177443,59.036488327721));
#46747=CARTESIAN_POINT('Ctrl Pts',(74.4688036207804,94.8934988938635,60.9106443932431));
#46748=CARTESIAN_POINT('Ctrl Pts',(70.0953489534175,94.4691868747589,58.6386088051227));
#46749=CARTESIAN_POINT('Ctrl Pts',(67.2456020024424,94.0448748556542,54.6176395492626));
#46750=CARTESIAN_POINT('Ctrl Pts',(68.2124227130756,93.5144848317734,47.9278708138097));
#46751=CARTESIAN_POINT('Ctrl Pts',(75.6226190920302,92.8780168031165,44.5698820123746));
#46752=CARTESIAN_POINT('Ctrl Pts',(82.4356513262645,92.2415487744595,48.9875332315941));
#46753=CARTESIAN_POINT('Ctrl Pts',(82.4156505377467,91.6050807458026,57.1074255022982));
#46754=CARTESIAN_POINT('Ctrl Pts',(75.5558024799644,90.9686127171457,61.4811634676289));
#46755=CARTESIAN_POINT('Ctrl Pts',(69.4237242117114,90.4382226932648,58.6376859958749));
#46756=CARTESIAN_POINT('Ctrl Pts',(67.6116142203724,90.0139106741602,54.0545092787436));
#46757=CARTESIAN_POINT('Ctrl Pts',(68.0967239942248,89.5895986550556,49.1500296989643));
#46758=CARTESIAN_POINT('Ctrl Pts',(73.2133383912805,89.0592086311748,44.7332429560714));
#46759=CARTESIAN_POINT('Ctrl Pts',(81.0099439184418,88.4227406025178,47.0570418757459));
#46760=CARTESIAN_POINT('Ctrl Pts',(83.2569888118268,87.7862725738611,54.8598516111228));
#46761=CARTESIAN_POINT('Ctrl Pts',(77.9174492393249,87.1498045452039,60.9772340311672));
#46762=CARTESIAN_POINT('Ctrl Pts',(69.870300303306,86.513336516547,59.7812017712456));
#46763=CARTESIAN_POINT('Ctrl Pts',(67.1051444032194,85.9829464926663,53.6134095512882));
#46764=CARTESIAN_POINT('Ctrl Pts',(68.74232243329,85.5586344735616,48.9648721964835));
#46765=CARTESIAN_POINT('Ctrl Pts',(72.3245826130747,85.1343224544571,45.5801028623201));
#46766=CARTESIAN_POINT('Ctrl Pts',(79.0838229603303,84.6039324305761,45.6005466482718));
#46767=CARTESIAN_POINT('Ctrl Pts',(83.4464602703434,83.9674644019194,52.4674597004751));
#46768=CARTESIAN_POINT('Ctrl Pts',(80.0264541074312,83.3309963732621,59.8320104922767));
#46769=CARTESIAN_POINT('Ctrl Pts',(71.9837779856266,82.6945283446056,60.9493337754575));
#46770=CARTESIAN_POINT('Ctrl Pts',(66.6924731135778,82.0580603159483,54.7695933346078));
#46771=CARTESIAN_POINT('Ctrl Pts',(68.6491803921887,81.5276702920678,48.2997367174807));
#46772=CARTESIAN_POINT('Ctrl Pts',(72.9334206715241,81.103358272963,45.8636462696356));
#46773=CARTESIAN_POINT('Ctrl Pts',(77.857505088695,80.6790462538584,45.6571418054232));
#46774=CARTESIAN_POINT('Ctrl Pts',(82.9473083685091,80.1486562299776,50.1047985584944));
#46775=CARTESIAN_POINT('Ctrl Pts',(81.738262429575,79.5121882013206,58.1500025386794));
#46776=CARTESIAN_POINT('Ctrl Pts',(74.327026064536,78.8757201726637,61.4676260949181));
#46777=CARTESIAN_POINT('Ctrl Pts',(67.5221666333459,78.2392521440068,57.0373960059586));
#46778=CARTESIAN_POINT('Ctrl Pts',(67.5794728051966,77.6027841153498,48.9020524257583));
#46779=CARTESIAN_POINT('Ctrl Pts',(73.299246492323,77.0723940914689,45.3003948922867));
#46780=CARTESIAN_POINT('Ctrl Pts',(78.1312489429735,76.6480820723644,46.2704483743535));
#46781=CARTESIAN_POINT('Ctrl Pts',(81.9843305554388,76.2237700532597,49.3433970444166));
#46782=CARTESIAN_POINT('Ctrl Pts',(82.9106666188498,75.693380029379,56.0388917623577));
#46783=CARTESIAN_POINT('Ctrl Pts',(76.7223762458708,75.0569120007221,61.3201947668195));
#46784=CARTESIAN_POINT('Ctrl Pts',(68.951454145031,74.4204439720651,58.9652382444899));
#46785=CARTESIAN_POINT('Ctrl Pts',(66.7188280111139,73.7839759434081,51.1582906293505));
#46786=CARTESIAN_POINT('Ctrl Pts',(72.0966649038226,73.1475079147512,45.0537046875637));
#46787=CARTESIAN_POINT('Ctrl Pts',(78.776786065805,72.6171178908704,46.0850772107525));
#46788=CARTESIAN_POINT('Ctrl Pts',(81.788844289455,72.1928058717658,49.9859433579692));
#46789=CARTESIAN_POINT('Ctrl Pts',(82.6828930144,71.7684938526612,54.8325842894381));
#46790=CARTESIAN_POINT('Ctrl Pts',(78.9918523597607,71.2381038287804,60.4950896453872));
#46791=CARTESIAN_POINT('Ctrl Pts',(70.8566121056435,70.6016358001233,60.4246256614701));
#46792=CARTESIAN_POINT('Ctrl Pts',(66.5337966215277,69.9651677714665,53.5510300369317));
#46793=CARTESIAN_POINT('Ctrl Pts',(69.9674022330036,69.3286997428095,46.1928099380068));
#46794=CARTESIAN_POINT('Ctrl Pts',(78.0306017252772,68.6922317141527,45.1102605797613));
#46795=CARTESIAN_POINT('Ctrl Pts',(82.3977761578423,68.1618416902719,50.2692852449376));
#46796=CARTESIAN_POINT('Ctrl Pts',(82.1139659178903,67.7375296711671,55.1895193032789));
#46797=CARTESIAN_POINT('Ctrl Pts',(79.6108932178857,67.3132176520626,59.4349731659012));
#46798=CARTESIAN_POINT('Ctrl Pts',(73.1111050136803,66.7828276281817,61.289832007114));
#46799=CARTESIAN_POINT('Ctrl Pts',(67.0152250258696,66.1463595995248,55.9021287543866));
#46800=CARTESIAN_POINT('Ctrl Pts',(68.2587182879284,65.5098915708679,47.8779917274786));
#46801=CARTESIAN_POINT('Ctrl Pts',(75.6760709899128,64.8734235422109,44.5740653642333));
#46802=CARTESIAN_POINT('Ctrl Pts',(82.4736232832814,64.236955513554,49.0440074202512));
#46803=CARTESIAN_POINT('Ctrl Pts',(82.3879127409199,63.7065654896732,55.8027352386563));
#46804=CARTESIAN_POINT('Ctrl Pts',(78.9473025349299,63.2822534705685,59.3313968619353));
#46805=CARTESIAN_POINT('Ctrl Pts',(74.2736270857796,62.857941451464,60.8953691242108));
#46806=CARTESIAN_POINT('Ctrl Pts',(68.1500214465859,62.3275514275831,58.03369094594));
#46807=CARTESIAN_POINT('Ctrl Pts',(67.0805147073622,61.6910833989263,49.9687511135548));
#46808=CARTESIAN_POINT('Ctrl Pts',(73.2809985327285,61.0546153702692,44.7259416710183));
#46809=CARTESIAN_POINT('Ctrl Pts',(81.0475568218978,60.4181473416123,47.095250190464));
#46810=CARTESIAN_POINT('Ctrl Pts',(83.2486258453396,59.7816793129554,54.9273887438406));
#46811=CARTESIAN_POINT('Ctrl Pts',(78.7520289407639,59.2512892890746,59.9740078396425));
#46812=CARTESIAN_POINT('Ctrl Pts',(73.8405357114601,58.8269772699699,60.3820344315018));
#46813=CARTESIAN_POINT('Ctrl Pts',(69.2863828551142,58.4026652508654,58.4981705292525));
#46814=CARTESIAN_POINT('Ctrl Pts',(66.5395584769716,57.8722752269845,52.3221925616754));
#46815=CARTESIAN_POINT('Ctrl Pts',(71.0204888657229,57.2358071983275,45.5318787238324));
#46816=CARTESIAN_POINT('Ctrl Pts',(79.1396938462357,56.5993391696707,45.6394008322464));
#46817=CARTESIAN_POINT('Ctrl Pts',(83.4498036605393,55.9628711410136,52.5209707045959));
#46818=CARTESIAN_POINT('Ctrl Pts',(79.9758541146286,55.3264031123569,59.8775170218364));
#46819=CARTESIAN_POINT('Ctrl Pts',(73.2717267795347,54.7960130884759,60.7391577214321));
#46820=CARTESIAN_POINT('Ctrl Pts',(69.2960078212935,54.3717010693713,57.8266141241198));
#46821=CARTESIAN_POINT('Ctrl Pts',(67.0929362059535,53.9473890502667,53.4180171932531));
#46822=CARTESIAN_POINT('Ctrl Pts',(69.0688513580473,53.416999026386,46.9540008464241));
#46823=CARTESIAN_POINT('Ctrl Pts',(76.9045396175281,52.780530997729,44.7656021931905));
#46824=CARTESIAN_POINT('Ctrl Pts',(82.9640129734279,52.1440629690721,50.1707694587362));
#46825=CARTESIAN_POINT('Ctrl Pts',(81.7056980278796,51.5075949404151,58.1925955611392));
#46826=CARTESIAN_POINT('Ctrl Pts',(74.2589833057556,50.871126911758,61.4688035845323));
#46827=CARTESIAN_POINT('Ctrl Pts',(68.6323828944269,50.3407368878774,57.7232574519121));
#46828=CARTESIAN_POINT('Ctrl Pts',(67.5405612290126,49.9164248687727,52.9173052161848));
#46829=CARTESIAN_POINT('Ctrl Pts',(68.7680874345769,49.4921128496681,48.1442107423851));
#46830=CARTESIAN_POINT('Ctrl Pts',(74.4985333885546,48.9617228257873,44.5595577342274));
#46831=CARTESIAN_POINT('Ctrl Pts',(81.8494514107689,48.3252547971304,48.0454010175555));
#46832=CARTESIAN_POINT('Ctrl Pts',(82.8800195992615,47.6887867684733,56.0996532937291));
#46833=CARTESIAN_POINT('Ctrl Pts',(76.6698607789289,47.0523187398166,61.3309990045025));
#46834=CARTESIAN_POINT('Ctrl Pts',(68.8993099268987,46.4158507111594,58.9215097181071));
#46835=CARTESIAN_POINT('Ctrl Pts',(67.1072999819816,45.8854606872789,52.4041138901965));
#46836=CARTESIAN_POINT('Ctrl Pts',(69.4343739189814,45.4611486681741,48.0596946732126));
#46837=CARTESIAN_POINT('Ctrl Pts',(73.4910037035292,45.0368366490696,45.2609438389505));
#46838=CARTESIAN_POINT('Ctrl Pts',(80.1680320593212,44.5064466251886,46.3121528363915));
#46839=CARTESIAN_POINT('Ctrl Pts',(83.4321916804705,43.8699785965318,53.7641566697841));
#46840=CARTESIAN_POINT('Ctrl Pts',(78.9288709150793,43.2335105678747,60.5208683406622));
#46841=CARTESIAN_POINT('Ctrl Pts',(70.8098784261097,42.5970425392179,60.3983469815706));
#46842=CARTESIAN_POINT('Ctrl Pts',(66.5231018828453,41.9605745105609,53.4838227005111));
#46843=CARTESIAN_POINT('Ctrl Pts',(69.4437766221635,41.4301844866802,47.3881351193222));
#46844=CARTESIAN_POINT('Ctrl Pts',(74.0494677974295,41.0058724675754,45.6340369922952));
#46845=CARTESIAN_POINT('Ctrl Pts',(78.9474314123798,40.5815604484709,46.1810323010362));
#46846=CARTESIAN_POINT('Ctrl Pts',(83.2992634568746,40.05117042459,51.3530054135783));
#46847=CARTESIAN_POINT('Ctrl Pts',(80.8772094409459,39.4147023959332,59.1196490586266));
#46848=CARTESIAN_POINT('Ctrl Pts',(73.0466503802297,38.7782343672763,61.267996171179));
#46849=CARTESIAN_POINT('Ctrl Pts',(66.9971728804178,38.1417663386192,55.8516438470915));
#46850=CARTESIAN_POINT('Ctrl Pts',(68.2947135064205,37.5052983099623,47.8202375263325));
#46851=CARTESIAN_POINT('Ctrl Pts',(74.4969270772327,36.9749082860815,45.1331768938991));
#46852=CARTESIAN_POINT('Ctrl Pts',(79.1244227975359,36.5505962669769,46.8289170861851));
#46853=CARTESIAN_POINT('Ctrl Pts',(82.4636925300972,36.1262842478722,50.453627984227));
#46854=CARTESIAN_POINT('Ctrl Pts',(82.3579078679477,35.5958942239916,57.2120714163713));
#46855=CARTESIAN_POINT('Ctrl Pts',(75.4364593130539,34.9594261953344,61.4876589862132));
#46856=CARTESIAN_POINT('Ctrl Pts',(68.1156767308743,34.3229581666776,57.9749402522543));
#46857=CARTESIAN_POINT('Ctrl Pts',(67.0999897413908,33.6864901380206,49.9187978467345));
#46858=CARTESIAN_POINT('Ctrl Pts',(73.3460458636487,33.0500221093637,44.7059404648168));
#46859=CARTESIAN_POINT('Ctrl Pts',(79.7906812734519,32.519632085483,46.7441805034492));
#46860=CARTESIAN_POINT('Ctrl Pts',(82.17248450487,32.0953200663783,51.0588374777756));
#46861=CARTESIAN_POINT('Ctrl Pts',(82.3168007726042,31.6710080472736,55.985136723764));
#46862=CARTESIAN_POINT('Ctrl Pts',(77.805234440245,31.1406180233928,61.0183779493088));
#46863=CARTESIAN_POINT('Ctrl Pts',(69.775937231011,30.5041499947359,59.7078492408087));
#46864=CARTESIAN_POINT('Ctrl Pts',(66.5521527695141,29.867681966079,52.255315154175));
#46865=CARTESIAN_POINT('Ctrl Pts',(71.0679482096409,29.2312139374221,45.5069344631459));
#46866=CARTESIAN_POINT('Ctrl Pts',(79.2019197609294,28.5947459087651,45.6669533075484));
#46867=CARTESIAN_POINT('Ctrl Pts',(82.7310720445922,28.0643558848842,51.4317457936056));
#46868=CARTESIAN_POINT('Ctrl Pts',(81.7000867943277,27.6400438657796,56.2511150970413));
#46869=CARTESIAN_POINT('Ctrl Pts',(78.5787338518511,27.215731846675,60.0650904415566));
#46870=CARTESIAN_POINT('Ctrl Pts',(71.8720769265383,26.6853418227943,60.9068148573381));
#46871=CARTESIAN_POINT('Ctrl Pts',(66.6693284787701,26.0488737941373,54.6523360552579));
#46872=CARTESIAN_POINT('Ctrl Pts',(69.1222134897098,25.4124057654804,46.9117666786429));
#46873=CARTESIAN_POINT('Ctrl Pts',(76.9567277562455,24.7759377368234,44.7778903714537));
#46874=CARTESIAN_POINT('Ctrl Pts',(82.992926824387,24.1394697081665,50.2323735386687));
#46875=CARTESIAN_POINT('Ctrl Pts',(81.8772919287,23.6090796842857,56.8989434446722));
#46876=CARTESIAN_POINT('Ctrl Pts',(77.9387078763277,23.1847676651811,59.8615040083881));
#46877=CARTESIAN_POINT('Ctrl Pts',(73.0811619366474,22.7604556460765,60.6942974202152));
#46878=CARTESIAN_POINT('Ctrl Pts',(67.4657179403036,22.2300656221957,56.9320340266631));
#46879=CARTESIAN_POINT('Ctrl Pts',(67.6388800071612,21.5935975935386,48.7983717706867));
#46880=CARTESIAN_POINT('Ctrl Pts',(74.5665295192065,20.9571295648818,44.5626166146362));
#46881=CARTESIAN_POINT('Ctrl Pts',(81.8807696047214,20.3206615362248,48.0889858384696));
#46882=CARTESIAN_POINT('Ctrl Pts',(82.8615055928374,19.6841935075679,56.1649530568178));
#46883=CARTESIAN_POINT('Ctrl Pts',(77.6476071831429,19.1538034836871,60.4671122954246));
#46884=CARTESIAN_POINT('Ctrl Pts',(72.7315637908718,18.7294914645825,60.1205020584682));
#46885=CARTESIAN_POINT('Ctrl Pts',(68.5176299076658,18.3051794454778,57.5653992266505));
#46886=CARTESIAN_POINT('Ctrl Pts',(66.7459211088642,17.774789421597,51.0396675832774));
#46887=CARTESIAN_POINT('Ctrl Pts',(72.2084562434742,17.1383213929401,45.0178404474499));
#46888=CARTESIAN_POINT('Ctrl Pts',(80.2192932876998,16.5018533642832,46.3527031218275));
#46889=CARTESIAN_POINT('Ctrl Pts',(83.4234792908833,15.8653853356262,53.8297790170139));
#46890=CARTESIAN_POINT('Ctrl Pts',(79.6377596034834,15.3349953117454,59.4154059749504));
#46891=CARTESIAN_POINT('Ctrl Pts',(74.8056885960671,14.9106832926407,60.4766449025428));
#46892=CARTESIAN_POINT('Ctrl Pts',(72.4431871575855,14.6985272830884,59.8257072724431));
#46893=CARTESIAN_POINT('Ctrl Pts',(71.4090089980051,14.5924492783123,59.2293593014411));
#46894=CARTESIAN_POINT('Ctrl Pts',(82.1675194498639,416.000000000001,49.6673071229103));
#46895=CARTESIAN_POINT('Ctrl Pts',(82.7266367873617,415.893921995224,50.8636168302151));
#46896=CARTESIAN_POINT('Ctrl Pts',(83.2199114808876,415.681765985672,53.5290146892342));
#46897=CARTESIAN_POINT('Ctrl Pts',(81.5919790563639,415.257453966567,58.7536428520482));
#46898=CARTESIAN_POINT('Ctrl Pts',(75.0770954668831,414.727063942687,62.3959325671766));
#46899=CARTESIAN_POINT('Ctrl Pts',(67.140757194596,414.090595914029,58.1554105274575));
#46900=CARTESIAN_POINT('Ctrl Pts',(66.4295467677559,413.454127885373,49.2002551082192));
#46901=CARTESIAN_POINT('Ctrl Pts',(73.5842173300634,412.817659856715,43.7513695000057));
#46902=CARTESIAN_POINT('Ctrl Pts',(80.6079888575398,412.287269832835,46.322952169211));
#46903=CARTESIAN_POINT('Ctrl Pts',(83.02416694298,411.86295781373,51.2093932239552));
#46904=CARTESIAN_POINT('Ctrl Pts',(82.9398220702424,411.438645794626,56.6601133855912));
#46905=CARTESIAN_POINT('Ctrl Pts',(77.7039374267809,410.908255770745,61.9981103880748));
#46906=CARTESIAN_POINT('Ctrl Pts',(68.8966609576623,410.271787742088,60.1511828265501));
#46907=CARTESIAN_POINT('Ctrl Pts',(65.7041703612452,409.635319713431,51.7558425715054));
#46908=CARTESIAN_POINT('Ctrl Pts',(71.029438885837,408.998851684774,44.5228669413054));
#46909=CARTESIAN_POINT('Ctrl Pts',(80.0097580407648,408.362383656117,45.1035870573125));
#46910=CARTESIAN_POINT('Ctrl Pts',(83.6233687599763,407.831993632237,51.6491061535822));
#46911=CARTESIAN_POINT('Ctrl Pts',(82.2447835214442,407.407681613132,56.9234798541325));
#46912=CARTESIAN_POINT('Ctrl Pts',(78.6062110227621,406.983369594028,60.983060830221));
#46913=CARTESIAN_POINT('Ctrl Pts',(71.1533325950583,406.452979570146,61.5801830353272));
#46914=CARTESIAN_POINT('Ctrl Pts',(65.7146841645151,405.81651154149,54.4104373561892));
#46915=CARTESIAN_POINT('Ctrl Pts',(68.8095528552745,405.180043512832,45.9786464084971));
#46916=CARTESIAN_POINT('Ctrl Pts',(77.5729088149027,404.543575484176,44.0096557413621));
#46917=CARTESIAN_POINT('Ctrl Pts',(83.9722721207543,403.907107455519,50.3367650503416));
#46918=CARTESIAN_POINT('Ctrl Pts',(82.4084379950837,403.376717431638,57.648147639214));
#46919=CARTESIAN_POINT('Ctrl Pts',(77.9090662557975,402.952405412533,60.7263149046133));
#46920=CARTESIAN_POINT('Ctrl Pts',(72.4999683740037,402.528093393429,61.4053720313486));
#46921=CARTESIAN_POINT('Ctrl Pts',(66.4815183774652,401.997703369548,56.9691401200638));
#46922=CARTESIAN_POINT('Ctrl Pts',(67.0767526293748,401.361235340891,47.9897268622084));
#46923=CARTESIAN_POINT('Ctrl Pts',(74.9423310373525,400.724767312234,43.6531386257255));
#46924=CARTESIAN_POINT('Ctrl Pts',(82.8497633290917,400.088299283577,47.9129315749583));
#46925=CARTESIAN_POINT('Ctrl Pts',(83.5324048115291,399.45183125492,56.8861231368181));
#46926=CARTESIAN_POINT('Ctrl Pts',(77.5574372048307,398.921441231039,61.3807483418143));
#46927=CARTESIAN_POINT('Ctrl Pts',(72.141983520554,398.497129211935,60.7543935454473));
#46928=CARTESIAN_POINT('Ctrl Pts',(67.6128520565103,398.07281719283,57.7201840750103));
#46929=CARTESIAN_POINT('Ctrl Pts',(65.9778985815363,397.542427168948,50.424375635435));
#46930=CARTESIAN_POINT('Ctrl Pts',(72.3153497046489,396.905959140293,44.0352536724918));
#46931=CARTESIAN_POINT('Ctrl Pts',(81.0974623299774,396.269491111635,45.9188192264581));
#46932=CARTESIAN_POINT('Ctrl Pts',(84.2742884644266,395.633023082978,54.3200749107313));
#46933=CARTESIAN_POINT('Ctrl Pts',(78.9057099164933,394.996555054322,61.5424381367421));
#46934=CARTESIAN_POINT('Ctrl Pts',(71.447374289968,394.46616503044,61.0179161312433));
#46935=CARTESIAN_POINT('Ctrl Pts',(67.7694391264492,394.041853011337,56.9939564067508));
#46936=CARTESIAN_POINT('Ctrl Pts',(66.3395721561712,393.617540992231,51.7332587934419));
#46937=CARTESIAN_POINT('Ctrl Pts',(69.8892509040224,393.087150968351,45.1528580123862));
#46938=CARTESIAN_POINT('Ctrl Pts',(78.8635348149744,392.450682939693,44.4847304204006));
#46939=CARTESIAN_POINT('Ctrl Pts',(84.2589006674125,391.814214911037,51.6654928227725));
#46940=CARTESIAN_POINT('Ctrl Pts',(81.1484592765518,391.177746882379,60.0915521457887));
#46941=CARTESIAN_POINT('Ctrl Pts',(72.3592921800129,390.541278853723,62.0240913931654));
#46942=CARTESIAN_POINT('Ctrl Pts',(67.0722118849917,390.010888829841,56.7374406948235));
#46943=CARTESIAN_POINT('Ctrl Pts',(66.9340026511513,389.586576810738,51.2876372911175));
#46944=CARTESIAN_POINT('Ctrl Pts',(69.3040424467103,389.162264791632,46.3782207984136));
#46945=CARTESIAN_POINT('Ctrl Pts',(76.2989923201939,388.631874767753,43.7376583735257));
#46946=CARTESIAN_POINT('Ctrl Pts',(83.5126631044287,387.995406739094,49.1179111566402));
#46947=CARTESIAN_POINT('Ctrl Pts',(82.8775247809523,387.358938710439,58.0772593846658));
#46948=CARTESIAN_POINT('Ctrl Pts',(75.0039483663863,386.722470681781,62.3993093386759));
#46949=CARTESIAN_POINT('Ctrl Pts',(67.1009304314964,386.086002653124,58.0950702985737));
#46950=CARTESIAN_POINT('Ctrl Pts',(66.5758023831447,385.555612629243,50.6367773179301));
#46951=CARTESIAN_POINT('Ctrl Pts',(70.045042324282,385.131300610139,46.4315623219777));
#46952=CARTESIAN_POINT('Ctrl Pts',(75.053657026783,384.706988591034,44.2790666324918));
#46953=CARTESIAN_POINT('Ctrl Pts',(82.0663161112484,384.176598567154,46.8722319217373));
#46954=CARTESIAN_POINT('Ctrl Pts',(83.9846374672821,383.540130538496,55.6645131597617));
#46955=CARTESIAN_POINT('Ctrl Pts',(77.6302160584578,382.90366250984,62.0123198612961));
#46956=CARTESIAN_POINT('Ctrl Pts',(68.8515981217496,382.267194481182,60.1125334305931));
#46957=CARTESIAN_POINT('Ctrl Pts',(65.7072493485604,381.630726452526,51.6806156780251));
#46958=CARTESIAN_POINT('Ctrl Pts',(70.2013890289615,381.100336428644,45.7052828684384));
#46959=CARTESIAN_POINT('Ctrl Pts',(75.5781324828351,380.67602440954,44.8052335572377));
#46960=CARTESIAN_POINT('Ctrl Pts',(80.7710747695743,380.251712390435,46.4643927834609));
#46961=CARTESIAN_POINT('Ctrl Pts',(84.3652035446419,379.721322366556,53.020621272502));
#46962=CARTESIAN_POINT('Ctrl Pts',(80.0481880045269,379.084854337897,60.9166673095976));
#46963=CARTESIAN_POINT('Ctrl Pts',(71.0881831371497,378.448386309242,61.542474098911));
#46964=CARTESIAN_POINT('Ctrl Pts',(65.7060922452434,377.811918280583,54.3517565413768));
#46965=CARTESIAN_POINT('Ctrl Pts',(68.8611599294873,377.175450251927,45.9238437451164));
#46966=CARTESIAN_POINT('Ctrl Pts',(76.1724154596052,376.645060228046,44.3594153429182));
#46967=CARTESIAN_POINT('Ctrl Pts',(80.8220300956532,376.220748208942,47.2055605724546));
#46968=CARTESIAN_POINT('Ctrl Pts',(83.6547311664345,375.796436189837,51.8633780415016));
#46969=CARTESIAN_POINT('Ctrl Pts',(82.0691877899781,375.266046165956,59.1700835818705));
#46970=CARTESIAN_POINT('Ctrl Pts',(73.6321954803594,374.629578137299,62.3007906842619));
#46971=CARTESIAN_POINT('Ctrl Pts',(66.4570562632811,373.993110108642,56.8979489711891));
#46972=CARTESIAN_POINT('Ctrl Pts',(67.1087450192595,373.356642079985,47.9397893875299));
#46973=CARTESIAN_POINT('Ctrl Pts',(75.017229542891,372.720174051328,43.6456027668752));
#46974=CARTESIAN_POINT('Ctrl Pts',(81.5630475868822,372.189784027447,47.2586568471847));
#46975=CARTESIAN_POINT('Ctrl Pts',(83.2071979870441,371.765472008343,52.4563706131603));
#46976=CARTESIAN_POINT('Ctrl Pts',(82.2916195454673,371.341159989238,57.8304914760256));
#46977=CARTESIAN_POINT('Ctrl Pts',(76.303328540101,370.810769965358,62.3073502505834));
#46978=CARTESIAN_POINT('Ctrl Pts',(67.8805296891691,370.1743019367,59.1386556123655));
#46979=CARTESIAN_POINT('Ctrl Pts',(66.0061117550362,369.537833908044,50.3545860105709));
#46980=CARTESIAN_POINT('Ctrl Pts',(72.3722492701013,368.901365879387,44.0185293109938));
#46981=CARTESIAN_POINT('Ctrl Pts',(81.1589519760789,368.26489785073,45.9622427030081));
#46982=CARTESIAN_POINT('Ctrl Pts',(83.731847557838,367.734507826849,52.9823639254405));
#46983=CARTESIAN_POINT('Ctrl Pts',(81.564891452265,367.310195807745,57.9847393779517));
#46984=CARTESIAN_POINT('Ctrl Pts',(77.3496717091796,366.885883788639,61.4418163873436));
#46985=CARTESIAN_POINT('Ctrl Pts',(69.8929268947405,366.35549376476,60.8951442510317));
#46986=CARTESIAN_POINT('Ctrl Pts',(65.6115368619148,365.719025736101,52.9797247687586));
#46987=CARTESIAN_POINT('Ctrl Pts',(69.9563147730001,365.082557707445,45.1186671895065));
#46988=CARTESIAN_POINT('Ctrl Pts',(78.9174604672025,364.446089678788,44.5094141975096));
#46989=CARTESIAN_POINT('Ctrl Pts',(84.2768512094807,363.809621650131,51.738597904202));
#46990=CARTESIAN_POINT('Ctrl Pts',(81.6160920770388,363.27923162625,58.7258902618615));
#46991=CARTESIAN_POINT('Ctrl Pts',(76.6998492575118,362.854919607146,61.081737343235));
#46992=CARTESIAN_POINT('Ctrl Pts',(71.2504678681829,362.430607588041,60.9277847368937));
#46993=CARTESIAN_POINT('Ctrl Pts',(65.979113088516,361.90021756416,55.6254538872424));
#46994=CARTESIAN_POINT('Ctrl Pts',(67.9370353160928,361.263749535503,46.8419063838533));
#46995=CARTESIAN_POINT('Ctrl Pts',(76.3720452392034,360.627281506846,43.7558200341216));
#46996=CARTESIAN_POINT('Ctrl Pts',(83.5371909925975,359.99081347819,49.1719078928615));
#46997=CARTESIAN_POINT('Ctrl Pts',(82.8431403597864,359.354345449532,58.1442241998485));
#46998=CARTESIAN_POINT('Ctrl Pts',(76.2525123631298,358.823955425652,61.6748780007709));
#46999=CARTESIAN_POINT('Ctrl Pts',(70.995967448003,358.399643406547,60.2298193560718));
#47000=CARTESIAN_POINT('Ctrl Pts',(66.9826497101512,357.975331387442,56.5402747139229));
#47001=CARTESIAN_POINT('Ctrl Pts',(66.4796762958856,357.444941363562,49.0804549173847));
#47002=CARTESIAN_POINT('Ctrl Pts',(73.7175186823536,356.808473334904,43.7327634732031));
#47003=CARTESIAN_POINT('Ctrl Pts',(82.1095617690253,356.172005306248,46.9338467574087));
#47004=CARTESIAN_POINT('Ctrl Pts',(83.9677487982834,355.53553727759,55.7213641727699));
#47005=CARTESIAN_POINT('Ctrl Pts',(77.5603452197334,354.899069248934,62.04033130159));
#47006=CARTESIAN_POINT('Ctrl Pts',(70.2692904454451,354.368679225053,60.3843077719843));
#47007=CARTESIAN_POINT('Ctrl Pts',(67.2481778544935,353.944367205949,55.8464296726782));
#47008=CARTESIAN_POINT('Ctrl Pts',(66.637470387959,353.520055186844,50.4291891092842));
#47009=CARTESIAN_POINT('Ctrl Pts',(71.1493379349456,352.989665162963,44.4672309669677));
#47010=CARTESIAN_POINT('Ctrl Pts',(80.1205199676786,352.353197134306,45.1757922763084));
#47011=CARTESIAN_POINT('Ctrl Pts',(84.3574513433622,351.716729105648,53.0954976924663));
#47012=CARTESIAN_POINT('Ctrl Pts',(79.9981583142393,351.080261076993,60.9485153065569));
#47013=CARTESIAN_POINT('Ctrl Pts',(71.0170629561984,350.443793048334,61.5178064125007));
#47014=CARTESIAN_POINT('Ctrl Pts',(66.5982362644239,349.913403024455,55.4865657175575));
#47015=CARTESIAN_POINT('Ctrl Pts',(67.292916921443,349.48909100535,50.0794520960279));
#47016=CARTESIAN_POINT('Ctrl Pts',(70.3840695694908,349.064778986245,45.5889917367961));
#47017=CARTESIAN_POINT('Ctrl Pts',(77.6999394516204,348.534388962364,44.046285828326));
#47018=CARTESIAN_POINT('Ctrl Pts',(84.0085351524569,347.897920933708,50.4639011546693));
#47019=CARTESIAN_POINT('Ctrl Pts',(82.0142363486943,347.26145290505,59.2215317498864));
#47020=CARTESIAN_POINT('Ctrl Pts',(73.5735395779143,346.624984876393,62.2920299805842));
#47021=CARTESIAN_POINT('Ctrl Pts',(66.4195359996401,345.988516847736,56.8326894530505));
#47022=CARTESIAN_POINT('Ctrl Pts',(67.0381855122534,345.458126823856,49.3815709844699));
#47023=CARTESIAN_POINT('Ctrl Pts',(71.1082622727451,345.033814804751,45.7547357118015));
#47024=CARTESIAN_POINT('Ctrl Pts',(76.3865941183634,344.609502785648,44.3914045492091));
#47025=CARTESIAN_POINT('Ctrl Pts',(82.9216519432451,344.079112761765,48.0238848145009));
#47026=CARTESIAN_POINT('Ctrl Pts',(83.4764165212709,343.44264473311,57.0058891819291));
#47027=CARTESIAN_POINT('Ctrl Pts',(76.2281043515981,342.806176704451,62.3101602960356));
#47028=CARTESIAN_POINT('Ctrl Pts',(67.8419892726382,342.169708675796,59.0935789985375));
#47029=CARTESIAN_POINT('Ctrl Pts',(66.0205765335468,341.533240647137,50.2807121649013));
#47030=CARTESIAN_POINT('Ctrl Pts',(71.373560763289,341.002850623258,45.0608028277178));
#47031=CARTESIAN_POINT('Ctrl Pts',(76.8246747903378,340.578538604152,44.9914141004164));
#47032=CARTESIAN_POINT('Ctrl Pts',(81.7037757041983,340.154226585048,47.4232515135116));
#47033=CARTESIAN_POINT('Ctrl Pts',(84.2558090592015,339.623836561167,54.4509836802375));
#47034=CARTESIAN_POINT('Ctrl Pts',(78.784904978247,338.987368532511,61.5961481101528));
#47035=CARTESIAN_POINT('Ctrl Pts',(69.8342902036576,338.350900503853,60.8479392369952));
#47036=CARTESIAN_POINT('Ctrl Pts',(65.6119969363752,337.714432475197,52.9204200206177));
#47037=CARTESIAN_POINT('Ctrl Pts',(70.0156767767625,337.077964446539,45.0723775859148));
#47038=CARTESIAN_POINT('Ctrl Pts',(77.4800055367938,336.547574422659,44.6414601756678));
#47039=CARTESIAN_POINT('Ctrl Pts',(81.641082531161,336.123262403554,48.1635188319527));
#47040=CARTESIAN_POINT('Ctrl Pts',(83.7301676223705,335.698950384449,53.1989118069898));
#47041=CARTESIAN_POINT('Ctrl Pts',(81.0486668554268,335.168560360569,60.1782704658609));
#47042=CARTESIAN_POINT('Ctrl Pts',(72.232865644344,334.532092331911,61.985427127637));
#47043=CARTESIAN_POINT('Ctrl Pts',(65.9657961792567,333.895624303255,55.5513645167554));
#47044=CARTESIAN_POINT('Ctrl Pts',(67.9762704426601,333.259156274598,46.7974331372456));
#47045=CARTESIAN_POINT('Ctrl Pts',(76.4472167768183,332.622688245941,43.7597968197546));
#47046=CARTESIAN_POINT('Ctrl Pts',(82.3653300504053,332.09229822206,48.3290231145748));
#47047=CARTESIAN_POINT('Ctrl Pts',(83.1974205860366,331.667986202955,53.7167020463484));
#47048=CARTESIAN_POINT('Ctrl Pts',(81.4728272659272,331.243674183851,58.8882817674393));
#47049=CARTESIAN_POINT('Ctrl Pts',(74.871741736091,330.71328415997,62.39934478027));
#47050=CARTESIAN_POINT('Ctrl Pts',(67.0308319601666,330.076816131312,57.9829774858364));
#47051=CARTESIAN_POINT('Ctrl Pts',(66.5182045234311,329.440348102657,49.0157853683406));
#47052=CARTESIAN_POINT('Ctrl Pts',(73.7763034444097,328.803880073998,43.7249138508815));
#47053=CARTESIAN_POINT('Ctrl Pts',(82.1637083950636,328.167412045343,46.9861412865685));
#47054=CARTESIAN_POINT('Ctrl Pts',(83.6356998168977,327.637022021461,54.316566574799));
#47055=CARTESIAN_POINT('Ctrl Pts',(80.7310751922223,327.212710002357,58.929875010303));
#47056=CARTESIAN_POINT('Ctrl Pts',(76.0378631809033,326.788397983252,61.7035404458194));
#47057=CARTESIAN_POINT('Ctrl Pts',(68.7517592205485,326.258007959371,60.0258686271432));
#47058=CARTESIAN_POINT('Ctrl Pts',(65.7278275580644,325.621539930714,51.5500203808521));
#47059=CARTESIAN_POINT('Ctrl Pts',(71.2208322668849,324.985071902058,44.4436696556311));
#47060=CARTESIAN_POINT('Ctrl Pts',(80.1700495252707,324.3486038734,45.208412634144));
#47061=CARTESIAN_POINT('Ctrl Pts',(84.364040928706,323.712135844744,53.1704853731638));
#47062=CARTESIAN_POINT('Ctrl Pts',(80.6686270260788,323.181745820862,59.6701630375215));
#47063=CARTESIAN_POINT('Ctrl Pts',(75.4505684539656,322.757433801758,61.2485557862883));
#47064=CARTESIAN_POINT('Ctrl Pts',(70.0884361107281,322.333121782653,60.2651964089632));
#47065=CARTESIAN_POINT('Ctrl Pts',(65.6875426553555,321.802731758773,54.2208576985052));
#47066=CARTESIAN_POINT('Ctrl Pts',(68.9623313898591,321.166263730115,45.8387383401391));
#47067=CARTESIAN_POINT('Ctrl Pts',(77.7693672924811,320.529795701459,44.0753779201171));
#47068=CARTESIAN_POINT('Ctrl Pts',(84.0245397640824,319.893327672802,50.5210073472171));
#47069=CARTESIAN_POINT('Ctrl Pts',(81.9700399621623,319.256859644145,59.2824682275405));
#47070=CARTESIAN_POINT('Ctrl Pts',(74.917992817877,318.726469620264,61.7665223185493));
#47071=CARTESIAN_POINT('Ctrl Pts',(69.9433762093293,318.302157601159,59.536578702821));
#47072=CARTESIAN_POINT('Ctrl Pts',(66.5397963443308,317.877845582055,55.2780457354786));
#47073=CARTESIAN_POINT('Ctrl Pts',(67.1805741364608,317.347455558174,47.8287976208435));
#47074=CARTESIAN_POINT('Ctrl Pts',(75.1494197109682,316.710987529517,43.6476893463325));
#47075=CARTESIAN_POINT('Ctrl Pts',(82.9549932889592,316.07451950086,48.0913750327353));
#47076=CARTESIAN_POINT('Ctrl Pts',(83.4510538437739,315.438051472203,57.0594988770483));
#47077=CARTESIAN_POINT('Ctrl Pts',(76.1547784530625,314.801583443546,62.3271863788299));
#47078=CARTESIAN_POINT('Ctrl Pts',(69.201637942207,314.271193419666,59.5784174382707));
#47079=CARTESIAN_POINT('Ctrl Pts',(66.9080513766019,313.846881400561,54.6328214582659));
#47080=CARTESIAN_POINT('Ctrl Pts',(67.130795872377,313.422569381456,49.1858182619233));
#47081=CARTESIAN_POINT('Ctrl Pts',(72.4992604523953,312.892179357576,43.9818311649589));
#47082=CARTESIAN_POINT('Ctrl Pts',(81.2573869801701,312.255711328918,46.050498832085));
#47083=CARTESIAN_POINT('Ctrl Pts',(84.2367264765035,311.619243300262,54.5238014660385));
#47084=CARTESIAN_POINT('Ctrl Pts',(78.7306028558601,310.982775271604,61.6199922776759));
#47085=CARTESIAN_POINT('Ctrl Pts',(69.767764865774,310.346307242948,60.8127120555743));
#47086=CARTESIAN_POINT('Ctrl Pts',(66.3206060972866,309.815917219067,54.1780311983573));
#47087=CARTESIAN_POINT('Ctrl Pts',(67.8319189521616,309.391605199962,48.9401506741324));
#47088=CARTESIAN_POINT('Ctrl Pts',(71.5718418442326,308.967293180858,44.9737372195454));
#47089=CARTESIAN_POINT('Ctrl Pts',(79.0374175729379,308.436903156977,44.5649919550533));
#47090=CARTESIAN_POINT('Ctrl Pts',(84.2932973842717,307.80043512832,51.8697776194207));
#47091=CARTESIAN_POINT('Ctrl Pts',(80.9865109093489,307.163967099662,60.2207347244622));
#47092=CARTESIAN_POINT('Ctrl Pts',(72.1762324002069,306.527499071007,61.9678220011371));
#47093=CARTESIAN_POINT('Ctrl Pts',(65.9386691644986,305.891031042348,55.4811455737152));
#47094=CARTESIAN_POINT('Ctrl Pts',(67.6866179108752,305.360641018469,48.2115810178204));
#47095=CARTESIAN_POINT('Ctrl Pts',(72.2622790062819,304.936328999363,45.2480047202793));
#47096=CARTESIAN_POINT('Ctrl Pts',(77.6867985749163,304.512016980259,44.7057442838956));
#47097=CARTESIAN_POINT('Ctrl Pts',(83.5913144144231,303.981626956378,49.2925281629657));
#47098=CARTESIAN_POINT('Ctrl Pts',(82.7695389938667,303.345158927721,58.2540487566874));
#47099=CARTESIAN_POINT('Ctrl Pts',(74.7969691643367,302.708690899064,62.3906478035181));
#47100=CARTESIAN_POINT('Ctrl Pts',(66.9996181792322,302.072222870408,57.9325496691043));
#47101=CARTESIAN_POINT('Ctrl Pts',(66.5437682104894,301.43575484175,48.9449823119422));
#47102=CARTESIAN_POINT('Ctrl Pts',(72.6303204709577,300.90536481787,44.602658598437));
#47103=CARTESIAN_POINT('Ctrl Pts',(78.028232009396,300.481052798765,45.365554367569));
#47104=CARTESIAN_POINT('Ctrl Pts',(82.4793053786608,300.05674077966,48.5131573909484));
#47105=CARTESIAN_POINT('Ctrl Pts',(83.9295177772661,299.52635075578,55.8479223940833));
#47106=CARTESIAN_POINT('Ctrl Pts',(77.4327613662142,298.889882727122,62.074986094495));
#47107=CARTESIAN_POINT('Ctrl Pts',(68.7010089731946,298.253414698466,59.9702719789989));
#47108=CARTESIAN_POINT('Ctrl Pts',(65.7373281557615,297.616946669808,51.4914797670529));
#47109=CARTESIAN_POINT('Ctrl Pts',(71.2865603157941,296.980478641152,44.4069763527274));
#47110=CARTESIAN_POINT('Ctrl Pts',(78.7292737431128,296.450088617271,45.1196547451927));
#47111=CARTESIAN_POINT('Ctrl Pts',(82.3044309221991,296.025776598167,49.2351996758424));
#47112=CARTESIAN_POINT('Ctrl Pts',(83.6010089300926,295.601464579062,54.5303242636882));
#47113=CARTESIAN_POINT('Ctrl Pts',(79.8863062500415,295.071074555181,61.0189972906718));
#47114=CARTESIAN_POINT('Ctrl Pts',(70.8980133686167,294.434606526524,61.4603104122333));
#47115=CARTESIAN_POINT('Ctrl Pts',(65.6856826182534,293.798138497867,54.1456040264796));
#47116=CARTESIAN_POINT('Ctrl Pts',(69.0078910237733,293.16167046921,45.8007701353069));
#47117=CARTESIAN_POINT('Ctrl Pts',(77.8430526165225,292.525202440553,44.0907742804756));
#47118=CARTESIAN_POINT('Ctrl Pts',(82.9949588197056,291.994812416672,49.5092386501921));
#47119=CARTESIAN_POINT('Ctrl Pts',(82.9955159782755,291.570500397568,54.9607942649627));
#47120=CARTESIAN_POINT('Ctrl Pts',(80.5022686396504,291.146188378463,59.8088017566861));
#47121=CARTESIAN_POINT('Ctrl Pts',(73.442874565269,290.615798354583,62.2718991877407));
#47122=CARTESIAN_POINT('Ctrl Pts',(66.3673555967205,289.979330325925,56.711215999567));
#47123=CARTESIAN_POINT('Ctrl Pts',(67.2285157374899,289.342862297269,47.7707616166553));
#47124=CARTESIAN_POINT('Ctrl Pts',(75.2087139229012,288.706394268612,43.6488981688282));
#47125=CARTESIAN_POINT('Ctrl Pts',(83.0005296951049,288.069926239954,48.1513167594931));
#47126=CARTESIAN_POINT('Ctrl Pts',(83.3371677688902,287.539536216074,55.6204913095729));
#47127=CARTESIAN_POINT('Ctrl Pts',(79.7628518963391,287.115224196969,59.73676692894));
#47128=CARTESIAN_POINT('Ctrl Pts',(74.7014834086863,286.690912177865,61.7621083726375));
#47129=CARTESIAN_POINT('Ctrl Pts',(67.7565378491218,286.160522153984,58.9926996222055));
#47130=CARTESIAN_POINT('Ctrl Pts',(66.0608339848255,285.524054125327,50.1547838838573));
#47131=CARTESIAN_POINT('Ctrl Pts',(72.5735120570497,284.88758609667,43.9694507733014));
#47132=CARTESIAN_POINT('Ctrl Pts',(81.3013612970727,284.251118068013,46.090292352582));
#47133=CARTESIAN_POINT('Ctrl Pts',(84.2318008882829,283.614650039356,54.5989168005053));
#47134=CARTESIAN_POINT('Ctrl Pts',(79.5882164210452,283.084260015475,60.4588670518221));
#47135=CARTESIAN_POINT('Ctrl Pts',(74.190460933948,282.659947996371,61.2228661571073));
#47136=CARTESIAN_POINT('Ctrl Pts',(69.0410682497914,282.235635977266,59.433113683797));
#47137=CARTESIAN_POINT('Ctrl Pts',(65.6136307451155,281.705245953385,52.7882234812563));
#47138=CARTESIAN_POINT('Ctrl Pts',(70.1286457211821,281.068777924728,45.0036999917018));
#47139=CARTESIAN_POINT('Ctrl Pts',(79.1015955077365,280.432309896071,44.6043336323989));
#47140=CARTESIAN_POINT('Ctrl Pts',(84.3004041615478,279.795841867414,51.9286568053638));
#47141=CARTESIAN_POINT('Ctrl Pts',(80.9335368906759,279.159373838757,60.2742167610446));
#47142=CARTESIAN_POINT('Ctrl Pts',(73.585110486313,278.628983814877,61.6535365325057));
#47143=CARTESIAN_POINT('Ctrl Pts',(69.0088437210826,278.204671795772,58.6908955780847));
#47144=CARTESIAN_POINT('Ctrl Pts',(66.2946561082543,277.780359776667,53.9630372327307));
#47145=CARTESIAN_POINT('Ctrl Pts',(68.0641889088541,277.249969752787,46.6986964285089));
#47146=CARTESIAN_POINT('Ctrl Pts',(76.5775418425126,276.613501724129,43.7820222916706));
#47147=CARTESIAN_POINT('Ctrl Pts',(83.6139711566449,275.977033695473,49.3643142822595));
#47148=CARTESIAN_POINT('Ctrl Pts',(82.7362958735918,275.340565666816,58.3031624999266));
#47149=CARTESIAN_POINT('Ctrl Pts',(74.7219042606049,274.704097638158,62.3962900653973));
#47150=CARTESIAN_POINT('Ctrl Pts',(68.2694031771755,274.173707614279,58.6191054762326));
#47151=CARTESIAN_POINT('Ctrl Pts',(66.7570197126837,273.749395595173,53.3815339790885));
#47152=CARTESIAN_POINT('Ctrl Pts',(67.8080032551739,273.32508357607,48.0322450053293));
#47153=CARTESIAN_POINT('Ctrl Pts',(73.9074260611533,272.794693552187,43.7080184749338));
#47154=CARTESIAN_POINT('Ctrl Pts',(82.247529620235,272.158225523532,47.0883792274754));
#47155=CARTESIAN_POINT('Ctrl Pts',(83.8995514050742,271.521757494873,55.9169773825275));
#47156=CARTESIAN_POINT('Ctrl Pts',(77.375457650676,270.885289466217,62.090268404729));
#47157=CARTESIAN_POINT('Ctrl Pts',(68.6406353786743,270.24882143756,59.9253097284314));
#47158=CARTESIAN_POINT('Ctrl Pts',(66.2458187949878,269.718431413679,52.8424609242579));
#47159=CARTESIAN_POINT('Ctrl Pts',(68.5383944154785,269.294119394575,47.8963962304133));
#47160=CARTESIAN_POINT('Ctrl Pts',(72.8395616968912,268.86980737547,44.5468561203877));
#47161=CARTESIAN_POINT('Ctrl Pts',(80.2801255265928,268.339417351589,45.2816374133041));
#47162=CARTESIAN_POINT('Ctrl Pts',(84.360285475917,267.702949322933,53.3026386588755));
#47163=CARTESIAN_POINT('Ctrl Pts',(79.8184004420758,267.066481294275,61.0514838438268));
#47164=CARTESIAN_POINT('Ctrl Pts',(70.8447281772513,266.430013265619,61.4342728777548));
#47165=CARTESIAN_POINT('Ctrl Pts',(65.6695837090906,265.793545236961,54.0720690007085));
#47166=CARTESIAN_POINT('Ctrl Pts',(68.5059242394298,265.263155213081,47.1541888305816));
#47167=CARTESIAN_POINT('Ctrl Pts',(73.4800849357431,264.838843193976,44.9232284323187));
#47168=CARTESIAN_POINT('Ctrl Pts',(78.9238415588416,264.414531174872,45.2147293068233));
#47169=CARTESIAN_POINT('Ctrl Pts',(84.0596313353204,263.88414115099,50.6484717578505));
#47170=CARTESIAN_POINT('Ctrl Pts',(81.8805480228633,263.247673122334,59.3797810589176));
#47171=CARTESIAN_POINT('Ctrl Pts',(73.3703035215419,262.611205093677,62.2518987251529));
#47172=CARTESIAN_POINT('Ctrl Pts',(66.3441989511637,261.97473706502,56.6566171480483));
#47173=CARTESIAN_POINT('Ctrl Pts',(67.2645800631255,261.338269036363,47.7046863617726));
#47174=CARTESIAN_POINT('Ctrl Pts',(73.9422560569281,260.807879012482,44.3415721838004));
#47175=CARTESIAN_POINT('Ctrl Pts',(79.1606371490594,260.383566993378,45.9188983100824));
#47176=CARTESIAN_POINT('Ctrl Pts',(83.0795139809074,259.959254974273,49.7086032205166));
#47177=CARTESIAN_POINT('Ctrl Pts',(83.3939659320291,259.428864950392,57.1787446932546));
#47178=CARTESIAN_POINT('Ctrl Pts',(76.0234015441845,258.792396921735,62.3419749610388));
#47179=CARTESIAN_POINT('Ctrl Pts',(67.7148617594967,258.155928893078,58.9300124748392));
#47180=CARTESIAN_POINT('Ctrl Pts',(66.0791527621555,257.519460864421,50.0983774372604));
#47181=CARTESIAN_POINT('Ctrl Pts',(72.6440679098571,256.882992835764,43.9432125087627));
#47182=CARTESIAN_POINT('Ctrl Pts',(79.8909833080085,256.352602811884,45.7828078078208));
#47183=CARTESIAN_POINT('Ctrl Pts',(82.796550848464,255.928290792779,50.3955224314691));
#47184=CARTESIAN_POINT('Ctrl Pts',(83.2702778056452,255.503978773674,55.8264562095043));
#47185=CARTESIAN_POINT('Ctrl Pts',(78.6093088355845,254.973588749794,61.6725884276815));
#47186=CARTESIAN_POINT('Ctrl Pts',(69.6588783577597,254.337120721137,60.7377299062148));
#47187=CARTESIAN_POINT('Ctrl Pts',(65.6232711108373,253.70065269248,52.7135666782166));
#47188=CARTESIAN_POINT('Ctrl Pts',(70.1794636249799,253.064184663823,44.9731254030021));
#47189=CARTESIAN_POINT('Ctrl Pts',(79.1720701519117,252.427716635165,44.6307892446532));
#47190=CARTESIAN_POINT('Ctrl Pts',(83.437198618748,251.897326611285,50.771682731245));
#47191=CARTESIAN_POINT('Ctrl Pts',(82.6062093610088,251.47301459218,56.159531632698));
#47192=CARTESIAN_POINT('Ctrl Pts',(79.4026577641557,251.048702573076,60.5705084063462));
#47193=CARTESIAN_POINT('Ctrl Pts',(72.0501669738483,250.518312549195,61.9279960971656));
#47194=CARTESIAN_POINT('Ctrl Pts',(65.9056280140869,249.881844520538,55.3531343369834));
#47195=CARTESIAN_POINT('Ctrl Pts',(68.1204219004477,249.245376491881,46.6486521925987));
#47196=CARTESIAN_POINT('Ctrl Pts',(76.6359578349168,248.608908463224,43.7922612687687));
#47197=CARTESIAN_POINT('Ctrl Pts',(83.6498316490372,247.972440434567,49.4305003833438));
#47198=CARTESIAN_POINT('Ctrl Pts',(82.8432379943956,247.442050410686,56.863622226054));
#47199=CARTESIAN_POINT('Ctrl Pts',(78.6828810081231,247.017738391582,60.3865313475242));
#47200=CARTESIAN_POINT('Ctrl Pts',(73.3718078452896,246.593426372477,61.6161494957285));
#47201=CARTESIAN_POINT('Ctrl Pts',(66.9305540631015,246.063036348596,57.8198166117822));
#47202=CARTESIAN_POINT('Ctrl Pts',(66.602762753682,245.426568319939,48.8266681613785));
#47203=CARTESIAN_POINT('Ctrl Pts',(73.9826972194987,244.790100291282,43.7071087427155));
#47204=CARTESIAN_POINT('Ctrl Pts',(82.2849195603449,244.153632262626,47.1344146181999));
#47205=CARTESIAN_POINT('Ctrl Pts',(83.8832259174092,243.517164233968,55.9904624377692));
#47206=CARTESIAN_POINT('Ctrl Pts',(78.4001452382172,242.986774210088,61.0735441720867));
#47207=CARTESIAN_POINT('Ctrl Pts',(72.9490171417447,242.562462190983,61.0052696731008));
#47208=CARTESIAN_POINT('Ctrl Pts',(68.1328759584309,242.138150171878,58.4510098911372));
#47209=CARTESIAN_POINT('Ctrl Pts',(65.7591071269122,241.607760147998,51.3610793423386));
#47210=CARTESIAN_POINT('Ctrl Pts',(71.4086829187869,240.971292119341,44.3563338390819));
#47211=CARTESIAN_POINT('Ctrl Pts',(80.3375515915834,240.334824090684,45.3303079583086));
#47212=CARTESIAN_POINT('Ctrl Pts',(84.3583280981011,239.698356062027,53.3619128817103));
#47213=CARTESIAN_POINT('Ctrl Pts',(79.7578885484422,239.06188803337,61.0962597929539));
#47214=CARTESIAN_POINT('Ctrl Pts',(72.2850589701853,238.531498009489,61.3385648622608));
#47215=CARTESIAN_POINT('Ctrl Pts',(68.2142409568424,238.107185990385,57.7125616033534));
#47216=CARTESIAN_POINT('Ctrl Pts',(66.2529660476571,237.68287397128,52.6260245041113));
#47217=CARTESIAN_POINT('Ctrl Pts',(69.1098412727704,237.152483947399,45.7165992313107));
#47218=CARTESIAN_POINT('Ctrl Pts',(77.9684625670151,236.516015918742,44.1326184995208));
#47219=CARTESIAN_POINT('Ctrl Pts',(84.0710732356509,235.879547890085,50.7228737592228));
#47220=CARTESIAN_POINT('Ctrl Pts',(81.8402024524585,235.243079861428,59.4232494355754));
#47221=CARTESIAN_POINT('Ctrl Pts',(73.295256365372,234.606611832771,62.2460251195998));
#47222=CARTESIAN_POINT('Ctrl Pts',(67.4944033500437,234.076221808891,57.5288227763841));
#47223=CARTESIAN_POINT('Ctrl Pts',(66.7986174745077,233.651909789786,52.1218512629794));
#47224=CARTESIAN_POINT('Ctrl Pts',(68.6532437724353,233.227597770681,46.9954665499086));
#47225=CARTESIAN_POINT('Ctrl Pts',(75.3408792960931,232.697207746801,43.6522009674354));
#47226=CARTESIAN_POINT('Ctrl Pts',(83.0677754633829,232.060739718143,48.2651438256912));
#47227=CARTESIAN_POINT('Ctrl Pts',(83.3538170768646,231.424271689487,57.2424207823375));
#47228=CARTESIAN_POINT('Ctrl Pts',(75.9644373210915,230.787803660829,62.3483377602821));
#47229=CARTESIAN_POINT('Ctrl Pts',(67.6620528386393,230.151335632173,58.8763674119568));
#47230=CARTESIAN_POINT('Ctrl Pts',(66.3756246135881,229.620945608292,51.5111114032393));
#47231=CARTESIAN_POINT('Ctrl Pts',(69.3958095830978,229.196633589187,46.9726158727042));
#47232=CARTESIAN_POINT('Ctrl Pts',(74.1575605310016,228.772321570083,44.3183387878161));
#47233=CARTESIAN_POINT('Ctrl Pts',(81.3989800721073,228.241931546202,46.1794504652647));
#47234=CARTESIAN_POINT('Ctrl Pts',(84.2079316976986,227.605463517545,54.7289508578227));
#47235=CARTESIAN_POINT('Ctrl Pts',(78.5372423724498,226.968995488888,61.6943369888106));
#47236=CARTESIAN_POINT('Ctrl Pts',(69.6101882604234,226.332527460231,60.703869323161));
#47237=CARTESIAN_POINT('Ctrl Pts',(65.6185770686265,225.696059431574,52.6384365187058));
#47238=CARTESIAN_POINT('Ctrl Pts',(69.4769301814605,225.165669407694,46.2341406960417));
#47239=CARTESIAN_POINT('Ctrl Pts',(74.7331795982254,224.741357388588,44.788007625873));
#47240=CARTESIAN_POINT('Ctrl Pts',(80.0687724266707,224.317045369484,45.9064477808886));
#47241=CARTESIAN_POINT('Ctrl Pts',(84.3156425901752,223.786655345603,52.0599822937235));
#47242=CARTESIAN_POINT('Ctrl Pts',(80.8302488352503,223.150187316947,60.3567404403693));
#47243=CARTESIAN_POINT('Ctrl Pts',(71.9814957245066,222.513719288289,61.8971602273444));
#47244=CARTESIAN_POINT('Ctrl Pts',(65.8910706731163,221.877251259633,55.2956422237384));
#47245=CARTESIAN_POINT('Ctrl Pts',(68.1661423876409,221.240783230975,46.5888511265689));
#47246=CARTESIAN_POINT('Ctrl Pts',(75.2786649412196,220.710393207095,44.2836537842132));
#47247=CARTESIAN_POINT('Ctrl Pts',(80.1953873273415,220.28608118799,46.6384960022359));
#47248=CARTESIAN_POINT('Ctrl Pts',(83.4903573672587,219.861769168885,50.9816117272898));
#47249=CARTESIAN_POINT('Ctrl Pts',(82.6616815663088,219.331379145005,58.412305433049));
#47250=CARTESIAN_POINT('Ctrl Pts',(74.5898182217719,218.694911116348,62.3908659254138));
#47251=CARTESIAN_POINT('Ctrl Pts',(66.8989104837742,218.058443087691,57.7515067942423));
#47252=CARTESIAN_POINT('Ctrl Pts',(66.6295031705657,217.421975059034,48.773714540667));
#47253=CARTESIAN_POINT('Ctrl Pts',(74.0563658043794,216.785507030377,43.6919424072075));
#47254=CARTESIAN_POINT('Ctrl Pts',(80.9380581568106,216.255117006496,46.6153945638555));
#47255=CARTESIAN_POINT('Ctrl Pts',(83.1057762484532,215.830804987391,51.6173385382644));
#47256=CARTESIAN_POINT('Ctrl Pts',(82.7460769485554,215.406492968287,57.0569580266549));
#47257=CARTESIAN_POINT('Ctrl Pts',(77.246790500885,214.876102944406,62.1237819597051));
#47258=CARTESIAN_POINT('Ctrl Pts',(68.545751476127,214.239634915749,59.8345390185409));
#47259=CARTESIAN_POINT('Ctrl Pts',(65.7776657511149,213.603166887092,51.2888705940134));
#47260=CARTESIAN_POINT('Ctrl Pts',(71.467994410054,212.966698858435,44.333676878713));
#47261=CARTESIAN_POINT('Ctrl Pts',(80.3946783686388,212.330230829778,45.3675402002628));
#47262=CARTESIAN_POINT('Ctrl Pts',(84.3546705587473,211.693762801122,53.4303690622235));
#47263=CARTESIAN_POINT('Ctrl Pts',(79.7000908952398,211.057294772464,61.1299535646553));
#47264=CARTESIAN_POINT('Ctrl Pts',(72.2248594979382,210.526904748583,61.3190877996643));
#47265=CARTESIAN_POINT('Ctrl Pts',(68.1806921804899,210.102592729479,57.6634682251856));
#47266=CARTESIAN_POINT('Ctrl Pts',(66.2559726813135,209.678280710374,52.5630858770229));
#47267=CARTESIAN_POINT('Ctrl Pts',(69.1627565133466,209.147890686494,45.6743363606337));
#47268=CARTESIAN_POINT('Ctrl Pts',(78.0325037599698,208.511422657836,44.1543757101699));
#47269=CARTESIAN_POINT('Ctrl Pts',(84.0874436263853,207.87495462918,50.7884572037047));
#47270=CARTESIAN_POINT('Ctrl Pts',(81.7938378778077,207.238486600523,59.4725281184584));
#47271=CARTESIAN_POINT('Ctrl Pts',(73.2287589465603,206.602018571866,62.2335685646996));
#47272=CARTESIAN_POINT('Ctrl Pts',(67.4620855006973,206.071628547985,57.4746411749747));
#47273=CARTESIAN_POINT('Ctrl Pts',(66.8053318710369,205.64731652888,52.0627878477779));
#47274=CARTESIAN_POINT('Ctrl Pts',(68.69689543346,205.223004509776,46.9499189678551));
#47275=CARTESIAN_POINT('Ctrl Pts',(75.408479543298,204.692614485895,43.654990956662));
#47276=CARTESIAN_POINT('Ctrl Pts',(83.1018916223794,204.056146457238,48.3235638753832));
#47277=CARTESIAN_POINT('Ctrl Pts',(83.3231548698706,203.419678428581,57.3026707259473));
#47278=CARTESIAN_POINT('Ctrl Pts',(75.8971280409304,202.783210399924,62.3551404458827));
#47279=CARTESIAN_POINT('Ctrl Pts',(67.6200100548619,202.146742371267,58.8233585704684));
#47280=CARTESIAN_POINT('Ctrl Pts',(66.3867557005124,201.616352347387,51.4490127090517));
#47281=CARTESIAN_POINT('Ctrl Pts',(69.4396073911285,201.192040328282,46.9324259705503));
#47282=CARTESIAN_POINT('Ctrl Pts',(74.2203850355754,200.767728309177,44.3125740849968));
#47283=CARTESIAN_POINT('Ctrl Pts',(81.4481881519756,200.237338285296,46.225884263212));
#47284=CARTESIAN_POINT('Ctrl Pts',(84.1953818886021,199.600870256639,54.795428755371));
#47285=CARTESIAN_POINT('Ctrl Pts',(78.4745848027485,198.964402227983,61.7197194784877));
#47286=CARTESIAN_POINT('Ctrl Pts',(69.5549092843256,198.327934199325,60.6648687671083));
#47287=CARTESIAN_POINT('Ctrl Pts',(65.6215942106805,197.691466170669,52.570846359881));
#47288=CARTESIAN_POINT('Ctrl Pts',(69.5260539756305,197.161076146787,46.1945553070724));
#47289=CARTESIAN_POINT('Ctrl Pts',(74.7926004648802,196.736764127683,44.7863837941532));
#47290=CARTESIAN_POINT('Ctrl Pts',(80.1199848267535,196.312452108578,45.9432912198386));
#47291=CARTESIAN_POINT('Ctrl Pts',(84.3223466667195,195.782062084698,52.1273067937318));
#47292=CARTESIAN_POINT('Ctrl Pts',(80.7771822922816,195.145594056041,60.3987018243377));
#47293=CARTESIAN_POINT('Ctrl Pts',(71.9175455395786,194.509126027384,61.8752376250712));
#47294=CARTESIAN_POINT('Ctrl Pts',(65.8749087090707,193.872657998727,55.2299489559789));
#47295=CARTESIAN_POINT('Ctrl Pts',(68.2127415241208,193.236189970069,46.5397991343424));
#47296=CARTESIAN_POINT('Ctrl Pts',(75.3417097194792,192.705799946189,44.28597879505));
#47297=CARTESIAN_POINT('Ctrl Pts',(80.2413157837291,192.281487927084,46.676233874856));
#47298=CARTESIAN_POINT('Ctrl Pts',(83.5048607349508,191.85717590798,51.0430099491149));
#47299=CARTESIAN_POINT('Ctrl Pts',(82.6226020895228,191.326785884099,58.467531033659));
#47300=CARTESIAN_POINT('Ctrl Pts',(74.5222286308205,190.690317855442,62.3877499080446));
#47301=CARTESIAN_POINT('Ctrl Pts',(66.8650204224245,190.053849826785,57.6930205426558));
#47302=CARTESIAN_POINT('Ctrl Pts',(66.6603458363777,189.417381798128,48.7135200178606));
#47303=CARTESIAN_POINT('Ctrl Pts',(74.1237762701942,188.780913769471,43.6854615105328));
#47304=CARTESIAN_POINT('Ctrl Pts',(80.9840213044134,188.250523745591,46.658495604309));
#47305=CARTESIAN_POINT('Ctrl Pts',(83.1158544222917,187.826211726486,51.6759398231201));
#47306=CARTESIAN_POINT('Ctrl Pts',(82.7164059182478,187.401899707381,57.1128414981536));
#47307=CARTESIAN_POINT('Ctrl Pts',(77.1818381244577,186.8715096835,62.1398140451468));
#47308=CARTESIAN_POINT('Ctrl Pts',(68.4954808173363,186.235041654843,59.787929072078));
#47309=CARTESIAN_POINT('Ctrl Pts',(65.7927731055032,185.598573626187,51.2223764112526));
#47310=CARTESIAN_POINT('Ctrl Pts',(71.5263523783918,184.96210559753,44.3086661134114));
#47311=CARTESIAN_POINT('Ctrl Pts',(80.4582605987755,184.325637568872,45.4064738088519));
#47312=CARTESIAN_POINT('Ctrl Pts',(83.6882266308899,183.795247544992,52.1495601262344));
#47313=CARTESIAN_POINT('Ctrl Pts',(82.0076774577441,183.370935525887,57.3356196523102));
#47314=CARTESIAN_POINT('Ctrl Pts',(78.1409673484235,182.946623506783,61.1785367554813));
#47315=CARTESIAN_POINT('Ctrl Pts',(70.6660574864011,182.416233482902,61.3447180026869));
#47316=CARTESIAN_POINT('Ctrl Pts',(65.6500767081934,181.779765454245,53.8731650833682));
#47317=CARTESIAN_POINT('Ctrl Pts',(69.2262103655614,181.143297425588,45.6339545977931));
#47318=CARTESIAN_POINT('Ctrl Pts',(78.0885597547107,180.506829396931,44.1737886258499));
#47319=CARTESIAN_POINT('Ctrl Pts',(84.1122641563528,179.870361368274,50.8595310285428));
#47320=CARTESIAN_POINT('Ctrl Pts',(82.1292509872868,179.339971344393,58.0685221107672));
#47321=CARTESIAN_POINT('Ctrl Pts',(77.4597973815361,178.915659325288,60.8820007325289));
#47322=CARTESIAN_POINT('Ctrl Pts',(72.0205337842822,178.491347306184,61.2478838435807));
#47323=CARTESIAN_POINT('Ctrl Pts',(66.268026665914,177.960957282303,56.4718441132811));
#47324=CARTESIAN_POINT('Ctrl Pts',(67.3802791548321,177.324489253646,47.5417231401684));
#47325=CARTESIAN_POINT('Ctrl Pts',(75.4829300407876,176.688021224989,43.6661109328775));
#47326=CARTESIAN_POINT('Ctrl Pts',(83.1314521309226,176.051553196332,48.3749782274283));
#47327=CARTESIAN_POINT('Ctrl Pts',(83.2953061451401,175.415085167676,57.372606695839));
#47328=CARTESIAN_POINT('Ctrl Pts',(77.0710005685769,174.884695143794,61.5150593198097));
#47329=CARTESIAN_POINT('Ctrl Pts',(71.7006991468909,174.46038312469,60.5773378411154));
#47330=CARTESIAN_POINT('Ctrl Pts',(67.3541495885463,174.036071105585,57.2869023276584));
#47331=CARTESIAN_POINT('Ctrl Pts',(66.1428036994951,173.505681081705,49.9089259933674));
#47332=CARTESIAN_POINT('Ctrl Pts',(72.8382799358942,172.869213053048,43.8960428112868));
#47333=CARTESIAN_POINT('Ctrl Pts',(81.4971068633349,172.232745024391,46.2830990740509));
#47334=CARTESIAN_POINT('Ctrl Pts',(84.1839859454567,171.596276995734,54.8536301053831));
#47335=CARTESIAN_POINT('Ctrl Pts',(78.4077002508318,170.959808967077,61.7542597699573));
#47336=CARTESIAN_POINT('Ctrl Pts',(70.9920444572424,170.429418943196,60.8003505482352));
#47337=CARTESIAN_POINT('Ctrl Pts',(67.5523709208179,170.005106924091,56.5709173835918));
#47338=CARTESIAN_POINT('Ctrl Pts',(66.4283673509715,169.580794904987,51.2364938058905));
#47339=CARTESIAN_POINT('Ctrl Pts',(70.3517484936913,169.050404881106,44.8718277454255));
#47340=CARTESIAN_POINT('Ctrl Pts',(79.3496302067614,168.413936852449,44.7225264690454));
#47341=CARTESIAN_POINT('Ctrl Pts',(84.3217628279609,167.777468823792,52.2025811853009));
#47342=CARTESIAN_POINT('Ctrl Pts',(80.7304141405317,167.141000795135,60.4351710552188));
#47343=CARTESIAN_POINT('Ctrl Pts',(71.8443988490916,166.504532766478,61.8574573955251));
#47344=CARTESIAN_POINT('Ctrl Pts',(66.8711028478376,165.974142742598,56.2746068211148));
#47345=CARTESIAN_POINT('Ctrl Pts',(67.0475151664259,165.549830723493,50.8259062764698));
#47346=CARTESIAN_POINT('Ctrl Pts',(69.6968251956563,165.125518704388,46.0613900050752));
#47347=CARTESIAN_POINT('Ctrl Pts',(76.8324561509156,164.595128680507,43.8287537779593));
#47348=CARTESIAN_POINT('Ctrl Pts',(83.7237343798985,163.95866065185,49.6161928112686));
#47349=CARTESIAN_POINT('Ctrl Pts',(82.5728017822342,163.322192623194,58.5239801637262));
#47350=CARTESIAN_POINT('Ctrl Pts',(74.46300490994,162.685724594536,62.3846169053924));
#47351=CARTESIAN_POINT('Ctrl Pts',(66.8214538524927,162.04925656588,57.6316321978683));
#47352=CARTESIAN_POINT('Ctrl Pts',(66.7274586184903,161.518866541999,50.1554661651839));
#47353=CARTESIAN_POINT('Ctrl Pts',(70.4335138360439,161.094554522894,46.1573899208122));
#47354=CARTESIAN_POINT('Ctrl Pts',(75.5579617346419,160.670242503789,44.2974187742837));
#47355=CARTESIAN_POINT('Ctrl Pts',(82.4093461241096,160.139852479909,47.2908157743563));
#47356=CARTESIAN_POINT('Ctrl Pts',(83.8172586007792,159.503384451252,56.179119811211));
#47357=CARTESIAN_POINT('Ctrl Pts',(77.1072237588872,158.866916422595,62.1497775456292));
#47358=CARTESIAN_POINT('Ctrl Pts',(68.4528214593998,158.230448393938,59.7467290235218));
#47359=CARTESIAN_POINT('Ctrl Pts',(65.8001345025756,157.593980365281,51.1474605602964));
#47360=CARTESIAN_POINT('Ctrl Pts',(70.631498190644,157.0635903414,45.4413394113987));
#47361=CARTESIAN_POINT('Ctrl Pts',(76.0512099245549,156.639278322296,44.8529656758553));
#47362=CARTESIAN_POINT('Ctrl Pts',(81.1397894996918,156.214966303191,46.8089352152041));
#47363=CARTESIAN_POINT('Ctrl Pts',(84.3497132445386,155.68457627931,53.5615853027291));
#47364=CARTESIAN_POINT('Ctrl Pts',(79.5843755134694,155.048108250653,61.1954390151329));
#47365=CARTESIAN_POINT('Ctrl Pts',(70.6031904907703,154.411640221996,61.3033137063913));
#47366=CARTESIAN_POINT('Ctrl Pts',(65.6448850210462,153.775172193339,53.8140862275469));
#47367=CARTESIAN_POINT('Ctrl Pts',(69.280892606685,153.138704164683,45.5822203983009));
#47368=CARTESIAN_POINT('Ctrl Pts',(76.670221815505,152.608314140801,44.4421732519235));
#47369=CARTESIAN_POINT('Ctrl Pts',(81.1479030539253,152.184002121697,47.5518082238235));
#47370=CARTESIAN_POINT('Ctrl Pts',(83.7071837783121,151.759690102592,52.3652831749524));
#47371=CARTESIAN_POINT('Ctrl Pts',(81.7027675047384,151.229300078712,59.5683525939235));
#47372=CARTESIAN_POINT('Ctrl Pts',(73.099219904014,150.592832050055,62.2071278544567));
#47373=CARTESIAN_POINT('Ctrl Pts',(66.2477121959153,149.956364021397,56.3993603413037));
#47374=CARTESIAN_POINT('Ctrl Pts',(67.4150990922498,149.319895992741,47.4937144245136));
#47375=CARTESIAN_POINT('Ctrl Pts',(75.5581385426594,148.683427964083,43.6629084123797));
#47376=CARTESIAN_POINT('Ctrl Pts',(81.884623426692,148.153037940203,47.6475643152638));
#47377=CARTESIAN_POINT('Ctrl Pts',(83.2261870129823,147.728725921098,52.931470642528));
#47378=CARTESIAN_POINT('Ctrl Pts',(82.0021079857598,147.304413901994,58.2438231785031));
#47379=CARTESIAN_POINT('Ctrl Pts',(75.7655261202681,146.774023878113,62.3677703516982));
#47380=CARTESIAN_POINT('Ctrl Pts',(67.5395518392587,146.137555849456,58.7184535222492));
#47381=CARTESIAN_POINT('Ctrl Pts',(66.1749959513619,145.501087820799,49.8408801719592));
#47382=CARTESIAN_POINT('Ctrl Pts',(72.8960495469659,144.864619792142,43.8826287568211));
#47383=CARTESIAN_POINT('Ctrl Pts',(81.5559890678473,144.228151763485,46.3299974842915));
#47384=CARTESIAN_POINT('Ctrl Pts',(83.7196190431261,143.697761739604,53.4868542651944));
#47385=CARTESIAN_POINT('Ctrl Pts',(81.2676918241373,143.2734497205,58.3558902934191));
#47386=CARTESIAN_POINT('Ctrl Pts',(76.8600581518627,142.849137701395,61.5640399692282));
#47387=CARTESIAN_POINT('Ctrl Pts',(69.4472683305171,142.318747677514,60.5881092765891));
#47388=CARTESIAN_POINT('Ctrl Pts',(65.6296376629961,141.682279648857,52.4388846337205));
#47389=CARTESIAN_POINT('Ctrl Pts',(70.4206730961357,141.0458116202,44.8415626819159));
#47390=CARTESIAN_POINT('Ctrl Pts',(79.4020420808101,140.409343591544,44.7502800324071));
#47391=CARTESIAN_POINT('Ctrl Pts',(84.3354661478493,139.772875562886,52.2766000607004));
#47392=CARTESIAN_POINT('Ctrl Pts',(81.2760512437821,139.242485539006,59.0987605760395));
#47393=CARTESIAN_POINT('Ctrl Pts',(76.2320903429111,138.818173519901,61.1670732607779));
#47394=CARTESIAN_POINT('Ctrl Pts',(70.8006655095353,138.393861500797,60.6990100057015));
#47395=CARTESIAN_POINT('Ctrl Pts',(65.8439734003519,137.863471476916,55.1014125758177));
#47396=CARTESIAN_POINT('Ctrl Pts',(68.3053452812459,137.227003448259,46.4454426903871));
#47397=CARTESIAN_POINT('Ctrl Pts',(76.9043396893177,136.590535419602,43.8510995112914));
#47398=CARTESIAN_POINT('Ctrl Pts',(83.745106425328,135.954067390945,49.6715146016838));
#47399=CARTESIAN_POINT('Ctrl Pts',(82.534611519294,135.317599362288,58.588849869352));
#47400=CARTESIAN_POINT('Ctrl Pts',(75.7512809928387,134.787209338407,61.7334198910148));
#47401=CARTESIAN_POINT('Ctrl Pts',(70.586853554311,134.362897319302,59.9875252310921));
#47402=CARTESIAN_POINT('Ctrl Pts',(66.7930640514994,133.938585300198,56.0726024809321));
#47403=CARTESIAN_POINT('Ctrl Pts',(66.7212746356957,133.408195276317,48.5961902443));
#47404=CARTESIAN_POINT('Ctrl Pts',(74.2555640080234,132.77172724766,43.6749454985511));
#47405=CARTESIAN_POINT('Ctrl Pts',(82.4489652898005,132.135259219003,47.3548227786709));
#47406=CARTESIAN_POINT('Ctrl Pts',(83.7971184038797,131.498791190346,56.2349018628892));
#47407=CARTESIAN_POINT('Ctrl Pts',(77.0358533411102,130.862323161689,62.1737115874476));
#47408=CARTESIAN_POINT('Ctrl Pts',(69.8524745233392,130.331933137809,60.0998354067952));
#47409=CARTESIAN_POINT('Ctrl Pts',(67.0981769230303,129.907621118704,55.39523088991));
#47410=CARTESIAN_POINT('Ctrl Pts',(66.8009993906768,129.483309099599,49.9517812074355));
#47411=CARTESIAN_POINT('Ctrl Pts',(71.6492898563576,128.952919075718,44.2600351473352));
#47412=CARTESIAN_POINT('Ctrl Pts',(80.5646556385358,128.316451047062,45.4849511295538));
#47413=CARTESIAN_POINT('Ctrl Pts',(84.3376544397274,127.679983018405,53.6358898121339));
#47414=CARTESIAN_POINT('Ctrl Pts',(79.5325918757471,127.043514989748,61.2243478318641));
#47415=CARTESIAN_POINT('Ctrl Pts',(70.5336117950437,126.407046961091,61.2745842791024));
#47416=CARTESIAN_POINT('Ctrl Pts',(66.4700777659095,125.87665693721,54.9984720393197));
#47417=CARTESIAN_POINT('Ctrl Pts',(67.475530190837,125.452344918105,49.6404384118989));
#47418=CARTESIAN_POINT('Ctrl Pts',(70.8205831694898,125.028032899,45.3357805275401));
#47419=CARTESIAN_POINT('Ctrl Pts',(78.2132659060374,124.49764287512,44.2176858942317));
#47420=CARTESIAN_POINT('Ctrl Pts',(84.1411323737424,123.861174846463,50.9885473855479));
#47421=CARTESIAN_POINT('Ctrl Pts',(81.6449396066654,123.224706817806,59.6165450113336));
#47422=CARTESIAN_POINT('Ctrl Pts',(73.0411670779897,122.588238789149,62.1949979652921));
#47423=CARTESIAN_POINT('Ctrl Pts',(66.2140191459775,121.951770760492,56.3320450140946));
#47424=CARTESIAN_POINT('Ctrl Pts',(67.2614827699121,121.421380736611,48.9290244407872));
#47425=CARTESIAN_POINT('Ctrl Pts',(71.5340082887178,120.997068717507,45.5430261208643));
#47426=CARTESIAN_POINT('Ctrl Pts',(76.8821983753521,120.572756698402,44.4864648455043));
#47427=CARTESIAN_POINT('Ctrl Pts',(83.1968202911535,120.042366674521,48.4898938398491));
#47428=CARTESIAN_POINT('Ctrl Pts',(83.2325019630988,119.405898645864,57.4889434014319));
#47429=CARTESIAN_POINT('Ctrl Pts',(75.690265100545,118.769430617208,62.3662361412734));
#47430=CARTESIAN_POINT('Ctrl Pts',(67.5036760124128,118.13296258855,58.6712286361326));
#47431=CARTESIAN_POINT('Ctrl Pts',(66.1936983173821,117.496494559894,49.7679638061925));
#47432=CARTESIAN_POINT('Ctrl Pts',(71.8388969564375,116.966104536013,44.8655535848941));
#47433=CARTESIAN_POINT('Ctrl Pts',(77.2849357849202,116.541792516908,45.1107474062347));
#47434=CARTESIAN_POINT('Ctrl Pts',(82.0156219478191,116.117480497803,47.8200032744614));
#47435=CARTESIAN_POINT('Ctrl Pts',(84.1579853752027,115.587090473923,54.9832548125056));
#47436=CARTESIAN_POINT('Ctrl Pts',(78.2839980460653,114.950622445266,61.8009112317351));
#47437=CARTESIAN_POINT('Ctrl Pts',(69.3914524812726,114.314154416609,60.5376002094376));
#47438=CARTESIAN_POINT('Ctrl Pts',(65.6335181775654,113.677686387952,52.3797051911137));
#47439=CARTESIAN_POINT('Ctrl Pts',(70.4826066212365,113.041218359295,44.798774677055));
#47440=CARTESIAN_POINT('Ctrl Pts',(77.9593635041953,112.510828335414,44.7991813808552));
#47441=CARTESIAN_POINT('Ctrl Pts',(81.9103282168794,112.086516316309,48.5554210923868));
#47442=CARTESIAN_POINT('Ctrl Pts',(83.7054495670612,111.662204297205,53.7029446007828));
#47443=CARTESIAN_POINT('Ctrl Pts',(80.6257852548025,111.131814273324,60.5159880745971));
#47444=CARTESIAN_POINT('Ctrl Pts',(71.720413347007,110.495346244667,61.8115641539429));
#47445=CARTESIAN_POINT('Ctrl Pts',(65.8349527787794,109.85887821601,55.0266783582341));
#47446=CARTESIAN_POINT('Ctrl Pts',(68.3470806648557,109.222410187353,46.4033069267711));
#47447=CARTESIAN_POINT('Ctrl Pts',(76.9791566232342,108.585942158696,43.8594062128452));
#47448=CARTESIAN_POINT('Ctrl Pts',(82.6238218883199,108.055552134816,48.7624305547607));
#47449=CARTESIAN_POINT('Ctrl Pts',(83.1437191728509,107.631240115711,54.1891391101288));
#47450=CARTESIAN_POINT('Ctrl Pts',(81.1236568876865,107.206928096606,59.2526168967316));
#47451=CARTESIAN_POINT('Ctrl Pts',(74.3310164083526,106.676538072725,62.3770254760937));
#47452=CARTESIAN_POINT('Ctrl Pts',(66.7579385956598,106.040070044068,57.5156821806215));
#47453=CARTESIAN_POINT('Ctrl Pts',(66.7634693934056,105.403602015411,48.5338510326177));
#47454=CARTESIAN_POINT('Ctrl Pts',(74.3147037050667,104.767133986755,43.6705001578233));
#47455=CARTESIAN_POINT('Ctrl Pts',(82.5000049447651,104.130665958098,47.4101538595609));
#47456=CARTESIAN_POINT('Ctrl Pts',(83.5466631767871,103.600275934217,54.813288344198));
#47457=CARTESIAN_POINT('Ctrl Pts',(80.3807406526305,103.175963915112,59.2513502525542));
#47458=CARTESIAN_POINT('Ctrl Pts',(75.5353357858924,102.751651896008,61.7496517973554));
#47459=CARTESIAN_POINT('Ctrl Pts',(68.3581483960137,102.221261872127,59.6544489854898));
#47460=CARTESIAN_POINT('Ctrl Pts',(65.8282122980566,101.58479384347,51.0182698804815));
#47461=CARTESIAN_POINT('Ctrl Pts',(71.7220243420383,100.948325814813,44.2406374803592));
#47462=CARTESIAN_POINT('Ctrl Pts',(80.6122208890652,100.311857786156,45.5203744518521));
#47463=CARTESIAN_POINT('Ctrl Pts',(84.3399071186501,99.6753897574987,53.7111327541886));
#47464=CARTESIAN_POINT('Ctrl Pts',(80.2756903258973,99.1449997336185,59.9868028788675));
#47465=CARTESIAN_POINT('Ctrl Pts',(74.975266539261,98.7206877145133,61.2615446619069));
#47466=CARTESIAN_POINT('Ctrl Pts',(69.6787927430372,98.2963756954092,59.9704891800327));
#47467=CARTESIAN_POINT('Ctrl Pts',(65.6339176906133,97.765985671528,53.6823352806308));
#47468=CARTESIAN_POINT('Ctrl Pts',(69.3868051882764,97.1295176428713,45.5030931627196));
#47469=CARTESIAN_POINT('Ctrl Pts',(78.2808998424165,96.4930496142142,44.2507347299335));
#47470=CARTESIAN_POINT('Ctrl Pts',(84.1538159569591,95.8565815855574,51.0464817582238));
#47471=CARTESIAN_POINT('Ctrl Pts',(81.5973014851276,95.2201135569003,59.6748303805756));
#47472=CARTESIAN_POINT('Ctrl Pts',(74.4136970897655,94.6897235330197,61.7479250583973));
#47473=CARTESIAN_POINT('Ctrl Pts',(69.57600733628,94.265411513915,59.234716595021));
#47474=CARTESIAN_POINT('Ctrl Pts',(66.4237643903003,93.8410994948103,54.786928005071));
#47475=CARTESIAN_POINT('Ctrl Pts',(67.4932115438736,93.3107094709297,47.387051219746));
#47476=CARTESIAN_POINT('Ctrl Pts',(75.6899881930776,92.6742414422725,43.6726173790922));
#47477=CARTESIAN_POINT('Ctrl Pts',(83.2262126967134,92.0377734136157,48.5591950763949));
#47478=CARTESIAN_POINT('Ctrl Pts',(83.2040888570857,91.4013053849587,57.5410006797626));
#47479=CARTESIAN_POINT('Ctrl Pts',(75.6160791065193,90.7648373563018,62.3790038028331));
#47480=CARTESIAN_POINT('Ctrl Pts',(68.8330907226962,90.234447332421,59.2336958310749));
#47481=CARTESIAN_POINT('Ctrl Pts',(66.8286282087238,89.8101353133163,54.1640223739926));
#47482=CARTESIAN_POINT('Ctrl Pts',(67.365231594555,89.3858232942118,48.7389402789752));
#47483=CARTESIAN_POINT('Ctrl Pts',(73.0249662720164,88.8554332703308,43.8533188207551));
#47484=CARTESIAN_POINT('Ctrl Pts',(81.64916877083,88.2189652416742,46.4237852089792));
#47485=CARTESIAN_POINT('Ctrl Pts',(84.1347338179463,87.582497213017,55.0548504826013));
#47486=CARTESIAN_POINT('Ctrl Pts',(78.2284108209353,86.9460291843602,61.8215830778757));
#47487=CARTESIAN_POINT('Ctrl Pts',(69.3270701386897,86.3095611557031,60.4985939425711));
#47488=CARTESIAN_POINT('Ctrl Pts',(66.2683974458044,85.7791711318225,53.6761006292671));
#47489=CARTESIAN_POINT('Ctrl Pts',(68.0793592558839,85.3548591127177,48.534128609332));
#47490=CARTESIAN_POINT('Ctrl Pts',(72.041870516237,84.9305470936133,44.7900715260408));
#47491=CARTESIAN_POINT('Ctrl Pts',(79.5185932117496,84.4001570697323,44.8126853865582));
#47492=CARTESIAN_POINT('Ctrl Pts',(84.3443173630294,83.7636890410754,52.4085100691904));
#47493=CARTESIAN_POINT('Ctrl Pts',(80.5612831190361,83.1272210124184,60.5547959265457));
#47494=CARTESIAN_POINT('Ctrl Pts',(71.6648900329446,82.4907529837615,61.7907212554865));
#47495=CARTESIAN_POINT('Ctrl Pts',(65.8119217712407,81.8542849551046,54.9550114371124));
#47496=CARTESIAN_POINT('Ctrl Pts',(67.9763303389007,81.3238949312238,47.798390083113));
#47497=CARTESIAN_POINT('Ctrl Pts',(72.7153357424512,80.8995829121191,45.1037126039912));
#47498=CARTESIAN_POINT('Ctrl Pts',(78.1621036964017,80.4752708930144,44.8752880274158));
#47499=CARTESIAN_POINT('Ctrl Pts',(83.7921813002151,79.9448808691338,49.7950562970919));
#47500=CARTESIAN_POINT('Ctrl Pts',(82.4547971050774,79.3084128404767,58.6942455696115));
#47501=CARTESIAN_POINT('Ctrl Pts',(74.256870076961,78.6719448118199,62.3640294600686));
#47502=CARTESIAN_POINT('Ctrl Pts',(66.7296859060944,78.0354767831629,57.4635376665013));
#47503=CARTESIAN_POINT('Ctrl Pts',(66.7930750347046,77.3990087545059,48.4646406223128));
#47504=CARTESIAN_POINT('Ctrl Pts',(73.1199933779918,76.8686187306251,44.4806730107902));
#47505=CARTESIAN_POINT('Ctrl Pts',(78.4649050147291,76.4443067115205,45.5536960892167));
#47506=CARTESIAN_POINT('Ctrl Pts',(82.72698496152,76.0199946924159,48.952833253046));
#47507=CARTESIAN_POINT('Ctrl Pts',(83.7516500885383,75.489604668535,56.3590438245701));
#47508=CARTESIAN_POINT('Ctrl Pts',(76.9064827766719,74.8531366398783,62.2009485367414));
#47509=CARTESIAN_POINT('Ctrl Pts',(68.3106899580314,74.2166686112211,59.5960172171136));
#47510=CARTESIAN_POINT('Ctrl Pts',(65.8410741982038,73.5802005825644,50.9603748345353));
#47511=CARTESIAN_POINT('Ctrl Pts',(71.7897597135541,72.9437325539072,44.2077970428327));
#47512=CARTESIAN_POINT('Ctrl Pts',(79.1789648512062,72.4133425300267,45.3486480786734));
#47513=CARTESIAN_POINT('Ctrl Pts',(82.510748146959,71.9890305109218,49.6635848107129));
#47514=CARTESIAN_POINT('Ctrl Pts',(83.4996986871477,71.5647184918175,55.0246887791533));
#47515=CARTESIAN_POINT('Ctrl Pts',(79.4168600817985,71.0343284679364,61.2882598512299));
#47516=CARTESIAN_POINT('Ctrl Pts',(70.4180773315886,70.3978604392796,61.2103162302436));
#47517=CARTESIAN_POINT('Ctrl Pts',(65.6364020281329,69.7613924106226,53.6070996311131));
#47518=CARTESIAN_POINT('Ctrl Pts',(69.4344792799938,69.1249243819657,45.4678164593667));
#47519=CARTESIAN_POINT('Ctrl Pts',(78.3535742588854,68.4884563533086,44.2703562508269));
#47520=CARTESIAN_POINT('Ctrl Pts',(83.1843171408831,67.9580663294281,49.9770029772597));
#47521=CARTESIAN_POINT('Ctrl Pts',(82.8703809064456,67.5337543103232,55.4195118630653));
#47522=CARTESIAN_POINT('Ctrl Pts',(80.1016111182479,67.1094422912187,60.1156137349725));
#47523=CARTESIAN_POINT('Ctrl Pts',(72.9118809879765,66.5790522673378,62.1673628195703));
#47524=CARTESIAN_POINT('Ctrl Pts',(66.1689332730775,65.942584238681,56.2077636461637));
#47525=CARTESIAN_POINT('Ctrl Pts',(67.5444213185558,65.306116210024,47.3318775496817));
#47526=CARTESIAN_POINT('Ctrl Pts',(75.7491139228169,64.6696481813672,43.6772447869338));
#47527=CARTESIAN_POINT('Ctrl Pts',(83.2682153150902,64.03318015271,48.6216639081496));
#47528=CARTESIAN_POINT('Ctrl Pts',(83.1734067383262,63.5027901288294,56.0978196707095));
#47529=CARTESIAN_POINT('Ctrl Pts',(79.367581365659,63.0784781097246,60.0010429751245));
#47530=CARTESIAN_POINT('Ctrl Pts',(74.1978028836267,62.6541660906201,61.7310283444492));
#47531=CARTESIAN_POINT('Ctrl Pts',(67.424186484631,62.1237760667393,58.5655876908371));
#47532=CARTESIAN_POINT('Ctrl Pts',(66.2411533478682,61.4873080380824,49.6445676375667));
#47533=CARTESIAN_POINT('Ctrl Pts',(73.0998084272228,60.8508400094254,43.8452425161916));
#47534=CARTESIAN_POINT('Ctrl Pts',(81.6907742226954,60.2143719807683,46.4660492740419));
#47535=CARTESIAN_POINT('Ctrl Pts',(84.1254831361944,59.5779039521116,55.129556571901));
#47536=CARTESIAN_POINT('Ctrl Pts',(79.1515797976825,59.0475139282307,60.7118660609407));
#47537=CARTESIAN_POINT('Ctrl Pts',(73.7187395656729,58.6232019091261,61.16320401062));
#47538=CARTESIAN_POINT('Ctrl Pts',(68.6811708049024,58.1988898900216,59.0793710250198));
#47539=CARTESIAN_POINT('Ctrl Pts',(65.6427754951433,57.6684998661406,52.2478230603257));
#47540=CARTESIAN_POINT('Ctrl Pts',(70.5993493427058,57.0320318374837,44.7367284738365));
#47541=CARTESIAN_POINT('Ctrl Pts',(79.5803947011489,56.3955638088268,44.8556638788466));
#47542=CARTESIAN_POINT('Ctrl Pts',(84.3480156486463,55.7590957801698,52.4677011791989));
#47543=CARTESIAN_POINT('Ctrl Pts',(80.5053120194535,55.122627751513,60.6051329000625));
#47544=CARTESIAN_POINT('Ctrl Pts',(73.0895524925331,54.5922377276321,61.5582353558216));
#47545=CARTESIAN_POINT('Ctrl Pts',(68.6918174455575,54.1679257085274,58.3365300018253));
#47546=CARTESIAN_POINT('Ctrl Pts',(66.2548933682926,53.7436136894228,53.4599676908307));
#47547=CARTESIAN_POINT('Ctrl Pts',(68.4405486939056,53.2132236655421,46.3098065423043));
#47548=CARTESIAN_POINT('Ctrl Pts',(77.1079824933874,52.5767556368851,43.8891129381638));
#47549=CARTESIAN_POINT('Ctrl Pts',(83.8106590717248,51.9402876082283,49.8680299008908));
#47550=CARTESIAN_POINT('Ctrl Pts',(82.4187760452078,51.3038195795712,58.7413597719972));
#47551=CARTESIAN_POINT('Ctrl Pts',(74.181604690216,50.6673515509143,62.3653319382867));
#47552=CARTESIAN_POINT('Ctrl Pts',(67.9577498141223,50.1369615270334,58.2222021872887));
#47553=CARTESIAN_POINT('Ctrl Pts',(66.7500330581167,49.7126495079289,52.9061059533381));
#47554=CARTESIAN_POINT('Ctrl Pts',(68.107859170072,49.2883374888242,47.6263552792002));
#47555=CARTESIAN_POINT('Ctrl Pts',(74.4465826239457,48.7579474649434,43.6611971956435));
#47556=CARTESIAN_POINT('Ctrl Pts',(82.5777886154376,48.1214794362866,47.5170570630991));
#47557=CARTESIAN_POINT('Ctrl Pts',(83.717749937762,47.4850114076295,56.4262550934819));
#47558=CARTESIAN_POINT('Ctrl Pts',(76.8483928784914,46.8485433789726,62.2128996266483));
#47559=CARTESIAN_POINT('Ctrl Pts',(68.2530107161164,46.2120753503157,59.5476469789136));
#47560=CARTESIAN_POINT('Ctrl Pts',(66.2707818357398,45.6816853264349,52.3384402043735));
#47561=CARTESIAN_POINT('Ctrl Pts',(68.8448708790405,45.2573733073303,47.5328679670094));
#47562=CARTESIAN_POINT('Ctrl Pts',(73.3321053046874,44.8330612882256,44.4370342924303));
#47563=CARTESIAN_POINT('Ctrl Pts',(80.7178893398119,44.3026712643448,45.5998274119405));
#47564=CARTESIAN_POINT('Ctrl Pts',(84.3285341855929,43.6662032356878,53.8428493087427));
#47565=CARTESIAN_POINT('Ctrl Pts',(79.3471932593963,43.029735207031,61.3167749130004));
#47566=CARTESIAN_POINT('Ctrl Pts',(70.3663829481276,42.393267178374,61.1812481112956));
#47567=CARTESIAN_POINT('Ctrl Pts',(65.6245720603672,41.7567991497171,53.5327583454499));
#47568=CARTESIAN_POINT('Ctrl Pts',(68.8552716638434,41.2264091258363,46.7900234608216));
#47569=CARTESIAN_POINT('Ctrl Pts',(73.949849452103,40.8020971067316,44.8497306760242));
#47570=CARTESIAN_POINT('Ctrl Pts',(79.3677239232426,40.377785087627,45.4547886454258));
#47571=CARTESIAN_POINT('Ctrl Pts',(84.1814958476775,39.8473950637462,51.1757582758122));
#47572=CARTESIAN_POINT('Ctrl Pts',(81.5023447448448,39.2109270350893,59.7668184875512));
#47573=CARTESIAN_POINT('Ctrl Pts',(72.8405846002177,38.5744590064323,62.1432091452338));
#47574=CARTESIAN_POINT('Ctrl Pts',(66.1489649218033,37.9379909777754,56.1519198482274));
#47575=CARTESIAN_POINT('Ctrl Pts',(67.5842373708341,37.3015229491184,47.2679928341982));
#47576=CARTESIAN_POINT('Ctrl Pts',(74.4448058052946,36.7711329252377,44.2957050943661));
#47577=CARTESIAN_POINT('Ctrl Pts',(79.5635026555143,36.346820906133,46.1714453447497));
#47578=CARTESIAN_POINT('Ctrl Pts',(83.2572304286379,35.9225088870284,50.1809133979266));
#47579=CARTESIAN_POINT('Ctrl Pts',(83.1402168969827,35.3921188631477,57.6567545870878));
#47580=CARTESIAN_POINT('Ctrl Pts',(75.4840678569184,34.7556508344906,62.38618881013));
#47581=CARTESIAN_POINT('Ctrl Pts',(67.3861961333135,34.1191828058337,58.5006007067545));
#47582=CARTESIAN_POINT('Ctrl Pts',(66.2626956250231,33.4827147771767,49.5893119128753));
#47583=CARTESIAN_POINT('Ctrl Pts',(73.1717604263215,32.8462467485199,43.8231182145451));
#47584=CARTESIAN_POINT('Ctrl Pts',(80.300483382939,32.315856724639,46.0777141118401));
#47585=CARTESIAN_POINT('Ctrl Pts',(82.9351111460744,31.8915447055345,50.8503648929889));
#47586=CARTESIAN_POINT('Ctrl Pts',(83.0947463504551,31.4672326864297,56.2995827762267));
#47587=CARTESIAN_POINT('Ctrl Pts',(78.1042846037941,30.936842662549,61.8670943558816));
#47588=CARTESIAN_POINT('Ctrl Pts',(69.2226905800411,30.3003746338921,60.4174551605608));
#47589=CARTESIAN_POINT('Ctrl Pts',(65.6567066513159,29.6639066052351,52.1738467249999));
#47590=CARTESIAN_POINT('Ctrl Pts',(70.6518464186429,29.0274385765782,44.7091364205264));
#47591=CARTESIAN_POINT('Ctrl Pts',(79.6492257952861,28.3909705479212,44.8861410045034));
#47592=CARTESIAN_POINT('Ctrl Pts',(83.552991842885,27.8605805240404,51.2628568188668));
#47593=CARTESIAN_POINT('Ctrl Pts',(82.4125691883584,27.4362685049358,56.5937943203991));
#47594=CARTESIAN_POINT('Ctrl Pts',(78.959889717477,27.0119564858311,60.812616932623));
#47595=CARTESIAN_POINT('Ctrl Pts',(71.5413320884577,26.4815664619504,61.743689023496));
#47596=CARTESIAN_POINT('Ctrl Pts',(65.7863203711639,25.8450984332935,54.8253074886375));
#47597=CARTESIAN_POINT('Ctrl Pts',(68.4995751288869,25.2086304046365,46.2630892864365));
#47598=CARTESIAN_POINT('Ctrl Pts',(77.1657103179859,24.5721623759795,43.9027054865252));
#47599=CARTESIAN_POINT('Ctrl Pts',(83.8426420808462,23.9356943473226,49.9361731535205));
#47600=CARTESIAN_POINT('Ctrl Pts',(82.6085843589776,23.4053043234418,57.3103885914542));
#47601=CARTESIAN_POINT('Ctrl Pts',(78.2519260276138,22.9809923043372,60.5874201313303));
#47602=CARTESIAN_POINT('Ctrl Pts',(72.8787595021107,22.5566802852326,61.5086132067331));
#47603=CARTESIAN_POINT('Ctrl Pts',(66.6672452762723,22.0262902613518,57.3469916847974));
#47604=CARTESIAN_POINT('Ctrl Pts',(66.85878821435,21.3898222326947,48.3499544346595));
#47605=CARTESIAN_POINT('Ctrl Pts',(74.5217964330623,20.7533542040379,43.664580771223));
#47606=CARTESIAN_POINT('Ctrl Pts',(82.6124311846432,20.1168861753809,47.5652683417291));
#47607=CARTESIAN_POINT('Ctrl Pts',(83.6972706997256,19.480418146724,56.4984863200123));
#47608=CARTESIAN_POINT('Ctrl Pts',(77.9299254702141,18.9500281228433,61.2573127511593));
#47609=CARTESIAN_POINT('Ctrl Pts',(72.4920520828531,18.5257161037386,60.8739104023719));
#47610=CARTESIAN_POINT('Ctrl Pts',(67.8308159848136,18.1014040846339,58.0475875686556));
#47611=CARTESIAN_POINT('Ctrl Pts',(65.8710431841307,17.5710140607531,50.8291601454251));
#47612=CARTESIAN_POINT('Ctrl Pts',(71.9134175217386,16.9345460320962,44.1681258720739));
#47613=CARTESIAN_POINT('Ctrl Pts',(80.7745918640496,16.2980780034393,45.6446820440961));
#47614=CARTESIAN_POINT('Ctrl Pts',(84.3188969900482,15.6616099747824,53.9154373611954));
#47615=CARTESIAN_POINT('Ctrl Pts',(80.1313293268964,15.1312199509016,60.0939695185882));
#47616=CARTESIAN_POINT('Ctrl Pts',(74.786341856204,14.7069079317969,61.2678572289885));
#47617=CARTESIAN_POINT('Ctrl Pts',(72.1730647398712,14.4947519222446,60.5478236301968));
#47618=CARTESIAN_POINT('Ctrl Pts',(71.0291102539094,14.3886739174684,59.8881742938589));
#47619=CARTESIAN_POINT('Ctrl Pts',(82.9129498948689,15.7216677763616,53.0228109606368));
#47620=CARTESIAN_POINT('Ctrl Pts',(82.9129498948686,15.5454469188779,55.216507035084));
#47621=CARTESIAN_POINT('Ctrl Pts',(81.9532970624634,15.3692260613942,57.3933791504626));
#47622=CARTESIAN_POINT('Ctrl Pts',(80.33387643929,15.1930052039106,58.8731694438102));
#47623=CARTESIAN_POINT('Ctrl Pts',(79.7426550745104,15.1286701359404,59.413414284651));
#47624=CARTESIAN_POINT('Ctrl Pts',(79.0690015640715,15.0643350679702,59.8632823964012));
#47625=CARTESIAN_POINT('Ctrl Pts',(78.3434537325938,15.,60.2023805156308));
#47626=CARTESIAN_POINT('Origin',(74.9879498948689,255.,53.0228109606356));
#48349=UNCERTAINTY_MEASURE_WITH_UNIT(LENGTH_MEASURE(0.01),#48370,
'DISTANCE_ACCURACY_VALUE',
'Maximum model space distance between geometric entities at asserted c
onnectivities');
#48356=UNCERTAINTY_MEASURE_WITH_UNIT(LENGTH_MEASURE(0.01),#48370,
'DISTANCE_ACCURACY_VALUE',
'Maximum model space distance between geometric entities at asserted c
onnectivities');
#48362=(
GEOMETRIC_REPRESENTATION_CONTEXT(3)
GLOBAL_UNCERTAINTY_ASSIGNED_CONTEXT((#48349))
GLOBAL_UNIT_ASSIGNED_CONTEXT((#48370,#48372,#48373))
REPRESENTATION_CONTEXT('','3D')
);
#48369=(
GEOMETRIC_REPRESENTATION_CONTEXT(3)
GLOBAL_UNCERTAINTY_ASSIGNED_CONTEXT((#48356))
GLOBAL_UNIT_ASSIGNED_CONTEXT((#48370,#48372,#48373))
REPRESENTATION_CONTEXT('','3D')
);
#48370=(
LENGTH_UNIT()
NAMED_UNIT(*)
SI_UNIT(.MILLI.,.METRE.)
);
#48372=(
NAMED_UNIT(*)
PLANE_ANGLE_UNIT()
SI_UNIT($,.RADIAN.)
);
#48373=(
NAMED_UNIT(*)
SI_UNIT($,.STERADIAN.)
SOLID_ANGLE_UNIT()
);
#48379=SHAPE_DEFINITION_REPRESENTATION(#48391,#48417);
#48391=PRODUCT_DEFINITION_SHAPE('',$,#48430);
#48417=SHAPE_REPRESENTATION('',(#21410),#48362);
#48424=PRODUCT_DEFINITION_CONTEXT('part definition',#48462,'design');
#48430=PRODUCT_DEFINITION('Screw','Screw',#48442,#48424);
#48442=PRODUCT_DEFINITION_FORMATION('',$,#48469);
#48462=APPLICATION_CONTEXT(
'Core Data for Automotive Mechanical Design Process');
#48463=PRODUCT_CONTEXT('part definition',#48462,'mechanical');
#48469=PRODUCT('Screw','Screw',$,(#48463));
#48518=COLOUR_RGB('Black',0.12,0.14,0.17);
#48519=FILL_AREA_STYLE_COLOUR('',#48518);
#48520=FILL_AREA_STYLE('',(#48519));
#48521=SURFACE_STYLE_FILL_AREA(#48520);
#48522=SURFACE_SIDE_STYLE('',(#48521));
#48523=SURFACE_STYLE_USAGE(.BOTH.,#48522);
#48524=PRESENTATION_STYLE_ASSIGNMENT((#48523));
ENDSEC;
END-ISO-10303-21;
